ISO-10303-21;
HEADER;
/* Generated by software containing ST-Developer
 * from STEP Tools, Inc. (www.steptools.com) 
 */

FILE_DESCRIPTION(
/* description */ ('XY cross-slide table'),
/* implementation_level */ '2;1');

FILE_NAME(
/* name */ 'Y Stage - 01 Supported TR12x3 screw.step',
/* time_stamp */ '2026-10-28T03:22:46-07:00',
/* author */ (''),
/* organization */ (''),
/* preprocessor_version */ 'ST-DEVELOPER v20.2',
/* originating_system */ 'Autodesk Translation Framework v15.17.0.0',
/* authorisation */ '');

FILE_SCHEMA (('AUTOMOTIVE_DESIGN { 1 0 10303 214 3 1 1 }'));
ENDSEC;

DATA;
#10=MECHANICAL_DESIGN_GEOMETRIC_PRESENTATION_REPRESENTATION('',(#1773),#62984);
#17=B_SPLINE_SURFACE_WITH_KNOTS('',3,3,((#58111,#58112,#58113,#58114,#58115,
#58116,#58117,#58118,#58119,#58120,#58121,#58122,#58123,#58124,#58125,#58126,
#58127,#58128,#58129,#58130,#58131,#58132,#58133,#58134,#58135,#58136,#58137,
#58138,#58139,#58140,#58141,#58142,#58143,#58144,#58145,#58146,#58147,#58148,
#58149,#58150,#58151,#58152,#58153,#58154,#58155,#58156,#58157,#58158,#58159,
#58160,#58161,#58162,#58163,#58164,#58165,#58166,#58167,#58168,#58169,#58170,
#58171,#58172,#58173,#58174,#58175,#58176,#58177,#58178,#58179,#58180,#58181,
#58182,#58183,#58184,#58185,#58186,#58187,#58188,#58189,#58190,#58191,#58192,
#58193,#58194,#58195,#58196,#58197,#58198,#58199,#58200,#58201,#58202,#58203,
#58204,#58205,#58206,#58207,#58208,#58209,#58210,#58211,#58212,#58213,#58214,
#58215,#58216,#58217,#58218,#58219,#58220,#58221,#58222,#58223,#58224,#58225,
#58226,#58227,#58228,#58229,#58230,#58231,#58232,#58233,#58234,#58235,#58236,
#58237,#58238,#58239,#58240,#58241,#58242,#58243,#58244,#58245,#58246,#58247,
#58248,#58249,#58250,#58251,#58252,#58253,#58254,#58255,#58256,#58257,#58258,
#58259,#58260,#58261,#58262,#58263,#58264,#58265,#58266,#58267,#58268,#58269,
#58270,#58271,#58272,#58273,#58274,#58275,#58276,#58277,#58278,#58279,#58280,
#58281,#58282,#58283,#58284,#58285,#58286,#58287,#58288,#58289,#58290,#58291,
#58292,#58293,#58294,#58295,#58296,#58297,#58298,#58299,#58300,#58301,#58302,
#58303,#58304,#58305,#58306,#58307,#58308,#58309,#58310,#58311,#58312,#58313,
#58314,#58315,#58316,#58317,#58318,#58319,#58320,#58321,#58322,#58323,#58324,
#58325,#58326,#58327,#58328,#58329,#58330,#58331,#58332,#58333,#58334,#58335,
#58336,#58337,#58338,#58339,#58340,#58341,#58342,#58343,#58344,#58345,#58346,
#58347,#58348,#58349,#58350,#58351,#58352,#58353,#58354,#58355,#58356,#58357,
#58358,#58359,#58360,#58361,#58362,#58363,#58364,#58365,#58366,#58367,#58368,
#58369,#58370,#58371,#58372,#58373,#58374,#58375,#58376,#58377,#58378,#58379,
#58380,#58381,#58382,#58383,#58384,#58385,#58386,#58387,#58388,#58389,#58390,
#58391,#58392,#58393,#58394,#58395,#58396,#58397,#58398,#58399,#58400,#58401,
#58402,#58403,#58404,#58405,#58406,#58407,#58408,#58409,#58410,#58411,#58412,
#58413,#58414,#58415,#58416,#58417,#58418,#58419,#58420,#58421,#58422,#58423,
#58424,#58425,#58426,#58427,#58428,#58429,#58430,#58431,#58432,#58433,#58434,
#58435,#58436,#58437,#58438,#58439,#58440,#58441,#58442,#58443,#58444,#58445,
#58446,#58447,#58448,#58449,#58450,#58451,#58452,#58453,#58454,#58455,#58456,
#58457,#58458,#58459,#58460,#58461,#58462,#58463,#58464,#58465,#58466,#58467,
#58468,#58469,#58470,#58471,#58472,#58473,#58474,#58475,#58476,#58477,#58478,
#58479,#58480,#58481,#58482,#58483,#58484,#58485,#58486,#58487,#58488,#58489,
#58490,#58491,#58492,#58493,#58494,#58495,#58496,#58497,#58498,#58499,#58500,
#58501,#58502,#58503,#58504,#58505,#58506,#58507,#58508,#58509,#58510,#58511,
#58512,#58513,#58514,#58515,#58516,#58517,#58518,#58519,#58520,#58521,#58522,
#58523,#58524,#58525,#58526,#58527,#58528,#58529,#58530,#58531,#58532,#58533,
#58534,#58535,#58536,#58537,#58538,#58539,#58540,#58541,#58542,#58543,#58544,
#58545,#58546,#58547,#58548,#58549,#58550,#58551,#58552,#58553,#58554,#58555,
#58556,#58557,#58558,#58559,#58560,#58561,#58562,#58563,#58564,#58565,#58566,
#58567,#58568,#58569,#58570,#58571,#58572,#58573,#58574,#58575,#58576,#58577,
#58578,#58579,#58580,#58581,#58582,#58583,#58584,#58585,#58586,#58587,#58588,
#58589,#58590,#58591,#58592,#58593,#58594,#58595,#58596,#58597,#58598,#58599,
#58600,#58601,#58602,#58603,#58604,#58605,#58606,#58607,#58608),(#58609,
#58610,#58611,#58612,#58613,#58614,#58615,#58616,#58617,#58618,#58619,#58620,
#58621,#58622,#58623,#58624,#58625,#58626,#58627,#58628,#58629,#58630,#58631,
#58632,#58633,#58634,#58635,#58636,#58637,#58638,#58639,#58640,#58641,#58642,
#58643,#58644,#58645,#58646,#58647,#58648,#58649,#58650,#58651,#58652,#58653,
#58654,#58655,#58656,#58657,#58658,#58659,#58660,#58661,#58662,#58663,#58664,
#58665,#58666,#58667,#58668,#58669,#58670,#58671,#58672,#58673,#58674,#58675,
#58676,#58677,#58678,#58679,#58680,#58681,#58682,#58683,#58684,#58685,#58686,
#58687,#58688,#58689,#58690,#58691,#58692,#58693,#58694,#58695,#58696,#58697,
#58698,#58699,#58700,#58701,#58702,#58703,#58704,#58705,#58706,#58707,#58708,
#58709,#58710,#58711,#58712,#58713,#58714,#58715,#58716,#58717,#58718,#58719,
#58720,#58721,#58722,#58723,#58724,#58725,#58726,#58727,#58728,#58729,#58730,
#58731,#58732,#58733,#58734,#58735,#58736,#58737,#58738,#58739,#58740,#58741,
#58742,#58743,#58744,#58745,#58746,#58747,#58748,#58749,#58750,#58751,#58752,
#58753,#58754,#58755,#58756,#58757,#58758,#58759,#58760,#58761,#58762,#58763,
#58764,#58765,#58766,#58767,#58768,#58769,#58770,#58771,#58772,#58773,#58774,
#58775,#58776,#58777,#58778,#58779,#58780,#58781,#58782,#58783,#58784,#58785,
#58786,#58787,#58788,#58789,#58790,#58791,#58792,#58793,#58794,#58795,#58796,
#58797,#58798,#58799,#58800,#58801,#58802,#58803,#58804,#58805,#58806,#58807,
#58808,#58809,#58810,#58811,#58812,#58813,#58814,#58815,#58816,#58817,#58818,
#58819,#58820,#58821,#58822,#58823,#58824,#58825,#58826,#58827,#58828,#58829,
#58830,#58831,#58832,#58833,#58834,#58835,#58836,#58837,#58838,#58839,#58840,
#58841,#58842,#58843,#58844,#58845,#58846,#58847,#58848,#58849,#58850,#58851,
#58852,#58853,#58854,#58855,#58856,#58857,#58858,#58859,#58860,#58861,#58862,
#58863,#58864,#58865,#58866,#58867,#58868,#58869,#58870,#58871,#58872,#58873,
#58874,#58875,#58876,#58877,#58878,#58879,#58880,#58881,#58882,#58883,#58884,
#58885,#58886,#58887,#58888,#58889,#58890,#58891,#58892,#58893,#58894,#58895,
#58896,#58897,#58898,#58899,#58900,#58901,#58902,#58903,#58904,#58905,#58906,
#58907,#58908,#58909,#58910,#58911,#58912,#58913,#58914,#58915,#58916,#58917,
#58918,#58919,#58920,#58921,#58922,#58923,#58924,#58925,#58926,#58927,#58928,
#58929,#58930,#58931,#58932,#58933,#58934,#58935,#58936,#58937,#58938,#58939,
#58940,#58941,#58942,#58943,#58944,#58945,#58946,#58947,#58948,#58949,#58950,
#58951,#58952,#58953,#58954,#58955,#58956,#58957,#58958,#58959,#58960,#58961,
#58962,#58963,#58964,#58965,#58966,#58967,#58968,#58969,#58970,#58971,#58972,
#58973,#58974,#58975,#58976,#58977,#58978,#58979,#58980,#58981,#58982,#58983,
#58984,#58985,#58986,#58987,#58988,#58989,#58990,#58991,#58992,#58993,#58994,
#58995,#58996,#58997,#58998,#58999,#59000,#59001,#59002,#59003,#59004,#59005,
#59006,#59007,#59008,#59009,#59010,#59011,#59012,#59013,#59014,#59015,#59016,
#59017,#59018,#59019,#59020,#59021,#59022,#59023,#59024,#59025,#59026,#59027,
#59028,#59029,#59030,#59031,#59032,#59033,#59034,#59035,#59036,#59037,#59038,
#59039,#59040,#59041,#59042,#59043,#59044,#59045,#59046,#59047,#59048,#59049,
#59050,#59051,#59052,#59053,#59054,#59055,#59056,#59057,#59058,#59059,#59060,
#59061,#59062,#59063,#59064,#59065,#59066,#59067,#59068,#59069,#59070,#59071,
#59072,#59073,#59074,#59075,#59076,#59077,#59078,#59079,#59080,#59081,#59082,
#59083,#59084,#59085,#59086,#59087,#59088,#59089,#59090,#59091,#59092,#59093,
#59094,#59095,#59096,#59097,#59098,#59099,#59100,#59101,#59102,#59103,#59104,
#59105,#59106),(#59107,#59108,#59109,#59110,#59111,#59112,#59113,#59114,
#59115,#59116,#59117,#59118,#59119,#59120,#59121,#59122,#59123,#59124,#59125,
#59126,#59127,#59128,#59129,#59130,#59131,#59132,#59133,#59134,#59135,#59136,
#59137,#59138,#59139,#59140,#59141,#59142,#59143,#59144,#59145,#59146,#59147,
#59148,#59149,#59150,#59151,#59152,#59153,#59154,#59155,#59156,#59157,#59158,
#59159,#59160,#59161,#59162,#59163,#59164,#59165,#59166,#59167,#59168,#59169,
#59170,#59171,#59172,#59173,#59174,#59175,#59176,#59177,#59178,#59179,#59180,
#59181,#59182,#59183,#59184,#59185,#59186,#59187,#59188,#59189,#59190,#59191,
#59192,#59193,#59194,#59195,#59196,#59197,#59198,#59199,#59200,#59201,#59202,
#59203,#59204,#59205,#59206,#59207,#59208,#59209,#59210,#59211,#59212,#59213,
#59214,#59215,#59216,#59217,#59218,#59219,#59220,#59221,#59222,#59223,#59224,
#59225,#59226,#59227,#59228,#59229,#59230,#59231,#59232,#59233,#59234,#59235,
#59236,#59237,#59238,#59239,#59240,#59241,#59242,#59243,#59244,#59245,#59246,
#59247,#59248,#59249,#59250,#59251,#59252,#59253,#59254,#59255,#59256,#59257,
#59258,#59259,#59260,#59261,#59262,#59263,#59264,#59265,#59266,#59267,#59268,
#59269,#59270,#59271,#59272,#59273,#59274,#59275,#59276,#59277,#59278,#59279,
#59280,#59281,#59282,#59283,#59284,#59285,#59286,#59287,#59288,#59289,#59290,
#59291,#59292,#59293,#59294,#59295,#59296,#59297,#59298,#59299,#59300,#59301,
#59302,#59303,#59304,#59305,#59306,#59307,#59308,#59309,#59310,#59311,#59312,
#59313,#59314,#59315,#59316,#59317,#59318,#59319,#59320,#59321,#59322,#59323,
#59324,#59325,#59326,#59327,#59328,#59329,#59330,#59331,#59332,#59333,#59334,
#59335,#59336,#59337,#59338,#59339,#59340,#59341,#59342,#59343,#59344,#59345,
#59346,#59347,#59348,#59349,#59350,#59351,#59352,#59353,#59354,#59355,#59356,
#59357,#59358,#59359,#59360,#59361,#59362,#59363,#59364,#59365,#59366,#59367,
#59368,#59369,#59370,#59371,#59372,#59373,#59374,#59375,#59376,#59377,#59378,
#59379,#59380,#59381,#59382,#59383,#59384,#59385,#59386,#59387,#59388,#59389,
#59390,#59391,#59392,#59393,#59394,#59395,#59396,#59397,#59398,#59399,#59400,
#59401,#59402,#59403,#59404,#59405,#59406,#59407,#59408,#59409,#59410,#59411,
#59412,#59413,#59414,#59415,#59416,#59417,#59418,#59419,#59420,#59421,#59422,
#59423,#59424,#59425,#59426,#59427,#59428,#59429,#59430,#59431,#59432,#59433,
#59434,#59435,#59436,#59437,#59438,#59439,#59440,#59441,#59442,#59443,#59444,
#59445,#59446,#59447,#59448,#59449,#59450,#59451,#59452,#59453,#59454,#59455,
#59456,#59457,#59458,#59459,#59460,#59461,#59462,#59463,#59464,#59465,#59466,
#59467,#59468,#59469,#59470,#59471,#59472,#59473,#59474,#59475,#59476,#59477,
#59478,#59479,#59480,#59481,#59482,#59483,#59484,#59485,#59486,#59487,#59488,
#59489,#59490,#59491,#59492,#59493,#59494,#59495,#59496,#59497,#59498,#59499,
#59500,#59501,#59502,#59503,#59504,#59505,#59506,#59507,#59508,#59509,#59510,
#59511,#59512,#59513,#59514,#59515,#59516,#59517,#59518,#59519,#59520,#59521,
#59522,#59523,#59524,#59525,#59526,#59527,#59528,#59529,#59530,#59531,#59532,
#59533,#59534,#59535,#59536,#59537,#59538,#59539,#59540,#59541,#59542,#59543,
#59544,#59545,#59546,#59547,#59548,#59549,#59550,#59551,#59552,#59553,#59554,
#59555,#59556,#59557,#59558,#59559,#59560,#59561,#59562,#59563,#59564,#59565,
#59566,#59567,#59568,#59569,#59570,#59571,#59572,#59573,#59574,#59575,#59576,
#59577,#59578,#59579,#59580,#59581,#59582,#59583,#59584,#59585,#59586,#59587,
#59588,#59589,#59590,#59591,#59592,#59593,#59594,#59595,#59596,#59597,#59598,
#59599,#59600,#59601,#59602,#59603,#59604),(#59605,#59606,#59607,#59608,
#59609,#59610,#59611,#59612,#59613,#59614,#59615,#59616,#59617,#59618,#59619,
#59620,#59621,#59622,#59623,#59624,#59625,#59626,#59627,#59628,#59629,#59630,
#59631,#59632,#59633,#59634,#59635,#59636,#59637,#59638,#59639,#59640,#59641,
#59642,#59643,#59644,#59645,#59646,#59647,#59648,#59649,#59650,#59651,#59652,
#59653,#59654,#59655,#59656,#59657,#59658,#59659,#59660,#59661,#59662,#59663,
#59664,#59665,#59666,#59667,#59668,#59669,#59670,#59671,#59672,#59673,#59674,
#59675,#59676,#59677,#59678,#59679,#59680,#59681,#59682,#59683,#59684,#59685,
#59686,#59687,#59688,#59689,#59690,#59691,#59692,#59693,#59694,#59695,#59696,
#59697,#59698,#59699,#59700,#59701,#59702,#59703,#59704,#59705,#59706,#59707,
#59708,#59709,#59710,#59711,#59712,#59713,#59714,#59715,#59716,#59717,#59718,
#59719,#59720,#59721,#59722,#59723,#59724,#59725,#59726,#59727,#59728,#59729,
#59730,#59731,#59732,#59733,#59734,#59735,#59736,#59737,#59738,#59739,#59740,
#59741,#59742,#59743,#59744,#59745,#59746,#59747,#59748,#59749,#59750,#59751,
#59752,#59753,#59754,#59755,#59756,#59757,#59758,#59759,#59760,#59761,#59762,
#59763,#59764,#59765,#59766,#59767,#59768,#59769,#59770,#59771,#59772,#59773,
#59774,#59775,#59776,#59777,#59778,#59779,#59780,#59781,#59782,#59783,#59784,
#59785,#59786,#59787,#59788,#59789,#59790,#59791,#59792,#59793,#59794,#59795,
#59796,#59797,#59798,#59799,#59800,#59801,#59802,#59803,#59804,#59805,#59806,
#59807,#59808,#59809,#59810,#59811,#59812,#59813,#59814,#59815,#59816,#59817,
#59818,#59819,#59820,#59821,#59822,#59823,#59824,#59825,#59826,#59827,#59828,
#59829,#59830,#59831,#59832,#59833,#59834,#59835,#59836,#59837,#59838,#59839,
#59840,#59841,#59842,#59843,#59844,#59845,#59846,#59847,#59848,#59849,#59850,
#59851,#59852,#59853,#59854,#59855,#59856,#59857,#59858,#59859,#59860,#59861,
#59862,#59863,#59864,#59865,#59866,#59867,#59868,#59869,#59870,#59871,#59872,
#59873,#59874,#59875,#59876,#59877,#59878,#59879,#59880,#59881,#59882,#59883,
#59884,#59885,#59886,#59887,#59888,#59889,#59890,#59891,#59892,#59893,#59894,
#59895,#59896,#59897,#59898,#59899,#59900,#59901,#59902,#59903,#59904,#59905,
#59906,#59907,#59908,#59909,#59910,#59911,#59912,#59913,#59914,#59915,#59916,
#59917,#59918,#59919,#59920,#59921,#59922,#59923,#59924,#59925,#59926,#59927,
#59928,#59929,#59930,#59931,#59932,#59933,#59934,#59935,#59936,#59937,#59938,
#59939,#59940,#59941,#59942,#59943,#59944,#59945,#59946,#59947,#59948,#59949,
#59950,#59951,#59952,#59953,#59954,#59955,#59956,#59957,#59958,#59959,#59960,
#59961,#59962,#59963,#59964,#59965,#59966,#59967,#59968,#59969,#59970,#59971,
#59972,#59973,#59974,#59975,#59976,#59977,#59978,#59979,#59980,#59981,#59982,
#59983,#59984,#59985,#59986,#59987,#59988,#59989,#59990,#59991,#59992,#59993,
#59994,#59995,#59996,#59997,#59998,#59999,#60000,#60001,#60002,#60003,#60004,
#60005,#60006,#60007,#60008,#60009,#60010,#60011,#60012,#60013,#60014,#60015,
#60016,#60017,#60018,#60019,#60020,#60021,#60022,#60023,#60024,#60025,#60026,
#60027,#60028,#60029,#60030,#60031,#60032,#60033,#60034,#60035,#60036,#60037,
#60038,#60039,#60040,#60041,#60042,#60043,#60044,#60045,#60046,#60047,#60048,
#60049,#60050,#60051,#60052,#60053,#60054,#60055,#60056,#60057,#60058,#60059,
#60060,#60061,#60062,#60063,#60064,#60065,#60066,#60067,#60068,#60069,#60070,
#60071,#60072,#60073,#60074,#60075,#60076,#60077,#60078,#60079,#60080,#60081,
#60082,#60083,#60084,#60085,#60086,#60087,#60088,#60089,#60090,#60091,#60092,
#60093,#60094,#60095,#60096,#60097,#60098,#60099,#60100,#60101,#60102)),
 .UNSPECIFIED.,.F.,.F.,.F.,(4,4),(4,1,1,1,1,1,1,1,1,1,1,1,1,1,1,1,1,1,1,
1,1,1,1,1,1,1,1,1,1,1,1,1,1,1,1,1,1,1,1,1,1,1,1,1,1,1,1,1,1,1,1,1,1,1,1,
1,1,1,1,1,1,1,1,1,1,1,1,1,1,1,1,1,1,1,1,1,1,1,1,1,1,1,1,1,1,1,1,1,1,1,1,
1,1,1,1,1,1,1,1,1,1,1,1,1,1,1,1,1,1,1,1,1,1,1,1,1,1,1,1,1,1,1,1,1,1,1,1,
1,1,1,1,1,1,1,1,1,1,1,1,1,1,1,1,1,1,1,1,1,1,1,1,1,1,1,1,1,1,1,1,1,1,1,1,
1,1,1,1,1,1,1,1,1,1,1,1,1,1,1,1,1,1,1,1,1,1,1,1,1,1,1,1,1,1,1,1,1,1,1,1,
1,1,1,1,1,1,1,1,1,1,1,1,1,1,1,1,1,1,1,1,1,1,1,1,1,1,1,1,1,1,1,1,1,1,1,1,
1,1,1,1,1,1,1,1,1,1,1,1,1,1,1,1,1,1,1,1,1,1,1,1,1,1,1,1,1,1,1,1,1,1,1,1,
1,1,1,1,1,1,1,1,1,1,1,1,1,1,1,1,1,1,1,1,1,1,1,1,1,1,1,1,1,1,1,1,1,1,1,1,
1,1,1,1,1,1,1,1,1,1,1,1,1,1,1,1,1,1,1,1,1,1,1,1,1,1,1,1,1,1,1,1,1,1,1,1,
1,1,1,1,1,1,1,1,1,1,1,1,1,1,1,1,1,1,1,1,1,1,1,1,1,1,1,1,1,1,1,1,1,1,1,1,
1,1,1,1,1,1,1,1,1,1,1,1,1,1,1,1,1,1,1,1,1,1,1,1,1,1,1,1,1,1,1,1,1,1,1,1,
1,1,1,1,1,1,1,1,1,1,1,1,1,1,1,1,1,1,1,1,1,1,1,1,1,1,1,1,1,1,1,1,1,1,1,1,
1,1,1,1,1,1,1,1,1,1,1,1,1,1,1,1,1,1,1,1,1,1,1,1,1,1,1,1,1,1,1,1,1,1,1,1,
1,1,1,1,1,1,1,1,4),(0.,0.184512097253587),(8.98171729021681,9.48139635699984,
9.98107542378286,10.4807544905659,10.9804335573489,11.4801126241319,11.979791690915,
12.479470757698,12.979149824481,13.478828891264,13.9785079580471,14.4781870248301,
14.9778660916131,15.4775451583961,15.9772242251791,16.4769032919622,16.9765823587452,
17.4762614255282,17.9759404923112,18.4756195590943,18.9752986258773,19.4749776926603,
19.9746567594433,20.4743358262264,20.9740148930094,21.4736939597924,21.9733730265754,
22.4730520933585,22.9727311601415,23.4724102269245,23.9720892937075,24.4717683604905,
24.9714474272736,25.4711264940566,25.9708055608396,26.4704846276226,26.9701636944057,
27.4698427611887,27.9695218279717,28.4692008947547,28.9688799615378,29.4685590283208,
29.9682380951038,30.4679171618868,30.9675962286699,31.4672752954529,31.9669543622359,
32.4666334290189,32.966312495802,33.465991562585,33.965670629368,34.465349696151,
34.965028762934,35.4647078297171,35.9643868965001,36.4640659632831,36.9637450300661,
37.4634240968492,37.9631031636322,38.4627822304152,38.9624612971982,39.4621403639813,
39.9618194307643,40.4614984975473,40.9611775643303,41.4608566311134,41.9605356978964,
42.4602147646794,42.9598938314624,43.4595728982454,43.9592519650285,44.4589310318115,
44.9586100985945,45.4582891653775,45.9579682321606,46.4576472989436,46.9573263657266,
47.4570054325096,47.9566844992927,48.4563635660757,48.9560426328587,49.4557216996417,
49.9554007664248,50.4550798332078,50.9547588999908,51.4544379667738,51.9541170335568,
52.4537961003399,52.9534751671229,53.4531542339059,53.9528333006889,54.452512367472,
54.952191434255,55.451870501038,55.951549567821,56.4512286346041,56.9509077013871,
57.4505867681701,57.9502658349531,58.4499449017362,58.9496239685192,59.9489821020852,
60.9483402356513,61.9476983692173,62.9470565027834,63.9464146363494,64.9457727699155,
65.9451309034815,66.9444890370476,67.9438471706136,68.9432053041797,69.9425634377457,
70.9419215713118,71.9412797048778,72.9406378384438,73.9399959720099,74.9393541055759,
75.938712239142,76.938070372708,77.9374285062741,78.9367866398401,79.9361447734062,
80.9355029069722,81.9348610405383,82.9342191741043,83.9335773076704,84.9329354412364,
85.9322935748025,86.9316517083685,87.9310098419346,88.9303679755006,89.9297261090666,
90.9290842426327,91.9284423761987,92.9278005097648,93.9271586433308,94.9265167768969,
95.9258749104629,96.925233044029,97.924591177595,98.9239493111611,99.9233074447271,
100.922665578293,101.922023711859,102.921381845425,103.920739978991,104.920098112557,
105.919456246123,106.918814379689,107.918172513255,108.917530646822,109.916888780388,
110.916246913954,111.91560504752,112.914963181086,113.914321314652,114.913679448218,
115.913037581784,116.91239571535,117.911753848916,118.911111982482,119.910470116048,
120.909828249614,121.90918638318,122.908544516746,123.907902650312,124.907260783878,
125.906618917444,126.90597705101,127.905335184576,128.904693318142,129.904051451709,
130.903409585275,131.902767718841,132.902125852407,133.901483985973,134.900842119539,
135.900200253105,136.899558386671,137.898916520237,138.898274653803,139.897632787369,
140.896990920935,141.896349054501,142.895707188067,143.895065321633,144.894423455199,
145.893781588765,146.893139722331,147.892497855897,148.891855989463,149.891214123029,
150.890572256596,151.889930390162,152.889288523728,153.888646657294,154.88800479086,
155.887362924426,156.886721057992,157.886079191558,158.885437325124,159.88479545869,
160.884153592256,161.883511725822,162.882869859388,163.882227992954,164.88158612652,
165.880944260086,166.880302393652,167.879660527218,168.879018660784,169.87837679435,
170.877734927916,171.877093061483,172.876451195049,173.875809328615,174.875167462181,
175.874525595747,176.873883729313,177.873241862879,178.872599996445,179.871958130011,
180.871316263577,181.870674397143,182.870032530709,183.869390664275,184.868748797841,
185.868106931407,186.867465064973,187.866823198539,188.866181332105,189.865539465671,
190.864897599237,191.864255732803,192.86361386637,193.862971999936,194.862330133502,
195.861688267068,196.861046400634,197.8604045342,198.859762667766,199.859120801332,
200.858478934898,201.857837068464,202.85719520203,203.856553335596,204.855911469162,
205.855269602728,206.854627736294,207.85398586986,208.853344003426,209.852702136992,
210.852060270558,211.851418404124,212.85077653769,213.850134671257,214.849492804823,
215.848850938389,216.848209071955,217.847567205521,218.846925339087,219.846283472653,
220.845641606219,221.844999739785,222.844357873351,223.843716006917,224.843074140483,
225.842432274049,226.841790407615,227.841148541181,228.840506674747,229.839864808313,
230.839222941879,231.838581075445,232.837939209011,233.837297342577,234.836655476144,
235.83601360971,236.835371743276,237.834729876842,238.834088010408,239.833446143974,
240.83280427754,241.832162411106,242.831520544672,243.830878678238,244.830236811804,
245.82959494537,246.828953078936,247.828311212502,248.827669346068,249.827027479634,
250.8263856132,251.825743746766,252.825101880332,253.824460013898,254.823818147464,
255.82317628103,256.822534414597,257.821892548163,258.821250681729,259.820608815295,
260.819966948861,261.819325082427,262.818683215993,263.818041349559,264.817399483125,
265.816757616691,266.816115750257,267.815473883823,268.814832017389,269.814190150955,
270.813548284521,271.812906418087,272.812264551653,273.811622685219,274.810980818785,
275.810338952351,276.809697085917,277.809055219484,278.80841335305,279.807771486616,
280.807129620182,281.806487753748,282.805845887314,283.80520402088,284.804562154446,
285.803920288012,286.803278421578,287.802636555144,288.80199468871,289.801352822276,
290.800710955842,291.800069089408,292.799427222974,293.79878535654,294.798143490106,
295.797501623672,296.796859757238,297.796217890804,298.795576024371,299.794934157937,
300.794292291503,301.793650425069,302.793008558635,303.792366692201,304.791724825767,
305.791082959333,306.790441092899,307.789799226465,308.789157360031,309.788515493597,
310.787873627163,311.787231760729,312.786589894295,313.785948027861,314.785306161427,
315.784664294993,316.784022428559,317.783380562125,318.782738695691,319.782096829258,
320.781454962824,321.78081309639,322.780171229956,323.779529363522,324.778887497088,
325.778245630654,326.77760376422,327.776961897786,328.776320031352,329.775678164918,
330.775036298484,331.77439443205,332.773752565616,333.773110699182,334.772468832748,
335.771826966314,336.77118509988,337.770543233446,338.769901367012,339.769259500578,
340.768617634145,341.767975767711,342.767333901277,343.766692034843,344.766050168409,
345.765408301975,346.764766435541,347.764124569107,348.763482702673,349.762840836239,
350.762198969805,351.761557103371,352.760915236937,353.760273370503,354.259952437286,
354.759631504069,355.259310570852,355.758989637635,356.258668704418,356.758347771201,
357.258026837984,357.757705904767,358.25738497155,358.757064038333,359.256743105116,
359.756422171899,360.256101238682,360.755780305465,361.255459372248,361.755138439031,
362.254817505815,362.754496572598,363.254175639381,363.753854706164,364.253533772947,
364.75321283973,365.252891906513,365.752570973296,366.252250040079,366.751929106862,
367.251608173645,367.751287240428,368.250966307211,368.750645373994,369.250324440777,
369.75000350756,370.249682574343,370.749361641126,371.249040707909,371.748719774692,
372.248398841475,372.748077908258,373.247756975041,373.747436041824,374.247115108607,
374.74679417539,375.246473242173,375.746152308956,376.245831375739,376.745510442522,
377.245189509305,377.744868576088,378.244547642871,378.744226709654,379.243905776437,
379.74358484322,380.243263910003,380.742942976786,381.242622043569,381.742301110352,
382.241980177135,382.741659243918,383.241338310702,383.741017377485,384.240696444268,
384.740375511051,385.240054577834,385.739733644617,386.2394127114,386.739091778183,
387.238770844966,387.738449911749,388.238128978532,388.737808045315,389.237487112098,
389.737166178881,390.236845245664,390.736524312447,391.23620337923,391.735882446013,
392.235561512796,392.735240579579,393.234919646362,393.734598713145,394.234277779928,
394.733956846711,395.233635913494,395.733314980277,396.23299404706,396.732673113843,
397.232352180626,397.732031247409,398.231710314192,398.731389380975,399.231068447758,
399.730747514541,400.230426581324,400.730105648107,401.22978471489,401.729463781673,
402.229142848456,402.728821915239,403.228500982022,403.728180048805),
 .UNSPECIFIED.);
#18=B_SPLINE_SURFACE_WITH_KNOTS('',3,3,((#60196,#60197,#60198,#60199,#60200,
#60201,#60202,#60203,#60204,#60205,#60206,#60207,#60208,#60209,#60210,#60211,
#60212,#60213,#60214,#60215,#60216,#60217,#60218,#60219,#60220,#60221,#60222,
#60223,#60224,#60225,#60226,#60227,#60228,#60229,#60230,#60231,#60232,#60233,
#60234,#60235,#60236,#60237,#60238,#60239,#60240,#60241,#60242,#60243,#60244,
#60245,#60246,#60247,#60248,#60249,#60250,#60251,#60252,#60253,#60254,#60255,
#60256,#60257,#60258,#60259,#60260,#60261,#60262,#60263,#60264,#60265,#60266,
#60267,#60268,#60269,#60270,#60271,#60272,#60273,#60274,#60275,#60276,#60277,
#60278,#60279,#60280,#60281,#60282,#60283,#60284,#60285,#60286,#60287,#60288,
#60289,#60290,#60291,#60292,#60293,#60294,#60295,#60296,#60297,#60298,#60299,
#60300,#60301,#60302,#60303,#60304,#60305,#60306,#60307,#60308,#60309,#60310,
#60311,#60312,#60313,#60314,#60315,#60316,#60317,#60318,#60319,#60320,#60321,
#60322,#60323,#60324,#60325,#60326,#60327,#60328,#60329,#60330,#60331,#60332,
#60333,#60334,#60335,#60336,#60337,#60338,#60339,#60340,#60341,#60342,#60343,
#60344,#60345,#60346,#60347,#60348,#60349,#60350,#60351,#60352,#60353,#60354,
#60355,#60356,#60357,#60358,#60359,#60360,#60361,#60362,#60363,#60364,#60365,
#60366,#60367,#60368,#60369,#60370,#60371,#60372,#60373,#60374,#60375,#60376,
#60377,#60378,#60379,#60380,#60381,#60382,#60383,#60384,#60385,#60386,#60387,
#60388,#60389,#60390,#60391,#60392,#60393,#60394,#60395,#60396,#60397,#60398,
#60399,#60400,#60401,#60402,#60403,#60404,#60405,#60406,#60407,#60408,#60409,
#60410,#60411,#60412,#60413,#60414,#60415,#60416,#60417,#60418,#60419,#60420,
#60421,#60422,#60423,#60424,#60425,#60426,#60427,#60428,#60429,#60430,#60431,
#60432,#60433,#60434,#60435,#60436,#60437,#60438,#60439,#60440,#60441,#60442,
#60443,#60444,#60445,#60446,#60447,#60448,#60449,#60450,#60451,#60452,#60453,
#60454,#60455,#60456,#60457,#60458,#60459,#60460,#60461,#60462,#60463,#60464,
#60465,#60466,#60467,#60468,#60469,#60470,#60471,#60472,#60473,#60474,#60475,
#60476,#60477,#60478,#60479,#60480,#60481,#60482,#60483,#60484,#60485,#60486,
#60487,#60488,#60489,#60490,#60491,#60492,#60493,#60494,#60495,#60496,#60497,
#60498,#60499,#60500,#60501,#60502,#60503,#60504,#60505,#60506,#60507,#60508,
#60509,#60510,#60511,#60512,#60513,#60514,#60515,#60516,#60517,#60518,#60519,
#60520,#60521,#60522,#60523,#60524,#60525,#60526,#60527,#60528,#60529,#60530,
#60531,#60532,#60533,#60534,#60535,#60536,#60537,#60538,#60539,#60540,#60541,
#60542,#60543,#60544,#60545,#60546,#60547,#60548,#60549,#60550,#60551,#60552,
#60553,#60554,#60555,#60556,#60557,#60558,#60559,#60560,#60561,#60562,#60563,
#60564,#60565,#60566,#60567,#60568,#60569,#60570,#60571,#60572,#60573,#60574,
#60575,#60576,#60577,#60578,#60579,#60580,#60581,#60582,#60583,#60584,#60585,
#60586,#60587,#60588,#60589,#60590,#60591,#60592,#60593,#60594,#60595,#60596,
#60597,#60598,#60599,#60600,#60601,#60602,#60603,#60604,#60605,#60606,#60607,
#60608,#60609,#60610,#60611,#60612,#60613,#60614,#60615,#60616,#60617,#60618,
#60619,#60620,#60621,#60622,#60623,#60624,#60625,#60626,#60627,#60628,#60629,
#60630,#60631,#60632,#60633,#60634,#60635,#60636,#60637,#60638,#60639,#60640,
#60641,#60642,#60643,#60644,#60645,#60646,#60647,#60648,#60649,#60650,#60651,
#60652,#60653,#60654,#60655,#60656,#60657,#60658,#60659,#60660,#60661,#60662,
#60663,#60664,#60665,#60666,#60667,#60668,#60669,#60670,#60671,#60672,#60673,
#60674,#60675,#60676,#60677,#60678,#60679,#60680,#60681,#60682,#60683,#60684,
#60685,#60686,#60687,#60688,#60689,#60690,#60691,#60692,#60693),(#60694,
#60695,#60696,#60697,#60698,#60699,#60700,#60701,#60702,#60703,#60704,#60705,
#60706,#60707,#60708,#60709,#60710,#60711,#60712,#60713,#60714,#60715,#60716,
#60717,#60718,#60719,#60720,#60721,#60722,#60723,#60724,#60725,#60726,#60727,
#60728,#60729,#60730,#60731,#60732,#60733,#60734,#60735,#60736,#60737,#60738,
#60739,#60740,#60741,#60742,#60743,#60744,#60745,#60746,#60747,#60748,#60749,
#60750,#60751,#60752,#60753,#60754,#60755,#60756,#60757,#60758,#60759,#60760,
#60761,#60762,#60763,#60764,#60765,#60766,#60767,#60768,#60769,#60770,#60771,
#60772,#60773,#60774,#60775,#60776,#60777,#60778,#60779,#60780,#60781,#60782,
#60783,#60784,#60785,#60786,#60787,#60788,#60789,#60790,#60791,#60792,#60793,
#60794,#60795,#60796,#60797,#60798,#60799,#60800,#60801,#60802,#60803,#60804,
#60805,#60806,#60807,#60808,#60809,#60810,#60811,#60812,#60813,#60814,#60815,
#60816,#60817,#60818,#60819,#60820,#60821,#60822,#60823,#60824,#60825,#60826,
#60827,#60828,#60829,#60830,#60831,#60832,#60833,#60834,#60835,#60836,#60837,
#60838,#60839,#60840,#60841,#60842,#60843,#60844,#60845,#60846,#60847,#60848,
#60849,#60850,#60851,#60852,#60853,#60854,#60855,#60856,#60857,#60858,#60859,
#60860,#60861,#60862,#60863,#60864,#60865,#60866,#60867,#60868,#60869,#60870,
#60871,#60872,#60873,#60874,#60875,#60876,#60877,#60878,#60879,#60880,#60881,
#60882,#60883,#60884,#60885,#60886,#60887,#60888,#60889,#60890,#60891,#60892,
#60893,#60894,#60895,#60896,#60897,#60898,#60899,#60900,#60901,#60902,#60903,
#60904,#60905,#60906,#60907,#60908,#60909,#60910,#60911,#60912,#60913,#60914,
#60915,#60916,#60917,#60918,#60919,#60920,#60921,#60922,#60923,#60924,#60925,
#60926,#60927,#60928,#60929,#60930,#60931,#60932,#60933,#60934,#60935,#60936,
#60937,#60938,#60939,#60940,#60941,#60942,#60943,#60944,#60945,#60946,#60947,
#60948,#60949,#60950,#60951,#60952,#60953,#60954,#60955,#60956,#60957,#60958,
#60959,#60960,#60961,#60962,#60963,#60964,#60965,#60966,#60967,#60968,#60969,
#60970,#60971,#60972,#60973,#60974,#60975,#60976,#60977,#60978,#60979,#60980,
#60981,#60982,#60983,#60984,#60985,#60986,#60987,#60988,#60989,#60990,#60991,
#60992,#60993,#60994,#60995,#60996,#60997,#60998,#60999,#61000,#61001,#61002,
#61003,#61004,#61005,#61006,#61007,#61008,#61009,#61010,#61011,#61012,#61013,
#61014,#61015,#61016,#61017,#61018,#61019,#61020,#61021,#61022,#61023,#61024,
#61025,#61026,#61027,#61028,#61029,#61030,#61031,#61032,#61033,#61034,#61035,
#61036,#61037,#61038,#61039,#61040,#61041,#61042,#61043,#61044,#61045,#61046,
#61047,#61048,#61049,#61050,#61051,#61052,#61053,#61054,#61055,#61056,#61057,
#61058,#61059,#61060,#61061,#61062,#61063,#61064,#61065,#61066,#61067,#61068,
#61069,#61070,#61071,#61072,#61073,#61074,#61075,#61076,#61077,#61078,#61079,
#61080,#61081,#61082,#61083,#61084,#61085,#61086,#61087,#61088,#61089,#61090,
#61091,#61092,#61093,#61094,#61095,#61096,#61097,#61098,#61099,#61100,#61101,
#61102,#61103,#61104,#61105,#61106,#61107,#61108,#61109,#61110,#61111,#61112,
#61113,#61114,#61115,#61116,#61117,#61118,#61119,#61120,#61121,#61122,#61123,
#61124,#61125,#61126,#61127,#61128,#61129,#61130,#61131,#61132,#61133,#61134,
#61135,#61136,#61137,#61138,#61139,#61140,#61141,#61142,#61143,#61144,#61145,
#61146,#61147,#61148,#61149,#61150,#61151,#61152,#61153,#61154,#61155,#61156,
#61157,#61158,#61159,#61160,#61161,#61162,#61163,#61164,#61165,#61166,#61167,
#61168,#61169,#61170,#61171,#61172,#61173,#61174,#61175,#61176,#61177,#61178,
#61179,#61180,#61181,#61182,#61183,#61184,#61185,#61186,#61187,#61188,#61189,
#61190,#61191),(#61192,#61193,#61194,#61195,#61196,#61197,#61198,#61199,
#61200,#61201,#61202,#61203,#61204,#61205,#61206,#61207,#61208,#61209,#61210,
#61211,#61212,#61213,#61214,#61215,#61216,#61217,#61218,#61219,#61220,#61221,
#61222,#61223,#61224,#61225,#61226,#61227,#61228,#61229,#61230,#61231,#61232,
#61233,#61234,#61235,#61236,#61237,#61238,#61239,#61240,#61241,#61242,#61243,
#61244,#61245,#61246,#61247,#61248,#61249,#61250,#61251,#61252,#61253,#61254,
#61255,#61256,#61257,#61258,#61259,#61260,#61261,#61262,#61263,#61264,#61265,
#61266,#61267,#61268,#61269,#61270,#61271,#61272,#61273,#61274,#61275,#61276,
#61277,#61278,#61279,#61280,#61281,#61282,#61283,#61284,#61285,#61286,#61287,
#61288,#61289,#61290,#61291,#61292,#61293,#61294,#61295,#61296,#61297,#61298,
#61299,#61300,#61301,#61302,#61303,#61304,#61305,#61306,#61307,#61308,#61309,
#61310,#61311,#61312,#61313,#61314,#61315,#61316,#61317,#61318,#61319,#61320,
#61321,#61322,#61323,#61324,#61325,#61326,#61327,#61328,#61329,#61330,#61331,
#61332,#61333,#61334,#61335,#61336,#61337,#61338,#61339,#61340,#61341,#61342,
#61343,#61344,#61345,#61346,#61347,#61348,#61349,#61350,#61351,#61352,#61353,
#61354,#61355,#61356,#61357,#61358,#61359,#61360,#61361,#61362,#61363,#61364,
#61365,#61366,#61367,#61368,#61369,#61370,#61371,#61372,#61373,#61374,#61375,
#61376,#61377,#61378,#61379,#61380,#61381,#61382,#61383,#61384,#61385,#61386,
#61387,#61388,#61389,#61390,#61391,#61392,#61393,#61394,#61395,#61396,#61397,
#61398,#61399,#61400,#61401,#61402,#61403,#61404,#61405,#61406,#61407,#61408,
#61409,#61410,#61411,#61412,#61413,#61414,#61415,#61416,#61417,#61418,#61419,
#61420,#61421,#61422,#61423,#61424,#61425,#61426,#61427,#61428,#61429,#61430,
#61431,#61432,#61433,#61434,#61435,#61436,#61437,#61438,#61439,#61440,#61441,
#61442,#61443,#61444,#61445,#61446,#61447,#61448,#61449,#61450,#61451,#61452,
#61453,#61454,#61455,#61456,#61457,#61458,#61459,#61460,#61461,#61462,#61463,
#61464,#61465,#61466,#61467,#61468,#61469,#61470,#61471,#61472,#61473,#61474,
#61475,#61476,#61477,#61478,#61479,#61480,#61481,#61482,#61483,#61484,#61485,
#61486,#61487,#61488,#61489,#61490,#61491,#61492,#61493,#61494,#61495,#61496,
#61497,#61498,#61499,#61500,#61501,#61502,#61503,#61504,#61505,#61506,#61507,
#61508,#61509,#61510,#61511,#61512,#61513,#61514,#61515,#61516,#61517,#61518,
#61519,#61520,#61521,#61522,#61523,#61524,#61525,#61526,#61527,#61528,#61529,
#61530,#61531,#61532,#61533,#61534,#61535,#61536,#61537,#61538,#61539,#61540,
#61541,#61542,#61543,#61544,#61545,#61546,#61547,#61548,#61549,#61550,#61551,
#61552,#61553,#61554,#61555,#61556,#61557,#61558,#61559,#61560,#61561,#61562,
#61563,#61564,#61565,#61566,#61567,#61568,#61569,#61570,#61571,#61572,#61573,
#61574,#61575,#61576,#61577,#61578,#61579,#61580,#61581,#61582,#61583,#61584,
#61585,#61586,#61587,#61588,#61589,#61590,#61591,#61592,#61593,#61594,#61595,
#61596,#61597,#61598,#61599,#61600,#61601,#61602,#61603,#61604,#61605,#61606,
#61607,#61608,#61609,#61610,#61611,#61612,#61613,#61614,#61615,#61616,#61617,
#61618,#61619,#61620,#61621,#61622,#61623,#61624,#61625,#61626,#61627,#61628,
#61629,#61630,#61631,#61632,#61633,#61634,#61635,#61636,#61637,#61638,#61639,
#61640,#61641,#61642,#61643,#61644,#61645,#61646,#61647,#61648,#61649,#61650,
#61651,#61652,#61653,#61654,#61655,#61656,#61657,#61658,#61659,#61660,#61661,
#61662,#61663,#61664,#61665,#61666,#61667,#61668,#61669,#61670,#61671,#61672,
#61673,#61674,#61675,#61676,#61677,#61678,#61679,#61680,#61681,#61682,#61683,
#61684,#61685,#61686,#61687,#61688,#61689),(#61690,#61691,#61692,#61693,
#61694,#61695,#61696,#61697,#61698,#61699,#61700,#61701,#61702,#61703,#61704,
#61705,#61706,#61707,#61708,#61709,#61710,#61711,#61712,#61713,#61714,#61715,
#61716,#61717,#61718,#61719,#61720,#61721,#61722,#61723,#61724,#61725,#61726,
#61727,#61728,#61729,#61730,#61731,#61732,#61733,#61734,#61735,#61736,#61737,
#61738,#61739,#61740,#61741,#61742,#61743,#61744,#61745,#61746,#61747,#61748,
#61749,#61750,#61751,#61752,#61753,#61754,#61755,#61756,#61757,#61758,#61759,
#61760,#61761,#61762,#61763,#61764,#61765,#61766,#61767,#61768,#61769,#61770,
#61771,#61772,#61773,#61774,#61775,#61776,#61777,#61778,#61779,#61780,#61781,
#61782,#61783,#61784,#61785,#61786,#61787,#61788,#61789,#61790,#61791,#61792,
#61793,#61794,#61795,#61796,#61797,#61798,#61799,#61800,#61801,#61802,#61803,
#61804,#61805,#61806,#61807,#61808,#61809,#61810,#61811,#61812,#61813,#61814,
#61815,#61816,#61817,#61818,#61819,#61820,#61821,#61822,#61823,#61824,#61825,
#61826,#61827,#61828,#61829,#61830,#61831,#61832,#61833,#61834,#61835,#61836,
#61837,#61838,#61839,#61840,#61841,#61842,#61843,#61844,#61845,#61846,#61847,
#61848,#61849,#61850,#61851,#61852,#61853,#61854,#61855,#61856,#61857,#61858,
#61859,#61860,#61861,#61862,#61863,#61864,#61865,#61866,#61867,#61868,#61869,
#61870,#61871,#61872,#61873,#61874,#61875,#61876,#61877,#61878,#61879,#61880,
#61881,#61882,#61883,#61884,#61885,#61886,#61887,#61888,#61889,#61890,#61891,
#61892,#61893,#61894,#61895,#61896,#61897,#61898,#61899,#61900,#61901,#61902,
#61903,#61904,#61905,#61906,#61907,#61908,#61909,#61910,#61911,#61912,#61913,
#61914,#61915,#61916,#61917,#61918,#61919,#61920,#61921,#61922,#61923,#61924,
#61925,#61926,#61927,#61928,#61929,#61930,#61931,#61932,#61933,#61934,#61935,
#61936,#61937,#61938,#61939,#61940,#61941,#61942,#61943,#61944,#61945,#61946,
#61947,#61948,#61949,#61950,#61951,#61952,#61953,#61954,#61955,#61956,#61957,
#61958,#61959,#61960,#61961,#61962,#61963,#61964,#61965,#61966,#61967,#61968,
#61969,#61970,#61971,#61972,#61973,#61974,#61975,#61976,#61977,#61978,#61979,
#61980,#61981,#61982,#61983,#61984,#61985,#61986,#61987,#61988,#61989,#61990,
#61991,#61992,#61993,#61994,#61995,#61996,#61997,#61998,#61999,#62000,#62001,
#62002,#62003,#62004,#62005,#62006,#62007,#62008,#62009,#62010,#62011,#62012,
#62013,#62014,#62015,#62016,#62017,#62018,#62019,#62020,#62021,#62022,#62023,
#62024,#62025,#62026,#62027,#62028,#62029,#62030,#62031,#62032,#62033,#62034,
#62035,#62036,#62037,#62038,#62039,#62040,#62041,#62042,#62043,#62044,#62045,
#62046,#62047,#62048,#62049,#62050,#62051,#62052,#62053,#62054,#62055,#62056,
#62057,#62058,#62059,#62060,#62061,#62062,#62063,#62064,#62065,#62066,#62067,
#62068,#62069,#62070,#62071,#62072,#62073,#62074,#62075,#62076,#62077,#62078,
#62079,#62080,#62081,#62082,#62083,#62084,#62085,#62086,#62087,#62088,#62089,
#62090,#62091,#62092,#62093,#62094,#62095,#62096,#62097,#62098,#62099,#62100,
#62101,#62102,#62103,#62104,#62105,#62106,#62107,#62108,#62109,#62110,#62111,
#62112,#62113,#62114,#62115,#62116,#62117,#62118,#62119,#62120,#62121,#62122,
#62123,#62124,#62125,#62126,#62127,#62128,#62129,#62130,#62131,#62132,#62133,
#62134,#62135,#62136,#62137,#62138,#62139,#62140,#62141,#62142,#62143,#62144,
#62145,#62146,#62147,#62148,#62149,#62150,#62151,#62152,#62153,#62154,#62155,
#62156,#62157,#62158,#62159,#62160,#62161,#62162,#62163,#62164,#62165,#62166,
#62167,#62168,#62169,#62170,#62171,#62172,#62173,#62174,#62175,#62176,#62177,
#62178,#62179,#62180,#62181,#62182,#62183,#62184,#62185,#62186,#62187)),
 .UNSPECIFIED.,.F.,.F.,.F.,(4,4),(4,1,1,1,1,1,1,1,1,1,1,1,1,1,1,1,1,1,1,
1,1,1,1,1,1,1,1,1,1,1,1,1,1,1,1,1,1,1,1,1,1,1,1,1,1,1,1,1,1,1,1,1,1,1,1,
1,1,1,1,1,1,1,1,1,1,1,1,1,1,1,1,1,1,1,1,1,1,1,1,1,1,1,1,1,1,1,1,1,1,1,1,
1,1,1,1,1,1,1,1,1,1,1,1,1,1,1,1,1,1,1,1,1,1,1,1,1,1,1,1,1,1,1,1,1,1,1,1,
1,1,1,1,1,1,1,1,1,1,1,1,1,1,1,1,1,1,1,1,1,1,1,1,1,1,1,1,1,1,1,1,1,1,1,1,
1,1,1,1,1,1,1,1,1,1,1,1,1,1,1,1,1,1,1,1,1,1,1,1,1,1,1,1,1,1,1,1,1,1,1,1,
1,1,1,1,1,1,1,1,1,1,1,1,1,1,1,1,1,1,1,1,1,1,1,1,1,1,1,1,1,1,1,1,1,1,1,1,
1,1,1,1,1,1,1,1,1,1,1,1,1,1,1,1,1,1,1,1,1,1,1,1,1,1,1,1,1,1,1,1,1,1,1,1,
1,1,1,1,1,1,1,1,1,1,1,1,1,1,1,1,1,1,1,1,1,1,1,1,1,1,1,1,1,1,1,1,1,1,1,1,
1,1,1,1,1,1,1,1,1,1,1,1,1,1,1,1,1,1,1,1,1,1,1,1,1,1,1,1,1,1,1,1,1,1,1,1,
1,1,1,1,1,1,1,1,1,1,1,1,1,1,1,1,1,1,1,1,1,1,1,1,1,1,1,1,1,1,1,1,1,1,1,1,
1,1,1,1,1,1,1,1,1,1,1,1,1,1,1,1,1,1,1,1,1,1,1,1,1,1,1,1,1,1,1,1,1,1,1,1,
1,1,1,1,1,1,1,1,1,1,1,1,1,1,1,1,1,1,1,1,1,1,1,1,1,1,1,1,1,1,1,1,1,1,1,1,
1,1,1,1,1,1,1,1,1,1,1,1,1,1,1,1,1,1,1,1,1,1,1,1,1,1,1,1,1,1,1,1,1,1,1,1,
1,1,1,1,1,1,1,1,4),(0.,0.184512097253587),(12.0092477762453,12.5089268430284,
13.0086059098114,13.5082849765944,14.0079640433774,14.5076431101605,15.0073221769435,
15.5070012437265,16.0066803105095,16.5063593772925,17.0060384440756,17.5057175108586,
18.0053965776416,18.5050756444246,19.0047547112077,19.5044337779907,20.0041128447737,
20.5037919115567,21.0034709783398,21.5031500451228,22.0028291119058,22.5025081786888,
23.0021872454719,23.5018663122549,24.0015453790379,24.5012244458209,25.0009035126039,
25.500582579387,26.00026164617,26.499940712953,26.999619779736,27.4992988465191,
27.9989779133021,28.4986569800851,28.9983360468681,29.4980151136512,29.9976941804342,
30.4973732472172,30.9970523140002,31.4967313807832,31.9964104475663,32.4960895143493,
32.9957685811323,33.4954476479153,33.9951267146984,34.4948057814814,34.9944848482644,
35.4941639150474,35.9938429818305,36.4935220486135,36.9932011153965,37.4928801821795,
37.9925592489626,38.4922383157456,38.9919173825286,39.4915964493116,39.9912755160946,
40.4909545828777,40.9906336496607,41.4903127164437,41.9899917832267,42.4896708500098,
42.9893499167928,43.4890289835758,43.9887080503588,44.4883871171419,44.9880661839249,
45.4877452507079,45.9874243174909,46.4871033842739,46.986782451057,47.48646151784,
47.986140584623,48.485819651406,48.9854987181891,49.4851777849721,49.9848568517551,
50.4845359185381,50.9842149853212,51.4838940521042,51.9835731188872,52.4832521856702,
52.9829312524532,53.4826103192363,53.9822893860193,54.4819684528023,54.9816475195853,
55.4813265863684,55.9810056531514,56.4806847199344,56.9803637867174,57.4800428535005,
57.9797219202835,58.4794009870665,58.9790800538495,59.4787591206325,59.9784381874156,
60.4781172541986,60.9777963209816,61.4774753877646,61.9771544545477,62.9765125881137,
63.9758707216798,64.9752288552458,65.9745869888119,66.9739451223779,67.9733032559439,
68.97266138951,69.972019523076,70.9713776566421,71.9707357902081,72.9700939237742,
73.9694520573402,74.9688101909063,75.9681683244723,76.9675264580384,77.9668845916044,
78.9662427251705,79.9656008587365,80.9649589923026,81.9643171258686,82.9636752594347,
83.9630333930007,84.9623915265667,85.9617496601328,86.9611077936988,87.9604659272649,
88.9598240608309,89.959182194397,90.958540327963,91.9578984615291,92.9572565950951,
93.9566147286612,94.9559728622272,95.9553309957932,96.9546891293593,97.9540472629253,
98.9534053964914,99.9527635300574,100.952121663623,101.95147979719,102.950837930756,
103.950196064322,104.949554197888,105.948912331454,106.94827046502,107.947628598586,
108.946986732152,109.946344865718,110.945702999284,111.94506113285,112.944419266416,
113.943777399982,114.943135533548,115.942493667114,116.94185180068,117.941209934246,
118.940568067812,119.939926201378,120.939284334944,121.93864246851,122.938000602077,
123.937358735643,124.936716869209,125.936075002775,126.935433136341,127.934791269907,
128.934149403473,129.933507537039,130.932865670605,131.932223804171,132.931581937737,
133.930940071303,134.930298204869,135.929656338435,136.929014472001,137.928372605567,
138.927730739133,139.927088872699,140.926447006265,141.925805139831,142.925163273397,
143.924521406963,144.92387954053,145.923237674096,146.922595807662,147.921953941228,
148.921312074794,149.92067020836,150.920028341926,151.919386475492,152.918744609058,
153.918102742624,154.91746087619,155.916819009756,156.916177143322,157.915535276888,
158.914893410454,159.91425154402,160.913609677586,161.912967811152,162.912325944718,
163.911684078284,164.91104221185,165.910400345416,166.909758478983,167.909116612549,
168.908474746115,169.907832879681,170.907191013247,171.906549146813,172.905907280379,
173.905265413945,174.904623547511,175.903981681077,176.903339814643,177.902697948209,
178.902056081775,179.901414215341,180.900772348907,181.900130482473,182.899488616039,
183.898846749605,184.898204883171,185.897563016737,186.896921150303,187.89627928387,
188.895637417436,189.894995551002,190.894353684568,191.893711818134,192.8930699517,
193.892428085266,194.891786218832,195.891144352398,196.890502485964,197.88986061953,
198.889218753096,199.888576886662,200.887935020228,201.887293153794,202.88665128736,
203.886009420926,204.885367554492,205.884725688058,206.884083821624,207.88344195519,
208.882800088756,209.882158222323,210.881516355889,211.880874489455,212.880232623021,
213.879590756587,214.878948890153,215.878307023719,216.877665157285,217.877023290851,
218.876381424417,219.875739557983,220.875097691549,221.874455825115,222.873813958681,
223.873172092247,224.872530225813,225.871888359379,226.871246492945,227.870604626511,
228.869962760077,229.869320893643,230.86867902721,231.868037160776,232.867395294342,
233.866753427908,234.866111561474,235.86546969504,236.864827828606,237.864185962172,
238.863544095738,239.862902229304,240.86226036287,241.861618496436,242.860976630002,
243.860334763568,244.859692897134,245.8590510307,246.858409164266,247.857767297832,
248.857125431398,249.856483564964,250.85584169853,251.855199832097,252.854557965663,
253.853916099229,254.853274232795,255.852632366361,256.851990499927,257.851348633493,
258.850706767059,259.850064900625,260.849423034191,261.848781167757,262.848139301323,
263.847497434889,264.846855568455,265.846213702021,266.845571835587,267.844929969153,
268.844288102719,269.843646236285,270.843004369851,271.842362503417,272.841720636983,
273.84107877055,274.840436904116,275.839795037682,276.839153171248,277.838511304814,
278.83786943838,279.837227571946,280.836585705512,281.835943839078,282.835301972644,
283.83466010621,284.834018239776,285.833376373342,286.832734506908,287.832092640474,
288.83145077404,289.830808907606,290.830167041172,291.829525174738,292.828883308304,
293.82824144187,294.827599575437,295.826957709003,296.826315842569,297.825673976135,
298.825032109701,299.824390243267,300.823748376833,301.823106510399,302.822464643965,
303.821822777531,304.821180911097,305.820539044663,306.819897178229,307.819255311795,
308.818613445361,309.817971578927,310.817329712493,311.816687846059,312.816045979625,
313.815404113191,314.814762246757,315.814120380323,316.81347851389,317.812836647456,
318.812194781022,319.811552914588,320.810911048154,321.81026918172,322.809627315286,
323.808985448852,324.808343582418,325.807701715984,326.80705984955,327.806417983116,
328.805776116682,329.805134250248,330.804492383814,331.80385051738,332.803208650946,
333.802566784512,334.801924918078,335.801283051644,336.80064118521,337.799999318776,
338.799357452343,339.798715585909,340.798073719475,341.797431853041,342.796789986607,
343.796148120173,344.795506253739,345.794864387305,346.794222520871,347.793580654437,
348.792938788003,349.792296921569,350.791655055135,351.791013188701,352.790371322267,
353.789729455833,354.789087589399,355.788445722965,356.787803856531,357.287482923314,
357.787161990097,358.28684105688,358.786520123663,359.286199190446,359.78587825723,
360.285557324013,360.785236390796,361.284915457579,361.784594524362,362.284273591145,
362.783952657928,363.283631724711,363.783310791494,364.282989858277,364.78266892506,
365.282347991843,365.782027058626,366.281706125409,366.781385192192,367.281064258975,
367.780743325758,368.280422392541,368.780101459324,369.279780526107,369.77945959289,
370.279138659673,370.778817726456,371.278496793239,371.778175860022,372.277854926805,
372.777533993588,373.277213060371,373.776892127154,374.276571193937,374.77625026072,
375.275929327503,375.775608394286,376.275287461069,376.774966527852,377.274645594635,
377.774324661418,378.274003728201,378.773682794984,379.273361861767,379.77304092855,
380.272719995333,380.772399062117,381.2720781289,381.771757195683,382.271436262466,
382.771115329249,383.270794396032,383.770473462815,384.270152529598,384.769831596381,
385.269510663164,385.769189729947,386.26886879673,386.768547863513,387.268226930296,
387.767905997079,388.267585063862,388.767264130645,389.266943197428,389.766622264211,
390.266301330994,390.765980397777,391.26565946456,391.765338531343,392.265017598126,
392.764696664909,393.264375731692,393.764054798475,394.263733865258,394.763412932041,
395.263091998824,395.762771065607,396.26245013239,396.762129199173,397.261808265956,
397.761487332739,398.261166399522,398.760845466305,399.260524533088,399.760203599871,
400.259882666654,400.759561733437,401.25924080022,401.758919867003,402.258598933787,
402.75827800057,403.257957067353,403.757636134136,404.257315200919,404.756994267702,
405.256673334485,405.756352401268,406.256031468051,406.755710534834),
 .UNSPECIFIED.);
#1112=B_SPLINE_CURVE_WITH_KNOTS('',3,(#52628,#52629,#52630,#52631,#52632,
#52633,#52634,#52635,#52636,#52637,#52638,#52639,#52640,#52641,#52642,#52643,
#52644,#52645,#52646),.UNSPECIFIED.,.F.,.F.,(4,3,3,3,3,3,4),(-3.69871549170445,
-3.49775346748116,-2.99807440069814,-2.49839533391511,-1.99871626713209,
-1.49903720034907,-1.00018350866767),.UNSPECIFIED.);
#1113=B_SPLINE_CURVE_WITH_KNOTS('',3,(#52649,#52650,#52651,#52652),
 .UNSPECIFIED.,.F.,.F.,(4,4),(0.,0.443060670554495),.UNSPECIFIED.);
#1114=B_SPLINE_CURVE_WITH_KNOTS('',3,(#52657,#52658,#52659,#52660,#52661,
#52662,#52663,#52664,#52665,#52666,#52667,#52668,#52669,#52670,#52671,#52672,
#52673,#52674,#52675,#52676,#52677,#52678,#52679,#52680,#52681,#52682,#52683,
#52684,#52685,#52686,#52687,#52688,#52689,#52690,#52691,#52692,#52693,#52694,
#52695,#52696),.UNSPECIFIED.,.F.,.F.,(4,3,3,3,3,3,3,3,3,3,3,3,3,4),(-9.98190079888403,
-9.49390226887744,-8.99422320209442,-8.4945441353114,-7.99486506852837,
-7.49518600174535,-6.99550693496233,-6.4958278681793,-5.99614880139628,
-5.49646973461325,-4.99679066783023,-4.49711160104721,-3.99743253426419,
-3.69871549170445),.UNSPECIFIED.);
#1115=B_SPLINE_CURVE_WITH_KNOTS('',3,(#52697,#52698,#52699,#52700,#52701,
#52702,#52703,#52704,#52705,#52706,#52707,#52708,#52709,#52710,#52711,#52712,
#52713,#52714,#52715,#52716,#52717,#52718,#52719,#52720,#52721,#52722,#52723,
#52724,#52725,#52726,#52727,#52728,#52729,#52730,#52731,#52732,#52733,#52734,
#52735,#52736,#52737,#52738,#52739),.UNSPECIFIED.,.F.,.F.,(4,3,3,3,3,3,
3,3,3,3,3,3,3,3,4),(0.443060670554495,0.49967906678306,0.999358133566079,
1.4990372003491,1.99871626713212,2.49839533391514,2.99807440069816,3.49775346748117,
3.99743253426419,4.49711160104721,4.99679066783023,5.49646973461325,5.99614880139627,
6.49582786817929,6.72624597773408),.UNSPECIFIED.);
#1116=B_SPLINE_CURVE_WITH_KNOTS('',3,(#52744,#52745,#52746,#52747,#52748,
#52749,#52750,#52751,#52752,#52753,#52754,#52755,#52756,#52757,#52758,#52759,
#52760,#52761,#52762,#52763,#52764,#52765,#52766,#52767,#52768,#52769,#52770,
#52771,#52772,#52773,#52774,#52775,#52776,#52777,#52778,#52779,#52780,#52781,
#52782,#52783,#52784,#52785,#52786),.UNSPECIFIED.,.F.,.F.,(4,3,3,3,3,3,
3,3,3,3,3,3,3,3,4),(-16.2650861060636,-15.9897301370567,-15.4900510702737,
-14.9903720034907,-14.4906929367077,-13.9910138699247,-13.4913348031416,
-12.9916557363586,-12.4919766695756,-11.9922976027926,-11.4926185360095,
-10.9929394692265,-10.4932604024435,-9.99358133566046,-9.98190079888403),
 .UNSPECIFIED.);
#1117=B_SPLINE_CURVE_WITH_KNOTS('',3,(#52787,#52788,#52789,#52790,#52791,
#52792,#52793,#52794,#52795,#52796,#52797,#52798,#52799,#52800,#52801,#52802,
#52803,#52804,#52805,#52806,#52807,#52808,#52809,#52810,#52811,#52812,#52813,
#52814,#52815,#52816,#52817,#52818,#52819,#52820,#52821,#52822,#52823,#52824,
#52825,#52826,#52827,#52828,#52829),.UNSPECIFIED.,.F.,.F.,(4,3,3,3,3,3,
3,3,3,3,3,3,3,3,4),(6.72624597773408,6.99550693496231,7.49518600174534,
7.99486506852837,8.49454413531139,8.99422320209442,9.49390226887745,9.99358133566048,
10.4932604024435,10.9929394692265,11.4926185360096,11.9922976027926,12.4919766695756,
12.9916557363586,13.0094312849137),.UNSPECIFIED.);
#1118=B_SPLINE_CURVE_WITH_KNOTS('',3,(#52834,#52835,#52836,#52837,#52838,
#52839,#52840,#52841,#52842,#52843,#52844,#52845,#52846,#52847,#52848,#52849,
#52850,#52851,#52852,#52853,#52854,#52855,#52856,#52857,#52858,#52859,#52860,
#52861,#52862,#52863,#52864,#52865,#52866,#52867,#52868,#52869,#52870,#52871,
#52872,#52873,#52874,#52875,#52876),.UNSPECIFIED.,.F.,.F.,(4,3,3,3,3,3,
3,3,3,3,3,3,3,3,4),(-22.5482714132432,-22.485558005236,-21.985878938453,
-21.48619987167,-20.986520804887,-20.486841738104,-19.9871626713209,-19.4874836045379,
-18.9878045377549,-18.4881254709719,-17.9884464041888,-17.4887673374058,
-16.9890882706228,-16.4894092038398,-16.2650861060636),.UNSPECIFIED.);
#1119=B_SPLINE_CURVE_WITH_KNOTS('',3,(#52877,#52878,#52879,#52880,#52881,
#52882,#52883,#52884,#52885,#52886,#52887,#52888,#52889,#52890,#52891,#52892,
#52893,#52894,#52895,#52896,#52897,#52898,#52899,#52900,#52901,#52902,#52903,
#52904,#52905,#52906,#52907,#52908,#52909,#52910,#52911,#52912,#52913,#52914,
#52915,#52916),.UNSPECIFIED.,.F.,.F.,(4,3,3,3,3,3,3,3,3,3,3,3,3,4),(13.0094312849137,
13.4913348031417,13.9910138699247,14.4906929367077,14.9903720034907,15.4900510702737,
15.9897301370568,16.4894092038398,16.9890882706228,17.4887673374058,17.9884464041888,
18.4881254709718,18.9878045377549,19.2926165920933),.UNSPECIFIED.);
#1120=B_SPLINE_CURVE_WITH_KNOTS('',3,(#52921,#52922,#52923,#52924,#52925,
#52926,#52927,#52928,#52929,#52930,#52931,#52932,#52933,#52934,#52935,#52936,
#52937,#52938,#52939,#52940,#52941,#52942,#52943,#52944,#52945,#52946,#52947,
#52948,#52949,#52950,#52951,#52952,#52953,#52954,#52955,#52956,#52957,#52958,
#52959,#52960),.UNSPECIFIED.,.F.,.F.,(4,3,3,3,3,3,3,3,3,3,3,3,3,4),(-28.8314567204228,
-28.4817068066323,-27.9820277398493,-27.4823486730663,-26.9826696062833,
-26.4829905395002,-25.9833114727172,-25.4836324059342,-24.9839533391512,
-24.4842742723681,-23.9845952055851,-23.4849161388021,-22.9852370720191,
-22.5482714132432),.UNSPECIFIED.);
#1121=B_SPLINE_CURVE_WITH_KNOTS('',3,(#52961,#52962,#52963,#52964,#52965,
#52966,#52967,#52968,#52969,#52970,#52971,#52972,#52973,#52974,#52975,#52976,
#52977,#52978,#52979,#52980,#52981,#52982,#52983,#52984,#52985,#52986,#52987,
#52988,#52989,#52990,#52991,#52992,#52993,#52994,#52995,#52996,#52997,#52998,
#52999,#53000,#53001,#53002,#53003),.UNSPECIFIED.,.F.,.F.,(4,3,3,3,3,3,
3,3,3,3,3,3,3,3,4),(19.2926165920933,19.4874836045379,19.9871626713209,
20.4868417381039,20.986520804887,21.48619987167,21.985878938453,22.4855580052361,
22.9852370720191,23.4849161388021,23.9845952055851,24.4842742723682,24.9839533391512,
25.4836324059342,25.5758018992728),.UNSPECIFIED.);
#1122=B_SPLINE_CURVE_WITH_KNOTS('',3,(#53008,#53009,#53010,#53011,#53012,
#53013,#53014,#53015,#53016,#53017,#53018,#53019,#53020,#53021,#53022,#53023,
#53024,#53025,#53026,#53027,#53028,#53029,#53030,#53031,#53032,#53033,#53034,
#53035,#53036,#53037,#53038,#53039,#53040,#53041,#53042,#53043,#53044,#53045,
#53046,#53047,#53048,#53049,#53050),.UNSPECIFIED.,.F.,.F.,(4,3,3,3,3,3,
3,3,3,3,3,3,3,3,4),(-35.1146420276024,-34.9775346748116,-34.4778556080286,
-33.9781765412456,-33.4784974744626,-32.9788184076795,-32.4791393408965,
-31.9794602741135,-31.4797812073305,-30.9801021405474,-30.4804230737644,
-29.9807440069814,-29.4810649401984,-28.9813858734153,-28.8314567204228),
 .UNSPECIFIED.);
#1123=B_SPLINE_CURVE_WITH_KNOTS('',3,(#53051,#53052,#53053,#53054,#53055,
#53056,#53057,#53058,#53059,#53060,#53061,#53062,#53063,#53064,#53065,#53066,
#53067,#53068,#53069,#53070,#53071,#53072,#53073,#53074,#53075,#53076,#53077,
#53078,#53079,#53080,#53081,#53082,#53083,#53084,#53085,#53086,#53087,#53088,
#53089,#53090),.UNSPECIFIED.,.F.,.F.,(4,3,3,3,3,3,3,3,3,3,3,3,3,4),(25.5758018992728,
25.9833114727172,26.4829905395003,26.9826696062833,27.4823486730663,27.9820277398493,
28.4817068066324,28.9813858734154,29.4810649401984,29.9807440069814,30.4804230737645,
30.9801021405475,31.4797812073305,31.8589872064524),.UNSPECIFIED.);
#1124=B_SPLINE_CURVE_WITH_KNOTS('',3,(#53095,#53096,#53097,#53098,#53099,
#53100,#53101,#53102,#53103,#53104,#53105,#53106,#53107,#53108,#53109,#53110,
#53111,#53112,#53113,#53114,#53115,#53116,#53117,#53118,#53119,#53120,#53121,
#53122,#53123,#53124,#53125,#53126,#53127,#53128,#53129,#53130,#53131,#53132,
#53133,#53134),.UNSPECIFIED.,.F.,.F.,(4,3,3,3,3,3,3,3,3,3,3,3,3,4),(-41.397827334782,
-40.9736834762079,-40.4740044094249,-39.9743253426419,-39.4746462758588,
-38.9749672090758,-38.4752881422928,-37.9756090755098,-37.4759300087267,
-36.9762509419437,-36.4765718751607,-35.9768928083777,-35.4772137415947,
-35.1146420276024),.UNSPECIFIED.);
#1125=B_SPLINE_CURVE_WITH_KNOTS('',3,(#53135,#53136,#53137,#53138,#53139,
#53140,#53141,#53142,#53143,#53144,#53145,#53146,#53147,#53148,#53149,#53150,
#53151,#53152,#53153,#53154,#53155,#53156,#53157,#53158,#53159,#53160,#53161,
#53162,#53163,#53164,#53165,#53166,#53167,#53168,#53169,#53170,#53171,#53172,
#53173,#53174,#53175,#53176,#53177),.UNSPECIFIED.,.F.,.F.,(4,3,3,3,3,3,
3,3,3,3,3,3,3,3,4),(31.8589872064524,31.9794602741135,32.4791393408966,
32.9788184076796,33.4784974744626,33.9781765412456,34.4778556080286,34.9775346748117,
35.4772137415947,35.9768928083777,36.4765718751607,36.9762509419437,37.4759300087267,
37.9756090755098,38.142172513632),.UNSPECIFIED.);
#1126=B_SPLINE_CURVE_WITH_KNOTS('',3,(#53182,#53183,#53184,#53185,#53186,
#53187,#53188,#53189,#53190,#53191,#53192,#53193,#53194,#53195,#53196,#53197,
#53198,#53199,#53200,#53201,#53202,#53203,#53204,#53205,#53206,#53207,#53208,
#53209,#53210,#53211,#53212,#53213,#53214,#53215,#53216,#53217,#53218,#53219,
#53220,#53221,#53222,#53223,#53224),.UNSPECIFIED.,.F.,.F.,(4,3,3,3,3,3,
3,3,3,3,3,3,3,3,4),(-47.6810126419616,-47.4695113443872,-46.9698322776042,
-46.4701532108212,-45.9704741440381,-45.4707950772551,-44.9711160104721,
-44.4714369436891,-43.971757876906,-43.472078810123,-42.97239974334,-42.472720676557,
-41.973041609774,-41.4733625429909,-41.397827334782),.UNSPECIFIED.);
#1127=B_SPLINE_CURVE_WITH_KNOTS('',3,(#53225,#53226,#53227,#53228,#53229,
#53230,#53231,#53232,#53233,#53234,#53235,#53236,#53237,#53238,#53239,#53240,
#53241,#53242,#53243,#53244,#53245,#53246,#53247,#53248,#53249,#53250,#53251,
#53252,#53253,#53254,#53255,#53256,#53257,#53258,#53259,#53260,#53261,#53262,
#53263,#53264),.UNSPECIFIED.,.F.,.F.,(4,3,3,3,3,3,3,3,3,3,3,3,3,4),(38.142172513632,
38.4752881422928,38.9749672090758,39.4746462758589,39.9743253426419,40.4740044094249,
40.973683476208,41.473362542991,41.973041609774,42.472720676557,42.9723997433401,
43.4720788101231,43.9717578769061,44.4253578208116),.UNSPECIFIED.);
#1128=B_SPLINE_CURVE_WITH_KNOTS('',3,(#53269,#53270,#53271,#53272,#53273,
#53274,#53275,#53276,#53277,#53278,#53279,#53280,#53281,#53282,#53283,#53284,
#53285,#53286,#53287,#53288,#53289,#53290,#53291,#53292,#53293,#53294,#53295,
#53296),.UNSPECIFIED.,.F.,.F.,(4,3,3,3,3,3,3,3,3,4),(-53.9641979491412,
-52.9659810790005,-51.9666229454344,-50.9672648118684,-49.9679066783023,
-49.4682276115193,-48.9685485447363,-48.4688694779533,-47.9691904111702,
-47.6810126419616),.UNSPECIFIED.);
#1129=B_SPLINE_CURVE_WITH_KNOTS('',3,(#53297,#53298,#53299,#53300,#53301,
#53302,#53303,#53304,#53305,#53306,#53307,#53308,#53309,#53310,#53311,#53312,
#53313,#53314,#53315,#53316,#53317,#53318,#53319,#53320,#53321,#53322,#53323,
#53324,#53325,#53326,#53327,#53328,#53329,#53330,#53331,#53332,#53333,#53334,
#53335,#53336),.UNSPECIFIED.,.F.,.F.,(4,3,3,3,3,3,3,3,3,3,3,3,3,4),(44.4253578208116,
44.4714369436892,44.9711160104722,45.4707950772552,45.9704741440382,46.4701532108212,
46.9698322776042,47.4695113443873,47.9691904111703,48.4688694779533,48.9685485447363,
49.4682276115193,49.9679066783024,50.7085431279912),.UNSPECIFIED.);
#1130=B_SPLINE_CURVE_WITH_KNOTS('',3,(#53341,#53342,#53343,#53344,#53345,
#53346,#53347,#53348,#53349,#53350,#53351,#53352,#53353,#53354,#53355,#53356,
#53357,#53358,#53359,#53360,#53361,#53362),.UNSPECIFIED.,.F.,.F.,(4,3,3,
3,3,3,3,4),(-60.2473832563207,-59.9614880139628,-58.9621298803968,-57.9627717468307,
-56.9634136132647,-55.9640554796986,-54.9646973461326,-53.9641979491412),
 .UNSPECIFIED.);
#1131=B_SPLINE_CURVE_WITH_KNOTS('',3,(#53363,#53364,#53365,#53366,#53367,
#53368,#53369,#53370,#53371,#53372,#53373,#53374,#53375,#53376,#53377,#53378,
#53379,#53380,#53381,#53382,#53383,#53384,#53385,#53386,#53387),
 .UNSPECIFIED.,.F.,.F.,(4,3,3,3,3,3,3,3,4),(50.7085431279912,50.9672648118684,
51.9666229454345,52.9659810790005,53.9653392125666,54.9646973461326,55.9640554796987,
56.9634136132647,56.9917284351708),.UNSPECIFIED.);
#1132=B_SPLINE_CURVE_WITH_KNOTS('',3,(#53392,#53393,#53394,#53395,#53396,
#53397,#53398,#53399,#53400,#53401,#53402,#53403,#53404,#53405,#53406,#53407,
#53408,#53409,#53410,#53411,#53412,#53413),.UNSPECIFIED.,.F.,.F.,(4,3,3,
3,3,3,3,4),(-66.5305685635003,-65.9576368153591,-64.958278681793,-63.958920548227,
-62.9595624146609,-61.9602042810949,-60.9608461475288,-60.2473832563207),
 .UNSPECIFIED.);
#1133=B_SPLINE_CURVE_WITH_KNOTS('',3,(#53414,#53415,#53416,#53417,#53418,
#53419,#53420,#53421,#53422,#53423,#53424,#53425,#53426,#53427,#53428,#53429,
#53430,#53431,#53432,#53433,#53434,#53435),.UNSPECIFIED.,.F.,.F.,(4,3,3,
3,3,3,3,4),(56.9917284351708,57.9627717468308,58.9621298803968,59.9614880139629,
60.9608461475289,61.960204281095,62.959562414661,63.2749137423504),
 .UNSPECIFIED.);
#1134=B_SPLINE_CURVE_WITH_KNOTS('',3,(#53440,#53441,#53442,#53443,#53444,
#53445,#53446,#53447,#53448,#53449,#53450,#53451,#53452,#53453,#53454,#53455,
#53456,#53457,#53458,#53459,#53460,#53461),.UNSPECIFIED.,.F.,.F.,(4,3,3,
3,3,3,3,4),(-72.8137538706799,-71.9537856167554,-70.9544274831893,-69.9550693496233,
-68.9557112160572,-67.9563530824912,-66.9569949489251,-66.5305685635003),
 .UNSPECIFIED.);
#1135=B_SPLINE_CURVE_WITH_KNOTS('',3,(#53462,#53463,#53464,#53465,#53466,
#53467,#53468,#53469,#53470,#53471,#53472,#53473,#53474,#53475,#53476,#53477,
#53478,#53479,#53480,#53481,#53482,#53483),.UNSPECIFIED.,.F.,.F.,(4,3,3,
3,3,3,3,4),(63.2749137423504,63.958920548227,64.9582786817931,65.9576368153591,
66.9569949489252,67.9563530824912,68.9557112160573,69.55809904953),
 .UNSPECIFIED.);
#1136=B_SPLINE_CURVE_WITH_KNOTS('',3,(#53488,#53489,#53490,#53491,#53492,
#53493,#53494,#53495,#53496,#53497,#53498,#53499,#53500,#53501,#53502,#53503,
#53504,#53505,#53506,#53507,#53508,#53509,#53510,#53511,#53512),
 .UNSPECIFIED.,.F.,.F.,(4,3,3,3,3,3,3,3,4),(-79.0969391778595,-78.9492925517177,
-77.9499344181516,-76.9505762845856,-75.9512181510195,-74.9518600174535,
-73.9525018838875,-72.9531437503214,-72.8137538706799),.UNSPECIFIED.);
#1137=B_SPLINE_CURVE_WITH_KNOTS('',3,(#53513,#53514,#53515,#53516,#53517,
#53518,#53519,#53520,#53521,#53522,#53523,#53524,#53525,#53526,#53527,#53528,
#53529,#53530,#53531,#53532,#53533,#53534),.UNSPECIFIED.,.F.,.F.,(4,3,3,
3,3,3,3,4),(69.55809904953,69.9550693496233,70.9544274831893,71.9537856167554,
72.9531437503215,73.9525018838875,74.9518600174536,75.8412843567096),
 .UNSPECIFIED.);
#1138=B_SPLINE_CURVE_WITH_KNOTS('',3,(#53539,#53540,#53541,#53542,#53543,
#53544,#53545,#53546,#53547,#53548,#53549,#53550,#53551,#53552,#53553,#53554,
#53555,#53556,#53557,#53558,#53559,#53560),.UNSPECIFIED.,.F.,.F.,(4,3,3,
3,3,3,3,4),(-85.3801244850391,-84.945441353114,-83.9460832195479,-82.9467250859819,
-81.9473669524158,-80.9480088188498,-79.9486506852837,-79.0969391778595),
 .UNSPECIFIED.);
#1139=B_SPLINE_CURVE_WITH_KNOTS('',3,(#53561,#53562,#53563,#53564,#53565,
#53566,#53567,#53568,#53569,#53570,#53571,#53572,#53573,#53574,#53575,#53576,
#53577,#53578,#53579,#53580,#53581,#53582,#53583,#53584,#53585),
 .UNSPECIFIED.,.F.,.F.,(4,3,3,3,3,3,3,3,4),(75.8412843567096,75.9512181510196,
76.9505762845857,77.9499344181517,78.9492925517178,79.9486506852838,80.9480088188499,
81.9473669524159,82.1244696638892),.UNSPECIFIED.);
#1140=B_SPLINE_CURVE_WITH_KNOTS('',3,(#53590,#53591,#53592,#53593,#53594,
#53595,#53596,#53597,#53598,#53599,#53600,#53601,#53602,#53603,#53604,#53605,
#53606,#53607,#53608,#53609,#53610,#53611),.UNSPECIFIED.,.F.,.F.,(4,3,3,
3,3,3,3,4),(-91.6633097922187,-90.9415901545102,-89.9422320209442,-88.9428738873782,
-87.9435157538121,-86.944157620246,-85.94479948668,-85.3801244850391),
 .UNSPECIFIED.);
#1141=B_SPLINE_CURVE_WITH_KNOTS('',3,(#53612,#53613,#53614,#53615,#53616,
#53617,#53618,#53619,#53620,#53621,#53622,#53623,#53624,#53625,#53626,#53627,
#53628,#53629,#53630,#53631,#53632,#53633),.UNSPECIFIED.,.F.,.F.,(4,3,3,
3,3,3,3,4),(82.1244696638892,82.946725085982,83.946083219548,84.9454413531141,
85.9447994866801,86.9441576202461,87.9435157538122,88.4076549710687),
 .UNSPECIFIED.);
#1142=B_SPLINE_CURVE_WITH_KNOTS('',3,(#53638,#53639,#53640,#53641,#53642,
#53643,#53644,#53645,#53646,#53647,#53648,#53649,#53650,#53651,#53652,#53653,
#53654,#53655,#53656,#53657,#53658,#53659,#53660,#53661,#53662),
 .UNSPECIFIED.,.F.,.F.,(4,3,3,3,3,3,3,3,4),(-97.9464950993983,-97.9370970894726,
-96.9377389559065,-95.9383808223405,-94.9390226887744,-93.9396645552084,
-92.9403064216423,-91.9409482880763,-91.6633097922187),.UNSPECIFIED.);
#1143=B_SPLINE_CURVE_WITH_KNOTS('',3,(#53663,#53664,#53665,#53666,#53667,
#53668,#53669,#53670,#53671,#53672,#53673,#53674,#53675,#53676,#53677,#53678,
#53679,#53680,#53681,#53682,#53683,#53684),.UNSPECIFIED.,.F.,.F.,(4,3,3,
3,3,3,3,4),(88.4076549710687,88.9428738873782,89.9422320209442,90.9415901545103,
91.9409482880763,92.9403064216424,93.9396645552084,94.6908402782483),
 .UNSPECIFIED.);
#1144=B_SPLINE_CURVE_WITH_KNOTS('',3,(#53689,#53690,#53691,#53692,#53693,
#53694,#53695,#53696,#53697,#53698,#53699,#53700,#53701,#53702,#53703,#53704,
#53705,#53706,#53707,#53708,#53709,#53710),.UNSPECIFIED.,.F.,.F.,(4,3,3,
3,3,3,3,4),(-104.229680406578,-103.933245890869,-102.933887757303,-101.934529623737,
-100.935171490171,-99.9358133566047,-98.9364552230386,-97.9464950993983),
 .UNSPECIFIED.);
#1145=B_SPLINE_CURVE_WITH_KNOTS('',3,(#53711,#53712,#53713,#53714,#53715,
#53716,#53717,#53718,#53719,#53720,#53721,#53722,#53723,#53724,#53725,#53726,
#53727,#53728,#53729,#53730,#53731,#53732,#53733,#53734,#53735),
 .UNSPECIFIED.,.F.,.F.,(4,3,3,3,3,3,3,3,4),(94.6908402782483,94.9390226887745,
95.9383808223405,96.9377389559065,97.9370970894726,98.9364552230386,99.9358133566047,
100.935171490171,100.974025585428),.UNSPECIFIED.);
#1146=B_SPLINE_CURVE_WITH_KNOTS('',3,(#53740,#53741,#53742,#53743,#53744,
#53745,#53746,#53747,#53748,#53749,#53750,#53751,#53752,#53753,#53754,#53755,
#53756,#53757,#53758,#53759,#53760,#53761),.UNSPECIFIED.,.F.,.F.,(4,3,3,
3,3,3,3,4),(-110.512865713757,-109.929394692265,-108.930036558699,-107.930678425133,
-106.931320291567,-105.931962158001,-104.932604024435,-104.229680406578),
 .UNSPECIFIED.);
#1147=B_SPLINE_CURVE_WITH_KNOTS('',3,(#53762,#53763,#53764,#53765,#53766,
#53767,#53768,#53769,#53770,#53771,#53772,#53773,#53774,#53775,#53776,#53777,
#53778,#53779,#53780,#53781,#53782,#53783),.UNSPECIFIED.,.F.,.F.,(4,3,3,
3,3,3,3,4),(100.974025585428,101.934529623737,102.933887757303,103.933245890869,
104.932604024435,105.931962158001,106.931320291567,107.257210892608),
 .UNSPECIFIED.);
#1148=B_SPLINE_CURVE_WITH_KNOTS('',3,(#53788,#53789,#53790,#53791,#53792,
#53793,#53794,#53795,#53796,#53797,#53798,#53799,#53800,#53801,#53802,#53803,
#53804,#53805,#53806,#53807,#53808,#53809),.UNSPECIFIED.,.F.,.F.,(4,3,3,
3,3,3,3,4),(-116.796051020937,-115.925543493661,-114.926185360095,-113.926827226529,
-112.927469092963,-111.928110959397,-110.928752825831,-110.512865713757),
 .UNSPECIFIED.);
#1149=B_SPLINE_CURVE_WITH_KNOTS('',3,(#53810,#53811,#53812,#53813,#53814,
#53815,#53816,#53817,#53818,#53819,#53820,#53821,#53822,#53823,#53824,#53825,
#53826,#53827,#53828,#53829,#53830,#53831),.UNSPECIFIED.,.F.,.F.,(4,3,3,
3,3,3,3,4),(107.257210892608,107.930678425133,108.930036558699,109.929394692265,
110.928752825831,111.928110959397,112.927469092963,113.540396199787),
 .UNSPECIFIED.);
#1150=B_SPLINE_CURVE_WITH_KNOTS('',3,(#53836,#53837,#53838,#53839,#53840,
#53841,#53842,#53843,#53844,#53845,#53846,#53847,#53848,#53849,#53850,#53851,
#53852,#53853,#53854,#53855,#53856,#53857,#53858,#53859,#53860),
 .UNSPECIFIED.,.F.,.F.,(4,3,3,3,3,3,3,3,4),(-123.079236328117,-122.921050428624,
-121.921692295058,-120.922334161492,-119.922976027926,-118.92361789436,
-117.924259760793,-116.924901627227,-116.796051020937),.UNSPECIFIED.);
#1151=B_SPLINE_CURVE_WITH_KNOTS('',3,(#53861,#53862,#53863,#53864,#53865,
#53866,#53867,#53868,#53869,#53870,#53871,#53872,#53873,#53874,#53875,#53876,
#53877,#53878,#53879,#53880,#53881,#53882),.UNSPECIFIED.,.F.,.F.,(4,3,3,
3,3,3,3,4),(113.540396199787,113.926827226529,114.926185360095,115.925543493661,
116.924901627228,117.924259760794,118.92361789436,119.823581506967),
 .UNSPECIFIED.);
#1152=B_SPLINE_CURVE_WITH_KNOTS('',3,(#53887,#53888,#53889,#53890,#53891,
#53892,#53893,#53894,#53895,#53896,#53897,#53898,#53899,#53900,#53901,#53902,
#53903,#53904,#53905,#53906,#53907,#53908),.UNSPECIFIED.,.F.,.F.,(4,3,3,
3,3,3,3,4),(-129.362421635296,-128.91719923002,-127.917841096454,-126.918482962888,
-125.919124829322,-124.919766695756,-123.92040856219,-123.079236328117),
 .UNSPECIFIED.);
#1153=B_SPLINE_CURVE_WITH_KNOTS('',3,(#53909,#53910,#53911,#53912,#53913,
#53914,#53915,#53916,#53917,#53918,#53919,#53920,#53921,#53922,#53923,#53924,
#53925,#53926,#53927,#53928,#53929,#53930,#53931,#53932,#53933),
 .UNSPECIFIED.,.F.,.F.,(4,3,3,3,3,3,3,3,4),(119.823581506967,119.922976027926,
120.922334161492,121.921692295058,122.921050428624,123.92040856219,124.919766695756,
125.919124829322,126.106766814146),.UNSPECIFIED.);
#1154=B_SPLINE_CURVE_WITH_KNOTS('',3,(#53938,#53939,#53940,#53941,#53942,
#53943,#53944,#53945,#53946,#53947,#53948,#53949,#53950,#53951,#53952,#53953,
#53954,#53955,#53956,#53957,#53958,#53959),.UNSPECIFIED.,.F.,.F.,(4,3,3,
3,3,3,3,4),(-135.645606942476,-134.913348031416,-133.91398989785,-132.914631764284,
-131.915273630718,-130.915915497152,-129.916557363586,-129.362421635296),
 .UNSPECIFIED.);
#1155=B_SPLINE_CURVE_WITH_KNOTS('',3,(#53960,#53961,#53962,#53963,#53964,
#53965,#53966,#53967,#53968,#53969,#53970,#53971,#53972,#53973,#53974,#53975,
#53976,#53977,#53978,#53979,#53980,#53981),.UNSPECIFIED.,.F.,.F.,(4,3,3,
3,3,3,3,4),(126.106766814146,126.918482962888,127.917841096454,128.91719923002,
129.916557363586,130.915915497152,131.915273630718,132.389952121326),
 .UNSPECIFIED.);
#1156=B_SPLINE_CURVE_WITH_KNOTS('',3,(#53986,#53987,#53988,#53989,#53990,
#53991,#53992,#53993,#53994,#53995,#53996,#53997,#53998,#53999,#54000,#54001,
#54002,#54003,#54004,#54005,#54006,#54007,#54008,#54009,#54010),
 .UNSPECIFIED.,.F.,.F.,(4,3,3,3,3,3,3,3,4),(-141.928792249655,-141.908854966379,
-140.909496832813,-139.910138699247,-138.91078056568,-137.911422432114,
-136.912064298548,-135.912706164982,-135.645606942476),.UNSPECIFIED.);
#1157=B_SPLINE_CURVE_WITH_KNOTS('',3,(#54011,#54012,#54013,#54014,#54015,
#54016,#54017,#54018,#54019,#54020,#54021,#54022,#54023,#54024,#54025,#54026,
#54027,#54028,#54029,#54030,#54031,#54032),.UNSPECIFIED.,.F.,.F.,(4,3,3,
3,3,3,3,4),(132.389952121326,132.914631764284,133.91398989785,134.913348031416,
135.912706164982,136.912064298549,137.911422432115,138.673137428505),
 .UNSPECIFIED.);
#1158=B_SPLINE_CURVE_WITH_KNOTS('',3,(#54037,#54038,#54039,#54040,#54041,
#54042,#54043,#54044,#54045,#54046,#54047,#54048,#54049,#54050,#54051,#54052,
#54053,#54054,#54055,#54056,#54057,#54058),.UNSPECIFIED.,.F.,.F.,(4,3,3,
3,3,3,3,4),(-148.211977556835,-147.905003767775,-146.905645634209,-145.906287500643,
-144.906929367077,-143.907571233511,-142.908213099945,-141.928792249655),
 .UNSPECIFIED.);
#1159=B_SPLINE_CURVE_WITH_KNOTS('',3,(#54059,#54060,#54061,#54062,#54063,
#54064,#54065,#54066,#54067,#54068,#54069,#54070,#54071,#54072,#54073,#54074,
#54075,#54076,#54077,#54078,#54079,#54080,#54081,#54082,#54083),
 .UNSPECIFIED.,.F.,.F.,(4,3,3,3,3,3,3,3,4),(138.673137428505,138.910780565681,
139.910138699247,140.909496832813,141.908854966379,142.908213099945,143.907571233511,
144.906929367077,144.956322735685),.UNSPECIFIED.);
#1160=B_SPLINE_CURVE_WITH_KNOTS('',3,(#54088,#54089,#54090,#54091,#54092,
#54093,#54094,#54095,#54096,#54097,#54098,#54099,#54100,#54101,#54102,#54103,
#54104,#54105,#54106,#54107,#54108,#54109),.UNSPECIFIED.,.F.,.F.,(4,3,3,
3,3,3,3,4),(-154.495162864015,-153.901152569171,-152.901794435605,-151.902436302039,
-150.903078168473,-149.903720034907,-148.904361901341,-148.211977556835),
 .UNSPECIFIED.);
#1161=B_SPLINE_CURVE_WITH_KNOTS('',3,(#54110,#54111,#54112,#54113,#54114,
#54115,#54116,#54117,#54118,#54119,#54120,#54121,#54122,#54123,#54124,#54125,
#54126,#54127,#54128,#54129,#54130,#54131),.UNSPECIFIED.,.F.,.F.,(4,3,3,
3,3,3,3,4),(144.956322735685,145.906287500643,146.905645634209,147.905003767775,
148.904361901341,149.903720034907,150.903078168473,151.239508042865),
 .UNSPECIFIED.);
#1162=B_SPLINE_CURVE_WITH_KNOTS('',3,(#54136,#54137,#54138,#54139,#54140,
#54141,#54142,#54143,#54144,#54145,#54146,#54147,#54148,#54149,#54150,#54151,
#54152,#54153,#54154,#54155,#54156,#54157),.UNSPECIFIED.,.F.,.F.,(4,3,3,
3,3,3,3,4),(-160.778348171194,-159.897301370567,-158.897943237001,-157.898585103435,
-156.899226969869,-155.899868836303,-154.900510702737,-154.495162864015),
 .UNSPECIFIED.);
#1163=B_SPLINE_CURVE_WITH_KNOTS('',3,(#54158,#54159,#54160,#54161,#54162,
#54163,#54164,#54165,#54166,#54167,#54168,#54169,#54170,#54171,#54172,#54173,
#54174,#54175,#54176,#54177,#54178,#54179),.UNSPECIFIED.,.F.,.F.,(4,3,3,
3,3,3,3,4),(151.239508042865,151.902436302039,152.901794435605,153.901152569171,
154.900510702737,155.899868836303,156.899226969869,157.522693350044),
 .UNSPECIFIED.);
#1164=B_SPLINE_CURVE_WITH_KNOTS('',3,(#54184,#54185,#54186,#54187,#54188,
#54189,#54190,#54191,#54192,#54193,#54194,#54195,#54196,#54197,#54198,#54199,
#54200,#54201,#54202,#54203,#54204,#54205,#54206,#54207,#54208),
 .UNSPECIFIED.,.F.,.F.,(4,3,3,3,3,3,3,3,4),(-167.061533478374,-166.89280830553,
-165.893450171964,-164.894092038398,-163.894733904832,-162.895375771266,
-161.8960176377,-160.896659504134,-160.778348171194),.UNSPECIFIED.);
#1165=B_SPLINE_CURVE_WITH_KNOTS('',3,(#54209,#54210,#54211,#54212,#54213,
#54214,#54215,#54216,#54217,#54218,#54219,#54220,#54221,#54222,#54223,#54224,
#54225,#54226,#54227,#54228,#54229,#54230),.UNSPECIFIED.,.F.,.F.,(4,3,3,
3,3,3,3,4),(157.522693350044,157.898585103435,158.897943237002,159.897301370568,
160.896659504134,161.8960176377,162.895375771266,163.805878657224),
 .UNSPECIFIED.);
#1166=B_SPLINE_CURVE_WITH_KNOTS('',3,(#54235,#54236,#54237,#54238,#54239,
#54240,#54241,#54242,#54243,#54244,#54245,#54246,#54247,#54248,#54249,#54250,
#54251,#54252,#54253,#54254,#54255,#54256),.UNSPECIFIED.,.F.,.F.,(4,3,3,
3,3,3,3,4),(-173.344718785553,-172.888957106926,-171.88959897336,-170.890240839794,
-169.890882706228,-168.891524572662,-167.892166439096,-167.061533478374),
 .UNSPECIFIED.);
#1167=B_SPLINE_CURVE_WITH_KNOTS('',3,(#54257,#54258,#54259,#54260,#54261,
#54262,#54263,#54264,#54265,#54266,#54267,#54268,#54269,#54270,#54271,#54272,
#54273,#54274,#54275,#54276,#54277,#54278,#54279,#54280,#54281),
 .UNSPECIFIED.,.F.,.F.,(4,3,3,3,3,3,3,3,4),(163.805878657224,163.894733904832,
164.894092038398,165.893450171964,166.89280830553,167.892166439096,168.891524572662,
169.890882706228,170.089063964403),.UNSPECIFIED.);
#1168=B_SPLINE_CURVE_WITH_KNOTS('',3,(#54286,#54287,#54288,#54289,#54290,
#54291,#54292,#54293,#54294,#54295,#54296,#54297,#54298,#54299,#54300,#54301,
#54302,#54303,#54304,#54305,#54306,#54307),.UNSPECIFIED.,.F.,.F.,(4,3,3,
3,3,3,3,4),(-179.627904092733,-178.885105908322,-177.885747774756,-176.88638964119,
-175.887031507624,-174.887673374058,-173.888315240492,-173.344718785553),
 .UNSPECIFIED.);
#1169=B_SPLINE_CURVE_WITH_KNOTS('',3,(#54308,#54309,#54310,#54311,#54312,
#54313,#54314,#54315,#54316,#54317,#54318,#54319,#54320,#54321,#54322,#54323,
#54324,#54325,#54326,#54327,#54328,#54329),.UNSPECIFIED.,.F.,.F.,(4,3,3,
3,3,3,3,4),(170.089063964403,170.890240839794,171.88959897336,172.888957106926,
173.888315240492,174.887673374058,175.887031507624,176.372249271583),
 .UNSPECIFIED.);
#1170=B_SPLINE_CURVE_WITH_KNOTS('',3,(#54334,#54335,#54336,#54337,#54338,
#54339,#54340,#54341,#54342,#54343,#54344,#54345,#54346,#54347,#54348,#54349,
#54350,#54351,#54352,#54353,#54354,#54355,#54356,#54357,#54358),
 .UNSPECIFIED.,.F.,.F.,(4,3,3,3,3,3,3,3,4),(-185.911089399912,-185.880612843285,
-184.881254709719,-183.881896576153,-182.882538442587,-181.88318030902,
-180.883822175454,-179.884464041888,-179.627904092733),.UNSPECIFIED.);
#1171=B_SPLINE_CURVE_WITH_KNOTS('',3,(#54359,#54360,#54361,#54362,#54363,
#54364,#54365,#54366,#54367,#54368,#54369,#54370,#54371,#54372,#54373,#54374,
#54375,#54376,#54377,#54378,#54379,#54380),.UNSPECIFIED.,.F.,.F.,(4,3,3,
3,3,3,3,4),(176.372249271583,176.88638964119,177.885747774756,178.885105908322,
179.884464041889,180.883822175455,181.883180309021,182.655434578762),
 .UNSPECIFIED.);
#1172=B_SPLINE_CURVE_WITH_KNOTS('',3,(#54385,#54386,#54387,#54388,#54389,
#54390,#54391,#54392,#54393,#54394,#54395,#54396,#54397,#54398,#54399,#54400,
#54401,#54402,#54403,#54404,#54405,#54406),.UNSPECIFIED.,.F.,.F.,(4,3,3,
3,3,3,3,4),(-192.194274707092,-191.876761644681,-190.877403511115,-189.878045377549,
-188.878687243983,-187.879329110417,-186.879970976851,-185.911089399912),
 .UNSPECIFIED.);
#1173=B_SPLINE_CURVE_WITH_KNOTS('',3,(#54407,#54408,#54409,#54410,#54411,
#54412,#54413,#54414,#54415,#54416,#54417,#54418,#54419,#54420,#54421,#54422,
#54423,#54424,#54425,#54426,#54427,#54428,#54429,#54430,#54431),
 .UNSPECIFIED.,.F.,.F.,(4,3,3,3,3,3,3,3,4),(182.655434578762,182.882538442587,
183.881896576153,184.881254709719,185.880612843285,186.879970976851,187.879329110417,
188.878687243983,188.938619885942),.UNSPECIFIED.);
#1174=B_SPLINE_CURVE_WITH_KNOTS('',3,(#54436,#54437,#54438,#54439,#54440,
#54441,#54442,#54443,#54444,#54445,#54446,#54447,#54448,#54449,#54450,#54451,
#54452,#54453,#54454,#54455,#54456,#54457),.UNSPECIFIED.,.F.,.F.,(4,3,3,
3,3,3,3,4),(-198.477460014271,-197.872910446077,-196.873552312511,-195.874194178945,
-194.874836045379,-193.875477911813,-192.876119778247,-192.194274707092),
 .UNSPECIFIED.);
#1175=B_SPLINE_CURVE_WITH_KNOTS('',3,(#54458,#54459,#54460,#54461,#54462,
#54463,#54464,#54465,#54466,#54467,#54468,#54469,#54470,#54471,#54472,#54473,
#54474,#54475,#54476,#54477,#54478,#54479),.UNSPECIFIED.,.F.,.F.,(4,3,3,
3,3,3,3,4),(188.938619885942,189.878045377549,190.877403511115,191.876761644681,
192.876119778247,193.875477911813,194.874836045379,195.221805193122),
 .UNSPECIFIED.);
#1176=B_SPLINE_CURVE_WITH_KNOTS('',3,(#54484,#54485,#54486,#54487,#54488,
#54489,#54490,#54491,#54492,#54493,#54494,#54495,#54496,#54497,#54498,#54499,
#54500,#54501,#54502,#54503,#54504,#54505),.UNSPECIFIED.,.F.,.F.,(4,3,3,
3,3,3,3,4),(-204.760645321451,-203.869059247473,-202.869701113907,-201.870342980341,
-200.870984846775,-199.871626713209,-198.872268579643,-198.477460014271),
 .UNSPECIFIED.);
#1177=B_SPLINE_CURVE_WITH_KNOTS('',3,(#54506,#54507,#54508,#54509,#54510,
#54511,#54512,#54513,#54514,#54515,#54516,#54517,#54518,#54519,#54520,#54521,
#54522,#54523,#54524,#54525,#54526,#54527),.UNSPECIFIED.,.F.,.F.,(4,3,3,
3,3,3,3,4),(195.221805193122,195.874194178945,196.873552312511,197.872910446077,
198.872268579643,199.871626713209,200.870984846776,201.504990500301),
 .UNSPECIFIED.);
#1178=B_SPLINE_CURVE_WITH_KNOTS('',3,(#54532,#54533,#54534,#54535,#54536,
#54537,#54538,#54539,#54540,#54541,#54542,#54543,#54544,#54545,#54546,#54547,
#54548,#54549,#54550,#54551,#54552,#54553,#54554,#54555,#54556),
 .UNSPECIFIED.,.F.,.F.,(4,3,3,3,3,3,3,3,4),(-211.043830628631,-210.864566182436,
-209.86520804887,-208.865849915304,-207.866491781738,-206.867133648172,
-205.867775514606,-204.86841738104,-204.760645321451),.UNSPECIFIED.);
#1179=B_SPLINE_CURVE_WITH_KNOTS('',3,(#54557,#54558,#54559,#54560,#54561,
#54562,#54563,#54564,#54565,#54566,#54567,#54568,#54569,#54570,#54571,#54572,
#54573,#54574,#54575,#54576,#54577,#54578),.UNSPECIFIED.,.F.,.F.,(4,3,3,
3,3,3,3,4),(201.504990500301,201.870342980342,202.869701113908,203.869059247474,
204.86841738104,205.867775514606,206.867133648172,207.788175807481),
 .UNSPECIFIED.);
#1180=B_SPLINE_CURVE_WITH_KNOTS('',3,(#54583,#54584,#54585,#54586,#54587,
#54588,#54589,#54590,#54591,#54592,#54593,#54594,#54595,#54596,#54597,#54598,
#54599,#54600,#54601,#54602,#54603,#54604),.UNSPECIFIED.,.F.,.F.,(4,3,3,
3,3,3,3,4),(-217.32701593581,-216.860714983832,-215.861356850266,-214.8619987167,
-213.862640583134,-212.863282449568,-211.863924316002,-211.043830628631),
 .UNSPECIFIED.);
#1181=B_SPLINE_CURVE_WITH_KNOTS('',3,(#54605,#54606,#54607,#54608,#54609,
#54610,#54611,#54612,#54613,#54614,#54615,#54616,#54617,#54618,#54619,#54620,
#54621,#54622,#54623,#54624,#54625,#54626,#54627,#54628,#54629),
 .UNSPECIFIED.,.F.,.F.,(4,3,3,3,3,3,3,3,4),(207.788175807481,207.866491781738,
208.865849915304,209.86520804887,210.864566182436,211.863924316002,212.863282449568,
213.862640583134,214.07136111466),.UNSPECIFIED.);
#1182=B_SPLINE_CURVE_WITH_KNOTS('',3,(#54634,#54635,#54636,#54637,#54638,
#54639,#54640,#54641,#54642,#54643,#54644,#54645,#54646,#54647,#54648,#54649,
#54650,#54651,#54652,#54653,#54654,#54655),.UNSPECIFIED.,.F.,.F.,(4,3,3,
3,3,3,3,4),(-223.61020124299,-222.856863785228,-221.857505651662,-220.858147518096,
-219.85878938453,-218.859431250964,-217.860073117398,-217.32701593581),
 .UNSPECIFIED.);
#1183=B_SPLINE_CURVE_WITH_KNOTS('',3,(#54656,#54657,#54658,#54659,#54660,
#54661,#54662,#54663,#54664,#54665,#54666,#54667,#54668,#54669,#54670,#54671,
#54672,#54673,#54674,#54675,#54676,#54677),.UNSPECIFIED.,.F.,.F.,(4,3,3,
3,3,3,3,4),(214.07136111466,214.8619987167,215.861356850266,216.860714983832,
217.860073117398,218.859431250964,219.85878938453,220.35454642184),
 .UNSPECIFIED.);
#1184=B_SPLINE_CURVE_WITH_KNOTS('',3,(#54682,#54683,#54684,#54685,#54686,
#54687,#54688,#54689,#54690,#54691,#54692,#54693,#54694,#54695,#54696,#54697,
#54698,#54699,#54700,#54701,#54702,#54703,#54704,#54705,#54706),
 .UNSPECIFIED.,.F.,.F.,(4,3,3,3,3,3,3,3,4),(-229.893386550169,-229.852370720191,
-228.853012586625,-227.853654453059,-226.854296319493,-225.854938185927,
-224.85558005236,-223.856221918794,-223.61020124299),.UNSPECIFIED.);
#1185=B_SPLINE_CURVE_WITH_KNOTS('',3,(#54707,#54708,#54709,#54710,#54711,
#54712,#54713,#54714,#54715,#54716,#54717,#54718,#54719,#54720,#54721,#54722,
#54723,#54724,#54725,#54726,#54727,#54728),.UNSPECIFIED.,.F.,.F.,(4,3,3,
3,3,3,3,4),(220.35454642184,220.858147518096,221.857505651663,222.856863785229,
223.856221918795,224.855580052361,225.854938185927,226.637731729019),
 .UNSPECIFIED.);
#1186=B_SPLINE_CURVE_WITH_KNOTS('',3,(#54733,#54734,#54735,#54736,#54737,
#54738,#54739,#54740,#54741,#54742,#54743,#54744,#54745,#54746,#54747,#54748,
#54749,#54750,#54751,#54752,#54753,#54754),.UNSPECIFIED.,.F.,.F.,(4,3,3,
3,3,3,3,4),(-236.176571857349,-235.848519521587,-234.849161388021,-233.849803254455,
-232.850445120889,-231.851086987323,-230.851728853757,-229.893386550169),
 .UNSPECIFIED.);
#1187=B_SPLINE_CURVE_WITH_KNOTS('',3,(#54755,#54756,#54757,#54758,#54759,
#54760,#54761,#54762,#54763,#54764,#54765,#54766,#54767,#54768,#54769,#54770,
#54771,#54772,#54773,#54774,#54775,#54776,#54777,#54778,#54779),
 .UNSPECIFIED.,.F.,.F.,(4,3,3,3,3,3,3,3,4),(226.637731729019,226.854296319493,
227.853654453059,228.853012586625,229.852370720191,230.851728853757,231.851086987323,
232.850445120889,232.920917036199),.UNSPECIFIED.);
#1188=B_SPLINE_CURVE_WITH_KNOTS('',3,(#54784,#54785,#54786,#54787,#54788,
#54789,#54790,#54791,#54792,#54793,#54794,#54795,#54796,#54797,#54798,#54799,
#54800,#54801,#54802,#54803,#54804,#54805),.UNSPECIFIED.,.F.,.F.,(4,3,3,
3,3,3,3,4),(-242.459757164528,-241.844668322983,-240.845310189417,-239.845952055851,
-238.846593922285,-237.847235788719,-236.847877655153,-236.176571857349),
 .UNSPECIFIED.);
#1189=B_SPLINE_CURVE_WITH_KNOTS('',3,(#54806,#54807,#54808,#54809,#54810,
#54811,#54812,#54813,#54814,#54815,#54816,#54817,#54818,#54819,#54820,#54821,
#54822,#54823,#54824,#54825,#54826,#54827),.UNSPECIFIED.,.F.,.F.,(4,3,3,
3,3,3,3,4),(232.920917036199,233.849803254455,234.849161388021,235.848519521587,
236.847877655153,237.847235788719,238.846593922285,239.204102343378),
 .UNSPECIFIED.);
#1190=B_SPLINE_CURVE_WITH_KNOTS('',3,(#54832,#54833,#54834,#54835,#54836,
#54837,#54838,#54839,#54840,#54841,#54842,#54843,#54844,#54845,#54846,#54847,
#54848,#54849,#54850,#54851,#54852,#54853),.UNSPECIFIED.,.F.,.F.,(4,3,3,
3,3,3,3,4),(-248.742942471708,-247.84081712438,-246.841458990814,-245.842100857247,
-244.842742723681,-243.843384590115,-242.844026456549,-242.459757164528),
 .UNSPECIFIED.);
#1191=B_SPLINE_CURVE_WITH_KNOTS('',3,(#54854,#54855,#54856,#54857,#54858,
#54859,#54860,#54861,#54862,#54863,#54864,#54865,#54866,#54867,#54868,#54869,
#54870,#54871,#54872,#54873,#54874,#54875),.UNSPECIFIED.,.F.,.F.,(4,3,3,
3,3,3,3,4),(239.204102343378,239.845952055851,240.845310189417,241.844668322983,
242.84402645655,243.843384590116,244.842742723682,245.487287650558),
 .UNSPECIFIED.);
#1192=B_SPLINE_CURVE_WITH_KNOTS('',3,(#54880,#54881,#54882,#54883,#54884,
#54885,#54886,#54887,#54888,#54889,#54890,#54891,#54892,#54893,#54894,#54895,
#54896,#54897,#54898,#54899,#54900,#54901,#54902,#54903,#54904),
 .UNSPECIFIED.,.F.,.F.,(4,3,3,3,3,3,3,3,4),(-255.026127778888,-254.836324059342,
-253.836965925776,-252.83760779221,-251.838249658644,-250.838891525078,
-249.839533391512,-248.840175257946,-248.742942471708),.UNSPECIFIED.);
#1193=B_SPLINE_CURVE_WITH_KNOTS('',3,(#54905,#54906,#54907,#54908,#54909,
#54910,#54911,#54912,#54913,#54914,#54915,#54916,#54917,#54918,#54919,#54920,
#54921,#54922,#54923,#54924,#54925,#54926),.UNSPECIFIED.,.F.,.F.,(4,3,3,
3,3,3,3,4),(245.487287650558,245.842100857248,246.841458990814,247.84081712438,
248.840175257946,249.839533391512,250.838891525078,251.770472957738),
 .UNSPECIFIED.);
#1194=B_SPLINE_CURVE_WITH_KNOTS('',3,(#54931,#54932,#54933,#54934,#54935,
#54936,#54937,#54938,#54939,#54940,#54941,#54942,#54943,#54944,#54945,#54946,
#54947,#54948,#54949,#54950,#54951,#54952),.UNSPECIFIED.,.F.,.F.,(4,3,3,
3,3,3,3,4),(-261.309313086067,-260.832472860738,-259.833114727172,-258.833756593606,
-257.83439846004,-256.835040326474,-255.835682192908,-255.026127778888),
 .UNSPECIFIED.);
#1195=B_SPLINE_CURVE_WITH_KNOTS('',3,(#54953,#54954,#54955,#54956,#54957,
#54958,#54959,#54960,#54961,#54962,#54963,#54964,#54965,#54966,#54967,#54968,
#54969,#54970,#54971,#54972,#54973,#54974,#54975,#54976,#54977),
 .UNSPECIFIED.,.F.,.F.,(4,3,3,3,3,3,3,3,4),(251.770472957738,251.838249658644,
252.83760779221,253.836965925776,254.836324059342,255.835682192908,256.835040326474,
257.83439846004,258.053658264917),.UNSPECIFIED.);
#1196=B_SPLINE_CURVE_WITH_KNOTS('',3,(#54982,#54983,#54984,#54985,#54986,
#54987,#54988,#54989,#54990,#54991,#54992,#54993,#54994,#54995,#54996,#54997,
#54998,#54999,#55000,#55001,#55002,#55003),.UNSPECIFIED.,.F.,.F.,(4,3,3,
3,3,3,3,4),(-267.592498393247,-266.828621662134,-265.829263528568,-264.829905395002,
-263.830547261436,-262.83118912787,-261.831830994304,-261.309313086067),
 .UNSPECIFIED.);
#1197=B_SPLINE_CURVE_WITH_KNOTS('',3,(#55004,#55005,#55006,#55007,#55008,
#55009,#55010,#55011,#55012,#55013,#55014,#55015,#55016,#55017,#55018,#55019,
#55020,#55021,#55022,#55023,#55024,#55025),.UNSPECIFIED.,.F.,.F.,(4,3,3,
3,3,3,3,4),(258.053658264917,258.833756593606,259.833114727172,260.832472860738,
261.831830994304,262.83118912787,263.830547261436,264.336843572097),
 .UNSPECIFIED.);
#1198=B_SPLINE_CURVE_WITH_KNOTS('',3,(#55030,#55031,#55032,#55033,#55034,
#55035,#55036,#55037,#55038,#55039,#55040,#55041,#55042,#55043,#55044,#55045,
#55046,#55047,#55048,#55049,#55050,#55051,#55052,#55053,#55054),
 .UNSPECIFIED.,.F.,.F.,(4,3,3,3,3,3,3,3,4),(-273.875683700426,-273.824128597097,
-272.824770463531,-271.825412329965,-270.826054196399,-269.826696062833,
-268.827337929266,-267.8279797957,-267.592498393247),.UNSPECIFIED.);
#1199=B_SPLINE_CURVE_WITH_KNOTS('',3,(#55055,#55056,#55057,#55058,#55059,
#55060,#55061,#55062,#55063,#55064,#55065,#55066,#55067,#55068,#55069,#55070,
#55071,#55072,#55073,#55074,#55075,#55076),.UNSPECIFIED.,.F.,.F.,(4,3,3,
3,3,3,3,4),(264.336843572097,264.829905395003,265.829263528569,266.828621662135,
267.827979795701,268.827337929267,269.826696062833,270.620028879276),
 .UNSPECIFIED.);
#1200=B_SPLINE_CURVE_WITH_KNOTS('',3,(#55081,#55082,#55083,#55084,#55085,
#55086,#55087,#55088,#55089,#55090,#55091,#55092,#55093,#55094,#55095,#55096,
#55097,#55098,#55099,#55100,#55101,#55102),.UNSPECIFIED.,.F.,.F.,(4,3,3,
3,3,3,3,4),(-280.158869007606,-279.820277398493,-278.820919264927,-277.821561131361,
-276.822202997795,-275.822844864229,-274.823486730663,-273.875683700426),
 .UNSPECIFIED.);
#1201=B_SPLINE_CURVE_WITH_KNOTS('',3,(#55103,#55104,#55105,#55106,#55107,
#55108,#55109,#55110,#55111,#55112,#55113,#55114,#55115,#55116,#55117,#55118,
#55119,#55120,#55121,#55122,#55123,#55124,#55125,#55126,#55127),
 .UNSPECIFIED.,.F.,.F.,(4,3,3,3,3,3,3,3,4),(270.620028879276,270.826054196399,
271.825412329965,272.824770463531,273.824128597097,274.823486730663,275.822844864229,
276.822202997795,276.903214186456),.UNSPECIFIED.);
#1202=B_SPLINE_CURVE_WITH_KNOTS('',3,(#55132,#55133,#55134,#55135,#55136,
#55137,#55138,#55139,#55140,#55141,#55142,#55143,#55144,#55145,#55146,#55147,
#55148,#55149,#55150,#55151,#55152,#55153),.UNSPECIFIED.,.F.,.F.,(4,3,3,
3,3,3,3,4),(-286.442054314785,-285.816426199889,-284.817068066323,-283.817709932757,
-282.818351799191,-281.818993665625,-280.819635532059,-280.158869007606),
 .UNSPECIFIED.);
#1203=B_SPLINE_CURVE_WITH_KNOTS('',3,(#55154,#55155,#55156,#55157,#55158,
#55159,#55160,#55161,#55162,#55163,#55164,#55165,#55166,#55167,#55168,#55169,
#55170,#55171,#55172,#55173,#55174,#55175),.UNSPECIFIED.,.F.,.F.,(4,3,3,
3,3,3,3,4),(276.903214186456,277.821561131361,278.820919264927,279.820277398493,
280.819635532059,281.818993665625,282.818351799191,283.186399493635),
 .UNSPECIFIED.);
#1204=B_SPLINE_CURVE_WITH_KNOTS('',3,(#55180,#55181,#55182,#55183,#55184,
#55185,#55186,#55187,#55188,#55189,#55190,#55191,#55192,#55193,#55194,#55195,
#55196,#55197,#55198,#55199,#55200,#55201),.UNSPECIFIED.,.F.,.F.,(4,3,3,
3,3,3,3,4),(-292.725239621965,-291.812575001286,-290.81321686772,-289.813858734153,
-288.814500600587,-287.815142467021,-286.815784333455,-286.442054314785),
 .UNSPECIFIED.);
#1205=B_SPLINE_CURVE_WITH_KNOTS('',3,(#55202,#55203,#55204,#55205,#55206,
#55207,#55208,#55209,#55210,#55211,#55212,#55213,#55214,#55215,#55216,#55217,
#55218,#55219,#55220,#55221,#55222,#55223),.UNSPECIFIED.,.F.,.F.,(4,3,3,
3,3,3,3,4),(283.186399493635,283.817709932757,284.817068066323,285.81642619989,
286.815784333456,287.815142467022,288.814500600588,289.469584800815),
 .UNSPECIFIED.);
#1206=B_SPLINE_CURVE_WITH_KNOTS('',3,(#55228,#55229,#55230,#55231,#55232,
#55233,#55234,#55235,#55236,#55237,#55238,#55239,#55240,#55241,#55242,#55243,
#55244,#55245,#55246,#55247,#55248,#55249,#55250,#55251,#55252),
 .UNSPECIFIED.,.F.,.F.,(4,3,3,3,3,3,3,3,4),(-299.008424929145,-298.808081936248,
-297.808723802682,-296.809365669116,-295.81000753555,-294.810649401984,
-293.811291268418,-292.811933134852,-292.725239621965),.UNSPECIFIED.);
#1207=B_SPLINE_CURVE_WITH_KNOTS('',3,(#55253,#55254,#55255,#55256,#55257,
#55258,#55259,#55260,#55261,#55262,#55263,#55264,#55265,#55266,#55267,#55268,
#55269,#55270,#55271,#55272,#55273,#55274),.UNSPECIFIED.,.F.,.F.,(4,3,3,
3,3,3,3,4),(289.469584800815,289.813858734154,290.81321686772,291.812575001286,
292.811933134852,293.811291268418,294.810649401984,295.752770107995),
 .UNSPECIFIED.);
#1208=B_SPLINE_CURVE_WITH_KNOTS('',3,(#55279,#55280,#55281,#55282,#55283,
#55284,#55285,#55286,#55287,#55288,#55289,#55290,#55291,#55292,#55293,#55294,
#55295,#55296,#55297,#55298,#55299,#55300),.UNSPECIFIED.,.F.,.F.,(4,3,3,
3,3,3,3,4),(-305.291610236324,-304.804230737644,-303.804872604078,-302.805514470512,
-301.806156336946,-300.80679820338,-299.807440069814,-299.008424929145),
 .UNSPECIFIED.);
#1209=B_SPLINE_CURVE_WITH_KNOTS('',3,(#55301,#55302,#55303,#55304,#55305,
#55306,#55307,#55308,#55309,#55310,#55311,#55312,#55313,#55314,#55315,#55316,
#55317,#55318,#55319,#55320,#55321,#55322,#55323,#55324,#55325),
 .UNSPECIFIED.,.F.,.F.,(4,3,3,3,3,3,3,3,4),(295.752770107995,295.81000753555,
296.809365669116,297.808723802682,298.808081936248,299.807440069814,300.80679820338,
301.806156336946,302.035955415174),.UNSPECIFIED.);
#1210=B_SPLINE_CURVE_WITH_KNOTS('',3,(#55330,#55331,#55332,#55333,#55334,
#55335,#55336,#55337,#55338,#55339,#55340,#55341,#55342,#55343,#55344,#55345,
#55346,#55347,#55348,#55349,#55350,#55351),.UNSPECIFIED.,.F.,.F.,(4,3,3,
3,3,3,3,4),(-311.574795543504,-310.80037953904,-309.801021405475,-308.801663271908,
-307.802305138342,-306.802947004776,-305.80358887121,-305.291610236324),
 .UNSPECIFIED.);
#1211=B_SPLINE_CURVE_WITH_KNOTS('',3,(#55352,#55353,#55354,#55355,#55356,
#55357,#55358,#55359,#55360,#55361,#55362,#55363,#55364,#55365,#55366,#55367,
#55368,#55369,#55370,#55371,#55372,#55373),.UNSPECIFIED.,.F.,.F.,(4,3,3,
3,3,3,3,4),(302.035955415174,302.805514470512,303.804872604078,304.804230737644,
305.80358887121,306.802947004777,307.802305138343,308.319140722354),
 .UNSPECIFIED.);
#1212=B_SPLINE_CURVE_WITH_KNOTS('',3,(#55378,#55379,#55380,#55381,#55382,
#55383,#55384,#55385,#55386,#55387,#55388,#55389,#55390,#55391,#55392,#55393,
#55394,#55395,#55396,#55397,#55398,#55399,#55400,#55401,#55402),
 .UNSPECIFIED.,.F.,.F.,(4,3,3,3,3,3,3,3,4),(-317.857980850683,-317.795886474003,
-316.796528340437,-315.797170206871,-314.797812073305,-313.798453939739,
-312.799095806173,-311.799737672607,-311.574795543504),.UNSPECIFIED.);
#1213=B_SPLINE_CURVE_WITH_KNOTS('',3,(#55403,#55404,#55405,#55406,#55407,
#55408,#55409,#55410,#55411,#55412,#55413,#55414,#55415,#55416,#55417,#55418,
#55419,#55420,#55421,#55422,#55423,#55424),.UNSPECIFIED.,.F.,.F.,(4,3,3,
3,3,3,3,4),(308.319140722354,308.801663271909,309.801021405475,310.800379539041,
311.799737672607,312.799095806173,313.798453939739,314.602326029533),
 .UNSPECIFIED.);
#1214=B_SPLINE_CURVE_WITH_KNOTS('',3,(#55429,#55430,#55431,#55432,#55433,
#55434,#55435,#55436,#55437,#55438,#55439,#55440,#55441,#55442,#55443,#55444,
#55445,#55446,#55447,#55448,#55449,#55450),.UNSPECIFIED.,.F.,.F.,(4,3,3,
3,3,3,3,4),(-324.141166157863,-323.792035275399,-322.792677141833,-321.793319008267,
-320.793960874701,-319.794602741135,-318.795244607569,-317.857980850683),
 .UNSPECIFIED.);
#1215=B_SPLINE_CURVE_WITH_KNOTS('',3,(#55451,#55452,#55453,#55454,#55455,
#55456,#55457,#55458,#55459,#55460,#55461,#55462,#55463,#55464,#55465,#55466,
#55467,#55468,#55469,#55470,#55471,#55472,#55473,#55474,#55475),
 .UNSPECIFIED.,.F.,.F.,(4,3,3,3,3,3,3,3,4),(314.602326029533,314.797812073305,
315.797170206871,316.796528340437,317.795886474003,318.795244607569,319.794602741135,
320.793960874701,320.885511336713),.UNSPECIFIED.);
#1216=B_SPLINE_CURVE_WITH_KNOTS('',3,(#55480,#55481,#55482,#55483,#55484,
#55485,#55486,#55487,#55488,#55489,#55490,#55491,#55492,#55493,#55494,#55495,
#55496,#55497,#55498,#55499,#55500,#55501),.UNSPECIFIED.,.F.,.F.,(4,3,3,
3,3,3,3,4),(-330.424351465042,-329.788184076795,-328.788825943229,-327.789467809663,
-326.790109676097,-325.790751542531,-324.791393408965,-324.141166157863),
 .UNSPECIFIED.);
#1217=B_SPLINE_CURVE_WITH_KNOTS('',3,(#55502,#55503,#55504,#55505,#55506,
#55507,#55508,#55509,#55510,#55511,#55512,#55513,#55514,#55515,#55516,#55517,
#55518,#55519,#55520,#55521,#55522,#55523),.UNSPECIFIED.,.F.,.F.,(4,3,3,
3,3,3,3,4),(320.885511336713,321.793319008267,322.792677141833,323.792035275399,
324.791393408965,325.790751542531,326.790109676097,327.168696643892),
 .UNSPECIFIED.);
#1218=B_SPLINE_CURVE_WITH_KNOTS('',3,(#55528,#55529,#55530,#55531,#55532,
#55533,#55534,#55535,#55536,#55537,#55538,#55539,#55540,#55541,#55542,#55543,
#55544,#55545,#55546,#55547,#55548,#55549),.UNSPECIFIED.,.F.,.F.,(4,3,3,
3,3,3,3,4),(-336.707536772222,-335.784332878192,-334.784974744626,-333.78561661106,
-332.786258477494,-331.786900343927,-330.787542210361,-330.424351465042),
 .UNSPECIFIED.);
#1219=B_SPLINE_CURVE_WITH_KNOTS('',3,(#55550,#55551,#55552,#55553,#55554,
#55555,#55556,#55557,#55558,#55559,#55560,#55561,#55562,#55563,#55564,#55565,
#55566,#55567,#55568,#55569,#55570,#55571),.UNSPECIFIED.,.F.,.F.,(4,3,3,
3,3,3,3,4),(327.168696643892,327.789467809663,328.78882594323,329.788184076796,
330.787542210362,331.786900343928,332.786258477494,333.451881951072),
 .UNSPECIFIED.);
#1220=B_SPLINE_CURVE_WITH_KNOTS('',3,(#55576,#55577,#55578,#55579,#55580,
#55581,#55582,#55583,#55584,#55585,#55586,#55587,#55588,#55589,#55590,#55591,
#55592,#55593,#55594,#55595,#55596,#55597,#55598,#55599,#55600),
 .UNSPECIFIED.,.F.,.F.,(4,3,3,3,3,3,3,3,4),(-342.990722079402,-342.779839813154,
-341.780481679588,-340.781123546022,-339.781765412456,-338.78240727889,
-337.783049145324,-336.783691011758,-336.707536772222),.UNSPECIFIED.);
#1221=B_SPLINE_CURVE_WITH_KNOTS('',3,(#55601,#55602,#55603,#55604,#55605,
#55606,#55607,#55608,#55609,#55610,#55611,#55612,#55613,#55614,#55615,#55616,
#55617,#55618,#55619,#55620,#55621,#55622),.UNSPECIFIED.,.F.,.F.,(4,3,3,
3,3,3,3,4),(333.451881951072,333.78561661106,334.784974744626,335.784332878192,
336.783691011758,337.783049145324,338.78240727889,339.735067258252),
 .UNSPECIFIED.);
#1222=B_SPLINE_CURVE_WITH_KNOTS('',3,(#55627,#55628,#55629,#55630,#55631,
#55632,#55633,#55634,#55635,#55636,#55637,#55638,#55639,#55640,#55641,#55642,
#55643,#55644,#55645,#55646,#55647,#55648,#55649,#55650,#55651,#55652,#55653,
#55654,#55655,#55656,#55657,#55658,#55659,#55660),.UNSPECIFIED.,.F.,.F.,
(4,3,3,3,3,3,3,3,3,3,3,4),(-349.273907386581,-348.77598861455,-348.276309547767,
-347.776630480984,-347.276951414201,-346.777272347418,-346.277593280635,
-345.777914213852,-345.278235147069,-344.778556080286,-343.77919794672,
-342.990722079402),.UNSPECIFIED.);
#1223=B_SPLINE_CURVE_WITH_KNOTS('',3,(#55661,#55662,#55663,#55664,#55665,
#55666,#55667,#55668,#55669,#55670,#55671,#55672,#55673,#55674,#55675,#55676,
#55677,#55678,#55679,#55680,#55681,#55682,#55683,#55684,#55685,#55686,#55687,
#55688),.UNSPECIFIED.,.F.,.F.,(4,3,3,3,3,3,3,3,3,4),(339.735067258252,339.781765412456,
340.781123546022,341.780481679588,342.779839813154,343.77919794672,344.778556080286,
345.278235147069,345.777914213852,346.018252565431),.UNSPECIFIED.);
#1224=B_SPLINE_CURVE_WITH_KNOTS('',3,(#55693,#55694,#55695,#55696,#55697,
#55698,#55699,#55700,#55701,#55702,#55703,#55704,#55705,#55706,#55707,#55708,
#55709,#55710,#55711,#55712,#55713,#55714,#55715,#55716,#55717,#55718,#55719,
#55720,#55721,#55722,#55723,#55724,#55725,#55726,#55727,#55728,#55729,#55730,
#55731,#55732,#55733,#55734,#55735),.UNSPECIFIED.,.F.,.F.,(4,3,3,3,3,3,
3,3,3,3,3,3,3,3,4),(-355.557092693761,-355.27181648273,-354.772137415947,
-354.272458349164,-353.77277928238,-353.273100215597,-352.773421148814,
-352.273742082031,-351.774063015248,-351.274383948465,-350.774704881682,
-350.275025814899,-349.775346748116,-349.275667681333,-349.273907386581),
 .UNSPECIFIED.);
#1225=B_SPLINE_CURVE_WITH_KNOTS('',3,(#55736,#55737,#55738,#55739,#55740,
#55741,#55742,#55743,#55744,#55745,#55746,#55747,#55748,#55749,#55750,#55751,
#55752,#55753,#55754,#55755,#55756,#55757,#55758,#55759,#55760,#55761,#55762,
#55763,#55764,#55765,#55766,#55767,#55768,#55769,#55770,#55771,#55772,#55773,
#55774,#55775,#55776,#55777,#55778),.UNSPECIFIED.,.F.,.F.,(4,3,3,3,3,3,
3,3,3,3,3,3,3,3,4),(346.018252565431,346.277593280635,346.777272347418,
347.276951414201,347.776630480984,348.276309547767,348.77598861455,349.275667681334,
349.775346748116,350.2750258149,350.774704881683,351.274383948466,351.774063015249,
352.273742082032,352.301437872611),.UNSPECIFIED.);
#1226=B_SPLINE_CURVE_WITH_KNOTS('',3,(#55783,#55784,#55785,#55786,#55787,
#55788,#55789,#55790,#55791,#55792,#55793,#55794,#55795,#55796,#55797,#55798,
#55799,#55800,#55801,#55802,#55803,#55804,#55805,#55806,#55807,#55808,#55809,
#55810,#55811,#55812,#55813,#55814,#55815,#55816,#55817,#55818,#55819,#55820,
#55821,#55822,#55823,#55824,#55825),.UNSPECIFIED.,.F.,.F.,(4,3,3,3,3,3,
3,3,3,3,3,3,3,3,4),(-361.84027800094,-361.767644350909,-361.267965284126,
-360.768286217343,-360.26860715056,-359.768928083777,-359.269249016994,
-358.769569950211,-358.269890883428,-357.770211816645,-357.270532749862,
-356.770853683079,-356.271174616296,-355.771495549513,-355.557092693761),
 .UNSPECIFIED.);
#1227=B_SPLINE_CURVE_WITH_KNOTS('',3,(#55826,#55827,#55828,#55829,#55830,
#55831,#55832,#55833,#55834,#55835,#55836,#55837,#55838,#55839,#55840,#55841,
#55842,#55843,#55844,#55845,#55846,#55847,#55848,#55849,#55850,#55851,#55852,
#55853,#55854,#55855,#55856,#55857,#55858,#55859,#55860,#55861,#55862,#55863,
#55864,#55865),.UNSPECIFIED.,.F.,.F.,(4,3,3,3,3,3,3,3,3,3,3,3,3,4),(352.301437872611,
352.773421148815,353.273100215598,353.772779282381,354.272458349164,354.772137415947,
355.27181648273,355.771495549513,356.271174616296,356.770853683079,357.270532749862,
357.770211816645,358.269890883428,358.58462317979),.UNSPECIFIED.);
#1228=B_SPLINE_CURVE_WITH_KNOTS('',3,(#55870,#55871,#55872,#55873,#55874,
#55875,#55876,#55877,#55878,#55879,#55880,#55881,#55882,#55883,#55884,#55885,
#55886,#55887,#55888,#55889,#55890,#55891,#55892,#55893,#55894,#55895,#55896,
#55897,#55898,#55899,#55900,#55901,#55902,#55903,#55904,#55905,#55906,#55907,
#55908,#55909),.UNSPECIFIED.,.F.,.F.,(4,3,3,3,3,3,3,3,3,3,3,3,3,4),(-368.12346330812,
-367.763793152305,-367.264114085522,-366.764435018739,-366.264755951956,
-365.765076885173,-365.26539781839,-364.765718751607,-364.266039684824,
-363.766360618041,-363.266681551258,-362.767002484475,-362.267323417692,
-361.84027800094),.UNSPECIFIED.);
#1229=B_SPLINE_CURVE_WITH_KNOTS('',3,(#55910,#55911,#55912,#55913,#55914,
#55915,#55916,#55917,#55918,#55919,#55920,#55921,#55922,#55923,#55924,#55925,
#55926,#55927,#55928,#55929,#55930,#55931,#55932,#55933,#55934,#55935,#55936,
#55937,#55938,#55939,#55940,#55941,#55942,#55943,#55944,#55945,#55946,#55947,
#55948,#55949,#55950,#55951,#55952),.UNSPECIFIED.,.F.,.F.,(4,3,3,3,3,3,
3,3,3,3,3,3,3,3,4),(358.58462317979,358.769569950211,359.269249016994,359.768928083777,
360.26860715056,360.768286217343,361.267965284126,361.767644350909,362.267323417692,
362.767002484475,363.266681551258,363.766360618041,364.266039684824,364.765718751607,
364.86780848697),.UNSPECIFIED.);
#1230=B_SPLINE_CURVE_WITH_KNOTS('',3,(#55957,#55958,#55959,#55960,#55961,
#55962,#55963,#55964,#55965,#55966,#55967,#55968,#55969,#55970,#55971,#55972,
#55973,#55974,#55975,#55976,#55977,#55978,#55979,#55980,#55981,#55982,#55983,
#55984,#55985,#55986,#55987,#55988,#55989,#55990,#55991,#55992,#55993,#55994,
#55995,#55996,#55997,#55998,#55999),.UNSPECIFIED.,.F.,.F.,(4,3,3,3,3,3,
3,3,3,3,3,3,3,3,4),(-374.406648615299,-374.259621020484,-373.759941953701,
-373.260262886918,-372.760583820135,-372.260904753352,-371.761225686569,
-371.261546619786,-370.761867553003,-370.26218848622,-369.762509419437,
-369.262830352654,-368.763151285871,-368.263472219088,-368.12346330812),
 .UNSPECIFIED.);
#1231=B_SPLINE_CURVE_WITH_KNOTS('',3,(#56000,#56001,#56002,#56003,#56004,
#56005,#56006,#56007,#56008,#56009,#56010,#56011,#56012,#56013,#56014,#56015,
#56016,#56017,#56018,#56019,#56020,#56021,#56022,#56023,#56024,#56025,#56026,
#56027,#56028,#56029,#56030,#56031,#56032,#56033,#56034,#56035,#56036,#56037,
#56038,#56039),.UNSPECIFIED.,.F.,.F.,(4,3,3,3,3,3,3,3,3,3,3,3,3,4),(364.86780848697,
365.26539781839,365.765076885173,366.264755951956,366.764435018739,367.264114085522,
367.763793152305,368.263472219088,368.763151285871,369.262830352654,369.762509419437,
370.26218848622,370.761867553004,371.150993794149),.UNSPECIFIED.);
#1232=B_SPLINE_CURVE_WITH_KNOTS('',3,(#56044,#56045,#56046,#56047,#56048,
#56049,#56050,#56051,#56052,#56053,#56054,#56055,#56056,#56057,#56058,#56059,
#56060,#56061,#56062,#56063,#56064,#56065,#56066,#56067,#56068,#56069,#56070,
#56071,#56072,#56073,#56074,#56075,#56076,#56077,#56078,#56079,#56080,#56081,
#56082,#56083),.UNSPECIFIED.,.F.,.F.,(4,3,3,3,3,3,3,3,3,3,3,3,3,4),(-380.689833922479,
-380.255769821881,-379.756090755098,-379.256411688315,-378.756732621532,
-378.257053554749,-377.757374487966,-377.257695421183,-376.7580163544,-376.258337287616,
-375.758658220834,-375.25897915405,-374.759300087267,-374.406648615299),
 .UNSPECIFIED.);
#1233=B_SPLINE_CURVE_WITH_KNOTS('',3,(#56084,#56085,#56086,#56087,#56088,
#56089,#56090,#56091,#56092,#56093,#56094,#56095,#56096,#56097,#56098,#56099,
#56100,#56101,#56102,#56103,#56104,#56105,#56106,#56107,#56108,#56109,#56110,
#56111,#56112,#56113,#56114,#56115,#56116,#56117,#56118,#56119,#56120,#56121,
#56122,#56123,#56124,#56125,#56126),.UNSPECIFIED.,.F.,.F.,(4,3,3,3,3,3,
3,3,3,3,3,3,3,3,4),(371.150993794149,371.261546619787,371.76122568657,372.260904753353,
372.760583820136,373.260262886919,373.759941953702,374.259621020485,374.759300087268,
375.258979154051,375.758658220834,376.258337287617,376.7580163544,377.257695421183,
377.434179101329),.UNSPECIFIED.);
#1234=B_SPLINE_CURVE_WITH_KNOTS('',3,(#56131,#56132,#56133,#56134,#56135,
#56136,#56137,#56138,#56139,#56140,#56141,#56142,#56143,#56144,#56145,#56146,
#56147,#56148,#56149,#56150,#56151,#56152,#56153,#56154,#56155,#56156,#56157,
#56158,#56159,#56160,#56161,#56162,#56163,#56164,#56165,#56166,#56167,#56168,
#56169,#56170,#56171,#56172,#56173),.UNSPECIFIED.,.F.,.F.,(4,3,3,3,3,3,
3,3,3,3,3,3,3,3,4),(-386.973019229658,-386.75159769006,-386.251918623277,
-385.752239556494,-385.252560489711,-384.752881422928,-384.253202356145,
-383.753523289362,-383.253844222579,-382.754165155796,-382.254486089013,
-381.75480702223,-381.255127955447,-380.755448888664,-380.689833922479),
 .UNSPECIFIED.);
#1235=B_SPLINE_CURVE_WITH_KNOTS('',3,(#56174,#56175,#56176,#56177,#56178,
#56179,#56180,#56181,#56182,#56183,#56184,#56185,#56186,#56187,#56188,#56189,
#56190,#56191,#56192,#56193,#56194,#56195,#56196,#56197,#56198,#56199,#56200,
#56201,#56202,#56203,#56204,#56205,#56206,#56207,#56208,#56209,#56210,#56211,
#56212,#56213),.UNSPECIFIED.,.F.,.F.,(4,3,3,3,3,3,3,3,3,3,3,3,3,4),(377.434179101329,
377.757374487966,378.257053554749,378.756732621532,379.256411688315,379.756090755098,
380.255769821881,380.755448888664,381.255127955447,381.75480702223,382.254486089013,
382.754165155796,383.253844222579,383.717364408508),.UNSPECIFIED.);
#1236=B_SPLINE_CURVE_WITH_KNOTS('',3,(#56218,#56219,#56220,#56221,#56222,
#56223,#56224,#56225,#56226,#56227,#56228,#56229,#56230,#56231,#56232,#56233,
#56234,#56235,#56236,#56237,#56238,#56239,#56240,#56241,#56242,#56243,#56244,
#56245,#56246,#56247,#56248,#56249,#56250,#56251,#56252,#56253,#56254,#56255,
#56256,#56257,#56258,#56259,#56260),.UNSPECIFIED.,.F.,.F.,(4,3,3,3,3,3,
3,3,3,3,3,3,3,3,4),(-393.256204536838,-393.247425558239,-392.747746491456,
-392.248067424673,-391.74838835789,-391.248709291107,-390.749030224324,
-390.249351157541,-389.749672090758,-389.249993023975,-388.750313957192,
-388.250634890409,-387.750955823626,-387.251276756843,-386.973019229658),
 .UNSPECIFIED.);
#1237=B_SPLINE_CURVE_WITH_KNOTS('',3,(#56261,#56262,#56263,#56264,#56265,
#56266,#56267,#56268,#56269,#56270,#56271,#56272,#56273,#56274,#56275,#56276,
#56277,#56278,#56279,#56280,#56281,#56282,#56283,#56284,#56285,#56286,#56287,
#56288,#56289,#56290,#56291,#56292,#56293,#56294,#56295,#56296,#56297,#56298,
#56299,#56300,#56301,#56302,#56303),.UNSPECIFIED.,.F.,.F.,(4,3,3,3,3,3,
3,3,3,3,3,3,3,3,4),(383.717364408508,383.753523289362,384.253202356145,
384.752881422928,385.252560489711,385.752239556494,386.251918623277,386.75159769006,
387.251276756843,387.750955823626,388.250634890409,388.750313957192,389.249993023975,
389.749672090758,390.000549715688),.UNSPECIFIED.);
#1238=B_SPLINE_CURVE_WITH_KNOTS('',3,(#56309,#56310,#56311,#56312),
 .UNSPECIFIED.,.F.,.F.,(4,4),(405.265452313083,405.755527026166),
 .UNSPECIFIED.);
#1239=B_SPLINE_CURVE_WITH_KNOTS('',3,(#56318,#56319,#56320,#56321,#56322,
#56323,#56324,#56325,#56326,#56327,#56328,#56329,#56330,#56331,#56332,#56333,
#56334),.UNSPECIFIED.,.F.,.F.,(4,1,1,1,1,1,1,1,1,1,1,1,1,1,4),(398.982267005903,
399.260524533088,399.760203599871,400.259882666654,400.759561733437,401.25924080022,
401.758919867003,402.258598933787,402.75827800057,403.257957067353,403.757636134136,
404.257315200919,404.756994267702,405.256673334485,405.265452313083),
 .UNSPECIFIED.);
#1240=B_SPLINE_CURVE_WITH_KNOTS('',3,(#56337,#56338,#56339,#56340,#56341,
#56342,#56343,#56344,#56345,#56346,#56347,#56348,#56349),.UNSPECIFIED.,
 .F.,.F.,(4,1,1,1,1,1,1,1,1,1,4),(398.982267005904,399.231068447758,399.730747514541,
400.230426581324,400.730105648107,401.22978471489,401.729463781673,402.229142848456,
402.728821915239,403.228500982022,403.728180048805),.UNSPECIFIED.);
#1241=B_SPLINE_CURVE_WITH_KNOTS('',3,(#56354,#56355,#56356,#56357,#56358,
#56359,#56360,#56361,#56362,#56363,#56364,#56365,#56366,#56367,#56368,#56369,
#56370),.UNSPECIFIED.,.F.,.F.,(4,1,1,1,1,1,1,1,1,1,1,1,1,1,4),(392.699081698724,
392.764696664909,393.264375731692,393.764054798475,394.263733865258,394.763412932041,
395.263091998824,395.762771065607,396.26245013239,396.762129199173,397.261808265956,
397.761487332739,398.261166399522,398.760845466305,398.982267005903),
 .UNSPECIFIED.);
#1242=B_SPLINE_CURVE_WITH_KNOTS('',3,(#56371,#56372,#56373,#56374,#56375,
#56376,#56377,#56378,#56379,#56380,#56381,#56382,#56383,#56384,#56385,#56386,
#56387),.UNSPECIFIED.,.F.,.F.,(4,1,1,1,1,1,1,1,1,1,1,1,1,1,4),(392.699081698724,
392.735240579579,393.234919646362,393.734598713145,394.234277779928,394.733956846711,
395.233635913494,395.733314980277,396.23299404706,396.732673113843,397.232352180626,
397.732031247409,398.231710314192,398.731389380975,398.982267005904),
 .UNSPECIFIED.);
#1243=B_SPLINE_CURVE_WITH_KNOTS('',3,(#56392,#56393,#56394,#56395,#56396,
#56397,#56398,#56399,#56400,#56401,#56402,#56403,#56404,#56405,#56406,#56407),
 .UNSPECIFIED.,.F.,.F.,(4,1,1,1,1,1,1,1,1,1,1,1,1,4),(386.415896391544,
386.768547863513,387.268226930296,387.767905997079,388.267585063862,388.767264130645,
389.266943197428,389.766622264211,390.266301330994,390.765980397777,391.26565946456,
391.765338531343,392.265017598126,392.699081698724),.UNSPECIFIED.);
#1244=B_SPLINE_CURVE_WITH_KNOTS('',3,(#56408,#56409,#56410,#56411,#56412,
#56413,#56414,#56415,#56416,#56417,#56418,#56419,#56420,#56421,#56422,#56423),
 .UNSPECIFIED.,.F.,.F.,(4,1,1,1,1,1,1,1,1,1,1,1,1,4),(386.415896391545,
386.739091778183,387.238770844966,387.738449911749,388.238128978532,388.737808045315,
389.237487112098,389.737166178881,390.236845245664,390.736524312447,391.23620337923,
391.735882446013,392.235561512796,392.699081698724),.UNSPECIFIED.);
#1245=B_SPLINE_CURVE_WITH_KNOTS('',3,(#56428,#56429,#56430,#56431,#56432,
#56433,#56434,#56435,#56436,#56437,#56438,#56439,#56440,#56441,#56442,#56443,
#56444),.UNSPECIFIED.,.F.,.F.,(4,1,1,1,1,1,1,1,1,1,1,1,1,1,4),(380.132711084365,
380.272719995333,380.772399062117,381.2720781289,381.771757195683,382.271436262466,
382.771115329249,383.270794396032,383.770473462815,384.270152529598,384.769831596381,
385.269510663164,385.769189729947,386.26886879673,386.415896391544),
 .UNSPECIFIED.);
#1246=B_SPLINE_CURVE_WITH_KNOTS('',3,(#56445,#56446,#56447,#56448,#56449,
#56450,#56451,#56452,#56453,#56454,#56455,#56456,#56457,#56458,#56459,#56460,
#56461),.UNSPECIFIED.,.F.,.F.,(4,1,1,1,1,1,1,1,1,1,1,1,1,1,4),(380.132711084365,
380.243263910003,380.742942976786,381.242622043569,381.742301110352,382.241980177135,
382.741659243918,383.241338310702,383.741017377485,384.240696444268,384.740375511051,
385.240054577834,385.739733644617,386.2394127114,386.415896391545),
 .UNSPECIFIED.);
#1247=B_SPLINE_CURVE_WITH_KNOTS('',3,(#56466,#56467,#56468,#56469,#56470,
#56471,#56472,#56473,#56474,#56475,#56476,#56477,#56478,#56479,#56480,#56481),
 .UNSPECIFIED.,.F.,.F.,(4,1,1,1,1,1,1,1,1,1,1,1,1,4),(373.849525777185,
374.276571193937,374.77625026072,375.275929327503,375.775608394286,376.275287461069,
376.774966527852,377.274645594635,377.774324661418,378.274003728201,378.773682794984,
379.273361861767,379.77304092855,380.132711084365),.UNSPECIFIED.);
#1248=B_SPLINE_CURVE_WITH_KNOTS('',3,(#56482,#56483,#56484,#56485,#56486,
#56487,#56488,#56489,#56490,#56491,#56492,#56493,#56494,#56495,#56496,#56497),
 .UNSPECIFIED.,.F.,.F.,(4,1,1,1,1,1,1,1,1,1,1,1,1,4),(373.849525777185,
374.247115108607,374.74679417539,375.246473242173,375.746152308956,376.245831375739,
376.745510442522,377.245189509305,377.744868576088,378.244547642871,378.744226709654,
379.243905776437,379.74358484322,380.132711084365),.UNSPECIFIED.);
#1249=B_SPLINE_CURVE_WITH_KNOTS('',3,(#56502,#56503,#56504,#56505,#56506,
#56507,#56508,#56509,#56510,#56511,#56512,#56513,#56514,#56515,#56516,#56517,
#56518),.UNSPECIFIED.,.F.,.F.,(4,1,1,1,1,1,1,1,1,1,1,1,1,1,4),(367.566340470006,
367.780743325758,368.280422392541,368.780101459324,369.279780526107,369.77945959289,
370.279138659673,370.778817726456,371.278496793239,371.778175860022,372.277854926805,
372.777533993588,373.277213060371,373.776892127154,373.849525777185),
 .UNSPECIFIED.);
#1250=B_SPLINE_CURVE_WITH_KNOTS('',3,(#56519,#56520,#56521,#56522,#56523,
#56524,#56525,#56526,#56527,#56528,#56529,#56530,#56531,#56532,#56533,#56534,
#56535),.UNSPECIFIED.,.F.,.F.,(4,1,1,1,1,1,1,1,1,1,1,1,1,1,4),(367.566340470006,
367.751287240428,368.250966307211,368.750645373994,369.250324440777,369.75000350756,
370.249682574343,370.749361641126,371.249040707909,371.748719774692,372.248398841475,
372.748077908258,373.247756975041,373.747436041824,373.849525777185),
 .UNSPECIFIED.);
#1251=B_SPLINE_CURVE_WITH_KNOTS('',3,(#56540,#56541,#56542,#56543,#56544,
#56545,#56546,#56547,#56548,#56549,#56550,#56551,#56552,#56553,#56554,#56555,
#56556),.UNSPECIFIED.,.F.,.F.,(4,1,1,1,1,1,1,1,1,1,1,1,1,1,4),(361.283155162826,
361.284915457579,361.784594524362,362.284273591145,362.783952657928,363.283631724711,
363.783310791494,364.282989858277,364.78266892506,365.282347991843,365.782027058626,
366.281706125409,366.781385192192,367.281064258975,367.566340470006),
 .UNSPECIFIED.);
#1252=B_SPLINE_CURVE_WITH_KNOTS('',3,(#56557,#56558,#56559,#56560,#56561,
#56562,#56563,#56564,#56565,#56566,#56567,#56568,#56569,#56570,#56571,#56572),
 .UNSPECIFIED.,.F.,.F.,(4,1,1,1,1,1,1,1,1,1,1,1,1,4),(361.283155162826,
361.755138439031,362.254817505815,362.754496572598,363.254175639381,363.753854706164,
364.253533772947,364.75321283973,365.252891906513,365.752570973296,366.252250040079,
366.751929106862,367.251608173645,367.566340470006),.UNSPECIFIED.);
#1253=B_SPLINE_CURVE_WITH_KNOTS('',3,(#56577,#56578,#56579,#56580,#56581,
#56582,#56583,#56584,#56585,#56586,#56587,#56588,#56589,#56590),
 .UNSPECIFIED.,.F.,.F.,(4,1,1,1,1,1,1,1,1,1,1,4),(354.999969855646,355.788445722965,
356.787803856531,357.287482923314,357.787161990097,358.28684105688,358.786520123663,
359.286199190446,359.78587825723,360.285557324013,360.785236390796,361.283155162826),
 .UNSPECIFIED.);
#1254=B_SPLINE_CURVE_WITH_KNOTS('',3,(#56591,#56592,#56593,#56594,#56595,
#56596,#56597,#56598,#56599,#56600,#56601,#56602,#56603,#56604,#56605,#56606,
#56607),.UNSPECIFIED.,.F.,.F.,(4,1,1,1,1,1,1,1,1,1,1,1,1,1,4),(354.999969855647,
355.259310570852,355.758989637635,356.258668704418,356.758347771201,357.258026837984,
357.757705904767,358.25738497155,358.757064038333,359.256743105116,359.756422171899,
360.256101238682,360.755780305465,361.255459372248,361.283155162826),
 .UNSPECIFIED.);
#1255=B_SPLINE_CURVE_WITH_KNOTS('',3,(#56612,#56613,#56614,#56615,#56616,
#56617,#56618,#56619,#56620,#56621,#56622),.UNSPECIFIED.,.F.,.F.,(4,1,1,
1,1,1,1,1,4),(348.716784548467,348.792938788003,349.792296921569,350.791655055135,
351.791013188701,352.790371322267,353.789729455833,354.789087589399,354.999969855646),
 .UNSPECIFIED.);
#1256=B_SPLINE_CURVE_WITH_KNOTS('',3,(#56623,#56624,#56625,#56626,#56627,
#56628,#56629,#56630,#56631,#56632,#56633,#56634),.UNSPECIFIED.,.F.,.F.,
(4,1,1,1,1,1,1,1,1,4),(348.716784548467,348.763482702673,349.762840836239,
350.762198969805,351.761557103371,352.760915236937,353.760273370503,354.259952437286,
354.759631504069,354.999969855647),.UNSPECIFIED.);
#1257=B_SPLINE_CURVE_WITH_KNOTS('',3,(#56639,#56640,#56641,#56642,#56643,
#56644,#56645,#56646,#56647,#56648),.UNSPECIFIED.,.F.,.F.,(4,1,1,1,1,1,
1,4),(342.433599241287,342.796789986607,343.796148120173,344.795506253739,
345.794864387305,346.794222520871,347.793580654437,348.716784548467),
 .UNSPECIFIED.);
#1258=B_SPLINE_CURVE_WITH_KNOTS('',3,(#56649,#56650,#56651,#56652,#56653,
#56654,#56655,#56656,#56657,#56658),.UNSPECIFIED.,.F.,.F.,(4,1,1,1,1,1,
1,4),(342.433599241288,342.767333901277,343.766692034843,344.766050168409,
345.765408301975,346.764766435541,347.764124569107,348.716784548467),
 .UNSPECIFIED.);
#1259=B_SPLINE_CURVE_WITH_KNOTS('',3,(#56663,#56664,#56665,#56666,#56667,
#56668,#56669,#56670,#56671,#56672),.UNSPECIFIED.,.F.,.F.,(4,1,1,1,1,1,
1,4),(336.150413934108,336.80064118521,337.799999318776,338.799357452343,
339.798715585909,340.798073719475,341.797431853041,342.433599241287),
 .UNSPECIFIED.);
#1260=B_SPLINE_CURVE_WITH_KNOTS('',3,(#56673,#56674,#56675,#56676,#56677,
#56678,#56679,#56680,#56681,#56682),.UNSPECIFIED.,.F.,.F.,(4,1,1,1,1,1,
1,4),(336.150413934108,336.77118509988,337.770543233446,338.769901367012,
339.769259500578,340.768617634145,341.767975767711,342.433599241288),
 .UNSPECIFIED.);
#1261=B_SPLINE_CURVE_WITH_KNOTS('',3,(#56687,#56688,#56689,#56690,#56691,
#56692,#56693,#56694,#56695,#56696),.UNSPECIFIED.,.F.,.F.,(4,1,1,1,1,1,
1,4),(329.867228626928,330.804492383814,331.80385051738,332.803208650946,
333.802566784512,334.801924918078,335.801283051644,336.150413934108),
 .UNSPECIFIED.);
#1262=B_SPLINE_CURVE_WITH_KNOTS('',3,(#56697,#56698,#56699,#56700,#56701,
#56702,#56703,#56704,#56705,#56706),.UNSPECIFIED.,.F.,.F.,(4,1,1,1,1,1,
1,4),(329.867228626928,330.775036298484,331.77439443205,332.773752565616,
333.773110699182,334.772468832748,335.771826966314,336.150413934108),
 .UNSPECIFIED.);
#1263=B_SPLINE_CURVE_WITH_KNOTS('',3,(#56711,#56712,#56713,#56714,#56715,
#56716,#56717,#56718,#56719,#56720,#56721),.UNSPECIFIED.,.F.,.F.,(4,1,1,
1,1,1,1,1,4),(323.584043319749,323.808985448852,324.808343582418,325.807701715984,
326.80705984955,327.806417983116,328.805776116682,329.805134250248,329.867228626928),
 .UNSPECIFIED.);
#1264=B_SPLINE_CURVE_WITH_KNOTS('',3,(#56722,#56723,#56724,#56725,#56726,
#56727,#56728,#56729,#56730,#56731,#56732),.UNSPECIFIED.,.F.,.F.,(4,1,1,
1,1,1,1,1,4),(323.584043319749,323.779529363522,324.778887497088,325.778245630654,
326.77760376422,327.776961897786,328.776320031352,329.775678164918,329.867228626928),
 .UNSPECIFIED.);
#1265=B_SPLINE_CURVE_WITH_KNOTS('',3,(#56737,#56738,#56739,#56740,#56741,
#56742,#56743,#56744,#56745,#56746),.UNSPECIFIED.,.F.,.F.,(4,1,1,1,1,1,
1,4),(317.300858012569,317.812836647456,318.812194781022,319.811552914588,
320.810911048154,321.81026918172,322.809627315286,323.584043319749),
 .UNSPECIFIED.);
#1266=B_SPLINE_CURVE_WITH_KNOTS('',3,(#56747,#56748,#56749,#56750,#56751,
#56752,#56753,#56754,#56755,#56756),.UNSPECIFIED.,.F.,.F.,(4,1,1,1,1,1,
1,4),(317.300858012569,317.783380562125,318.782738695691,319.782096829258,
320.781454962824,321.78081309639,322.780171229956,323.584043319749),
 .UNSPECIFIED.);
#1267=B_SPLINE_CURVE_WITH_KNOTS('',3,(#56761,#56762,#56763,#56764,#56765,
#56766,#56767,#56768,#56769,#56770),.UNSPECIFIED.,.F.,.F.,(4,1,1,1,1,1,
1,4),(311.017672705389,311.816687846059,312.816045979625,313.815404113191,
314.814762246757,315.814120380323,316.81347851389,317.300858012569),
 .UNSPECIFIED.);
#1268=B_SPLINE_CURVE_WITH_KNOTS('',3,(#56771,#56772,#56773,#56774,#56775,
#56776,#56777,#56778,#56779,#56780),.UNSPECIFIED.,.F.,.F.,(4,1,1,1,1,1,
1,4),(311.01767270539,311.787231760729,312.786589894295,313.785948027861,
314.785306161427,315.784664294993,316.784022428559,317.300858012569),
 .UNSPECIFIED.);
#1269=B_SPLINE_CURVE_WITH_KNOTS('',3,(#56785,#56786,#56787,#56788,#56789,
#56790,#56791,#56792,#56793,#56794,#56795),.UNSPECIFIED.,.F.,.F.,(4,1,1,
1,1,1,1,1,4),(304.73448739821,304.821180911097,305.820539044663,306.819897178229,
307.819255311795,308.818613445361,309.817971578927,310.817329712493,311.017672705389),
 .UNSPECIFIED.);
#1270=B_SPLINE_CURVE_WITH_KNOTS('',3,(#56796,#56797,#56798,#56799,#56800,
#56801,#56802,#56803,#56804,#56805,#56806),.UNSPECIFIED.,.F.,.F.,(4,1,1,
1,1,1,1,1,4),(304.73448739821,304.791724825767,305.791082959333,306.790441092899,
307.789799226465,308.789157360031,309.788515493597,310.787873627163,311.01767270539),
 .UNSPECIFIED.);
#1271=B_SPLINE_CURVE_WITH_KNOTS('',3,(#56811,#56812,#56813,#56814,#56815,
#56816,#56817,#56818,#56819,#56820),.UNSPECIFIED.,.F.,.F.,(4,1,1,1,1,1,
1,4),(298.45130209103,298.825032109701,299.824390243267,300.823748376833,
301.823106510399,302.822464643965,303.821822777531,304.73448739821),
 .UNSPECIFIED.);
#1272=B_SPLINE_CURVE_WITH_KNOTS('',3,(#56821,#56822,#56823,#56824,#56825,
#56826,#56827,#56828,#56829,#56830),.UNSPECIFIED.,.F.,.F.,(4,1,1,1,1,1,
1,4),(298.451302091031,298.795576024371,299.794934157937,300.794292291503,
301.793650425069,302.793008558635,303.792366692201,304.73448739821),
 .UNSPECIFIED.);
#1273=B_SPLINE_CURVE_WITH_KNOTS('',3,(#56835,#56836,#56837,#56838,#56839,
#56840,#56841,#56842,#56843,#56844),.UNSPECIFIED.,.F.,.F.,(4,1,1,1,1,1,
1,4),(292.168116783851,292.828883308304,293.82824144187,294.827599575437,
295.826957709003,296.826315842569,297.825673976135,298.45130209103),
 .UNSPECIFIED.);
#1274=B_SPLINE_CURVE_WITH_KNOTS('',3,(#56845,#56846,#56847,#56848,#56849,
#56850,#56851,#56852,#56853,#56854),.UNSPECIFIED.,.F.,.F.,(4,1,1,1,1,1,
1,4),(292.168116783851,292.799427222974,293.79878535654,294.798143490106,
295.797501623672,296.796859757238,297.796217890804,298.451302091031),
 .UNSPECIFIED.);
#1275=B_SPLINE_CURVE_WITH_KNOTS('',3,(#56859,#56860,#56861,#56862,#56863,
#56864,#56865,#56866,#56867,#56868),.UNSPECIFIED.,.F.,.F.,(4,1,1,1,1,1,
1,4),(285.884931476671,286.832734506908,287.832092640474,288.83145077404,
289.830808907606,290.830167041172,291.829525174738,292.168116783851),
 .UNSPECIFIED.);
#1276=B_SPLINE_CURVE_WITH_KNOTS('',3,(#56869,#56870,#56871,#56872,#56873,
#56874,#56875,#56876,#56877,#56878),.UNSPECIFIED.,.F.,.F.,(4,1,1,1,1,1,
1,4),(285.884931476672,286.803278421578,287.802636555144,288.80199468871,
289.801352822276,290.800710955842,291.800069089408,292.168116783851),
 .UNSPECIFIED.);
#1277=B_SPLINE_CURVE_WITH_KNOTS('',3,(#56883,#56884,#56885,#56886,#56887,
#56888,#56889,#56890,#56891,#56892,#56893),.UNSPECIFIED.,.F.,.F.,(4,1,1,
1,1,1,1,1,4),(279.601746169492,279.837227571946,280.836585705512,281.835943839078,
282.835301972644,283.83466010621,284.834018239776,285.833376373342,285.884931476671),
 .UNSPECIFIED.);
#1278=B_SPLINE_CURVE_WITH_KNOTS('',3,(#56894,#56895,#56896,#56897,#56898,
#56899,#56900,#56901,#56902,#56903,#56904),.UNSPECIFIED.,.F.,.F.,(4,1,1,
1,1,1,1,1,4),(279.601746169492,279.807771486616,280.807129620182,281.806487753748,
282.805845887314,283.80520402088,284.804562154446,285.803920288012,285.884931476672),
 .UNSPECIFIED.);
#1279=B_SPLINE_CURVE_WITH_KNOTS('',3,(#56909,#56910,#56911,#56912,#56913,
#56914,#56915,#56916,#56917,#56918),.UNSPECIFIED.,.F.,.F.,(4,1,1,1,1,1,
1,4),(273.318560862312,273.84107877055,274.840436904116,275.839795037682,
276.839153171248,277.838511304814,278.83786943838,279.601746169492),
 .UNSPECIFIED.);
#1280=B_SPLINE_CURVE_WITH_KNOTS('',3,(#56919,#56920,#56921,#56922,#56923,
#56924,#56925,#56926,#56927,#56928),.UNSPECIFIED.,.F.,.F.,(4,1,1,1,1,1,
1,4),(273.318560862312,273.811622685219,274.810980818785,275.810338952351,
276.809697085917,277.809055219484,278.80841335305,279.601746169492),
 .UNSPECIFIED.);
#1281=B_SPLINE_CURVE_WITH_KNOTS('',3,(#56933,#56934,#56935,#56936,#56937,
#56938,#56939,#56940,#56941,#56942),.UNSPECIFIED.,.F.,.F.,(4,1,1,1,1,1,
1,4),(267.035375555133,267.844929969153,268.844288102719,269.843646236285,
270.843004369851,271.842362503417,272.841720636983,273.318560862312),
 .UNSPECIFIED.);
#1282=B_SPLINE_CURVE_WITH_KNOTS('',3,(#56943,#56944,#56945,#56946,#56947,
#56948,#56949,#56950,#56951,#56952),.UNSPECIFIED.,.F.,.F.,(4,1,1,1,1,1,
1,4),(267.035375555133,267.815473883823,268.814832017389,269.814190150955,
270.813548284521,271.812906418087,272.812264551653,273.318560862312),
 .UNSPECIFIED.);
#1283=B_SPLINE_CURVE_WITH_KNOTS('',3,(#56957,#56958,#56959,#56960,#56961,
#56962,#56963,#56964,#56965,#56966,#56967),.UNSPECIFIED.,.F.,.F.,(4,1,1,
1,1,1,1,1,4),(260.752190247953,260.849423034191,261.848781167757,262.848139301323,
263.847497434889,264.846855568455,265.846213702021,266.845571835587,267.035375555133),
 .UNSPECIFIED.);
#1284=B_SPLINE_CURVE_WITH_KNOTS('',3,(#56968,#56969,#56970,#56971,#56972,
#56973,#56974,#56975,#56976,#56977,#56978),.UNSPECIFIED.,.F.,.F.,(4,1,1,
1,1,1,1,1,4),(260.752190247953,260.819966948861,261.819325082427,262.818683215993,
263.818041349559,264.817399483125,265.816757616691,266.816115750257,267.035375555133),
 .UNSPECIFIED.);
#1285=B_SPLINE_CURVE_WITH_KNOTS('',3,(#56983,#56984,#56985,#56986,#56987,
#56988,#56989,#56990,#56991,#56992),.UNSPECIFIED.,.F.,.F.,(4,1,1,1,1,1,
1,4),(254.469004940773,254.853274232795,255.852632366361,256.851990499927,
257.851348633493,258.850706767059,259.850064900625,260.752190247953),
 .UNSPECIFIED.);
#1286=B_SPLINE_CURVE_WITH_KNOTS('',3,(#56993,#56994,#56995,#56996,#56997,
#56998,#56999,#57000,#57001,#57002),.UNSPECIFIED.,.F.,.F.,(4,1,1,1,1,1,
1,4),(254.469004940774,254.823818147464,255.82317628103,256.822534414597,
257.821892548163,258.821250681729,259.820608815295,260.752190247953),
 .UNSPECIFIED.);
#1287=B_SPLINE_CURVE_WITH_KNOTS('',3,(#57007,#57008,#57009,#57010,#57011,
#57012,#57013,#57014,#57015,#57016),.UNSPECIFIED.,.F.,.F.,(4,1,1,1,1,1,
1,4),(248.185819633594,248.857125431398,249.856483564964,250.85584169853,
251.855199832097,252.854557965663,253.853916099229,254.469004940773),
 .UNSPECIFIED.);
#1288=B_SPLINE_CURVE_WITH_KNOTS('',3,(#57017,#57018,#57019,#57020,#57021,
#57022,#57023,#57024,#57025,#57026),.UNSPECIFIED.,.F.,.F.,(4,1,1,1,1,1,
1,4),(248.185819633594,248.827669346068,249.827027479634,250.8263856132,
251.825743746766,252.825101880332,253.824460013898,254.469004940774),
 .UNSPECIFIED.);
#1289=B_SPLINE_CURVE_WITH_KNOTS('',3,(#57031,#57032,#57033,#57034,#57035,
#57036,#57037,#57038,#57039,#57040),.UNSPECIFIED.,.F.,.F.,(4,1,1,1,1,1,
1,4),(241.902634326414,242.860976630002,243.860334763568,244.859692897134,
245.8590510307,246.858409164266,247.857767297832,248.185819633594),
 .UNSPECIFIED.);
#1290=B_SPLINE_CURVE_WITH_KNOTS('',3,(#57041,#57042,#57043,#57044,#57045,
#57046,#57047,#57048,#57049,#57050),.UNSPECIFIED.,.F.,.F.,(4,1,1,1,1,1,
1,4),(241.902634326415,242.831520544672,243.830878678238,244.830236811804,
245.82959494537,246.828953078936,247.828311212502,248.185819633594),
 .UNSPECIFIED.);
#1291=B_SPLINE_CURVE_WITH_KNOTS('',3,(#57055,#57056,#57057,#57058,#57059,
#57060,#57061,#57062,#57063,#57064,#57065),.UNSPECIFIED.,.F.,.F.,(4,1,1,
1,1,1,1,1,4),(235.619449019235,235.86546969504,236.864827828606,237.864185962172,
238.863544095738,239.862902229304,240.86226036287,241.861618496436,241.902634326414),
 .UNSPECIFIED.);
#1292=B_SPLINE_CURVE_WITH_KNOTS('',3,(#57066,#57067,#57068,#57069,#57070,
#57071,#57072,#57073,#57074,#57075,#57076),.UNSPECIFIED.,.F.,.F.,(4,1,1,
1,1,1,1,1,4),(235.619449019235,235.83601360971,236.835371743276,237.834729876842,
238.834088010408,239.833446143974,240.83280427754,241.832162411106,241.902634326415),
 .UNSPECIFIED.);
#1293=B_SPLINE_CURVE_WITH_KNOTS('',3,(#57081,#57082,#57083,#57084,#57085,
#57086,#57087,#57088,#57089,#57090),.UNSPECIFIED.,.F.,.F.,(4,1,1,1,1,1,
1,4),(229.336263712055,229.869320893643,230.86867902721,231.868037160776,
232.867395294342,233.866753427908,234.866111561474,235.619449019235),
 .UNSPECIFIED.);
#1294=B_SPLINE_CURVE_WITH_KNOTS('',3,(#57091,#57092,#57093,#57094,#57095,
#57096,#57097,#57098,#57099,#57100),.UNSPECIFIED.,.F.,.F.,(4,1,1,1,1,1,
1,4),(229.336263712055,229.839864808313,230.839222941879,231.838581075445,
232.837939209011,233.837297342577,234.836655476144,235.619449019235),
 .UNSPECIFIED.);
#1295=B_SPLINE_CURVE_WITH_KNOTS('',3,(#57105,#57106,#57107,#57108,#57109,
#57110,#57111,#57112,#57113,#57114),.UNSPECIFIED.,.F.,.F.,(4,1,1,1,1,1,
1,4),(223.053078404876,223.873172092247,224.872530225813,225.871888359379,
226.871246492945,227.870604626511,228.869962760077,229.336263712055),
 .UNSPECIFIED.);
#1296=B_SPLINE_CURVE_WITH_KNOTS('',3,(#57115,#57116,#57117,#57118,#57119,
#57120,#57121,#57122,#57123,#57124),.UNSPECIFIED.,.F.,.F.,(4,1,1,1,1,1,
1,4),(223.053078404876,223.843716006917,224.843074140483,225.842432274049,
226.841790407615,227.841148541181,228.840506674747,229.336263712055),
 .UNSPECIFIED.);
#1297=B_SPLINE_CURVE_WITH_KNOTS('',3,(#57129,#57130,#57131,#57132,#57133,
#57134,#57135,#57136,#57137,#57138,#57139),.UNSPECIFIED.,.F.,.F.,(4,1,1,
1,1,1,1,1,4),(216.769893097696,216.877665157285,217.877023290851,218.876381424417,
219.875739557983,220.875097691549,221.874455825115,222.873813958681,223.053078404876),
 .UNSPECIFIED.);
#1298=B_SPLINE_CURVE_WITH_KNOTS('',3,(#57140,#57141,#57142,#57143,#57144,
#57145,#57146,#57147,#57148,#57149,#57150),.UNSPECIFIED.,.F.,.F.,(4,1,1,
1,1,1,1,1,4),(216.769893097696,216.848209071955,217.847567205521,218.846925339087,
219.846283472653,220.845641606219,221.844999739785,222.844357873351,223.053078404876),
 .UNSPECIFIED.);
#1299=B_SPLINE_CURVE_WITH_KNOTS('',3,(#57155,#57156,#57157,#57158,#57159,
#57160,#57161,#57162,#57163,#57164),.UNSPECIFIED.,.F.,.F.,(4,1,1,1,1,1,
1,4),(210.486707790516,210.881516355889,211.880874489455,212.880232623021,
213.879590756587,214.878948890153,215.878307023719,216.769893097696),
 .UNSPECIFIED.);
#1300=B_SPLINE_CURVE_WITH_KNOTS('',3,(#57165,#57166,#57167,#57168,#57169,
#57170,#57171,#57172,#57173,#57174),.UNSPECIFIED.,.F.,.F.,(4,1,1,1,1,1,
1,4),(210.486707790517,210.852060270558,211.851418404124,212.85077653769,
213.850134671257,214.849492804823,215.848850938389,216.769893097696),
 .UNSPECIFIED.);
#1301=B_SPLINE_CURVE_WITH_KNOTS('',3,(#57179,#57180,#57181,#57182,#57183,
#57184,#57185,#57186,#57187,#57188),.UNSPECIFIED.,.F.,.F.,(4,1,1,1,1,1,
1,4),(204.203522483337,204.885367554492,205.884725688058,206.884083821624,
207.88344195519,208.882800088756,209.882158222323,210.486707790516),
 .UNSPECIFIED.);
#1302=B_SPLINE_CURVE_WITH_KNOTS('',3,(#57189,#57190,#57191,#57192,#57193,
#57194,#57195,#57196,#57197,#57198),.UNSPECIFIED.,.F.,.F.,(4,1,1,1,1,1,
1,4),(204.203522483337,204.855911469162,205.855269602728,206.854627736294,
207.85398586986,208.853344003426,209.852702136992,210.486707790517),
 .UNSPECIFIED.);
#1303=B_SPLINE_CURVE_WITH_KNOTS('',3,(#57203,#57204,#57205,#57206,#57207,
#57208,#57209,#57210,#57211,#57212),.UNSPECIFIED.,.F.,.F.,(4,1,1,1,1,1,
1,4),(197.920337176157,198.889218753096,199.888576886662,200.887935020228,
201.887293153794,202.88665128736,203.886009420926,204.203522483337),
 .UNSPECIFIED.);
#1304=B_SPLINE_CURVE_WITH_KNOTS('',3,(#57213,#57214,#57215,#57216,#57217,
#57218,#57219,#57220,#57221,#57222),.UNSPECIFIED.,.F.,.F.,(4,1,1,1,1,1,
1,4),(197.920337176158,198.859762667766,199.859120801332,200.858478934898,
201.857837068464,202.85719520203,203.856553335596,204.203522483337),
 .UNSPECIFIED.);
#1305=B_SPLINE_CURVE_WITH_KNOTS('',3,(#57227,#57228,#57229,#57230,#57231,
#57232,#57233,#57234,#57235,#57236,#57237),.UNSPECIFIED.,.F.,.F.,(4,1,1,
1,1,1,1,1,4),(191.637151868978,191.893711818134,192.8930699517,193.892428085266,
194.891786218832,195.891144352398,196.890502485964,197.88986061953,197.920337176157),
 .UNSPECIFIED.);
#1306=B_SPLINE_CURVE_WITH_KNOTS('',3,(#57238,#57239,#57240,#57241,#57242,
#57243,#57244,#57245,#57246,#57247,#57248),.UNSPECIFIED.,.F.,.F.,(4,1,1,
1,1,1,1,1,4),(191.637151868978,191.864255732803,192.86361386637,193.862971999936,
194.862330133502,195.861688267068,196.861046400634,197.8604045342,197.920337176158),
 .UNSPECIFIED.);
#1307=B_SPLINE_CURVE_WITH_KNOTS('',3,(#57253,#57254,#57255,#57256,#57257,
#57258,#57259,#57260,#57261,#57262),.UNSPECIFIED.,.F.,.F.,(4,1,1,1,1,1,
1,4),(185.353966561798,185.897563016737,186.896921150303,187.89627928387,
188.895637417436,189.894995551002,190.894353684568,191.637151868978),
 .UNSPECIFIED.);
#1308=B_SPLINE_CURVE_WITH_KNOTS('',3,(#57263,#57264,#57265,#57266,#57267,
#57268,#57269,#57270,#57271,#57272),.UNSPECIFIED.,.F.,.F.,(4,1,1,1,1,1,
1,4),(185.353966561799,185.868106931407,186.867465064973,187.866823198539,
188.866181332105,189.865539465671,190.864897599237,191.637151868978),
 .UNSPECIFIED.);
#1309=B_SPLINE_CURVE_WITH_KNOTS('',3,(#57277,#57278,#57279,#57280,#57281,
#57282,#57283,#57284,#57285,#57286),.UNSPECIFIED.,.F.,.F.,(4,1,1,1,1,1,
1,4),(179.070781254619,179.901414215341,180.900772348907,181.900130482473,
182.899488616039,183.898846749605,184.898204883171,185.353966561798),
 .UNSPECIFIED.);
#1310=B_SPLINE_CURVE_WITH_KNOTS('',3,(#57287,#57288,#57289,#57290,#57291,
#57292,#57293,#57294,#57295,#57296),.UNSPECIFIED.,.F.,.F.,(4,1,1,1,1,1,
1,4),(179.070781254619,179.871958130011,180.871316263577,181.870674397143,
182.870032530709,183.869390664275,184.868748797841,185.353966561799),
 .UNSPECIFIED.);
#1311=B_SPLINE_CURVE_WITH_KNOTS('',3,(#57301,#57302,#57303,#57304,#57305,
#57306,#57307,#57308,#57309,#57310,#57311),.UNSPECIFIED.,.F.,.F.,(4,1,1,
1,1,1,1,1,4),(172.787595947439,172.905907280379,173.905265413945,174.904623547511,
175.903981681077,176.903339814643,177.902697948209,178.902056081775,179.070781254619),
 .UNSPECIFIED.);
#1312=B_SPLINE_CURVE_WITH_KNOTS('',3,(#57312,#57313,#57314,#57315,#57316,
#57317,#57318,#57319,#57320,#57321,#57322),.UNSPECIFIED.,.F.,.F.,(4,1,1,
1,1,1,1,1,4),(172.787595947439,172.876451195049,173.875809328615,174.875167462181,
175.874525595747,176.873883729313,177.873241862879,178.872599996445,179.070781254619),
 .UNSPECIFIED.);
#1313=B_SPLINE_CURVE_WITH_KNOTS('',3,(#57327,#57328,#57329,#57330,#57331,
#57332,#57333,#57334,#57335,#57336),.UNSPECIFIED.,.F.,.F.,(4,1,1,1,1,1,
1,4),(166.504410640259,166.909758478983,167.909116612549,168.908474746115,
169.907832879681,170.907191013247,171.906549146813,172.787595947439),
 .UNSPECIFIED.);
#1314=B_SPLINE_CURVE_WITH_KNOTS('',3,(#57337,#57338,#57339,#57340,#57341,
#57342,#57343,#57344,#57345,#57346),.UNSPECIFIED.,.F.,.F.,(4,1,1,1,1,1,
1,4),(166.50441064026,166.880302393652,167.879660527218,168.879018660784,
169.87837679435,170.877734927916,171.877093061483,172.787595947439),
 .UNSPECIFIED.);
#1315=B_SPLINE_CURVE_WITH_KNOTS('',3,(#57351,#57352,#57353,#57354,#57355,
#57356,#57357,#57358,#57359,#57360),.UNSPECIFIED.,.F.,.F.,(4,1,1,1,1,1,
1,4),(160.22122533308,160.913609677586,161.912967811152,162.912325944718,
163.911684078284,164.91104221185,165.910400345416,166.504410640259),
 .UNSPECIFIED.);
#1316=B_SPLINE_CURVE_WITH_KNOTS('',3,(#57361,#57362,#57363,#57364,#57365,
#57366,#57367,#57368,#57369,#57370),.UNSPECIFIED.,.F.,.F.,(4,1,1,1,1,1,
1,4),(160.22122533308,160.884153592256,161.883511725822,162.882869859388,
163.882227992954,164.88158612652,165.880944260086,166.50441064026),
 .UNSPECIFIED.);
#1317=B_SPLINE_CURVE_WITH_KNOTS('',3,(#57375,#57376,#57377,#57378,#57379,
#57380,#57381,#57382,#57383,#57384),.UNSPECIFIED.,.F.,.F.,(4,1,1,1,1,1,
1,4),(153.9380400259,154.91746087619,155.916819009756,156.916177143322,
157.915535276888,158.914893410454,159.91425154402,160.22122533308),
 .UNSPECIFIED.);
#1318=B_SPLINE_CURVE_WITH_KNOTS('',3,(#57385,#57386,#57387,#57388,#57389,
#57390,#57391,#57392,#57393,#57394),.UNSPECIFIED.,.F.,.F.,(4,1,1,1,1,1,
1,4),(153.938040025901,154.88800479086,155.887362924426,156.886721057992,
157.886079191558,158.885437325124,159.88479545869,160.22122533308),
 .UNSPECIFIED.);
#1319=B_SPLINE_CURVE_WITH_KNOTS('',3,(#57399,#57400,#57401,#57402,#57403,
#57404,#57405,#57406,#57407,#57408,#57409),.UNSPECIFIED.,.F.,.F.,(4,1,1,
1,1,1,1,1,4),(147.654854718721,147.921953941228,148.921312074794,149.92067020836,
150.920028341926,151.919386475492,152.918744609058,153.918102742624,153.9380400259),
 .UNSPECIFIED.);
#1320=B_SPLINE_CURVE_WITH_KNOTS('',3,(#57410,#57411,#57412,#57413,#57414,
#57415,#57416,#57417,#57418,#57419,#57420),.UNSPECIFIED.,.F.,.F.,(4,1,1,
1,1,1,1,1,4),(147.654854718721,147.892497855897,148.891855989463,149.891214123029,
150.890572256596,151.889930390162,152.889288523728,153.888646657294,153.938040025901),
 .UNSPECIFIED.);
#1321=B_SPLINE_CURVE_WITH_KNOTS('',3,(#57425,#57426,#57427,#57428,#57429,
#57430,#57431,#57432,#57433,#57434),.UNSPECIFIED.,.F.,.F.,(4,1,1,1,1,1,
1,4),(141.371669411541,141.925805139831,142.925163273397,143.924521406963,
144.92387954053,145.923237674096,146.922595807662,147.654854718721),
 .UNSPECIFIED.);
#1322=B_SPLINE_CURVE_WITH_KNOTS('',3,(#57435,#57436,#57437,#57438,#57439,
#57440,#57441,#57442,#57443,#57444),.UNSPECIFIED.,.F.,.F.,(4,1,1,1,1,1,
1,4),(141.371669411542,141.896349054501,142.895707188067,143.895065321633,
144.894423455199,145.893781588765,146.893139722331,147.654854718721),
 .UNSPECIFIED.);
#1323=B_SPLINE_CURVE_WITH_KNOTS('',3,(#57449,#57450,#57451,#57452,#57453,
#57454,#57455,#57456,#57457,#57458),.UNSPECIFIED.,.F.,.F.,(4,1,1,1,1,1,
1,4),(135.088484104362,135.929656338435,136.929014472001,137.928372605567,
138.927730739133,139.927088872699,140.926447006265,141.371669411541),
 .UNSPECIFIED.);
#1324=B_SPLINE_CURVE_WITH_KNOTS('',3,(#57459,#57460,#57461,#57462,#57463,
#57464,#57465,#57466,#57467,#57468),.UNSPECIFIED.,.F.,.F.,(4,1,1,1,1,1,
1,4),(135.088484104362,135.900200253105,136.899558386671,137.898916520237,
138.898274653803,139.897632787369,140.896990920935,141.371669411542),
 .UNSPECIFIED.);
#1325=B_SPLINE_CURVE_WITH_KNOTS('',3,(#57473,#57474,#57475,#57476,#57477,
#57478,#57479,#57480,#57481,#57482,#57483),.UNSPECIFIED.,.F.,.F.,(4,1,1,
1,1,1,1,1,4),(128.805298797182,128.934149403473,129.933507537039,130.932865670605,
131.932223804171,132.931581937737,133.930940071303,134.930298204869,135.088484104362),
 .UNSPECIFIED.);
#1326=B_SPLINE_CURVE_WITH_KNOTS('',3,(#57484,#57485,#57486,#57487,#57488,
#57489,#57490,#57491,#57492,#57493,#57494),.UNSPECIFIED.,.F.,.F.,(4,1,1,
1,1,1,1,1,4),(128.805298797182,128.904693318142,129.904051451709,130.903409585275,
131.902767718841,132.902125852407,133.901483985973,134.900842119539,135.088484104362),
 .UNSPECIFIED.);
#1327=B_SPLINE_CURVE_WITH_KNOTS('',3,(#57499,#57500,#57501,#57502,#57503,
#57504,#57505,#57506,#57507,#57508),.UNSPECIFIED.,.F.,.F.,(4,1,1,1,1,1,
1,4),(122.522113490002,122.938000602077,123.937358735643,124.936716869209,
125.936075002775,126.935433136341,127.934791269907,128.805298797182),
 .UNSPECIFIED.);
#1328=B_SPLINE_CURVE_WITH_KNOTS('',3,(#57509,#57510,#57511,#57512,#57513,
#57514,#57515,#57516,#57517,#57518),.UNSPECIFIED.,.F.,.F.,(4,1,1,1,1,1,
1,4),(122.522113490003,122.908544516746,123.907902650312,124.907260783878,
125.906618917444,126.90597705101,127.905335184576,128.805298797182),
 .UNSPECIFIED.);
#1329=B_SPLINE_CURVE_WITH_KNOTS('',3,(#57523,#57524,#57525,#57526,#57527,
#57528,#57529,#57530,#57531,#57532),.UNSPECIFIED.,.F.,.F.,(4,1,1,1,1,1,
1,4),(116.238928182823,116.94185180068,117.941209934246,118.940568067812,
119.939926201378,120.939284334944,121.93864246851,122.522113490002),
 .UNSPECIFIED.);
#1330=B_SPLINE_CURVE_WITH_KNOTS('',3,(#57533,#57534,#57535,#57536,#57537,
#57538,#57539,#57540,#57541,#57542),.UNSPECIFIED.,.F.,.F.,(4,1,1,1,1,1,
1,4),(116.238928182823,116.91239571535,117.911753848916,118.911111982482,
119.910470116048,120.909828249614,121.90918638318,122.522113490003),
 .UNSPECIFIED.);
#1331=B_SPLINE_CURVE_WITH_KNOTS('',3,(#57547,#57548,#57549,#57550,#57551,
#57552,#57553,#57554,#57555,#57556),.UNSPECIFIED.,.F.,.F.,(4,1,1,1,1,1,
1,4),(109.955742875643,110.945702999284,111.94506113285,112.944419266416,
113.943777399982,114.943135533548,115.942493667114,116.238928182823),
 .UNSPECIFIED.);
#1332=B_SPLINE_CURVE_WITH_KNOTS('',3,(#57557,#57558,#57559,#57560,#57561,
#57562,#57563,#57564,#57565,#57566),.UNSPECIFIED.,.F.,.F.,(4,1,1,1,1,1,
1,4),(109.955742875644,110.916246913954,111.91560504752,112.914963181086,
113.914321314652,114.913679448218,115.913037581784,116.238928182823),
 .UNSPECIFIED.);
#1333=B_SPLINE_CURVE_WITH_KNOTS('',3,(#57571,#57572,#57573,#57574,#57575,
#57576,#57577,#57578,#57579,#57580,#57581),.UNSPECIFIED.,.F.,.F.,(4,1,1,
1,1,1,1,1,4),(103.672557568464,103.950196064322,104.949554197888,105.948912331454,
106.94827046502,107.947628598586,108.946986732152,109.946344865718,109.955742875643),
 .UNSPECIFIED.);
#1334=B_SPLINE_CURVE_WITH_KNOTS('',3,(#57582,#57583,#57584,#57585,#57586,
#57587,#57588,#57589,#57590,#57591,#57592),.UNSPECIFIED.,.F.,.F.,(4,1,1,
1,1,1,1,1,4),(103.672557568464,103.920739978991,104.920098112557,105.919456246123,
106.918814379689,107.918172513255,108.917530646822,109.916888780388,109.955742875644),
 .UNSPECIFIED.);
#1335=B_SPLINE_CURVE_WITH_KNOTS('',3,(#57597,#57598,#57599,#57600,#57601,
#57602,#57603,#57604,#57605,#57606),.UNSPECIFIED.,.F.,.F.,(4,1,1,1,1,1,
1,4),(97.3893722612841,97.9540472629253,98.9534053964914,99.9527635300574,
100.952121663623,101.95147979719,102.950837930756,103.672557568464),
 .UNSPECIFIED.);
#1336=B_SPLINE_CURVE_WITH_KNOTS('',3,(#57607,#57608,#57609,#57610,#57611,
#57612,#57613,#57614,#57615,#57616),.UNSPECIFIED.,.F.,.F.,(4,1,1,1,1,1,
1,4),(97.3893722612845,97.924591177595,98.9239493111611,99.9233074447271,
100.922665578293,101.922023711859,102.921381845425,103.672557568464),
 .UNSPECIFIED.);
#1337=B_SPLINE_CURVE_WITH_KNOTS('',3,(#57621,#57622,#57623,#57624,#57625,
#57626,#57627,#57628,#57629,#57630),.UNSPECIFIED.,.F.,.F.,(4,1,1,1,1,1,
1,4),(91.1061869541045,91.9578984615291,92.9572565950951,93.9566147286612,
94.9559728622272,95.9553309957932,96.9546891293593,97.3893722612841),
 .UNSPECIFIED.);
#1338=B_SPLINE_CURVE_WITH_KNOTS('',3,(#57631,#57632,#57633,#57634,#57635,
#57636,#57637,#57638,#57639,#57640),.UNSPECIFIED.,.F.,.F.,(4,1,1,1,1,1,
1,4),(91.1061869541048,91.9284423761987,92.9278005097648,93.9271586433308,
94.9265167768969,95.9258749104629,96.925233044029,97.3893722612845),
 .UNSPECIFIED.);
#1339=B_SPLINE_CURVE_WITH_KNOTS('',3,(#57645,#57646,#57647,#57648,#57649,
#57650,#57651,#57652,#57653,#57654,#57655),.UNSPECIFIED.,.F.,.F.,(4,1,1,
1,1,1,1,1,4),(84.8230016469249,84.9623915265667,85.9617496601328,86.9611077936988,
87.9604659272649,88.9598240608309,89.959182194397,90.958540327963,91.1061869541045),
 .UNSPECIFIED.);
#1340=B_SPLINE_CURVE_WITH_KNOTS('',3,(#57656,#57657,#57658,#57659,#57660,
#57661,#57662,#57663,#57664,#57665,#57666),.UNSPECIFIED.,.F.,.F.,(4,1,1,
1,1,1,1,1,4),(84.8230016469253,84.9329354412364,85.9322935748025,86.9316517083685,
87.9310098419346,88.9303679755006,89.9297261090666,90.9290842426327,91.1061869541048),
 .UNSPECIFIED.);
#1341=B_SPLINE_CURVE_WITH_KNOTS('',3,(#57671,#57672,#57673,#57674,#57675,
#57676,#57677,#57678,#57679,#57680),.UNSPECIFIED.,.F.,.F.,(4,1,1,1,1,1,
1,4),(78.5398163397454,78.9662427251705,79.9656008587365,80.9649589923026,
81.9643171258686,82.9636752594347,83.9630333930007,84.8230016469249),
 .UNSPECIFIED.);
#1342=B_SPLINE_CURVE_WITH_KNOTS('',3,(#57681,#57682,#57683,#57684,#57685,
#57686,#57687,#57688,#57689,#57690),.UNSPECIFIED.,.F.,.F.,(4,1,1,1,1,1,
1,4),(78.5398163397457,78.9367866398401,79.9361447734062,80.9355029069722,
81.9348610405383,82.9342191741043,83.9335773076704,84.8230016469253),
 .UNSPECIFIED.);
#1343=B_SPLINE_CURVE_WITH_KNOTS('',3,(#57695,#57696,#57697,#57698,#57699,
#57700,#57701,#57702,#57703,#57704),.UNSPECIFIED.,.F.,.F.,(4,1,1,1,1,1,
1,4),(72.2566310325658,72.9700939237742,73.9694520573402,74.9688101909063,
75.9681683244723,76.9675264580384,77.9668845916044,78.5398163397454),
 .UNSPECIFIED.);
#1344=B_SPLINE_CURVE_WITH_KNOTS('',3,(#57705,#57706,#57707,#57708,#57709,
#57710,#57711,#57712,#57713,#57714),.UNSPECIFIED.,.F.,.F.,(4,1,1,1,1,1,
1,4),(72.2566310325661,72.9406378384438,73.9399959720099,74.9393541055759,
75.938712239142,76.938070372708,77.9374285062741,78.5398163397457),
 .UNSPECIFIED.);
#1345=B_SPLINE_CURVE_WITH_KNOTS('',3,(#57719,#57720,#57721,#57722,#57723,
#57724,#57725,#57726,#57727,#57728,#57729),.UNSPECIFIED.,.F.,.F.,(4,1,1,
1,1,1,1,1,4),(65.9734457253862,65.9745869888119,66.9739451223779,67.9733032559439,
68.97266138951,69.972019523076,70.9713776566421,71.9707357902081,72.2566310325658),
 .UNSPECIFIED.);
#1346=B_SPLINE_CURVE_WITH_KNOTS('',3,(#57730,#57731,#57732,#57733,#57734,
#57735,#57736,#57737,#57738,#57739),.UNSPECIFIED.,.F.,.F.,(4,1,1,1,1,1,
1,4),(65.9734457253865,66.9444890370476,67.9438471706136,68.9432053041797,
69.9425634377457,70.9419215713118,71.9412797048778,72.2566310325661),
 .UNSPECIFIED.);
#1347=B_SPLINE_CURVE_WITH_KNOTS('',3,(#57744,#57745,#57746,#57747,#57748,
#57749,#57750,#57751,#57752,#57753,#57754,#57755),.UNSPECIFIED.,.F.,.F.,
(4,1,1,1,1,1,1,1,1,4),(59.6902604182066,59.9784381874156,60.4781172541986,
60.9777963209816,61.4774753877646,61.9771544545477,62.9765125881137,63.9758707216798,
64.9752288552458,65.9734457253862),.UNSPECIFIED.);
#1348=B_SPLINE_CURVE_WITH_KNOTS('',3,(#57756,#57757,#57758,#57759,#57760,
#57761,#57762,#57763,#57764,#57765,#57766),.UNSPECIFIED.,.F.,.F.,(4,1,1,
1,1,1,1,1,4),(59.6902604182069,59.9489821020852,60.9483402356513,61.9476983692173,
62.9470565027834,63.9464146363494,64.9457727699155,65.9451309034815,65.9734457253865),
 .UNSPECIFIED.);
#1349=B_SPLINE_CURVE_WITH_KNOTS('',3,(#57771,#57772,#57773,#57774,#57775,
#57776,#57777,#57778,#57779,#57780,#57781,#57782,#57783,#57784,#57785,#57786,
#57787),.UNSPECIFIED.,.F.,.F.,(4,1,1,1,1,1,1,1,1,1,1,1,1,1,4),(53.407075111027,
53.4826103192363,53.9822893860193,54.4819684528023,54.9816475195853,55.4813265863684,
55.9810056531514,56.4806847199344,56.9803637867174,57.4800428535005,57.9797219202835,
58.4794009870665,58.9790800538495,59.4787591206325,59.6902604182066),
 .UNSPECIFIED.);
#1350=B_SPLINE_CURVE_WITH_KNOTS('',3,(#57788,#57789,#57790,#57791,#57792,
#57793,#57794,#57795,#57796,#57797,#57798,#57799,#57800,#57801,#57802,#57803),
 .UNSPECIFIED.,.F.,.F.,(4,1,1,1,1,1,1,1,1,1,1,1,1,4),(53.4070751110273,
53.4531542339059,53.9528333006889,54.452512367472,54.952191434255,55.451870501038,
55.951549567821,56.4512286346041,56.9509077013871,57.4505867681701,57.9502658349531,
58.4499449017362,58.9496239685192,59.6902604182069),.UNSPECIFIED.);
#1351=B_SPLINE_CURVE_WITH_KNOTS('',3,(#57808,#57809,#57810,#57811,#57812,
#57813,#57814,#57815,#57816,#57817,#57818,#57819,#57820,#57821,#57822,#57823),
 .UNSPECIFIED.,.F.,.F.,(4,1,1,1,1,1,1,1,1,1,1,1,1,4),(47.1238898038474,
47.48646151784,47.986140584623,48.485819651406,48.9854987181891,49.4851777849721,
49.9848568517551,50.4845359185381,50.9842149853212,51.4838940521042,51.9835731188872,
52.4832521856702,52.9829312524532,53.407075111027),.UNSPECIFIED.);
#1352=B_SPLINE_CURVE_WITH_KNOTS('',3,(#57824,#57825,#57826,#57827,#57828,
#57829,#57830,#57831,#57832,#57833,#57834,#57835,#57836,#57837,#57838,#57839),
 .UNSPECIFIED.,.F.,.F.,(4,1,1,1,1,1,1,1,1,1,1,1,1,4),(47.1238898038477,
47.4570054325096,47.9566844992927,48.4563635660757,48.9560426328587,49.4557216996417,
49.9554007664248,50.4550798332078,50.9547588999908,51.4544379667738,51.9541170335568,
52.4537961003399,52.9534751671229,53.4070751110273),.UNSPECIFIED.);
#1353=B_SPLINE_CURVE_WITH_KNOTS('',3,(#57844,#57845,#57846,#57847,#57848,
#57849,#57850,#57851,#57852,#57853,#57854,#57855,#57856,#57857,#57858,#57859,
#57860),.UNSPECIFIED.,.F.,.F.,(4,1,1,1,1,1,1,1,1,1,1,1,1,1,4),(40.8407044966678,
40.9906336496607,41.4903127164437,41.9899917832267,42.4896708500098,42.9893499167928,
43.4890289835758,43.9887080503588,44.4883871171419,44.9880661839249,45.4877452507079,
45.9874243174909,46.4871033842739,46.986782451057,47.1238898038474),
 .UNSPECIFIED.);
#1354=B_SPLINE_CURVE_WITH_KNOTS('',3,(#57861,#57862,#57863,#57864,#57865,
#57866,#57867,#57868,#57869,#57870,#57871,#57872,#57873,#57874,#57875,#57876,
#57877),.UNSPECIFIED.,.F.,.F.,(4,1,1,1,1,1,1,1,1,1,1,1,1,1,4),(40.8407044966681,
40.9611775643303,41.4608566311134,41.9605356978964,42.4602147646794,42.9598938314624,
43.4595728982454,43.9592519650285,44.4589310318115,44.9586100985945,45.4582891653775,
45.9579682321606,46.4576472989436,46.9573263657266,47.1238898038477),
 .UNSPECIFIED.);
#1355=B_SPLINE_CURVE_WITH_KNOTS('',3,(#57882,#57883,#57884,#57885,#57886,
#57887,#57888,#57889,#57890,#57891,#57892,#57893,#57894,#57895,#57896,#57897),
 .UNSPECIFIED.,.F.,.F.,(4,1,1,1,1,1,1,1,1,1,1,1,1,4),(34.5575191894882,
34.9944848482644,35.4941639150474,35.9938429818305,36.4935220486135,36.9932011153965,
37.4928801821795,37.9925592489626,38.4922383157456,38.9919173825286,39.4915964493116,
39.9912755160946,40.4909545828777,40.8407044966678),.UNSPECIFIED.);
#1356=B_SPLINE_CURVE_WITH_KNOTS('',3,(#57898,#57899,#57900,#57901,#57902,
#57903,#57904,#57905,#57906,#57907,#57908,#57909,#57910,#57911,#57912,#57913),
 .UNSPECIFIED.,.F.,.F.,(4,1,1,1,1,1,1,1,1,1,1,1,1,4),(34.5575191894886,
34.965028762934,35.4647078297171,35.9643868965001,36.4640659632831,36.9637450300661,
37.4634240968492,37.9631031636322,38.4627822304152,38.9624612971982,39.4621403639813,
39.9618194307643,40.4614984975473,40.8407044966681),.UNSPECIFIED.);
#1357=B_SPLINE_CURVE_WITH_KNOTS('',3,(#57918,#57919,#57920,#57921,#57922,
#57923,#57924,#57925,#57926,#57927,#57928,#57929,#57930,#57931,#57932,#57933,
#57934),.UNSPECIFIED.,.F.,.F.,(4,1,1,1,1,1,1,1,1,1,1,1,1,1,4),(28.2743338823086,
28.4986569800851,28.9983360468681,29.4980151136512,29.9976941804342,30.4973732472172,
30.9970523140002,31.4967313807832,31.9964104475663,32.4960895143493,32.9957685811323,
33.4954476479153,33.9951267146984,34.4948057814814,34.5575191894882),
 .UNSPECIFIED.);
#1358=B_SPLINE_CURVE_WITH_KNOTS('',3,(#57935,#57936,#57937,#57938,#57939,
#57940,#57941,#57942,#57943,#57944,#57945,#57946,#57947,#57948,#57949,#57950,
#57951),.UNSPECIFIED.,.F.,.F.,(4,1,1,1,1,1,1,1,1,1,1,1,1,1,4),(28.2743338823089,
28.4692008947547,28.9688799615378,29.4685590283208,29.9682380951038,30.4679171618868,
30.9675962286699,31.4672752954529,31.9669543622359,32.4666334290189,32.966312495802,
33.465991562585,33.965670629368,34.465349696151,34.5575191894886),
 .UNSPECIFIED.);
#1359=B_SPLINE_CURVE_WITH_KNOTS('',3,(#57956,#57957,#57958,#57959,#57960,
#57961,#57962,#57963,#57964,#57965,#57966,#57967,#57968,#57969,#57970,#57971,
#57972),.UNSPECIFIED.,.F.,.F.,(4,1,1,1,1,1,1,1,1,1,1,1,1,1,4),(21.991148575129,
22.0028291119058,22.5025081786888,23.0021872454719,23.5018663122549,24.0015453790379,
24.5012244458209,25.0009035126039,25.500582579387,26.00026164617,26.499940712953,
26.999619779736,27.4992988465191,27.9989779133021,28.2743338823086),
 .UNSPECIFIED.);
#1360=B_SPLINE_CURVE_WITH_KNOTS('',3,(#57973,#57974,#57975,#57976,#57977,
#57978,#57979,#57980,#57981,#57982,#57983,#57984,#57985,#57986,#57987,#57988),
 .UNSPECIFIED.,.F.,.F.,(4,1,1,1,1,1,1,1,1,1,1,1,1,4),(21.9911485751294,
22.4730520933585,22.9727311601415,23.4724102269245,23.9720892937075,24.4717683604905,
24.9714474272736,25.4711264940566,25.9708055608396,26.4704846276226,26.9701636944057,
27.4698427611887,27.9695218279717,28.2743338823089),.UNSPECIFIED.);
#1361=B_SPLINE_CURVE_WITH_KNOTS('',3,(#57993,#57994,#57995,#57996,#57997,
#57998,#57999,#58000,#58001,#58002,#58003,#58004,#58005,#58006,#58007,#58008),
 .UNSPECIFIED.,.F.,.F.,(4,1,1,1,1,1,1,1,1,1,1,1,1,4),(15.7079632679495,
16.0066803105095,16.5063593772925,17.0060384440756,17.5057175108586,18.0053965776416,
18.5050756444246,19.0047547112077,19.5044337779907,20.0041128447737,20.5037919115567,
21.0034709783398,21.5031500451228,21.991148575129),.UNSPECIFIED.);
#1362=B_SPLINE_CURVE_WITH_KNOTS('',3,(#58009,#58010,#58011,#58012,#58013,
#58014,#58015,#58016,#58017,#58018,#58019,#58020,#58021,#58022,#58023,#58024,
#58025),.UNSPECIFIED.,.F.,.F.,(4,1,1,1,1,1,1,1,1,1,1,1,1,1,4),(15.7079632679498,
15.9772242251791,16.4769032919622,16.9765823587452,17.4762614255282,17.9759404923112,
18.4756195590943,18.9752986258773,19.4749776926603,19.9746567594433,20.4743358262264,
20.9740148930094,21.4736939597924,21.9733730265754,21.9911485751294),
 .UNSPECIFIED.);
#1363=B_SPLINE_CURVE_WITH_KNOTS('',3,(#58030,#58031,#58032,#58033,#58034,
#58035,#58036,#58037,#58038,#58039,#58040,#58041,#58042,#58043,#58044,#58045,
#58046,#58047,#58048,#58049,#58050,#58051,#58052,#58053,#58054,#58055,#58056,
#58057,#58058,#58059,#58060,#58061,#58062,#58063,#58064,#58065,#58066),
 .UNSPECIFIED.,.F.,.F.,(4,3,3,3,3,3,3,3,3,3,3,3,4),(0.,0.000373494560508806,
0.0620760815771024,0.112839239637108,0.153038169722591,0.175804963675793,
0.247183842626883,0.319084136954533,0.344742425233931,0.363606980156396,
0.439518700737557,0.51795432283266,0.534785019937482),.UNSPECIFIED.);
#1364=B_SPLINE_CURVE_WITH_KNOTS('',3,(#58068,#58069,#58070,#58071,#58072,
#58073,#58074,#58075,#58076,#58077,#58078,#58079,#58080,#58081,#58082,#58083,
#58084,#58085,#58086,#58087,#58088,#58089,#58090,#58091,#58092,#58093,#58094,
#58095,#58096,#58097,#58098,#58099,#58100,#58101,#58102,#58103,#58104),
 .UNSPECIFIED.,.F.,.F.,(4,3,3,3,3,3,3,3,3,3,3,3,4),(0.,0.000511892384038064,
0.078754853834616,0.155070466132989,0.20164291816609,0.227017770490094,
0.290460834304131,0.352619921814331,0.383703668213755,0.403796492255862,
0.466621120797767,0.52704524650008,0.539097184344933),.UNSPECIFIED.);
#1365=B_SPLINE_CURVE_WITH_KNOTS('',3,(#60104,#60105,#60106,#60107,#60108,
#60109,#60110,#60111,#60112,#60113,#60114,#60115,#60116,#60117,#60118,#60119,
#60120,#60121,#60122,#60123,#60124,#60125,#60126,#60127,#60128,#60129,#60130,
#60131,#60132,#60133,#60134,#60135,#60136,#60137,#60138,#60139,#60140,#60141,
#60142,#60143),.UNSPECIFIED.,.F.,.F.,(4,3,3,3,3,3,3,3,3,3,3,3,3,4),(-0.53478501993692,
-0.534277081309421,-0.456439695901019,-0.38064245929011,-0.348102919117109,
-0.328886681298388,-0.258595553176405,-0.246742105655551,-0.185056579241663,
-0.163339235199672,-0.143463957830519,-0.0808484674142256,-0.0206857924044652,
0.),.UNSPECIFIED.);
#1366=B_SPLINE_CURVE_WITH_KNOTS('',3,(#60144,#60145,#60146,#60147,#60148,
#60149,#60150,#60151,#60152,#60153,#60154,#60155,#60156,#60157,#60158,#60159,
#60160,#60161,#60162,#60163,#60164,#60165,#60166,#60167,#60168),
 .UNSPECIFIED.,.F.,.F.,(4,3,3,3,3,3,3,3,4),(390.000549715688,390.249351157541,
390.749030224325,391.248709291108,391.748388357891,392.248067424674,392.747746491457,
393.24742555824,393.746279249921),.UNSPECIFIED.);
#1367=B_SPLINE_CURVE_WITH_KNOTS('',3,(#60169,#60170,#60171,#60172,#60173,
#60174,#60175,#60176,#60177,#60178,#60179,#60180,#60181,#60182,#60183),
 .UNSPECIFIED.,.F.,.F.,(4,1,1,1,1,1,1,1,1,1,1,1,4),(9.98190079888485,10.4807544905659,
10.9804335573489,11.4801126241319,11.979791690915,12.479470757698,12.979149824481,
13.478828891264,13.9785079580471,14.4781870248301,14.9778660916131,15.4775451583961,
15.7079632679498),.UNSPECIFIED.);
#1368=B_SPLINE_CURVE_WITH_KNOTS('',3,(#60185,#60186,#60187,#60188,#60189,
#60190,#60191,#60192,#60193,#60194,#60195),.UNSPECIFIED.,.F.,.F.,(4,1,1,
1,1,1,1,1,4),(12.0092477762453,12.5089268430284,13.0086059098114,13.5082849765944,
14.0079640433774,14.5076431101605,15.0073221769435,15.5070012437265,15.7079632679495),
 .UNSPECIFIED.);
#1369=B_SPLINE_CURVE_WITH_KNOTS('',3,(#62189,#62190,#62191,#62192,#62193,
#62194,#62195,#62196,#62197,#62198,#62199,#62200,#62201,#62202,#62203,#62204,
#62205,#62206,#62207,#62208,#62209,#62210,#62211,#62212,#62213,#62214,#62215,
#62216,#62217,#62218,#62219,#62220,#62221,#62222,#62223,#62224,#62225,#62226,
#62227,#62228),.UNSPECIFIED.,.F.,.F.,(4,3,3,3,3,3,3,3,3,3,3,3,3,4),(-0.539097184344981,
-0.538720824057998,-0.476544551511477,-0.429912347101587,-0.401091234701428,
-0.381803774975435,-0.313681369269712,-0.290015733871917,-0.24230273417063,
-0.214804629165427,-0.192593514291413,-0.116696500404398,-0.0381316372362206,
0.),.UNSPECIFIED.);
#1370=B_SPLINE_CURVE_WITH_KNOTS('',3,(#62229,#62230,#62231,#62232,#62233,
#62234,#62235,#62236,#62237,#62238),.UNSPECIFIED.,.F.,.F.,(4,3,3,4),(-394.746462758588,
-394.246783691805,-393.747104625022,-393.256204536838),.UNSPECIFIED.);
#1577=SHAPE_REPRESENTATION_RELATIONSHIP('SRR','None',#63437,#1660);
#1660=ADVANCED_BREP_SHAPE_REPRESENTATION('',(#1878),#62974);
#1773=STYLED_ITEM('',(#63919),#1878);
#1878=MANIFOLD_SOLID_BREP('Body1',#23075);
#2272=FACE_BOUND('',#5791,.T.);
#2273=FACE_BOUND('',#5803,.T.);
#2274=FACE_BOUND('',#5806,.T.);
#2275=FACE_BOUND('',#5809,.T.);
#2809=PLANE('',#26257);
#2810=PLANE('',#26262);
#2811=PLANE('',#26264);
#2812=PLANE('',#26265);
#2813=PLANE('',#26267);
#2814=PLANE('',#26268);
#2815=PLANE('',#26269);
#2816=PLANE('',#26274);
#2817=PLANE('',#26275);
#2818=PLANE('',#26280);
#3965=FACE_OUTER_BOUND('',#5664,.T.);
#3966=FACE_OUTER_BOUND('',#5665,.T.);
#3967=FACE_OUTER_BOUND('',#5666,.T.);
#3968=FACE_OUTER_BOUND('',#5667,.T.);
#3969=FACE_OUTER_BOUND('',#5668,.T.);
#3970=FACE_OUTER_BOUND('',#5669,.T.);
#3971=FACE_OUTER_BOUND('',#5670,.T.);
#3972=FACE_OUTER_BOUND('',#5671,.T.);
#3973=FACE_OUTER_BOUND('',#5672,.T.);
#3974=FACE_OUTER_BOUND('',#5673,.T.);
#3975=FACE_OUTER_BOUND('',#5674,.T.);
#3976=FACE_OUTER_BOUND('',#5675,.T.);
#3977=FACE_OUTER_BOUND('',#5676,.T.);
#3978=FACE_OUTER_BOUND('',#5677,.T.);
#3979=FACE_OUTER_BOUND('',#5678,.T.);
#3980=FACE_OUTER_BOUND('',#5679,.T.);
#3981=FACE_OUTER_BOUND('',#5680,.T.);
#3982=FACE_OUTER_BOUND('',#5681,.T.);
#3983=FACE_OUTER_BOUND('',#5682,.T.);
#3984=FACE_OUTER_BOUND('',#5683,.T.);
#3985=FACE_OUTER_BOUND('',#5684,.T.);
#3986=FACE_OUTER_BOUND('',#5685,.T.);
#3987=FACE_OUTER_BOUND('',#5686,.T.);
#3988=FACE_OUTER_BOUND('',#5687,.T.);
#3989=FACE_OUTER_BOUND('',#5688,.T.);
#3990=FACE_OUTER_BOUND('',#5689,.T.);
#3991=FACE_OUTER_BOUND('',#5690,.T.);
#3992=FACE_OUTER_BOUND('',#5691,.T.);
#3993=FACE_OUTER_BOUND('',#5692,.T.);
#3994=FACE_OUTER_BOUND('',#5693,.T.);
#3995=FACE_OUTER_BOUND('',#5694,.T.);
#3996=FACE_OUTER_BOUND('',#5695,.T.);
#3997=FACE_OUTER_BOUND('',#5696,.T.);
#3998=FACE_OUTER_BOUND('',#5697,.T.);
#3999=FACE_OUTER_BOUND('',#5698,.T.);
#4000=FACE_OUTER_BOUND('',#5699,.T.);
#4001=FACE_OUTER_BOUND('',#5700,.T.);
#4002=FACE_OUTER_BOUND('',#5701,.T.);
#4003=FACE_OUTER_BOUND('',#5702,.T.);
#4004=FACE_OUTER_BOUND('',#5703,.T.);
#4005=FACE_OUTER_BOUND('',#5704,.T.);
#4006=FACE_OUTER_BOUND('',#5705,.T.);
#4007=FACE_OUTER_BOUND('',#5706,.T.);
#4008=FACE_OUTER_BOUND('',#5707,.T.);
#4009=FACE_OUTER_BOUND('',#5708,.T.);
#4010=FACE_OUTER_BOUND('',#5709,.T.);
#4011=FACE_OUTER_BOUND('',#5710,.T.);
#4012=FACE_OUTER_BOUND('',#5711,.T.);
#4013=FACE_OUTER_BOUND('',#5712,.T.);
#4014=FACE_OUTER_BOUND('',#5713,.T.);
#4015=FACE_OUTER_BOUND('',#5714,.T.);
#4016=FACE_OUTER_BOUND('',#5715,.T.);
#4017=FACE_OUTER_BOUND('',#5716,.T.);
#4018=FACE_OUTER_BOUND('',#5717,.T.);
#4019=FACE_OUTER_BOUND('',#5718,.T.);
#4020=FACE_OUTER_BOUND('',#5719,.T.);
#4021=FACE_OUTER_BOUND('',#5720,.T.);
#4022=FACE_OUTER_BOUND('',#5721,.T.);
#4023=FACE_OUTER_BOUND('',#5722,.T.);
#4024=FACE_OUTER_BOUND('',#5723,.T.);
#4025=FACE_OUTER_BOUND('',#5724,.T.);
#4026=FACE_OUTER_BOUND('',#5725,.T.);
#4027=FACE_OUTER_BOUND('',#5726,.T.);
#4028=FACE_OUTER_BOUND('',#5727,.T.);
#4029=FACE_OUTER_BOUND('',#5728,.T.);
#4030=FACE_OUTER_BOUND('',#5729,.T.);
#4031=FACE_OUTER_BOUND('',#5730,.T.);
#4032=FACE_OUTER_BOUND('',#5731,.T.);
#4033=FACE_OUTER_BOUND('',#5732,.T.);
#4034=FACE_OUTER_BOUND('',#5733,.T.);
#4035=FACE_OUTER_BOUND('',#5734,.T.);
#4036=FACE_OUTER_BOUND('',#5735,.T.);
#4037=FACE_OUTER_BOUND('',#5736,.T.);
#4038=FACE_OUTER_BOUND('',#5737,.T.);
#4039=FACE_OUTER_BOUND('',#5738,.T.);
#4040=FACE_OUTER_BOUND('',#5739,.T.);
#4041=FACE_OUTER_BOUND('',#5740,.T.);
#4042=FACE_OUTER_BOUND('',#5741,.T.);
#4043=FACE_OUTER_BOUND('',#5742,.T.);
#4044=FACE_OUTER_BOUND('',#5743,.T.);
#4045=FACE_OUTER_BOUND('',#5744,.T.);
#4046=FACE_OUTER_BOUND('',#5745,.T.);
#4047=FACE_OUTER_BOUND('',#5746,.T.);
#4048=FACE_OUTER_BOUND('',#5747,.T.);
#4049=FACE_OUTER_BOUND('',#5748,.T.);
#4050=FACE_OUTER_BOUND('',#5749,.T.);
#4051=FACE_OUTER_BOUND('',#5750,.T.);
#4052=FACE_OUTER_BOUND('',#5751,.T.);
#4053=FACE_OUTER_BOUND('',#5752,.T.);
#4054=FACE_OUTER_BOUND('',#5753,.T.);
#4055=FACE_OUTER_BOUND('',#5754,.T.);
#4056=FACE_OUTER_BOUND('',#5755,.T.);
#4057=FACE_OUTER_BOUND('',#5756,.T.);
#4058=FACE_OUTER_BOUND('',#5757,.T.);
#4059=FACE_OUTER_BOUND('',#5758,.T.);
#4060=FACE_OUTER_BOUND('',#5759,.T.);
#4061=FACE_OUTER_BOUND('',#5760,.T.);
#4062=FACE_OUTER_BOUND('',#5761,.T.);
#4063=FACE_OUTER_BOUND('',#5762,.T.);
#4064=FACE_OUTER_BOUND('',#5763,.T.);
#4065=FACE_OUTER_BOUND('',#5764,.T.);
#4066=FACE_OUTER_BOUND('',#5765,.T.);
#4067=FACE_OUTER_BOUND('',#5766,.T.);
#4068=FACE_OUTER_BOUND('',#5767,.T.);
#4069=FACE_OUTER_BOUND('',#5768,.T.);
#4070=FACE_OUTER_BOUND('',#5769,.T.);
#4071=FACE_OUTER_BOUND('',#5770,.T.);
#4072=FACE_OUTER_BOUND('',#5771,.T.);
#4073=FACE_OUTER_BOUND('',#5772,.T.);
#4074=FACE_OUTER_BOUND('',#5773,.T.);
#4075=FACE_OUTER_BOUND('',#5774,.T.);
#4076=FACE_OUTER_BOUND('',#5775,.T.);
#4077=FACE_OUTER_BOUND('',#5776,.T.);
#4078=FACE_OUTER_BOUND('',#5777,.T.);
#4079=FACE_OUTER_BOUND('',#5778,.T.);
#4080=FACE_OUTER_BOUND('',#5779,.T.);
#4081=FACE_OUTER_BOUND('',#5780,.T.);
#4082=FACE_OUTER_BOUND('',#5781,.T.);
#4083=FACE_OUTER_BOUND('',#5782,.T.);
#4084=FACE_OUTER_BOUND('',#5783,.T.);
#4085=FACE_OUTER_BOUND('',#5784,.T.);
#4086=FACE_OUTER_BOUND('',#5785,.T.);
#4087=FACE_OUTER_BOUND('',#5786,.T.);
#4088=FACE_OUTER_BOUND('',#5787,.T.);
#4089=FACE_OUTER_BOUND('',#5788,.T.);
#4090=FACE_OUTER_BOUND('',#5789,.T.);
#4091=FACE_OUTER_BOUND('',#5790,.T.);
#4092=FACE_OUTER_BOUND('',#5792,.T.);
#4093=FACE_OUTER_BOUND('',#5793,.T.);
#4094=FACE_OUTER_BOUND('',#5794,.T.);
#4095=FACE_OUTER_BOUND('',#5795,.T.);
#4096=FACE_OUTER_BOUND('',#5796,.T.);
#4097=FACE_OUTER_BOUND('',#5797,.T.);
#4098=FACE_OUTER_BOUND('',#5798,.T.);
#4099=FACE_OUTER_BOUND('',#5799,.T.);
#4100=FACE_OUTER_BOUND('',#5800,.T.);
#4101=FACE_OUTER_BOUND('',#5801,.T.);
#4102=FACE_OUTER_BOUND('',#5802,.T.);
#4103=FACE_OUTER_BOUND('',#5804,.T.);
#4104=FACE_OUTER_BOUND('',#5805,.T.);
#4105=FACE_OUTER_BOUND('',#5807,.T.);
#4106=FACE_OUTER_BOUND('',#5808,.T.);
#4107=FACE_OUTER_BOUND('',#5810,.T.);
#5664=EDGE_LOOP('',(#19908,#19909,#19910,#19911));
#5665=EDGE_LOOP('',(#19912,#19913,#19914,#19915));
#5666=EDGE_LOOP('',(#19916,#19917,#19918,#19919));
#5667=EDGE_LOOP('',(#19920,#19921,#19922,#19923));
#5668=EDGE_LOOP('',(#19924,#19925,#19926,#19927));
#5669=EDGE_LOOP('',(#19928,#19929,#19930,#19931));
#5670=EDGE_LOOP('',(#19932,#19933,#19934,#19935));
#5671=EDGE_LOOP('',(#19936,#19937,#19938,#19939));
#5672=EDGE_LOOP('',(#19940,#19941,#19942,#19943));
#5673=EDGE_LOOP('',(#19944,#19945,#19946,#19947));
#5674=EDGE_LOOP('',(#19948,#19949,#19950,#19951));
#5675=EDGE_LOOP('',(#19952,#19953,#19954,#19955));
#5676=EDGE_LOOP('',(#19956,#19957,#19958,#19959));
#5677=EDGE_LOOP('',(#19960,#19961,#19962,#19963));
#5678=EDGE_LOOP('',(#19964,#19965,#19966,#19967));
#5679=EDGE_LOOP('',(#19968,#19969,#19970,#19971));
#5680=EDGE_LOOP('',(#19972,#19973,#19974,#19975));
#5681=EDGE_LOOP('',(#19976,#19977,#19978,#19979));
#5682=EDGE_LOOP('',(#19980,#19981,#19982,#19983));
#5683=EDGE_LOOP('',(#19984,#19985,#19986,#19987));
#5684=EDGE_LOOP('',(#19988,#19989,#19990,#19991));
#5685=EDGE_LOOP('',(#19992,#19993,#19994,#19995));
#5686=EDGE_LOOP('',(#19996,#19997,#19998,#19999));
#5687=EDGE_LOOP('',(#20000,#20001,#20002,#20003));
#5688=EDGE_LOOP('',(#20004,#20005,#20006,#20007));
#5689=EDGE_LOOP('',(#20008,#20009,#20010,#20011));
#5690=EDGE_LOOP('',(#20012,#20013,#20014,#20015));
#5691=EDGE_LOOP('',(#20016,#20017,#20018,#20019));
#5692=EDGE_LOOP('',(#20020,#20021,#20022,#20023));
#5693=EDGE_LOOP('',(#20024,#20025,#20026,#20027));
#5694=EDGE_LOOP('',(#20028,#20029,#20030,#20031));
#5695=EDGE_LOOP('',(#20032,#20033,#20034,#20035));
#5696=EDGE_LOOP('',(#20036,#20037,#20038,#20039));
#5697=EDGE_LOOP('',(#20040,#20041,#20042,#20043));
#5698=EDGE_LOOP('',(#20044,#20045,#20046,#20047));
#5699=EDGE_LOOP('',(#20048,#20049,#20050,#20051));
#5700=EDGE_LOOP('',(#20052,#20053,#20054,#20055));
#5701=EDGE_LOOP('',(#20056,#20057,#20058,#20059));
#5702=EDGE_LOOP('',(#20060,#20061,#20062,#20063));
#5703=EDGE_LOOP('',(#20064,#20065,#20066,#20067));
#5704=EDGE_LOOP('',(#20068,#20069,#20070,#20071));
#5705=EDGE_LOOP('',(#20072,#20073,#20074,#20075));
#5706=EDGE_LOOP('',(#20076,#20077,#20078,#20079));
#5707=EDGE_LOOP('',(#20080,#20081,#20082,#20083));
#5708=EDGE_LOOP('',(#20084,#20085,#20086,#20087));
#5709=EDGE_LOOP('',(#20088,#20089,#20090,#20091));
#5710=EDGE_LOOP('',(#20092,#20093,#20094,#20095));
#5711=EDGE_LOOP('',(#20096,#20097,#20098,#20099));
#5712=EDGE_LOOP('',(#20100,#20101,#20102,#20103));
#5713=EDGE_LOOP('',(#20104,#20105,#20106,#20107));
#5714=EDGE_LOOP('',(#20108,#20109,#20110,#20111));
#5715=EDGE_LOOP('',(#20112,#20113,#20114,#20115));
#5716=EDGE_LOOP('',(#20116,#20117,#20118,#20119));
#5717=EDGE_LOOP('',(#20120,#20121,#20122,#20123));
#5718=EDGE_LOOP('',(#20124,#20125,#20126,#20127));
#5719=EDGE_LOOP('',(#20128,#20129,#20130,#20131));
#5720=EDGE_LOOP('',(#20132,#20133,#20134,#20135));
#5721=EDGE_LOOP('',(#20136,#20137,#20138,#20139));
#5722=EDGE_LOOP('',(#20140,#20141,#20142,#20143));
#5723=EDGE_LOOP('',(#20144,#20145,#20146,#20147));
#5724=EDGE_LOOP('',(#20148,#20149,#20150,#20151));
#5725=EDGE_LOOP('',(#20152,#20153,#20154,#20155));
#5726=EDGE_LOOP('',(#20156,#20157,#20158,#20159));
#5727=EDGE_LOOP('',(#20160,#20161,#20162));
#5728=EDGE_LOOP('',(#20163,#20164,#20165,#20166,#20167));
#5729=EDGE_LOOP('',(#20168,#20169,#20170,#20171));
#5730=EDGE_LOOP('',(#20172,#20173,#20174,#20175));
#5731=EDGE_LOOP('',(#20176,#20177,#20178,#20179));
#5732=EDGE_LOOP('',(#20180,#20181,#20182,#20183));
#5733=EDGE_LOOP('',(#20184,#20185,#20186,#20187));
#5734=EDGE_LOOP('',(#20188,#20189,#20190,#20191));
#5735=EDGE_LOOP('',(#20192,#20193,#20194,#20195));
#5736=EDGE_LOOP('',(#20196,#20197,#20198,#20199));
#5737=EDGE_LOOP('',(#20200,#20201,#20202,#20203));
#5738=EDGE_LOOP('',(#20204,#20205,#20206,#20207));
#5739=EDGE_LOOP('',(#20208,#20209,#20210,#20211));
#5740=EDGE_LOOP('',(#20212,#20213,#20214,#20215));
#5741=EDGE_LOOP('',(#20216,#20217,#20218,#20219));
#5742=EDGE_LOOP('',(#20220,#20221,#20222,#20223));
#5743=EDGE_LOOP('',(#20224,#20225,#20226,#20227));
#5744=EDGE_LOOP('',(#20228,#20229,#20230,#20231));
#5745=EDGE_LOOP('',(#20232,#20233,#20234,#20235));
#5746=EDGE_LOOP('',(#20236,#20237,#20238,#20239));
#5747=EDGE_LOOP('',(#20240,#20241,#20242,#20243));
#5748=EDGE_LOOP('',(#20244,#20245,#20246,#20247));
#5749=EDGE_LOOP('',(#20248,#20249,#20250,#20251));
#5750=EDGE_LOOP('',(#20252,#20253,#20254,#20255));
#5751=EDGE_LOOP('',(#20256,#20257,#20258,#20259));
#5752=EDGE_LOOP('',(#20260,#20261,#20262,#20263));
#5753=EDGE_LOOP('',(#20264,#20265,#20266,#20267));
#5754=EDGE_LOOP('',(#20268,#20269,#20270,#20271));
#5755=EDGE_LOOP('',(#20272,#20273,#20274,#20275));
#5756=EDGE_LOOP('',(#20276,#20277,#20278,#20279));
#5757=EDGE_LOOP('',(#20280,#20281,#20282,#20283));
#5758=EDGE_LOOP('',(#20284,#20285,#20286,#20287));
#5759=EDGE_LOOP('',(#20288,#20289,#20290,#20291));
#5760=EDGE_LOOP('',(#20292,#20293,#20294,#20295));
#5761=EDGE_LOOP('',(#20296,#20297,#20298,#20299));
#5762=EDGE_LOOP('',(#20300,#20301,#20302,#20303));
#5763=EDGE_LOOP('',(#20304,#20305,#20306,#20307));
#5764=EDGE_LOOP('',(#20308,#20309,#20310,#20311));
#5765=EDGE_LOOP('',(#20312,#20313,#20314,#20315));
#5766=EDGE_LOOP('',(#20316,#20317,#20318,#20319));
#5767=EDGE_LOOP('',(#20320,#20321,#20322,#20323));
#5768=EDGE_LOOP('',(#20324,#20325,#20326,#20327));
#5769=EDGE_LOOP('',(#20328,#20329,#20330,#20331));
#5770=EDGE_LOOP('',(#20332,#20333,#20334,#20335));
#5771=EDGE_LOOP('',(#20336,#20337,#20338,#20339));
#5772=EDGE_LOOP('',(#20340,#20341,#20342,#20343));
#5773=EDGE_LOOP('',(#20344,#20345,#20346,#20347));
#5774=EDGE_LOOP('',(#20348,#20349,#20350,#20351));
#5775=EDGE_LOOP('',(#20352,#20353,#20354,#20355));
#5776=EDGE_LOOP('',(#20356,#20357,#20358,#20359));
#5777=EDGE_LOOP('',(#20360,#20361,#20362,#20363));
#5778=EDGE_LOOP('',(#20364,#20365,#20366,#20367));
#5779=EDGE_LOOP('',(#20368,#20369,#20370,#20371));
#5780=EDGE_LOOP('',(#20372,#20373,#20374,#20375));
#5781=EDGE_LOOP('',(#20376,#20377,#20378,#20379));
#5782=EDGE_LOOP('',(#20380,#20381,#20382,#20383));
#5783=EDGE_LOOP('',(#20384,#20385,#20386,#20387));
#5784=EDGE_LOOP('',(#20388,#20389,#20390,#20391));
#5785=EDGE_LOOP('',(#20392,#20393,#20394,#20395));
#5786=EDGE_LOOP('',(#20396,#20397,#20398,#20399));
#5787=EDGE_LOOP('',(#20400,#20401,#20402,#20403));
#5788=EDGE_LOOP('',(#20404,#20405,#20406,#20407));
#5789=EDGE_LOOP('',(#20408,#20409,#20410,#20411));
#5790=EDGE_LOOP('',(#20412));
#5791=EDGE_LOOP('',(#20413,#20414,#20415,#20416));
#5792=EDGE_LOOP('',(#20417,#20418,#20419,#20420));
#5793=EDGE_LOOP('',(#20421));
#5794=EDGE_LOOP('',(#20422,#20423,#20424,#20425,#20426,#20427,#20428,#20429,
#20430,#20431,#20432,#20433,#20434,#20435,#20436,#20437,#20438,#20439,#20440,
#20441,#20442,#20443,#20444,#20445,#20446,#20447,#20448,#20449,#20450,#20451,
#20452,#20453,#20454,#20455,#20456,#20457,#20458,#20459,#20460,#20461,#20462,
#20463,#20464,#20465,#20466,#20467,#20468,#20469,#20470,#20471,#20472,#20473,
#20474,#20475,#20476,#20477,#20478,#20479,#20480,#20481,#20482,#20483,#20484,
#20485,#20486,#20487,#20488,#20489,#20490,#20491,#20492,#20493,#20494,#20495,
#20496,#20497,#20498,#20499,#20500,#20501,#20502,#20503,#20504,#20505,#20506,
#20507,#20508,#20509,#20510,#20511,#20512,#20513,#20514,#20515,#20516,#20517,
#20518,#20519,#20520,#20521,#20522,#20523,#20524,#20525,#20526,#20527,#20528,
#20529,#20530,#20531,#20532,#20533,#20534,#20535,#20536,#20537,#20538,#20539,
#20540,#20541,#20542,#20543,#20544,#20545,#20546,#20547,#20548,#20549,#20550));
#5795=EDGE_LOOP('',(#20551,#20552,#20553,#20554));
#5796=EDGE_LOOP('',(#20555,#20556,#20557,#20558,#20559,#20560,#20561,#20562,
#20563,#20564,#20565,#20566,#20567,#20568,#20569,#20570,#20571,#20572,#20573,
#20574,#20575,#20576,#20577,#20578,#20579,#20580,#20581,#20582,#20583,#20584,
#20585,#20586,#20587,#20588,#20589,#20590,#20591,#20592,#20593,#20594,#20595,
#20596,#20597,#20598,#20599,#20600,#20601,#20602,#20603,#20604,#20605,#20606,
#20607,#20608,#20609,#20610,#20611,#20612,#20613,#20614,#20615,#20616,#20617,
#20618,#20619,#20620,#20621,#20622,#20623,#20624,#20625,#20626,#20627,#20628,
#20629,#20630,#20631,#20632,#20633,#20634,#20635,#20636,#20637,#20638,#20639,
#20640,#20641,#20642,#20643,#20644,#20645,#20646,#20647,#20648,#20649,#20650,
#20651,#20652,#20653,#20654,#20655,#20656,#20657,#20658,#20659,#20660,#20661,
#20662,#20663,#20664,#20665,#20666,#20667,#20668,#20669,#20670,#20671,#20672,
#20673,#20674,#20675,#20676,#20677,#20678,#20679,#20680,#20681,#20682,#20683,
#20684));
#5797=EDGE_LOOP('',(#20685,#20686,#20687,#20688));
#5798=EDGE_LOOP('',(#20689,#20690,#20691,#20692));
#5799=EDGE_LOOP('',(#20693,#20694,#20695,#20696));
#5800=EDGE_LOOP('',(#20697,#20698,#20699,#20700));
#5801=EDGE_LOOP('',(#20701,#20702,#20703,#20704));
#5802=EDGE_LOOP('',(#20705,#20706,#20707,#20708));
#5803=EDGE_LOOP('',(#20709,#20710,#20711,#20712));
#5804=EDGE_LOOP('',(#20713));
#5805=EDGE_LOOP('',(#20714));
#5806=EDGE_LOOP('',(#20715,#20716,#20717,#20718,#20719));
#5807=EDGE_LOOP('',(#20720,#20721,#20722,#20723));
#5808=EDGE_LOOP('',(#20724));
#5809=EDGE_LOOP('',(#20725));
#5810=EDGE_LOOP('',(#20726,#20727,#20728,#20729));
#7153=LINE('',#52626,#8640);
#7154=LINE('',#52656,#8641);
#7155=LINE('',#52743,#8642);
#7156=LINE('',#52833,#8643);
#7157=LINE('',#52920,#8644);
#7158=LINE('',#53007,#8645);
#7159=LINE('',#53094,#8646);
#7160=LINE('',#53181,#8647);
#7161=LINE('',#53268,#8648);
#7162=LINE('',#53340,#8649);
#7163=LINE('',#53391,#8650);
#7164=LINE('',#53439,#8651);
#7165=LINE('',#53487,#8652);
#7166=LINE('',#53538,#8653);
#7167=LINE('',#53589,#8654);
#7168=LINE('',#53637,#8655);
#7169=LINE('',#53688,#8656);
#7170=LINE('',#53739,#8657);
#7171=LINE('',#53787,#8658);
#7172=LINE('',#53835,#8659);
#7173=LINE('',#53886,#8660);
#7174=LINE('',#53937,#8661);
#7175=LINE('',#53985,#8662);
#7176=LINE('',#54036,#8663);
#7177=LINE('',#54087,#8664);
#7178=LINE('',#54135,#8665);
#7179=LINE('',#54183,#8666);
#7180=LINE('',#54234,#8667);
#7181=LINE('',#54285,#8668);
#7182=LINE('',#54333,#8669);
#7183=LINE('',#54384,#8670);
#7184=LINE('',#54435,#8671);
#7185=LINE('',#54483,#8672);
#7186=LINE('',#54531,#8673);
#7187=LINE('',#54582,#8674);
#7188=LINE('',#54633,#8675);
#7189=LINE('',#54681,#8676);
#7190=LINE('',#54732,#8677);
#7191=LINE('',#54783,#8678);
#7192=LINE('',#54831,#8679);
#7193=LINE('',#54879,#8680);
#7194=LINE('',#54930,#8681);
#7195=LINE('',#54981,#8682);
#7196=LINE('',#55029,#8683);
#7197=LINE('',#55080,#8684);
#7198=LINE('',#55131,#8685);
#7199=LINE('',#55179,#8686);
#7200=LINE('',#55227,#8687);
#7201=LINE('',#55278,#8688);
#7202=LINE('',#55329,#8689);
#7203=LINE('',#55377,#8690);
#7204=LINE('',#55428,#8691);
#7205=LINE('',#55479,#8692);
#7206=LINE('',#55527,#8693);
#7207=LINE('',#55575,#8694);
#7208=LINE('',#55626,#8695);
#7209=LINE('',#55692,#8696);
#7210=LINE('',#55782,#8697);
#7211=LINE('',#55869,#8698);
#7212=LINE('',#55956,#8699);
#7213=LINE('',#56043,#8700);
#7214=LINE('',#56130,#8701);
#7215=LINE('',#56217,#8702);
#7216=LINE('',#56307,#8703);
#7217=LINE('',#56317,#8704);
#7218=LINE('',#56353,#8705);
#7219=LINE('',#56391,#8706);
#7220=LINE('',#56427,#8707);
#7221=LINE('',#56465,#8708);
#7222=LINE('',#56501,#8709);
#7223=LINE('',#56539,#8710);
#7224=LINE('',#56576,#8711);
#7225=LINE('',#56611,#8712);
#7226=LINE('',#56638,#8713);
#7227=LINE('',#56662,#8714);
#7228=LINE('',#56686,#8715);
#7229=LINE('',#56710,#8716);
#7230=LINE('',#56736,#8717);
#7231=LINE('',#56760,#8718);
#7232=LINE('',#56784,#8719);
#7233=LINE('',#56810,#8720);
#7234=LINE('',#56834,#8721);
#7235=LINE('',#56858,#8722);
#7236=LINE('',#56882,#8723);
#7237=LINE('',#56908,#8724);
#7238=LINE('',#56932,#8725);
#7239=LINE('',#56956,#8726);
#7240=LINE('',#56982,#8727);
#7241=LINE('',#57006,#8728);
#7242=LINE('',#57030,#8729);
#7243=LINE('',#57054,#8730);
#7244=LINE('',#57080,#8731);
#7245=LINE('',#57104,#8732);
#7246=LINE('',#57128,#8733);
#7247=LINE('',#57154,#8734);
#7248=LINE('',#57178,#8735);
#7249=LINE('',#57202,#8736);
#7250=LINE('',#57226,#8737);
#7251=LINE('',#57252,#8738);
#7252=LINE('',#57276,#8739);
#7253=LINE('',#57300,#8740);
#7254=LINE('',#57326,#8741);
#7255=LINE('',#57350,#8742);
#7256=LINE('',#57374,#8743);
#7257=LINE('',#57398,#8744);
#7258=LINE('',#57424,#8745);
#7259=LINE('',#57448,#8746);
#7260=LINE('',#57472,#8747);
#7261=LINE('',#57498,#8748);
#7262=LINE('',#57522,#8749);
#7263=LINE('',#57546,#8750);
#7264=LINE('',#57570,#8751);
#7265=LINE('',#57596,#8752);
#7266=LINE('',#57620,#8753);
#7267=LINE('',#57644,#8754);
#7268=LINE('',#57670,#8755);
#7269=LINE('',#57694,#8756);
#7270=LINE('',#57718,#8757);
#7271=LINE('',#57743,#8758);
#7272=LINE('',#57770,#8759);
#7273=LINE('',#57807,#8760);
#7274=LINE('',#57843,#8761);
#7275=LINE('',#57881,#8762);
#7276=LINE('',#57917,#8763);
#7277=LINE('',#57955,#8764);
#7278=LINE('',#57992,#8765);
#7279=LINE('',#58108,#8766);
#7280=LINE('',#62242,#8767);
#7281=LINE('',#62244,#8768);
#7282=LINE('',#62246,#8769);
#7283=LINE('',#62247,#8770);
#7284=LINE('',#62252,#8771);
#7285=LINE('',#62253,#8772);
#7286=LINE('',#62256,#8773);
#7287=LINE('',#62257,#8774);
#7288=LINE('',#62260,#8775);
#7289=LINE('',#62261,#8776);
#7290=LINE('',#62268,#8777);
#7291=LINE('',#62278,#8778);
#8640=VECTOR('',#31966,0.6);
#8641=VECTOR('',#31971,0.6);
#8642=VECTOR('',#31974,0.6);
#8643=VECTOR('',#31977,0.6);
#8644=VECTOR('',#31980,0.6);
#8645=VECTOR('',#31983,0.6);
#8646=VECTOR('',#31986,0.6);
#8647=VECTOR('',#31989,0.6);
#8648=VECTOR('',#31992,0.6);
#8649=VECTOR('',#31995,0.6);
#8650=VECTOR('',#31998,0.6);
#8651=VECTOR('',#32001,0.6);
#8652=VECTOR('',#32004,0.6);
#8653=VECTOR('',#32007,0.6);
#8654=VECTOR('',#32010,0.6);
#8655=VECTOR('',#32013,0.6);
#8656=VECTOR('',#32016,0.6);
#8657=VECTOR('',#32019,0.6);
#8658=VECTOR('',#32022,0.6);
#8659=VECTOR('',#32025,0.6);
#8660=VECTOR('',#32028,0.6);
#8661=VECTOR('',#32031,0.6);
#8662=VECTOR('',#32034,0.6);
#8663=VECTOR('',#32037,0.6);
#8664=VECTOR('',#32040,0.6);
#8665=VECTOR('',#32043,0.6);
#8666=VECTOR('',#32046,0.6);
#8667=VECTOR('',#32049,0.6);
#8668=VECTOR('',#32052,0.6);
#8669=VECTOR('',#32055,0.6);
#8670=VECTOR('',#32058,0.6);
#8671=VECTOR('',#32061,0.6);
#8672=VECTOR('',#32064,0.6);
#8673=VECTOR('',#32067,0.6);
#8674=VECTOR('',#32070,0.6);
#8675=VECTOR('',#32073,0.6);
#8676=VECTOR('',#32076,0.6);
#8677=VECTOR('',#32079,0.6);
#8678=VECTOR('',#32082,0.6);
#8679=VECTOR('',#32085,0.6);
#8680=VECTOR('',#32088,0.6);
#8681=VECTOR('',#32091,0.6);
#8682=VECTOR('',#32094,0.6);
#8683=VECTOR('',#32097,0.6);
#8684=VECTOR('',#32100,0.6);
#8685=VECTOR('',#32103,0.6);
#8686=VECTOR('',#32106,0.6);
#8687=VECTOR('',#32109,0.6);
#8688=VECTOR('',#32112,0.6);
#8689=VECTOR('',#32115,0.6);
#8690=VECTOR('',#32118,0.6);
#8691=VECTOR('',#32121,0.6);
#8692=VECTOR('',#32124,0.6);
#8693=VECTOR('',#32127,0.6);
#8694=VECTOR('',#32130,0.6);
#8695=VECTOR('',#32133,0.6);
#8696=VECTOR('',#32136,0.6);
#8697=VECTOR('',#32139,0.6);
#8698=VECTOR('',#32142,0.6);
#8699=VECTOR('',#32145,0.6);
#8700=VECTOR('',#32148,0.6);
#8701=VECTOR('',#32151,0.6);
#8702=VECTOR('',#32154,0.6);
#8703=VECTOR('',#32157,0.415875);
#8704=VECTOR('',#32162,0.415875);
#8705=VECTOR('',#32167,0.415875);
#8706=VECTOR('',#32170,0.415875);
#8707=VECTOR('',#32173,0.415875);
#8708=VECTOR('',#32176,0.415875);
#8709=VECTOR('',#32179,0.415875);
#8710=VECTOR('',#32182,0.415875);
#8711=VECTOR('',#32185,0.415875);
#8712=VECTOR('',#32188,0.415875);
#8713=VECTOR('',#32191,0.415875);
#8714=VECTOR('',#32194,0.415875);
#8715=VECTOR('',#32197,0.415875);
#8716=VECTOR('',#32200,0.415875);
#8717=VECTOR('',#32203,0.415875);
#8718=VECTOR('',#32206,0.415875);
#8719=VECTOR('',#32209,0.415875);
#8720=VECTOR('',#32212,0.415875);
#8721=VECTOR('',#32215,0.415875);
#8722=VECTOR('',#32218,0.415875);
#8723=VECTOR('',#32221,0.415875);
#8724=VECTOR('',#32224,0.415875);
#8725=VECTOR('',#32227,0.415875);
#8726=VECTOR('',#32230,0.415875);
#8727=VECTOR('',#32233,0.415875);
#8728=VECTOR('',#32236,0.415875);
#8729=VECTOR('',#32239,0.415875);
#8730=VECTOR('',#32242,0.415875);
#8731=VECTOR('',#32245,0.415875);
#8732=VECTOR('',#32248,0.415875);
#8733=VECTOR('',#32251,0.415875);
#8734=VECTOR('',#32254,0.415875);
#8735=VECTOR('',#32257,0.415875);
#8736=VECTOR('',#32260,0.415875);
#8737=VECTOR('',#32263,0.415875);
#8738=VECTOR('',#32266,0.415875);
#8739=VECTOR('',#32269,0.415875);
#8740=VECTOR('',#32272,0.415875);
#8741=VECTOR('',#32275,0.415875);
#8742=VECTOR('',#32278,0.415875);
#8743=VECTOR('',#32281,0.415875);
#8744=VECTOR('',#32284,0.415875);
#8745=VECTOR('',#32287,0.415875);
#8746=VECTOR('',#32290,0.415875);
#8747=VECTOR('',#32293,0.415875);
#8748=VECTOR('',#32296,0.415875);
#8749=VECTOR('',#32299,0.415875);
#8750=VECTOR('',#32302,0.415875);
#8751=VECTOR('',#32305,0.415875);
#8752=VECTOR('',#32308,0.415875);
#8753=VECTOR('',#32311,0.415875);
#8754=VECTOR('',#32314,0.415875);
#8755=VECTOR('',#32317,0.415875);
#8756=VECTOR('',#32320,0.415875);
#8757=VECTOR('',#32323,0.415875);
#8758=VECTOR('',#32326,0.415875);
#8759=VECTOR('',#32329,0.415875);
#8760=VECTOR('',#32332,0.415875);
#8761=VECTOR('',#32335,0.415875);
#8762=VECTOR('',#32338,0.415875);
#8763=VECTOR('',#32341,0.415875);
#8764=VECTOR('',#32344,0.415875);
#8765=VECTOR('',#32347,0.415875);
#8766=VECTOR('',#32356,0.6);
#8767=VECTOR('',#32365,1.);
#8768=VECTOR('',#32366,1.);
#8769=VECTOR('',#32367,1.);
#8770=VECTOR('',#32368,1.);
#8771=VECTOR('',#32373,1.);
#8772=VECTOR('',#32374,1.);
#8773=VECTOR('',#32377,1.);
#8774=VECTOR('',#32378,1.);
#8775=VECTOR('',#32381,1.);
#8776=VECTOR('',#32382,1.);
#8777=VECTOR('',#32391,1.);
#8778=VECTOR('',#32406,1.35);
#9716=CIRCLE('',#26129,0.5941);
#9717=CIRCLE('',#26193,0.415875);
#9718=CIRCLE('',#26195,0.415875);
#9719=CIRCLE('',#26258,0.6);
#9720=CIRCLE('',#26259,0.415875);
#9721=CIRCLE('',#26261,0.6);
#9722=CIRCLE('',#26266,1.);
#9723=CIRCLE('',#26270,1.);
#9724=CIRCLE('',#26272,1.);
#9725=CIRCLE('',#26273,1.);
#9726=CIRCLE('',#26276,1.35);
#9727=CIRCLE('',#26277,0.5941);
#9728=CIRCLE('',#26279,1.35);
#11460=VERTEX_POINT('',#52624);
#11461=VERTEX_POINT('',#52625);
#11462=VERTEX_POINT('',#52627);
#11463=VERTEX_POINT('',#52647);
#11464=VERTEX_POINT('',#52654);
#11465=VERTEX_POINT('',#52655);
#11466=VERTEX_POINT('',#52741);
#11467=VERTEX_POINT('',#52742);
#11468=VERTEX_POINT('',#52831);
#11469=VERTEX_POINT('',#52832);
#11470=VERTEX_POINT('',#52918);
#11471=VERTEX_POINT('',#52919);
#11472=VERTEX_POINT('',#53005);
#11473=VERTEX_POINT('',#53006);
#11474=VERTEX_POINT('',#53092);
#11475=VERTEX_POINT('',#53093);
#11476=VERTEX_POINT('',#53179);
#11477=VERTEX_POINT('',#53180);
#11478=VERTEX_POINT('',#53266);
#11479=VERTEX_POINT('',#53267);
#11480=VERTEX_POINT('',#53338);
#11481=VERTEX_POINT('',#53339);
#11482=VERTEX_POINT('',#53389);
#11483=VERTEX_POINT('',#53390);
#11484=VERTEX_POINT('',#53437);
#11485=VERTEX_POINT('',#53438);
#11486=VERTEX_POINT('',#53485);
#11487=VERTEX_POINT('',#53486);
#11488=VERTEX_POINT('',#53536);
#11489=VERTEX_POINT('',#53537);
#11490=VERTEX_POINT('',#53587);
#11491=VERTEX_POINT('',#53588);
#11492=VERTEX_POINT('',#53635);
#11493=VERTEX_POINT('',#53636);
#11494=VERTEX_POINT('',#53686);
#11495=VERTEX_POINT('',#53687);
#11496=VERTEX_POINT('',#53737);
#11497=VERTEX_POINT('',#53738);
#11498=VERTEX_POINT('',#53785);
#11499=VERTEX_POINT('',#53786);
#11500=VERTEX_POINT('',#53833);
#11501=VERTEX_POINT('',#53834);
#11502=VERTEX_POINT('',#53884);
#11503=VERTEX_POINT('',#53885);
#11504=VERTEX_POINT('',#53935);
#11505=VERTEX_POINT('',#53936);
#11506=VERTEX_POINT('',#53983);
#11507=VERTEX_POINT('',#53984);
#11508=VERTEX_POINT('',#54034);
#11509=VERTEX_POINT('',#54035);
#11510=VERTEX_POINT('',#54085);
#11511=VERTEX_POINT('',#54086);
#11512=VERTEX_POINT('',#54133);
#11513=VERTEX_POINT('',#54134);
#11514=VERTEX_POINT('',#54181);
#11515=VERTEX_POINT('',#54182);
#11516=VERTEX_POINT('',#54232);
#11517=VERTEX_POINT('',#54233);
#11518=VERTEX_POINT('',#54283);
#11519=VERTEX_POINT('',#54284);
#11520=VERTEX_POINT('',#54331);
#11521=VERTEX_POINT('',#54332);
#11522=VERTEX_POINT('',#54382);
#11523=VERTEX_POINT('',#54383);
#11524=VERTEX_POINT('',#54433);
#11525=VERTEX_POINT('',#54434);
#11526=VERTEX_POINT('',#54481);
#11527=VERTEX_POINT('',#54482);
#11528=VERTEX_POINT('',#54529);
#11529=VERTEX_POINT('',#54530);
#11530=VERTEX_POINT('',#54580);
#11531=VERTEX_POINT('',#54581);
#11532=VERTEX_POINT('',#54631);
#11533=VERTEX_POINT('',#54632);
#11534=VERTEX_POINT('',#54679);
#11535=VERTEX_POINT('',#54680);
#11536=VERTEX_POINT('',#54730);
#11537=VERTEX_POINT('',#54731);
#11538=VERTEX_POINT('',#54781);
#11539=VERTEX_POINT('',#54782);
#11540=VERTEX_POINT('',#54829);
#11541=VERTEX_POINT('',#54830);
#11542=VERTEX_POINT('',#54877);
#11543=VERTEX_POINT('',#54878);
#11544=VERTEX_POINT('',#54928);
#11545=VERTEX_POINT('',#54929);
#11546=VERTEX_POINT('',#54979);
#11547=VERTEX_POINT('',#54980);
#11548=VERTEX_POINT('',#55027);
#11549=VERTEX_POINT('',#55028);
#11550=VERTEX_POINT('',#55078);
#11551=VERTEX_POINT('',#55079);
#11552=VERTEX_POINT('',#55129);
#11553=VERTEX_POINT('',#55130);
#11554=VERTEX_POINT('',#55177);
#11555=VERTEX_POINT('',#55178);
#11556=VERTEX_POINT('',#55225);
#11557=VERTEX_POINT('',#55226);
#11558=VERTEX_POINT('',#55276);
#11559=VERTEX_POINT('',#55277);
#11560=VERTEX_POINT('',#55327);
#11561=VERTEX_POINT('',#55328);
#11562=VERTEX_POINT('',#55375);
#11563=VERTEX_POINT('',#55376);
#11564=VERTEX_POINT('',#55426);
#11565=VERTEX_POINT('',#55427);
#11566=VERTEX_POINT('',#55477);
#11567=VERTEX_POINT('',#55478);
#11568=VERTEX_POINT('',#55525);
#11569=VERTEX_POINT('',#55526);
#11570=VERTEX_POINT('',#55573);
#11571=VERTEX_POINT('',#55574);
#11572=VERTEX_POINT('',#55624);
#11573=VERTEX_POINT('',#55625);
#11574=VERTEX_POINT('',#55690);
#11575=VERTEX_POINT('',#55691);
#11576=VERTEX_POINT('',#55780);
#11577=VERTEX_POINT('',#55781);
#11578=VERTEX_POINT('',#55867);
#11579=VERTEX_POINT('',#55868);
#11580=VERTEX_POINT('',#55954);
#11581=VERTEX_POINT('',#55955);
#11582=VERTEX_POINT('',#56041);
#11583=VERTEX_POINT('',#56042);
#11584=VERTEX_POINT('',#56128);
#11585=VERTEX_POINT('',#56129);
#11586=VERTEX_POINT('',#56215);
#11587=VERTEX_POINT('',#56216);
#11588=VERTEX_POINT('',#56305);
#11589=VERTEX_POINT('',#56306);
#11590=VERTEX_POINT('',#56308);
#11591=VERTEX_POINT('',#56315);
#11592=VERTEX_POINT('',#56316);
#11593=VERTEX_POINT('',#56335);
#11594=VERTEX_POINT('',#56351);
#11595=VERTEX_POINT('',#56352);
#11596=VERTEX_POINT('',#56389);
#11597=VERTEX_POINT('',#56390);
#11598=VERTEX_POINT('',#56425);
#11599=VERTEX_POINT('',#56426);
#11600=VERTEX_POINT('',#56463);
#11601=VERTEX_POINT('',#56464);
#11602=VERTEX_POINT('',#56499);
#11603=VERTEX_POINT('',#56500);
#11604=VERTEX_POINT('',#56537);
#11605=VERTEX_POINT('',#56538);
#11606=VERTEX_POINT('',#56574);
#11607=VERTEX_POINT('',#56575);
#11608=VERTEX_POINT('',#56609);
#11609=VERTEX_POINT('',#56610);
#11610=VERTEX_POINT('',#56636);
#11611=VERTEX_POINT('',#56637);
#11612=VERTEX_POINT('',#56660);
#11613=VERTEX_POINT('',#56661);
#11614=VERTEX_POINT('',#56684);
#11615=VERTEX_POINT('',#56685);
#11616=VERTEX_POINT('',#56708);
#11617=VERTEX_POINT('',#56709);
#11618=VERTEX_POINT('',#56734);
#11619=VERTEX_POINT('',#56735);
#11620=VERTEX_POINT('',#56758);
#11621=VERTEX_POINT('',#56759);
#11622=VERTEX_POINT('',#56782);
#11623=VERTEX_POINT('',#56783);
#11624=VERTEX_POINT('',#56808);
#11625=VERTEX_POINT('',#56809);
#11626=VERTEX_POINT('',#56832);
#11627=VERTEX_POINT('',#56833);
#11628=VERTEX_POINT('',#56856);
#11629=VERTEX_POINT('',#56857);
#11630=VERTEX_POINT('',#56880);
#11631=VERTEX_POINT('',#56881);
#11632=VERTEX_POINT('',#56906);
#11633=VERTEX_POINT('',#56907);
#11634=VERTEX_POINT('',#56930);
#11635=VERTEX_POINT('',#56931);
#11636=VERTEX_POINT('',#56954);
#11637=VERTEX_POINT('',#56955);
#11638=VERTEX_POINT('',#56980);
#11639=VERTEX_POINT('',#56981);
#11640=VERTEX_POINT('',#57004);
#11641=VERTEX_POINT('',#57005);
#11642=VERTEX_POINT('',#57028);
#11643=VERTEX_POINT('',#57029);
#11644=VERTEX_POINT('',#57052);
#11645=VERTEX_POINT('',#57053);
#11646=VERTEX_POINT('',#57078);
#11647=VERTEX_POINT('',#57079);
#11648=VERTEX_POINT('',#57102);
#11649=VERTEX_POINT('',#57103);
#11650=VERTEX_POINT('',#57126);
#11651=VERTEX_POINT('',#57127);
#11652=VERTEX_POINT('',#57152);
#11653=VERTEX_POINT('',#57153);
#11654=VERTEX_POINT('',#57176);
#11655=VERTEX_POINT('',#57177);
#11656=VERTEX_POINT('',#57200);
#11657=VERTEX_POINT('',#57201);
#11658=VERTEX_POINT('',#57224);
#11659=VERTEX_POINT('',#57225);
#11660=VERTEX_POINT('',#57250);
#11661=VERTEX_POINT('',#57251);
#11662=VERTEX_POINT('',#57274);
#11663=VERTEX_POINT('',#57275);
#11664=VERTEX_POINT('',#57298);
#11665=VERTEX_POINT('',#57299);
#11666=VERTEX_POINT('',#57324);
#11667=VERTEX_POINT('',#57325);
#11668=VERTEX_POINT('',#57348);
#11669=VERTEX_POINT('',#57349);
#11670=VERTEX_POINT('',#57372);
#11671=VERTEX_POINT('',#57373);
#11672=VERTEX_POINT('',#57396);
#11673=VERTEX_POINT('',#57397);
#11674=VERTEX_POINT('',#57422);
#11675=VERTEX_POINT('',#57423);
#11676=VERTEX_POINT('',#57446);
#11677=VERTEX_POINT('',#57447);
#11678=VERTEX_POINT('',#57470);
#11679=VERTEX_POINT('',#57471);
#11680=VERTEX_POINT('',#57496);
#11681=VERTEX_POINT('',#57497);
#11682=VERTEX_POINT('',#57520);
#11683=VERTEX_POINT('',#57521);
#11684=VERTEX_POINT('',#57544);
#11685=VERTEX_POINT('',#57545);
#11686=VERTEX_POINT('',#57568);
#11687=VERTEX_POINT('',#57569);
#11688=VERTEX_POINT('',#57594);
#11689=VERTEX_POINT('',#57595);
#11690=VERTEX_POINT('',#57618);
#11691=VERTEX_POINT('',#57619);
#11692=VERTEX_POINT('',#57642);
#11693=VERTEX_POINT('',#57643);
#11694=VERTEX_POINT('',#57668);
#11695=VERTEX_POINT('',#57669);
#11696=VERTEX_POINT('',#57692);
#11697=VERTEX_POINT('',#57693);
#11698=VERTEX_POINT('',#57716);
#11699=VERTEX_POINT('',#57717);
#11700=VERTEX_POINT('',#57741);
#11701=VERTEX_POINT('',#57742);
#11702=VERTEX_POINT('',#57768);
#11703=VERTEX_POINT('',#57769);
#11704=VERTEX_POINT('',#57805);
#11705=VERTEX_POINT('',#57806);
#11706=VERTEX_POINT('',#57841);
#11707=VERTEX_POINT('',#57842);
#11708=VERTEX_POINT('',#57879);
#11709=VERTEX_POINT('',#57880);
#11710=VERTEX_POINT('',#57915);
#11711=VERTEX_POINT('',#57916);
#11712=VERTEX_POINT('',#57953);
#11713=VERTEX_POINT('',#57954);
#11714=VERTEX_POINT('',#57990);
#11715=VERTEX_POINT('',#57991);
#11716=VERTEX_POINT('',#58027);
#11717=VERTEX_POINT('',#58029);
#11718=VERTEX_POINT('',#58067);
#11719=VERTEX_POINT('',#58107);
#11720=VERTEX_POINT('',#60103);
#11721=VERTEX_POINT('',#62188);
#11722=VERTEX_POINT('',#62240);
#11723=VERTEX_POINT('',#62241);
#11724=VERTEX_POINT('',#62243);
#11725=VERTEX_POINT('',#62245);
#11726=VERTEX_POINT('',#62249);
#11727=VERTEX_POINT('',#62251);
#11728=VERTEX_POINT('',#62255);
#11729=VERTEX_POINT('',#62259);
#11730=VERTEX_POINT('',#62265);
#11731=VERTEX_POINT('',#62267);
#11732=VERTEX_POINT('',#62272);
#11733=VERTEX_POINT('',#62276);
#14338=EDGE_CURVE('',#11460,#11461,#7153,.T.);
#14339=EDGE_CURVE('',#11460,#11462,#1112,.T.);
#14340=EDGE_CURVE('',#11462,#11463,#9716,.F.);
#14341=EDGE_CURVE('',#11463,#11461,#1113,.T.);
#14342=EDGE_CURVE('',#11464,#11465,#7154,.T.);
#14343=EDGE_CURVE('',#11464,#11460,#1114,.T.);
#14344=EDGE_CURVE('',#11461,#11465,#1115,.T.);
#14345=EDGE_CURVE('',#11466,#11467,#7155,.T.);
#14346=EDGE_CURVE('',#11466,#11464,#1116,.T.);
#14347=EDGE_CURVE('',#11465,#11467,#1117,.T.);
#14348=EDGE_CURVE('',#11468,#11469,#7156,.T.);
#14349=EDGE_CURVE('',#11468,#11466,#1118,.T.);
#14350=EDGE_CURVE('',#11467,#11469,#1119,.T.);
#14351=EDGE_CURVE('',#11470,#11471,#7157,.T.);
#14352=EDGE_CURVE('',#11470,#11468,#1120,.T.);
#14353=EDGE_CURVE('',#11469,#11471,#1121,.T.);
#14354=EDGE_CURVE('',#11472,#11473,#7158,.T.);
#14355=EDGE_CURVE('',#11472,#11470,#1122,.T.);
#14356=EDGE_CURVE('',#11471,#11473,#1123,.T.);
#14357=EDGE_CURVE('',#11474,#11475,#7159,.T.);
#14358=EDGE_CURVE('',#11474,#11472,#1124,.T.);
#14359=EDGE_CURVE('',#11473,#11475,#1125,.T.);
#14360=EDGE_CURVE('',#11476,#11477,#7160,.T.);
#14361=EDGE_CURVE('',#11476,#11474,#1126,.T.);
#14362=EDGE_CURVE('',#11475,#11477,#1127,.T.);
#14363=EDGE_CURVE('',#11478,#11479,#7161,.T.);
#14364=EDGE_CURVE('',#11478,#11476,#1128,.T.);
#14365=EDGE_CURVE('',#11477,#11479,#1129,.T.);
#14366=EDGE_CURVE('',#11480,#11481,#7162,.T.);
#14367=EDGE_CURVE('',#11480,#11478,#1130,.T.);
#14368=EDGE_CURVE('',#11479,#11481,#1131,.T.);
#14369=EDGE_CURVE('',#11482,#11483,#7163,.T.);
#14370=EDGE_CURVE('',#11482,#11480,#1132,.T.);
#14371=EDGE_CURVE('',#11481,#11483,#1133,.T.);
#14372=EDGE_CURVE('',#11484,#11485,#7164,.T.);
#14373=EDGE_CURVE('',#11484,#11482,#1134,.T.);
#14374=EDGE_CURVE('',#11483,#11485,#1135,.T.);
#14375=EDGE_CURVE('',#11486,#11487,#7165,.T.);
#14376=EDGE_CURVE('',#11486,#11484,#1136,.T.);
#14377=EDGE_CURVE('',#11485,#11487,#1137,.T.);
#14378=EDGE_CURVE('',#11488,#11489,#7166,.T.);
#14379=EDGE_CURVE('',#11488,#11486,#1138,.T.);
#14380=EDGE_CURVE('',#11487,#11489,#1139,.T.);
#14381=EDGE_CURVE('',#11490,#11491,#7167,.T.);
#14382=EDGE_CURVE('',#11490,#11488,#1140,.T.);
#14383=EDGE_CURVE('',#11489,#11491,#1141,.T.);
#14384=EDGE_CURVE('',#11492,#11493,#7168,.T.);
#14385=EDGE_CURVE('',#11492,#11490,#1142,.T.);
#14386=EDGE_CURVE('',#11491,#11493,#1143,.T.);
#14387=EDGE_CURVE('',#11494,#11495,#7169,.T.);
#14388=EDGE_CURVE('',#11494,#11492,#1144,.T.);
#14389=EDGE_CURVE('',#11493,#11495,#1145,.T.);
#14390=EDGE_CURVE('',#11496,#11497,#7170,.T.);
#14391=EDGE_CURVE('',#11496,#11494,#1146,.T.);
#14392=EDGE_CURVE('',#11495,#11497,#1147,.T.);
#14393=EDGE_CURVE('',#11498,#11499,#7171,.T.);
#14394=EDGE_CURVE('',#11498,#11496,#1148,.T.);
#14395=EDGE_CURVE('',#11497,#11499,#1149,.T.);
#14396=EDGE_CURVE('',#11500,#11501,#7172,.T.);
#14397=EDGE_CURVE('',#11500,#11498,#1150,.T.);
#14398=EDGE_CURVE('',#11499,#11501,#1151,.T.);
#14399=EDGE_CURVE('',#11502,#11503,#7173,.T.);
#14400=EDGE_CURVE('',#11502,#11500,#1152,.T.);
#14401=EDGE_CURVE('',#11501,#11503,#1153,.T.);
#14402=EDGE_CURVE('',#11504,#11505,#7174,.T.);
#14403=EDGE_CURVE('',#11504,#11502,#1154,.T.);
#14404=EDGE_CURVE('',#11503,#11505,#1155,.T.);
#14405=EDGE_CURVE('',#11506,#11507,#7175,.T.);
#14406=EDGE_CURVE('',#11506,#11504,#1156,.T.);
#14407=EDGE_CURVE('',#11505,#11507,#1157,.T.);
#14408=EDGE_CURVE('',#11508,#11509,#7176,.T.);
#14409=EDGE_CURVE('',#11508,#11506,#1158,.T.);
#14410=EDGE_CURVE('',#11507,#11509,#1159,.T.);
#14411=EDGE_CURVE('',#11510,#11511,#7177,.T.);
#14412=EDGE_CURVE('',#11510,#11508,#1160,.T.);
#14413=EDGE_CURVE('',#11509,#11511,#1161,.T.);
#14414=EDGE_CURVE('',#11512,#11513,#7178,.T.);
#14415=EDGE_CURVE('',#11512,#11510,#1162,.T.);
#14416=EDGE_CURVE('',#11511,#11513,#1163,.T.);
#14417=EDGE_CURVE('',#11514,#11515,#7179,.T.);
#14418=EDGE_CURVE('',#11514,#11512,#1164,.T.);
#14419=EDGE_CURVE('',#11513,#11515,#1165,.T.);
#14420=EDGE_CURVE('',#11516,#11517,#7180,.T.);
#14421=EDGE_CURVE('',#11516,#11514,#1166,.T.);
#14422=EDGE_CURVE('',#11515,#11517,#1167,.T.);
#14423=EDGE_CURVE('',#11518,#11519,#7181,.T.);
#14424=EDGE_CURVE('',#11518,#11516,#1168,.T.);
#14425=EDGE_CURVE('',#11517,#11519,#1169,.T.);
#14426=EDGE_CURVE('',#11520,#11521,#7182,.T.);
#14427=EDGE_CURVE('',#11520,#11518,#1170,.T.);
#14428=EDGE_CURVE('',#11519,#11521,#1171,.T.);
#14429=EDGE_CURVE('',#11522,#11523,#7183,.T.);
#14430=EDGE_CURVE('',#11522,#11520,#1172,.T.);
#14431=EDGE_CURVE('',#11521,#11523,#1173,.T.);
#14432=EDGE_CURVE('',#11524,#11525,#7184,.T.);
#14433=EDGE_CURVE('',#11524,#11522,#1174,.T.);
#14434=EDGE_CURVE('',#11523,#11525,#1175,.T.);
#14435=EDGE_CURVE('',#11526,#11527,#7185,.T.);
#14436=EDGE_CURVE('',#11526,#11524,#1176,.T.);
#14437=EDGE_CURVE('',#11525,#11527,#1177,.T.);
#14438=EDGE_CURVE('',#11528,#11529,#7186,.T.);
#14439=EDGE_CURVE('',#11528,#11526,#1178,.T.);
#14440=EDGE_CURVE('',#11527,#11529,#1179,.T.);
#14441=EDGE_CURVE('',#11530,#11531,#7187,.T.);
#14442=EDGE_CURVE('',#11530,#11528,#1180,.T.);
#14443=EDGE_CURVE('',#11529,#11531,#1181,.T.);
#14444=EDGE_CURVE('',#11532,#11533,#7188,.T.);
#14445=EDGE_CURVE('',#11532,#11530,#1182,.T.);
#14446=EDGE_CURVE('',#11531,#11533,#1183,.T.);
#14447=EDGE_CURVE('',#11534,#11535,#7189,.T.);
#14448=EDGE_CURVE('',#11534,#11532,#1184,.T.);
#14449=EDGE_CURVE('',#11533,#11535,#1185,.T.);
#14450=EDGE_CURVE('',#11536,#11537,#7190,.T.);
#14451=EDGE_CURVE('',#11536,#11534,#1186,.T.);
#14452=EDGE_CURVE('',#11535,#11537,#1187,.T.);
#14453=EDGE_CURVE('',#11538,#11539,#7191,.T.);
#14454=EDGE_CURVE('',#11538,#11536,#1188,.T.);
#14455=EDGE_CURVE('',#11537,#11539,#1189,.T.);
#14456=EDGE_CURVE('',#11540,#11541,#7192,.T.);
#14457=EDGE_CURVE('',#11540,#11538,#1190,.T.);
#14458=EDGE_CURVE('',#11539,#11541,#1191,.T.);
#14459=EDGE_CURVE('',#11542,#11543,#7193,.T.);
#14460=EDGE_CURVE('',#11542,#11540,#1192,.T.);
#14461=EDGE_CURVE('',#11541,#11543,#1193,.T.);
#14462=EDGE_CURVE('',#11544,#11545,#7194,.T.);
#14463=EDGE_CURVE('',#11544,#11542,#1194,.T.);
#14464=EDGE_CURVE('',#11543,#11545,#1195,.T.);
#14465=EDGE_CURVE('',#11546,#11547,#7195,.T.);
#14466=EDGE_CURVE('',#11546,#11544,#1196,.T.);
#14467=EDGE_CURVE('',#11545,#11547,#1197,.T.);
#14468=EDGE_CURVE('',#11548,#11549,#7196,.T.);
#14469=EDGE_CURVE('',#11548,#11546,#1198,.T.);
#14470=EDGE_CURVE('',#11547,#11549,#1199,.T.);
#14471=EDGE_CURVE('',#11550,#11551,#7197,.T.);
#14472=EDGE_CURVE('',#11550,#11548,#1200,.T.);
#14473=EDGE_CURVE('',#11549,#11551,#1201,.T.);
#14474=EDGE_CURVE('',#11552,#11553,#7198,.T.);
#14475=EDGE_CURVE('',#11552,#11550,#1202,.T.);
#14476=EDGE_CURVE('',#11551,#11553,#1203,.T.);
#14477=EDGE_CURVE('',#11554,#11555,#7199,.T.);
#14478=EDGE_CURVE('',#11554,#11552,#1204,.T.);
#14479=EDGE_CURVE('',#11553,#11555,#1205,.T.);
#14480=EDGE_CURVE('',#11556,#11557,#7200,.T.);
#14481=EDGE_CURVE('',#11556,#11554,#1206,.T.);
#14482=EDGE_CURVE('',#11555,#11557,#1207,.T.);
#14483=EDGE_CURVE('',#11558,#11559,#7201,.T.);
#14484=EDGE_CURVE('',#11558,#11556,#1208,.T.);
#14485=EDGE_CURVE('',#11557,#11559,#1209,.T.);
#14486=EDGE_CURVE('',#11560,#11561,#7202,.T.);
#14487=EDGE_CURVE('',#11560,#11558,#1210,.T.);
#14488=EDGE_CURVE('',#11559,#11561,#1211,.T.);
#14489=EDGE_CURVE('',#11562,#11563,#7203,.T.);
#14490=EDGE_CURVE('',#11562,#11560,#1212,.T.);
#14491=EDGE_CURVE('',#11561,#11563,#1213,.T.);
#14492=EDGE_CURVE('',#11564,#11565,#7204,.T.);
#14493=EDGE_CURVE('',#11564,#11562,#1214,.T.);
#14494=EDGE_CURVE('',#11563,#11565,#1215,.T.);
#14495=EDGE_CURVE('',#11566,#11567,#7205,.T.);
#14496=EDGE_CURVE('',#11566,#11564,#1216,.T.);
#14497=EDGE_CURVE('',#11565,#11567,#1217,.T.);
#14498=EDGE_CURVE('',#11568,#11569,#7206,.T.);
#14499=EDGE_CURVE('',#11568,#11566,#1218,.T.);
#14500=EDGE_CURVE('',#11567,#11569,#1219,.T.);
#14501=EDGE_CURVE('',#11570,#11571,#7207,.T.);
#14502=EDGE_CURVE('',#11570,#11568,#1220,.T.);
#14503=EDGE_CURVE('',#11569,#11571,#1221,.T.);
#14504=EDGE_CURVE('',#11572,#11573,#7208,.T.);
#14505=EDGE_CURVE('',#11572,#11570,#1222,.T.);
#14506=EDGE_CURVE('',#11571,#11573,#1223,.T.);
#14507=EDGE_CURVE('',#11574,#11575,#7209,.T.);
#14508=EDGE_CURVE('',#11574,#11572,#1224,.T.);
#14509=EDGE_CURVE('',#11573,#11575,#1225,.T.);
#14510=EDGE_CURVE('',#11576,#11577,#7210,.T.);
#14511=EDGE_CURVE('',#11576,#11574,#1226,.T.);
#14512=EDGE_CURVE('',#11575,#11577,#1227,.T.);
#14513=EDGE_CURVE('',#11578,#11579,#7211,.T.);
#14514=EDGE_CURVE('',#11578,#11576,#1228,.T.);
#14515=EDGE_CURVE('',#11577,#11579,#1229,.T.);
#14516=EDGE_CURVE('',#11580,#11581,#7212,.T.);
#14517=EDGE_CURVE('',#11580,#11578,#1230,.T.);
#14518=EDGE_CURVE('',#11579,#11581,#1231,.T.);
#14519=EDGE_CURVE('',#11582,#11583,#7213,.T.);
#14520=EDGE_CURVE('',#11582,#11580,#1232,.T.);
#14521=EDGE_CURVE('',#11581,#11583,#1233,.T.);
#14522=EDGE_CURVE('',#11584,#11585,#7214,.T.);
#14523=EDGE_CURVE('',#11584,#11582,#1234,.T.);
#14524=EDGE_CURVE('',#11583,#11585,#1235,.T.);
#14525=EDGE_CURVE('',#11586,#11587,#7215,.T.);
#14526=EDGE_CURVE('',#11586,#11584,#1236,.T.);
#14527=EDGE_CURVE('',#11585,#11587,#1237,.T.);
#14528=EDGE_CURVE('',#11588,#11589,#7216,.T.);
#14529=EDGE_CURVE('',#11588,#11590,#1238,.T.);
#14530=EDGE_CURVE('',#11589,#11590,#9717,.T.);
#14531=EDGE_CURVE('',#11591,#11592,#7217,.T.);
#14532=EDGE_CURVE('',#11591,#11588,#1239,.T.);
#14533=EDGE_CURVE('',#11593,#11589,#9718,.T.);
#14534=EDGE_CURVE('',#11592,#11593,#1240,.T.);
#14535=EDGE_CURVE('',#11594,#11595,#7218,.T.);
#14536=EDGE_CURVE('',#11594,#11591,#1241,.T.);
#14537=EDGE_CURVE('',#11595,#11592,#1242,.T.);
#14538=EDGE_CURVE('',#11596,#11597,#7219,.T.);
#14539=EDGE_CURVE('',#11596,#11594,#1243,.T.);
#14540=EDGE_CURVE('',#11597,#11595,#1244,.T.);
#14541=EDGE_CURVE('',#11598,#11599,#7220,.T.);
#14542=EDGE_CURVE('',#11598,#11596,#1245,.T.);
#14543=EDGE_CURVE('',#11599,#11597,#1246,.T.);
#14544=EDGE_CURVE('',#11600,#11601,#7221,.T.);
#14545=EDGE_CURVE('',#11600,#11598,#1247,.T.);
#14546=EDGE_CURVE('',#11601,#11599,#1248,.T.);
#14547=EDGE_CURVE('',#11602,#11603,#7222,.T.);
#14548=EDGE_CURVE('',#11602,#11600,#1249,.T.);
#14549=EDGE_CURVE('',#11603,#11601,#1250,.T.);
#14550=EDGE_CURVE('',#11604,#11605,#7223,.T.);
#14551=EDGE_CURVE('',#11604,#11602,#1251,.T.);
#14552=EDGE_CURVE('',#11605,#11603,#1252,.T.);
#14553=EDGE_CURVE('',#11606,#11607,#7224,.T.);
#14554=EDGE_CURVE('',#11606,#11604,#1253,.T.);
#14555=EDGE_CURVE('',#11607,#11605,#1254,.T.);
#14556=EDGE_CURVE('',#11608,#11609,#7225,.T.);
#14557=EDGE_CURVE('',#11608,#11606,#1255,.T.);
#14558=EDGE_CURVE('',#11609,#11607,#1256,.T.);
#14559=EDGE_CURVE('',#11610,#11611,#7226,.T.);
#14560=EDGE_CURVE('',#11610,#11608,#1257,.T.);
#14561=EDGE_CURVE('',#11611,#11609,#1258,.T.);
#14562=EDGE_CURVE('',#11612,#11613,#7227,.T.);
#14563=EDGE_CURVE('',#11612,#11610,#1259,.T.);
#14564=EDGE_CURVE('',#11613,#11611,#1260,.T.);
#14565=EDGE_CURVE('',#11614,#11615,#7228,.T.);
#14566=EDGE_CURVE('',#11614,#11612,#1261,.T.);
#14567=EDGE_CURVE('',#11615,#11613,#1262,.T.);
#14568=EDGE_CURVE('',#11616,#11617,#7229,.T.);
#14569=EDGE_CURVE('',#11616,#11614,#1263,.T.);
#14570=EDGE_CURVE('',#11617,#11615,#1264,.T.);
#14571=EDGE_CURVE('',#11618,#11619,#7230,.T.);
#14572=EDGE_CURVE('',#11618,#11616,#1265,.T.);
#14573=EDGE_CURVE('',#11619,#11617,#1266,.T.);
#14574=EDGE_CURVE('',#11620,#11621,#7231,.T.);
#14575=EDGE_CURVE('',#11620,#11618,#1267,.T.);
#14576=EDGE_CURVE('',#11621,#11619,#1268,.T.);
#14577=EDGE_CURVE('',#11622,#11623,#7232,.T.);
#14578=EDGE_CURVE('',#11622,#11620,#1269,.T.);
#14579=EDGE_CURVE('',#11623,#11621,#1270,.T.);
#14580=EDGE_CURVE('',#11624,#11625,#7233,.T.);
#14581=EDGE_CURVE('',#11624,#11622,#1271,.T.);
#14582=EDGE_CURVE('',#11625,#11623,#1272,.T.);
#14583=EDGE_CURVE('',#11626,#11627,#7234,.T.);
#14584=EDGE_CURVE('',#11626,#11624,#1273,.T.);
#14585=EDGE_CURVE('',#11627,#11625,#1274,.T.);
#14586=EDGE_CURVE('',#11628,#11629,#7235,.T.);
#14587=EDGE_CURVE('',#11628,#11626,#1275,.T.);
#14588=EDGE_CURVE('',#11629,#11627,#1276,.T.);
#14589=EDGE_CURVE('',#11630,#11631,#7236,.T.);
#14590=EDGE_CURVE('',#11630,#11628,#1277,.T.);
#14591=EDGE_CURVE('',#11631,#11629,#1278,.T.);
#14592=EDGE_CURVE('',#11632,#11633,#7237,.T.);
#14593=EDGE_CURVE('',#11632,#11630,#1279,.T.);
#14594=EDGE_CURVE('',#11633,#11631,#1280,.T.);
#14595=EDGE_CURVE('',#11634,#11635,#7238,.T.);
#14596=EDGE_CURVE('',#11634,#11632,#1281,.T.);
#14597=EDGE_CURVE('',#11635,#11633,#1282,.T.);
#14598=EDGE_CURVE('',#11636,#11637,#7239,.T.);
#14599=EDGE_CURVE('',#11636,#11634,#1283,.T.);
#14600=EDGE_CURVE('',#11637,#11635,#1284,.T.);
#14601=EDGE_CURVE('',#11638,#11639,#7240,.T.);
#14602=EDGE_CURVE('',#11638,#11636,#1285,.T.);
#14603=EDGE_CURVE('',#11639,#11637,#1286,.T.);
#14604=EDGE_CURVE('',#11640,#11641,#7241,.T.);
#14605=EDGE_CURVE('',#11640,#11638,#1287,.T.);
#14606=EDGE_CURVE('',#11641,#11639,#1288,.T.);
#14607=EDGE_CURVE('',#11642,#11643,#7242,.T.);
#14608=EDGE_CURVE('',#11642,#11640,#1289,.T.);
#14609=EDGE_CURVE('',#11643,#11641,#1290,.T.);
#14610=EDGE_CURVE('',#11644,#11645,#7243,.T.);
#14611=EDGE_CURVE('',#11644,#11642,#1291,.T.);
#14612=EDGE_CURVE('',#11645,#11643,#1292,.T.);
#14613=EDGE_CURVE('',#11646,#11647,#7244,.T.);
#14614=EDGE_CURVE('',#11646,#11644,#1293,.T.);
#14615=EDGE_CURVE('',#11647,#11645,#1294,.T.);
#14616=EDGE_CURVE('',#11648,#11649,#7245,.T.);
#14617=EDGE_CURVE('',#11648,#11646,#1295,.T.);
#14618=EDGE_CURVE('',#11649,#11647,#1296,.T.);
#14619=EDGE_CURVE('',#11650,#11651,#7246,.T.);
#14620=EDGE_CURVE('',#11650,#11648,#1297,.T.);
#14621=EDGE_CURVE('',#11651,#11649,#1298,.T.);
#14622=EDGE_CURVE('',#11652,#11653,#7247,.T.);
#14623=EDGE_CURVE('',#11652,#11650,#1299,.T.);
#14624=EDGE_CURVE('',#11653,#11651,#1300,.T.);
#14625=EDGE_CURVE('',#11654,#11655,#7248,.T.);
#14626=EDGE_CURVE('',#11654,#11652,#1301,.T.);
#14627=EDGE_CURVE('',#11655,#11653,#1302,.T.);
#14628=EDGE_CURVE('',#11656,#11657,#7249,.T.);
#14629=EDGE_CURVE('',#11656,#11654,#1303,.T.);
#14630=EDGE_CURVE('',#11657,#11655,#1304,.T.);
#14631=EDGE_CURVE('',#11658,#11659,#7250,.T.);
#14632=EDGE_CURVE('',#11658,#11656,#1305,.T.);
#14633=EDGE_CURVE('',#11659,#11657,#1306,.T.);
#14634=EDGE_CURVE('',#11660,#11661,#7251,.T.);
#14635=EDGE_CURVE('',#11660,#11658,#1307,.T.);
#14636=EDGE_CURVE('',#11661,#11659,#1308,.T.);
#14637=EDGE_CURVE('',#11662,#11663,#7252,.T.);
#14638=EDGE_CURVE('',#11662,#11660,#1309,.T.);
#14639=EDGE_CURVE('',#11663,#11661,#1310,.T.);
#14640=EDGE_CURVE('',#11664,#11665,#7253,.T.);
#14641=EDGE_CURVE('',#11664,#11662,#1311,.T.);
#14642=EDGE_CURVE('',#11665,#11663,#1312,.T.);
#14643=EDGE_CURVE('',#11666,#11667,#7254,.T.);
#14644=EDGE_CURVE('',#11666,#11664,#1313,.T.);
#14645=EDGE_CURVE('',#11667,#11665,#1314,.T.);
#14646=EDGE_CURVE('',#11668,#11669,#7255,.T.);
#14647=EDGE_CURVE('',#11668,#11666,#1315,.T.);
#14648=EDGE_CURVE('',#11669,#11667,#1316,.T.);
#14649=EDGE_CURVE('',#11670,#11671,#7256,.T.);
#14650=EDGE_CURVE('',#11670,#11668,#1317,.T.);
#14651=EDGE_CURVE('',#11671,#11669,#1318,.T.);
#14652=EDGE_CURVE('',#11672,#11673,#7257,.T.);
#14653=EDGE_CURVE('',#11672,#11670,#1319,.T.);
#14654=EDGE_CURVE('',#11673,#11671,#1320,.T.);
#14655=EDGE_CURVE('',#11674,#11675,#7258,.T.);
#14656=EDGE_CURVE('',#11674,#11672,#1321,.T.);
#14657=EDGE_CURVE('',#11675,#11673,#1322,.T.);
#14658=EDGE_CURVE('',#11676,#11677,#7259,.T.);
#14659=EDGE_CURVE('',#11676,#11674,#1323,.T.);
#14660=EDGE_CURVE('',#11677,#11675,#1324,.T.);
#14661=EDGE_CURVE('',#11678,#11679,#7260,.T.);
#14662=EDGE_CURVE('',#11678,#11676,#1325,.T.);
#14663=EDGE_CURVE('',#11679,#11677,#1326,.T.);
#14664=EDGE_CURVE('',#11680,#11681,#7261,.T.);
#14665=EDGE_CURVE('',#11680,#11678,#1327,.T.);
#14666=EDGE_CURVE('',#11681,#11679,#1328,.T.);
#14667=EDGE_CURVE('',#11682,#11683,#7262,.T.);
#14668=EDGE_CURVE('',#11682,#11680,#1329,.T.);
#14669=EDGE_CURVE('',#11683,#11681,#1330,.T.);
#14670=EDGE_CURVE('',#11684,#11685,#7263,.T.);
#14671=EDGE_CURVE('',#11684,#11682,#1331,.T.);
#14672=EDGE_CURVE('',#11685,#11683,#1332,.T.);
#14673=EDGE_CURVE('',#11686,#11687,#7264,.T.);
#14674=EDGE_CURVE('',#11686,#11684,#1333,.T.);
#14675=EDGE_CURVE('',#11687,#11685,#1334,.T.);
#14676=EDGE_CURVE('',#11688,#11689,#7265,.T.);
#14677=EDGE_CURVE('',#11688,#11686,#1335,.T.);
#14678=EDGE_CURVE('',#11689,#11687,#1336,.T.);
#14679=EDGE_CURVE('',#11690,#11691,#7266,.T.);
#14680=EDGE_CURVE('',#11690,#11688,#1337,.T.);
#14681=EDGE_CURVE('',#11691,#11689,#1338,.T.);
#14682=EDGE_CURVE('',#11692,#11693,#7267,.T.);
#14683=EDGE_CURVE('',#11692,#11690,#1339,.T.);
#14684=EDGE_CURVE('',#11693,#11691,#1340,.T.);
#14685=EDGE_CURVE('',#11694,#11695,#7268,.T.);
#14686=EDGE_CURVE('',#11694,#11692,#1341,.T.);
#14687=EDGE_CURVE('',#11695,#11693,#1342,.T.);
#14688=EDGE_CURVE('',#11696,#11697,#7269,.T.);
#14689=EDGE_CURVE('',#11696,#11694,#1343,.T.);
#14690=EDGE_CURVE('',#11697,#11695,#1344,.T.);
#14691=EDGE_CURVE('',#11698,#11699,#7270,.T.);
#14692=EDGE_CURVE('',#11698,#11696,#1345,.T.);
#14693=EDGE_CURVE('',#11699,#11697,#1346,.T.);
#14694=EDGE_CURVE('',#11700,#11701,#7271,.T.);
#14695=EDGE_CURVE('',#11700,#11698,#1347,.T.);
#14696=EDGE_CURVE('',#11701,#11699,#1348,.T.);
#14697=EDGE_CURVE('',#11702,#11703,#7272,.T.);
#14698=EDGE_CURVE('',#11702,#11700,#1349,.T.);
#14699=EDGE_CURVE('',#11703,#11701,#1350,.T.);
#14700=EDGE_CURVE('',#11704,#11705,#7273,.T.);
#14701=EDGE_CURVE('',#11704,#11702,#1351,.T.);
#14702=EDGE_CURVE('',#11705,#11703,#1352,.T.);
#14703=EDGE_CURVE('',#11706,#11707,#7274,.T.);
#14704=EDGE_CURVE('',#11706,#11704,#1353,.T.);
#14705=EDGE_CURVE('',#11707,#11705,#1354,.T.);
#14706=EDGE_CURVE('',#11708,#11709,#7275,.T.);
#14707=EDGE_CURVE('',#11708,#11706,#1355,.T.);
#14708=EDGE_CURVE('',#11709,#11707,#1356,.T.);
#14709=EDGE_CURVE('',#11710,#11711,#7276,.T.);
#14710=EDGE_CURVE('',#11710,#11708,#1357,.T.);
#14711=EDGE_CURVE('',#11711,#11709,#1358,.T.);
#14712=EDGE_CURVE('',#11712,#11713,#7277,.T.);
#14713=EDGE_CURVE('',#11712,#11710,#1359,.T.);
#14714=EDGE_CURVE('',#11713,#11711,#1360,.T.);
#14715=EDGE_CURVE('',#11714,#11715,#7278,.T.);
#14716=EDGE_CURVE('',#11714,#11712,#1361,.T.);
#14717=EDGE_CURVE('',#11715,#11713,#1362,.T.);
#14718=EDGE_CURVE('',#11716,#11716,#9719,.T.);
#14719=EDGE_CURVE('',#11717,#11463,#1363,.T.);
#14720=EDGE_CURVE('',#11462,#11718,#1364,.T.);
#14721=EDGE_CURVE('',#11718,#11717,#9720,.T.);
#14722=EDGE_CURVE('',#11716,#11719,#7279,.T.);
#14723=EDGE_CURVE('',#11719,#11719,#9721,.T.);
#14724=EDGE_CURVE('',#11720,#11593,#1365,.T.);
#14725=EDGE_CURVE('',#11587,#11720,#1366,.T.);
#14726=EDGE_CURVE('',#11717,#11715,#1367,.T.);
#14727=EDGE_CURVE('',#11718,#11714,#1368,.T.);
#14728=EDGE_CURVE('',#11590,#11721,#1369,.T.);
#14729=EDGE_CURVE('',#11721,#11586,#1370,.T.);
#14730=EDGE_CURVE('',#11722,#11723,#7280,.T.);
#14731=EDGE_CURVE('',#11722,#11724,#7281,.T.);
#14732=EDGE_CURVE('',#11725,#11724,#7282,.T.);
#14733=EDGE_CURVE('',#11723,#11725,#7283,.T.);
#14734=EDGE_CURVE('',#11723,#11726,#9722,.T.);
#14735=EDGE_CURVE('',#11725,#11727,#7284,.T.);
#14736=EDGE_CURVE('',#11727,#11726,#7285,.T.);
#14737=EDGE_CURVE('',#11724,#11728,#7286,.T.);
#14738=EDGE_CURVE('',#11727,#11728,#7287,.T.);
#14739=EDGE_CURVE('',#11726,#11729,#7288,.T.);
#14740=EDGE_CURVE('',#11728,#11729,#7289,.T.);
#14741=EDGE_CURVE('',#11729,#11722,#9723,.T.);
#14742=EDGE_CURVE('',#11730,#11730,#9724,.T.);
#14743=EDGE_CURVE('',#11730,#11731,#7290,.T.);
#14744=EDGE_CURVE('',#11731,#11731,#9725,.T.);
#14745=EDGE_CURVE('',#11732,#11732,#9726,.T.);
#14746=EDGE_CURVE('',#11721,#11720,#9727,.F.);
#14747=EDGE_CURVE('',#11733,#11733,#9728,.T.);
#14748=EDGE_CURVE('',#11733,#11732,#7291,.T.);
#19908=ORIENTED_EDGE('',*,*,#14338,.F.);
#19909=ORIENTED_EDGE('',*,*,#14339,.T.);
#19910=ORIENTED_EDGE('',*,*,#14340,.T.);
#19911=ORIENTED_EDGE('',*,*,#14341,.T.);
#19912=ORIENTED_EDGE('',*,*,#14342,.F.);
#19913=ORIENTED_EDGE('',*,*,#14343,.T.);
#19914=ORIENTED_EDGE('',*,*,#14338,.T.);
#19915=ORIENTED_EDGE('',*,*,#14344,.T.);
#19916=ORIENTED_EDGE('',*,*,#14345,.F.);
#19917=ORIENTED_EDGE('',*,*,#14346,.T.);
#19918=ORIENTED_EDGE('',*,*,#14342,.T.);
#19919=ORIENTED_EDGE('',*,*,#14347,.T.);
#19920=ORIENTED_EDGE('',*,*,#14348,.F.);
#19921=ORIENTED_EDGE('',*,*,#14349,.T.);
#19922=ORIENTED_EDGE('',*,*,#14345,.T.);
#19923=ORIENTED_EDGE('',*,*,#14350,.T.);
#19924=ORIENTED_EDGE('',*,*,#14351,.F.);
#19925=ORIENTED_EDGE('',*,*,#14352,.T.);
#19926=ORIENTED_EDGE('',*,*,#14348,.T.);
#19927=ORIENTED_EDGE('',*,*,#14353,.T.);
#19928=ORIENTED_EDGE('',*,*,#14354,.F.);
#19929=ORIENTED_EDGE('',*,*,#14355,.T.);
#19930=ORIENTED_EDGE('',*,*,#14351,.T.);
#19931=ORIENTED_EDGE('',*,*,#14356,.T.);
#19932=ORIENTED_EDGE('',*,*,#14357,.F.);
#19933=ORIENTED_EDGE('',*,*,#14358,.T.);
#19934=ORIENTED_EDGE('',*,*,#14354,.T.);
#19935=ORIENTED_EDGE('',*,*,#14359,.T.);
#19936=ORIENTED_EDGE('',*,*,#14360,.F.);
#19937=ORIENTED_EDGE('',*,*,#14361,.T.);
#19938=ORIENTED_EDGE('',*,*,#14357,.T.);
#19939=ORIENTED_EDGE('',*,*,#14362,.T.);
#19940=ORIENTED_EDGE('',*,*,#14363,.F.);
#19941=ORIENTED_EDGE('',*,*,#14364,.T.);
#19942=ORIENTED_EDGE('',*,*,#14360,.T.);
#19943=ORIENTED_EDGE('',*,*,#14365,.T.);
#19944=ORIENTED_EDGE('',*,*,#14366,.F.);
#19945=ORIENTED_EDGE('',*,*,#14367,.T.);
#19946=ORIENTED_EDGE('',*,*,#14363,.T.);
#19947=ORIENTED_EDGE('',*,*,#14368,.T.);
#19948=ORIENTED_EDGE('',*,*,#14369,.F.);
#19949=ORIENTED_EDGE('',*,*,#14370,.T.);
#19950=ORIENTED_EDGE('',*,*,#14366,.T.);
#19951=ORIENTED_EDGE('',*,*,#14371,.T.);
#19952=ORIENTED_EDGE('',*,*,#14372,.F.);
#19953=ORIENTED_EDGE('',*,*,#14373,.T.);
#19954=ORIENTED_EDGE('',*,*,#14369,.T.);
#19955=ORIENTED_EDGE('',*,*,#14374,.T.);
#19956=ORIENTED_EDGE('',*,*,#14375,.F.);
#19957=ORIENTED_EDGE('',*,*,#14376,.T.);
#19958=ORIENTED_EDGE('',*,*,#14372,.T.);
#19959=ORIENTED_EDGE('',*,*,#14377,.T.);
#19960=ORIENTED_EDGE('',*,*,#14378,.F.);
#19961=ORIENTED_EDGE('',*,*,#14379,.T.);
#19962=ORIENTED_EDGE('',*,*,#14375,.T.);
#19963=ORIENTED_EDGE('',*,*,#14380,.T.);
#19964=ORIENTED_EDGE('',*,*,#14381,.F.);
#19965=ORIENTED_EDGE('',*,*,#14382,.T.);
#19966=ORIENTED_EDGE('',*,*,#14378,.T.);
#19967=ORIENTED_EDGE('',*,*,#14383,.T.);
#19968=ORIENTED_EDGE('',*,*,#14384,.F.);
#19969=ORIENTED_EDGE('',*,*,#14385,.T.);
#19970=ORIENTED_EDGE('',*,*,#14381,.T.);
#19971=ORIENTED_EDGE('',*,*,#14386,.T.);
#19972=ORIENTED_EDGE('',*,*,#14387,.F.);
#19973=ORIENTED_EDGE('',*,*,#14388,.T.);
#19974=ORIENTED_EDGE('',*,*,#14384,.T.);
#19975=ORIENTED_EDGE('',*,*,#14389,.T.);
#19976=ORIENTED_EDGE('',*,*,#14390,.F.);
#19977=ORIENTED_EDGE('',*,*,#14391,.T.);
#19978=ORIENTED_EDGE('',*,*,#14387,.T.);
#19979=ORIENTED_EDGE('',*,*,#14392,.T.);
#19980=ORIENTED_EDGE('',*,*,#14393,.F.);
#19981=ORIENTED_EDGE('',*,*,#14394,.T.);
#19982=ORIENTED_EDGE('',*,*,#14390,.T.);
#19983=ORIENTED_EDGE('',*,*,#14395,.T.);
#19984=ORIENTED_EDGE('',*,*,#14396,.F.);
#19985=ORIENTED_EDGE('',*,*,#14397,.T.);
#19986=ORIENTED_EDGE('',*,*,#14393,.T.);
#19987=ORIENTED_EDGE('',*,*,#14398,.T.);
#19988=ORIENTED_EDGE('',*,*,#14399,.F.);
#19989=ORIENTED_EDGE('',*,*,#14400,.T.);
#19990=ORIENTED_EDGE('',*,*,#14396,.T.);
#19991=ORIENTED_EDGE('',*,*,#14401,.T.);
#19992=ORIENTED_EDGE('',*,*,#14402,.F.);
#19993=ORIENTED_EDGE('',*,*,#14403,.T.);
#19994=ORIENTED_EDGE('',*,*,#14399,.T.);
#19995=ORIENTED_EDGE('',*,*,#14404,.T.);
#19996=ORIENTED_EDGE('',*,*,#14405,.F.);
#19997=ORIENTED_EDGE('',*,*,#14406,.T.);
#19998=ORIENTED_EDGE('',*,*,#14402,.T.);
#19999=ORIENTED_EDGE('',*,*,#14407,.T.);
#20000=ORIENTED_EDGE('',*,*,#14408,.F.);
#20001=ORIENTED_EDGE('',*,*,#14409,.T.);
#20002=ORIENTED_EDGE('',*,*,#14405,.T.);
#20003=ORIENTED_EDGE('',*,*,#14410,.T.);
#20004=ORIENTED_EDGE('',*,*,#14411,.F.);
#20005=ORIENTED_EDGE('',*,*,#14412,.T.);
#20006=ORIENTED_EDGE('',*,*,#14408,.T.);
#20007=ORIENTED_EDGE('',*,*,#14413,.T.);
#20008=ORIENTED_EDGE('',*,*,#14414,.F.);
#20009=ORIENTED_EDGE('',*,*,#14415,.T.);
#20010=ORIENTED_EDGE('',*,*,#14411,.T.);
#20011=ORIENTED_EDGE('',*,*,#14416,.T.);
#20012=ORIENTED_EDGE('',*,*,#14417,.F.);
#20013=ORIENTED_EDGE('',*,*,#14418,.T.);
#20014=ORIENTED_EDGE('',*,*,#14414,.T.);
#20015=ORIENTED_EDGE('',*,*,#14419,.T.);
#20016=ORIENTED_EDGE('',*,*,#14420,.F.);
#20017=ORIENTED_EDGE('',*,*,#14421,.T.);
#20018=ORIENTED_EDGE('',*,*,#14417,.T.);
#20019=ORIENTED_EDGE('',*,*,#14422,.T.);
#20020=ORIENTED_EDGE('',*,*,#14423,.F.);
#20021=ORIENTED_EDGE('',*,*,#14424,.T.);
#20022=ORIENTED_EDGE('',*,*,#14420,.T.);
#20023=ORIENTED_EDGE('',*,*,#14425,.T.);
#20024=ORIENTED_EDGE('',*,*,#14426,.F.);
#20025=ORIENTED_EDGE('',*,*,#14427,.T.);
#20026=ORIENTED_EDGE('',*,*,#14423,.T.);
#20027=ORIENTED_EDGE('',*,*,#14428,.T.);
#20028=ORIENTED_EDGE('',*,*,#14429,.F.);
#20029=ORIENTED_EDGE('',*,*,#14430,.T.);
#20030=ORIENTED_EDGE('',*,*,#14426,.T.);
#20031=ORIENTED_EDGE('',*,*,#14431,.T.);
#20032=ORIENTED_EDGE('',*,*,#14432,.F.);
#20033=ORIENTED_EDGE('',*,*,#14433,.T.);
#20034=ORIENTED_EDGE('',*,*,#14429,.T.);
#20035=ORIENTED_EDGE('',*,*,#14434,.T.);
#20036=ORIENTED_EDGE('',*,*,#14435,.F.);
#20037=ORIENTED_EDGE('',*,*,#14436,.T.);
#20038=ORIENTED_EDGE('',*,*,#14432,.T.);
#20039=ORIENTED_EDGE('',*,*,#14437,.T.);
#20040=ORIENTED_EDGE('',*,*,#14438,.F.);
#20041=ORIENTED_EDGE('',*,*,#14439,.T.);
#20042=ORIENTED_EDGE('',*,*,#14435,.T.);
#20043=ORIENTED_EDGE('',*,*,#14440,.T.);
#20044=ORIENTED_EDGE('',*,*,#14441,.F.);
#20045=ORIENTED_EDGE('',*,*,#14442,.T.);
#20046=ORIENTED_EDGE('',*,*,#14438,.T.);
#20047=ORIENTED_EDGE('',*,*,#14443,.T.);
#20048=ORIENTED_EDGE('',*,*,#14444,.F.);
#20049=ORIENTED_EDGE('',*,*,#14445,.T.);
#20050=ORIENTED_EDGE('',*,*,#14441,.T.);
#20051=ORIENTED_EDGE('',*,*,#14446,.T.);
#20052=ORIENTED_EDGE('',*,*,#14447,.F.);
#20053=ORIENTED_EDGE('',*,*,#14448,.T.);
#20054=ORIENTED_EDGE('',*,*,#14444,.T.);
#20055=ORIENTED_EDGE('',*,*,#14449,.T.);
#20056=ORIENTED_EDGE('',*,*,#14450,.F.);
#20057=ORIENTED_EDGE('',*,*,#14451,.T.);
#20058=ORIENTED_EDGE('',*,*,#14447,.T.);
#20059=ORIENTED_EDGE('',*,*,#14452,.T.);
#20060=ORIENTED_EDGE('',*,*,#14453,.F.);
#20061=ORIENTED_EDGE('',*,*,#14454,.T.);
#20062=ORIENTED_EDGE('',*,*,#14450,.T.);
#20063=ORIENTED_EDGE('',*,*,#14455,.T.);
#20064=ORIENTED_EDGE('',*,*,#14456,.F.);
#20065=ORIENTED_EDGE('',*,*,#14457,.T.);
#20066=ORIENTED_EDGE('',*,*,#14453,.T.);
#20067=ORIENTED_EDGE('',*,*,#14458,.T.);
#20068=ORIENTED_EDGE('',*,*,#14459,.F.);
#20069=ORIENTED_EDGE('',*,*,#14460,.T.);
#20070=ORIENTED_EDGE('',*,*,#14456,.T.);
#20071=ORIENTED_EDGE('',*,*,#14461,.T.);
#20072=ORIENTED_EDGE('',*,*,#14462,.F.);
#20073=ORIENTED_EDGE('',*,*,#14463,.T.);
#20074=ORIENTED_EDGE('',*,*,#14459,.T.);
#20075=ORIENTED_EDGE('',*,*,#14464,.T.);
#20076=ORIENTED_EDGE('',*,*,#14465,.F.);
#20077=ORIENTED_EDGE('',*,*,#14466,.T.);
#20078=ORIENTED_EDGE('',*,*,#14462,.T.);
#20079=ORIENTED_EDGE('',*,*,#14467,.T.);
#20080=ORIENTED_EDGE('',*,*,#14468,.F.);
#20081=ORIENTED_EDGE('',*,*,#14469,.T.);
#20082=ORIENTED_EDGE('',*,*,#14465,.T.);
#20083=ORIENTED_EDGE('',*,*,#14470,.T.);
#20084=ORIENTED_EDGE('',*,*,#14471,.F.);
#20085=ORIENTED_EDGE('',*,*,#14472,.T.);
#20086=ORIENTED_EDGE('',*,*,#14468,.T.);
#20087=ORIENTED_EDGE('',*,*,#14473,.T.);
#20088=ORIENTED_EDGE('',*,*,#14474,.F.);
#20089=ORIENTED_EDGE('',*,*,#14475,.T.);
#20090=ORIENTED_EDGE('',*,*,#14471,.T.);
#20091=ORIENTED_EDGE('',*,*,#14476,.T.);
#20092=ORIENTED_EDGE('',*,*,#14477,.F.);
#20093=ORIENTED_EDGE('',*,*,#14478,.T.);
#20094=ORIENTED_EDGE('',*,*,#14474,.T.);
#20095=ORIENTED_EDGE('',*,*,#14479,.T.);
#20096=ORIENTED_EDGE('',*,*,#14480,.F.);
#20097=ORIENTED_EDGE('',*,*,#14481,.T.);
#20098=ORIENTED_EDGE('',*,*,#14477,.T.);
#20099=ORIENTED_EDGE('',*,*,#14482,.T.);
#20100=ORIENTED_EDGE('',*,*,#14483,.F.);
#20101=ORIENTED_EDGE('',*,*,#14484,.T.);
#20102=ORIENTED_EDGE('',*,*,#14480,.T.);
#20103=ORIENTED_EDGE('',*,*,#14485,.T.);
#20104=ORIENTED_EDGE('',*,*,#14486,.F.);
#20105=ORIENTED_EDGE('',*,*,#14487,.T.);
#20106=ORIENTED_EDGE('',*,*,#14483,.T.);
#20107=ORIENTED_EDGE('',*,*,#14488,.T.);
#20108=ORIENTED_EDGE('',*,*,#14489,.F.);
#20109=ORIENTED_EDGE('',*,*,#14490,.T.);
#20110=ORIENTED_EDGE('',*,*,#14486,.T.);
#20111=ORIENTED_EDGE('',*,*,#14491,.T.);
#20112=ORIENTED_EDGE('',*,*,#14492,.F.);
#20113=ORIENTED_EDGE('',*,*,#14493,.T.);
#20114=ORIENTED_EDGE('',*,*,#14489,.T.);
#20115=ORIENTED_EDGE('',*,*,#14494,.T.);
#20116=ORIENTED_EDGE('',*,*,#14495,.F.);
#20117=ORIENTED_EDGE('',*,*,#14496,.T.);
#20118=ORIENTED_EDGE('',*,*,#14492,.T.);
#20119=ORIENTED_EDGE('',*,*,#14497,.T.);
#20120=ORIENTED_EDGE('',*,*,#14498,.F.);
#20121=ORIENTED_EDGE('',*,*,#14499,.T.);
#20122=ORIENTED_EDGE('',*,*,#14495,.T.);
#20123=ORIENTED_EDGE('',*,*,#14500,.T.);
#20124=ORIENTED_EDGE('',*,*,#14501,.F.);
#20125=ORIENTED_EDGE('',*,*,#14502,.T.);
#20126=ORIENTED_EDGE('',*,*,#14498,.T.);
#20127=ORIENTED_EDGE('',*,*,#14503,.T.);
#20128=ORIENTED_EDGE('',*,*,#14504,.F.);
#20129=ORIENTED_EDGE('',*,*,#14505,.T.);
#20130=ORIENTED_EDGE('',*,*,#14501,.T.);
#20131=ORIENTED_EDGE('',*,*,#14506,.T.);
#20132=ORIENTED_EDGE('',*,*,#14507,.F.);
#20133=ORIENTED_EDGE('',*,*,#14508,.T.);
#20134=ORIENTED_EDGE('',*,*,#14504,.T.);
#20135=ORIENTED_EDGE('',*,*,#14509,.T.);
#20136=ORIENTED_EDGE('',*,*,#14510,.F.);
#20137=ORIENTED_EDGE('',*,*,#14511,.T.);
#20138=ORIENTED_EDGE('',*,*,#14507,.T.);
#20139=ORIENTED_EDGE('',*,*,#14512,.T.);
#20140=ORIENTED_EDGE('',*,*,#14513,.F.);
#20141=ORIENTED_EDGE('',*,*,#14514,.T.);
#20142=ORIENTED_EDGE('',*,*,#14510,.T.);
#20143=ORIENTED_EDGE('',*,*,#14515,.T.);
#20144=ORIENTED_EDGE('',*,*,#14516,.F.);
#20145=ORIENTED_EDGE('',*,*,#14517,.T.);
#20146=ORIENTED_EDGE('',*,*,#14513,.T.);
#20147=ORIENTED_EDGE('',*,*,#14518,.T.);
#20148=ORIENTED_EDGE('',*,*,#14519,.F.);
#20149=ORIENTED_EDGE('',*,*,#14520,.T.);
#20150=ORIENTED_EDGE('',*,*,#14516,.T.);
#20151=ORIENTED_EDGE('',*,*,#14521,.T.);
#20152=ORIENTED_EDGE('',*,*,#14522,.F.);
#20153=ORIENTED_EDGE('',*,*,#14523,.T.);
#20154=ORIENTED_EDGE('',*,*,#14519,.T.);
#20155=ORIENTED_EDGE('',*,*,#14524,.T.);
#20156=ORIENTED_EDGE('',*,*,#14525,.F.);
#20157=ORIENTED_EDGE('',*,*,#14526,.T.);
#20158=ORIENTED_EDGE('',*,*,#14522,.T.);
#20159=ORIENTED_EDGE('',*,*,#14527,.T.);
#20160=ORIENTED_EDGE('',*,*,#14528,.F.);
#20161=ORIENTED_EDGE('',*,*,#14529,.T.);
#20162=ORIENTED_EDGE('',*,*,#14530,.F.);
#20163=ORIENTED_EDGE('',*,*,#14531,.F.);
#20164=ORIENTED_EDGE('',*,*,#14532,.T.);
#20165=ORIENTED_EDGE('',*,*,#14528,.T.);
#20166=ORIENTED_EDGE('',*,*,#14533,.F.);
#20167=ORIENTED_EDGE('',*,*,#14534,.F.);
#20168=ORIENTED_EDGE('',*,*,#14535,.F.);
#20169=ORIENTED_EDGE('',*,*,#14536,.T.);
#20170=ORIENTED_EDGE('',*,*,#14531,.T.);
#20171=ORIENTED_EDGE('',*,*,#14537,.F.);
#20172=ORIENTED_EDGE('',*,*,#14538,.F.);
#20173=ORIENTED_EDGE('',*,*,#14539,.T.);
#20174=ORIENTED_EDGE('',*,*,#14535,.T.);
#20175=ORIENTED_EDGE('',*,*,#14540,.F.);
#20176=ORIENTED_EDGE('',*,*,#14541,.F.);
#20177=ORIENTED_EDGE('',*,*,#14542,.T.);
#20178=ORIENTED_EDGE('',*,*,#14538,.T.);
#20179=ORIENTED_EDGE('',*,*,#14543,.F.);
#20180=ORIENTED_EDGE('',*,*,#14544,.F.);
#20181=ORIENTED_EDGE('',*,*,#14545,.T.);
#20182=ORIENTED_EDGE('',*,*,#14541,.T.);
#20183=ORIENTED_EDGE('',*,*,#14546,.F.);
#20184=ORIENTED_EDGE('',*,*,#14547,.F.);
#20185=ORIENTED_EDGE('',*,*,#14548,.T.);
#20186=ORIENTED_EDGE('',*,*,#14544,.T.);
#20187=ORIENTED_EDGE('',*,*,#14549,.F.);
#20188=ORIENTED_EDGE('',*,*,#14550,.F.);
#20189=ORIENTED_EDGE('',*,*,#14551,.T.);
#20190=ORIENTED_EDGE('',*,*,#14547,.T.);
#20191=ORIENTED_EDGE('',*,*,#14552,.F.);
#20192=ORIENTED_EDGE('',*,*,#14553,.F.);
#20193=ORIENTED_EDGE('',*,*,#14554,.T.);
#20194=ORIENTED_EDGE('',*,*,#14550,.T.);
#20195=ORIENTED_EDGE('',*,*,#14555,.F.);
#20196=ORIENTED_EDGE('',*,*,#14556,.F.);
#20197=ORIENTED_EDGE('',*,*,#14557,.T.);
#20198=ORIENTED_EDGE('',*,*,#14553,.T.);
#20199=ORIENTED_EDGE('',*,*,#14558,.F.);
#20200=ORIENTED_EDGE('',*,*,#14559,.F.);
#20201=ORIENTED_EDGE('',*,*,#14560,.T.);
#20202=ORIENTED_EDGE('',*,*,#14556,.T.);
#20203=ORIENTED_EDGE('',*,*,#14561,.F.);
#20204=ORIENTED_EDGE('',*,*,#14562,.F.);
#20205=ORIENTED_EDGE('',*,*,#14563,.T.);
#20206=ORIENTED_EDGE('',*,*,#14559,.T.);
#20207=ORIENTED_EDGE('',*,*,#14564,.F.);
#20208=ORIENTED_EDGE('',*,*,#14565,.F.);
#20209=ORIENTED_EDGE('',*,*,#14566,.T.);
#20210=ORIENTED_EDGE('',*,*,#14562,.T.);
#20211=ORIENTED_EDGE('',*,*,#14567,.F.);
#20212=ORIENTED_EDGE('',*,*,#14568,.F.);
#20213=ORIENTED_EDGE('',*,*,#14569,.T.);
#20214=ORIENTED_EDGE('',*,*,#14565,.T.);
#20215=ORIENTED_EDGE('',*,*,#14570,.F.);
#20216=ORIENTED_EDGE('',*,*,#14571,.F.);
#20217=ORIENTED_EDGE('',*,*,#14572,.T.);
#20218=ORIENTED_EDGE('',*,*,#14568,.T.);
#20219=ORIENTED_EDGE('',*,*,#14573,.F.);
#20220=ORIENTED_EDGE('',*,*,#14574,.F.);
#20221=ORIENTED_EDGE('',*,*,#14575,.T.);
#20222=ORIENTED_EDGE('',*,*,#14571,.T.);
#20223=ORIENTED_EDGE('',*,*,#14576,.F.);
#20224=ORIENTED_EDGE('',*,*,#14577,.F.);
#20225=ORIENTED_EDGE('',*,*,#14578,.T.);
#20226=ORIENTED_EDGE('',*,*,#14574,.T.);
#20227=ORIENTED_EDGE('',*,*,#14579,.F.);
#20228=ORIENTED_EDGE('',*,*,#14580,.F.);
#20229=ORIENTED_EDGE('',*,*,#14581,.T.);
#20230=ORIENTED_EDGE('',*,*,#14577,.T.);
#20231=ORIENTED_EDGE('',*,*,#14582,.F.);
#20232=ORIENTED_EDGE('',*,*,#14583,.F.);
#20233=ORIENTED_EDGE('',*,*,#14584,.T.);
#20234=ORIENTED_EDGE('',*,*,#14580,.T.);
#20235=ORIENTED_EDGE('',*,*,#14585,.F.);
#20236=ORIENTED_EDGE('',*,*,#14586,.F.);
#20237=ORIENTED_EDGE('',*,*,#14587,.T.);
#20238=ORIENTED_EDGE('',*,*,#14583,.T.);
#20239=ORIENTED_EDGE('',*,*,#14588,.F.);
#20240=ORIENTED_EDGE('',*,*,#14589,.F.);
#20241=ORIENTED_EDGE('',*,*,#14590,.T.);
#20242=ORIENTED_EDGE('',*,*,#14586,.T.);
#20243=ORIENTED_EDGE('',*,*,#14591,.F.);
#20244=ORIENTED_EDGE('',*,*,#14592,.F.);
#20245=ORIENTED_EDGE('',*,*,#14593,.T.);
#20246=ORIENTED_EDGE('',*,*,#14589,.T.);
#20247=ORIENTED_EDGE('',*,*,#14594,.F.);
#20248=ORIENTED_EDGE('',*,*,#14595,.F.);
#20249=ORIENTED_EDGE('',*,*,#14596,.T.);
#20250=ORIENTED_EDGE('',*,*,#14592,.T.);
#20251=ORIENTED_EDGE('',*,*,#14597,.F.);
#20252=ORIENTED_EDGE('',*,*,#14598,.F.);
#20253=ORIENTED_EDGE('',*,*,#14599,.T.);
#20254=ORIENTED_EDGE('',*,*,#14595,.T.);
#20255=ORIENTED_EDGE('',*,*,#14600,.F.);
#20256=ORIENTED_EDGE('',*,*,#14601,.F.);
#20257=ORIENTED_EDGE('',*,*,#14602,.T.);
#20258=ORIENTED_EDGE('',*,*,#14598,.T.);
#20259=ORIENTED_EDGE('',*,*,#14603,.F.);
#20260=ORIENTED_EDGE('',*,*,#14604,.F.);
#20261=ORIENTED_EDGE('',*,*,#14605,.T.);
#20262=ORIENTED_EDGE('',*,*,#14601,.T.);
#20263=ORIENTED_EDGE('',*,*,#14606,.F.);
#20264=ORIENTED_EDGE('',*,*,#14607,.F.);
#20265=ORIENTED_EDGE('',*,*,#14608,.T.);
#20266=ORIENTED_EDGE('',*,*,#14604,.T.);
#20267=ORIENTED_EDGE('',*,*,#14609,.F.);
#20268=ORIENTED_EDGE('',*,*,#14610,.F.);
#20269=ORIENTED_EDGE('',*,*,#14611,.T.);
#20270=ORIENTED_EDGE('',*,*,#14607,.T.);
#20271=ORIENTED_EDGE('',*,*,#14612,.F.);
#20272=ORIENTED_EDGE('',*,*,#14613,.F.);
#20273=ORIENTED_EDGE('',*,*,#14614,.T.);
#20274=ORIENTED_EDGE('',*,*,#14610,.T.);
#20275=ORIENTED_EDGE('',*,*,#14615,.F.);
#20276=ORIENTED_EDGE('',*,*,#14616,.F.);
#20277=ORIENTED_EDGE('',*,*,#14617,.T.);
#20278=ORIENTED_EDGE('',*,*,#14613,.T.);
#20279=ORIENTED_EDGE('',*,*,#14618,.F.);
#20280=ORIENTED_EDGE('',*,*,#14619,.F.);
#20281=ORIENTED_EDGE('',*,*,#14620,.T.);
#20282=ORIENTED_EDGE('',*,*,#14616,.T.);
#20283=ORIENTED_EDGE('',*,*,#14621,.F.);
#20284=ORIENTED_EDGE('',*,*,#14622,.F.);
#20285=ORIENTED_EDGE('',*,*,#14623,.T.);
#20286=ORIENTED_EDGE('',*,*,#14619,.T.);
#20287=ORIENTED_EDGE('',*,*,#14624,.F.);
#20288=ORIENTED_EDGE('',*,*,#14625,.F.);
#20289=ORIENTED_EDGE('',*,*,#14626,.T.);
#20290=ORIENTED_EDGE('',*,*,#14622,.T.);
#20291=ORIENTED_EDGE('',*,*,#14627,.F.);
#20292=ORIENTED_EDGE('',*,*,#14628,.F.);
#20293=ORIENTED_EDGE('',*,*,#14629,.T.);
#20294=ORIENTED_EDGE('',*,*,#14625,.T.);
#20295=ORIENTED_EDGE('',*,*,#14630,.F.);
#20296=ORIENTED_EDGE('',*,*,#14631,.F.);
#20297=ORIENTED_EDGE('',*,*,#14632,.T.);
#20298=ORIENTED_EDGE('',*,*,#14628,.T.);
#20299=ORIENTED_EDGE('',*,*,#14633,.F.);
#20300=ORIENTED_EDGE('',*,*,#14634,.F.);
#20301=ORIENTED_EDGE('',*,*,#14635,.T.);
#20302=ORIENTED_EDGE('',*,*,#14631,.T.);
#20303=ORIENTED_EDGE('',*,*,#14636,.F.);
#20304=ORIENTED_EDGE('',*,*,#14637,.F.);
#20305=ORIENTED_EDGE('',*,*,#14638,.T.);
#20306=ORIENTED_EDGE('',*,*,#14634,.T.);
#20307=ORIENTED_EDGE('',*,*,#14639,.F.);
#20308=ORIENTED_EDGE('',*,*,#14640,.F.);
#20309=ORIENTED_EDGE('',*,*,#14641,.T.);
#20310=ORIENTED_EDGE('',*,*,#14637,.T.);
#20311=ORIENTED_EDGE('',*,*,#14642,.F.);
#20312=ORIENTED_EDGE('',*,*,#14643,.F.);
#20313=ORIENTED_EDGE('',*,*,#14644,.T.);
#20314=ORIENTED_EDGE('',*,*,#14640,.T.);
#20315=ORIENTED_EDGE('',*,*,#14645,.F.);
#20316=ORIENTED_EDGE('',*,*,#14646,.F.);
#20317=ORIENTED_EDGE('',*,*,#14647,.T.);
#20318=ORIENTED_EDGE('',*,*,#14643,.T.);
#20319=ORIENTED_EDGE('',*,*,#14648,.F.);
#20320=ORIENTED_EDGE('',*,*,#14649,.F.);
#20321=ORIENTED_EDGE('',*,*,#14650,.T.);
#20322=ORIENTED_EDGE('',*,*,#14646,.T.);
#20323=ORIENTED_EDGE('',*,*,#14651,.F.);
#20324=ORIENTED_EDGE('',*,*,#14652,.F.);
#20325=ORIENTED_EDGE('',*,*,#14653,.T.);
#20326=ORIENTED_EDGE('',*,*,#14649,.T.);
#20327=ORIENTED_EDGE('',*,*,#14654,.F.);
#20328=ORIENTED_EDGE('',*,*,#14655,.F.);
#20329=ORIENTED_EDGE('',*,*,#14656,.T.);
#20330=ORIENTED_EDGE('',*,*,#14652,.T.);
#20331=ORIENTED_EDGE('',*,*,#14657,.F.);
#20332=ORIENTED_EDGE('',*,*,#14658,.F.);
#20333=ORIENTED_EDGE('',*,*,#14659,.T.);
#20334=ORIENTED_EDGE('',*,*,#14655,.T.);
#20335=ORIENTED_EDGE('',*,*,#14660,.F.);
#20336=ORIENTED_EDGE('',*,*,#14661,.F.);
#20337=ORIENTED_EDGE('',*,*,#14662,.T.);
#20338=ORIENTED_EDGE('',*,*,#14658,.T.);
#20339=ORIENTED_EDGE('',*,*,#14663,.F.);
#20340=ORIENTED_EDGE('',*,*,#14664,.F.);
#20341=ORIENTED_EDGE('',*,*,#14665,.T.);
#20342=ORIENTED_EDGE('',*,*,#14661,.T.);
#20343=ORIENTED_EDGE('',*,*,#14666,.F.);
#20344=ORIENTED_EDGE('',*,*,#14667,.F.);
#20345=ORIENTED_EDGE('',*,*,#14668,.T.);
#20346=ORIENTED_EDGE('',*,*,#14664,.T.);
#20347=ORIENTED_EDGE('',*,*,#14669,.F.);
#20348=ORIENTED_EDGE('',*,*,#14670,.F.);
#20349=ORIENTED_EDGE('',*,*,#14671,.T.);
#20350=ORIENTED_EDGE('',*,*,#14667,.T.);
#20351=ORIENTED_EDGE('',*,*,#14672,.F.);
#20352=ORIENTED_EDGE('',*,*,#14673,.F.);
#20353=ORIENTED_EDGE('',*,*,#14674,.T.);
#20354=ORIENTED_EDGE('',*,*,#14670,.T.);
#20355=ORIENTED_EDGE('',*,*,#14675,.F.);
#20356=ORIENTED_EDGE('',*,*,#14676,.F.);
#20357=ORIENTED_EDGE('',*,*,#14677,.T.);
#20358=ORIENTED_EDGE('',*,*,#14673,.T.);
#20359=ORIENTED_EDGE('',*,*,#14678,.F.);
#20360=ORIENTED_EDGE('',*,*,#14679,.F.);
#20361=ORIENTED_EDGE('',*,*,#14680,.T.);
#20362=ORIENTED_EDGE('',*,*,#14676,.T.);
#20363=ORIENTED_EDGE('',*,*,#14681,.F.);
#20364=ORIENTED_EDGE('',*,*,#14682,.F.);
#20365=ORIENTED_EDGE('',*,*,#14683,.T.);
#20366=ORIENTED_EDGE('',*,*,#14679,.T.);
#20367=ORIENTED_EDGE('',*,*,#14684,.F.);
#20368=ORIENTED_EDGE('',*,*,#14685,.F.);
#20369=ORIENTED_EDGE('',*,*,#14686,.T.);
#20370=ORIENTED_EDGE('',*,*,#14682,.T.);
#20371=ORIENTED_EDGE('',*,*,#14687,.F.);
#20372=ORIENTED_EDGE('',*,*,#14688,.F.);
#20373=ORIENTED_EDGE('',*,*,#14689,.T.);
#20374=ORIENTED_EDGE('',*,*,#14685,.T.);
#20375=ORIENTED_EDGE('',*,*,#14690,.F.);
#20376=ORIENTED_EDGE('',*,*,#14691,.F.);
#20377=ORIENTED_EDGE('',*,*,#14692,.T.);
#20378=ORIENTED_EDGE('',*,*,#14688,.T.);
#20379=ORIENTED_EDGE('',*,*,#14693,.F.);
#20380=ORIENTED_EDGE('',*,*,#14694,.F.);
#20381=ORIENTED_EDGE('',*,*,#14695,.T.);
#20382=ORIENTED_EDGE('',*,*,#14691,.T.);
#20383=ORIENTED_EDGE('',*,*,#14696,.F.);
#20384=ORIENTED_EDGE('',*,*,#14697,.F.);
#20385=ORIENTED_EDGE('',*,*,#14698,.T.);
#20386=ORIENTED_EDGE('',*,*,#14694,.T.);
#20387=ORIENTED_EDGE('',*,*,#14699,.F.);
#20388=ORIENTED_EDGE('',*,*,#14700,.F.);
#20389=ORIENTED_EDGE('',*,*,#14701,.T.);
#20390=ORIENTED_EDGE('',*,*,#14697,.T.);
#20391=ORIENTED_EDGE('',*,*,#14702,.F.);
#20392=ORIENTED_EDGE('',*,*,#14703,.F.);
#20393=ORIENTED_EDGE('',*,*,#14704,.T.);
#20394=ORIENTED_EDGE('',*,*,#14700,.T.);
#20395=ORIENTED_EDGE('',*,*,#14705,.F.);
#20396=ORIENTED_EDGE('',*,*,#14706,.F.);
#20397=ORIENTED_EDGE('',*,*,#14707,.T.);
#20398=ORIENTED_EDGE('',*,*,#14703,.T.);
#20399=ORIENTED_EDGE('',*,*,#14708,.F.);
#20400=ORIENTED_EDGE('',*,*,#14709,.F.);
#20401=ORIENTED_EDGE('',*,*,#14710,.T.);
#20402=ORIENTED_EDGE('',*,*,#14706,.T.);
#20403=ORIENTED_EDGE('',*,*,#14711,.F.);
#20404=ORIENTED_EDGE('',*,*,#14712,.F.);
#20405=ORIENTED_EDGE('',*,*,#14713,.T.);
#20406=ORIENTED_EDGE('',*,*,#14709,.T.);
#20407=ORIENTED_EDGE('',*,*,#14714,.F.);
#20408=ORIENTED_EDGE('',*,*,#14715,.F.);
#20409=ORIENTED_EDGE('',*,*,#14716,.T.);
#20410=ORIENTED_EDGE('',*,*,#14712,.T.);
#20411=ORIENTED_EDGE('',*,*,#14717,.F.);
#20412=ORIENTED_EDGE('',*,*,#14718,.T.);
#20413=ORIENTED_EDGE('',*,*,#14719,.T.);
#20414=ORIENTED_EDGE('',*,*,#14340,.F.);
#20415=ORIENTED_EDGE('',*,*,#14720,.T.);
#20416=ORIENTED_EDGE('',*,*,#14721,.T.);
#20417=ORIENTED_EDGE('',*,*,#14718,.F.);
#20418=ORIENTED_EDGE('',*,*,#14722,.T.);
#20419=ORIENTED_EDGE('',*,*,#14723,.T.);
#20420=ORIENTED_EDGE('',*,*,#14722,.F.);
#20421=ORIENTED_EDGE('',*,*,#14723,.F.);
#20422=ORIENTED_EDGE('',*,*,#14724,.F.);
#20423=ORIENTED_EDGE('',*,*,#14725,.F.);
#20424=ORIENTED_EDGE('',*,*,#14527,.F.);
#20425=ORIENTED_EDGE('',*,*,#14524,.F.);
#20426=ORIENTED_EDGE('',*,*,#14521,.F.);
#20427=ORIENTED_EDGE('',*,*,#14518,.F.);
#20428=ORIENTED_EDGE('',*,*,#14515,.F.);
#20429=ORIENTED_EDGE('',*,*,#14512,.F.);
#20430=ORIENTED_EDGE('',*,*,#14509,.F.);
#20431=ORIENTED_EDGE('',*,*,#14506,.F.);
#20432=ORIENTED_EDGE('',*,*,#14503,.F.);
#20433=ORIENTED_EDGE('',*,*,#14500,.F.);
#20434=ORIENTED_EDGE('',*,*,#14497,.F.);
#20435=ORIENTED_EDGE('',*,*,#14494,.F.);
#20436=ORIENTED_EDGE('',*,*,#14491,.F.);
#20437=ORIENTED_EDGE('',*,*,#14488,.F.);
#20438=ORIENTED_EDGE('',*,*,#14485,.F.);
#20439=ORIENTED_EDGE('',*,*,#14482,.F.);
#20440=ORIENTED_EDGE('',*,*,#14479,.F.);
#20441=ORIENTED_EDGE('',*,*,#14476,.F.);
#20442=ORIENTED_EDGE('',*,*,#14473,.F.);
#20443=ORIENTED_EDGE('',*,*,#14470,.F.);
#20444=ORIENTED_EDGE('',*,*,#14467,.F.);
#20445=ORIENTED_EDGE('',*,*,#14464,.F.);
#20446=ORIENTED_EDGE('',*,*,#14461,.F.);
#20447=ORIENTED_EDGE('',*,*,#14458,.F.);
#20448=ORIENTED_EDGE('',*,*,#14455,.F.);
#20449=ORIENTED_EDGE('',*,*,#14452,.F.);
#20450=ORIENTED_EDGE('',*,*,#14449,.F.);
#20451=ORIENTED_EDGE('',*,*,#14446,.F.);
#20452=ORIENTED_EDGE('',*,*,#14443,.F.);
#20453=ORIENTED_EDGE('',*,*,#14440,.F.);
#20454=ORIENTED_EDGE('',*,*,#14437,.F.);
#20455=ORIENTED_EDGE('',*,*,#14434,.F.);
#20456=ORIENTED_EDGE('',*,*,#14431,.F.);
#20457=ORIENTED_EDGE('',*,*,#14428,.F.);
#20458=ORIENTED_EDGE('',*,*,#14425,.F.);
#20459=ORIENTED_EDGE('',*,*,#14422,.F.);
#20460=ORIENTED_EDGE('',*,*,#14419,.F.);
#20461=ORIENTED_EDGE('',*,*,#14416,.F.);
#20462=ORIENTED_EDGE('',*,*,#14413,.F.);
#20463=ORIENTED_EDGE('',*,*,#14410,.F.);
#20464=ORIENTED_EDGE('',*,*,#14407,.F.);
#20465=ORIENTED_EDGE('',*,*,#14404,.F.);
#20466=ORIENTED_EDGE('',*,*,#14401,.F.);
#20467=ORIENTED_EDGE('',*,*,#14398,.F.);
#20468=ORIENTED_EDGE('',*,*,#14395,.F.);
#20469=ORIENTED_EDGE('',*,*,#14392,.F.);
#20470=ORIENTED_EDGE('',*,*,#14389,.F.);
#20471=ORIENTED_EDGE('',*,*,#14386,.F.);
#20472=ORIENTED_EDGE('',*,*,#14383,.F.);
#20473=ORIENTED_EDGE('',*,*,#14380,.F.);
#20474=ORIENTED_EDGE('',*,*,#14377,.F.);
#20475=ORIENTED_EDGE('',*,*,#14374,.F.);
#20476=ORIENTED_EDGE('',*,*,#14371,.F.);
#20477=ORIENTED_EDGE('',*,*,#14368,.F.);
#20478=ORIENTED_EDGE('',*,*,#14365,.F.);
#20479=ORIENTED_EDGE('',*,*,#14362,.F.);
#20480=ORIENTED_EDGE('',*,*,#14359,.F.);
#20481=ORIENTED_EDGE('',*,*,#14356,.F.);
#20482=ORIENTED_EDGE('',*,*,#14353,.F.);
#20483=ORIENTED_EDGE('',*,*,#14350,.F.);
#20484=ORIENTED_EDGE('',*,*,#14347,.F.);
#20485=ORIENTED_EDGE('',*,*,#14344,.F.);
#20486=ORIENTED_EDGE('',*,*,#14341,.F.);
#20487=ORIENTED_EDGE('',*,*,#14719,.F.);
#20488=ORIENTED_EDGE('',*,*,#14726,.T.);
#20489=ORIENTED_EDGE('',*,*,#14717,.T.);
#20490=ORIENTED_EDGE('',*,*,#14714,.T.);
#20491=ORIENTED_EDGE('',*,*,#14711,.T.);
#20492=ORIENTED_EDGE('',*,*,#14708,.T.);
#20493=ORIENTED_EDGE('',*,*,#14705,.T.);
#20494=ORIENTED_EDGE('',*,*,#14702,.T.);
#20495=ORIENTED_EDGE('',*,*,#14699,.T.);
#20496=ORIENTED_EDGE('',*,*,#14696,.T.);
#20497=ORIENTED_EDGE('',*,*,#14693,.T.);
#20498=ORIENTED_EDGE('',*,*,#14690,.T.);
#20499=ORIENTED_EDGE('',*,*,#14687,.T.);
#20500=ORIENTED_EDGE('',*,*,#14684,.T.);
#20501=ORIENTED_EDGE('',*,*,#14681,.T.);
#20502=ORIENTED_EDGE('',*,*,#14678,.T.);
#20503=ORIENTED_EDGE('',*,*,#14675,.T.);
#20504=ORIENTED_EDGE('',*,*,#14672,.T.);
#20505=ORIENTED_EDGE('',*,*,#14669,.T.);
#20506=ORIENTED_EDGE('',*,*,#14666,.T.);
#20507=ORIENTED_EDGE('',*,*,#14663,.T.);
#20508=ORIENTED_EDGE('',*,*,#14660,.T.);
#20509=ORIENTED_EDGE('',*,*,#14657,.T.);
#20510=ORIENTED_EDGE('',*,*,#14654,.T.);
#20511=ORIENTED_EDGE('',*,*,#14651,.T.);
#20512=ORIENTED_EDGE('',*,*,#14648,.T.);
#20513=ORIENTED_EDGE('',*,*,#14645,.T.);
#20514=ORIENTED_EDGE('',*,*,#14642,.T.);
#20515=ORIENTED_EDGE('',*,*,#14639,.T.);
#20516=ORIENTED_EDGE('',*,*,#14636,.T.);
#20517=ORIENTED_EDGE('',*,*,#14633,.T.);
#20518=ORIENTED_EDGE('',*,*,#14630,.T.);
#20519=ORIENTED_EDGE('',*,*,#14627,.T.);
#20520=ORIENTED_EDGE('',*,*,#14624,.T.);
#20521=ORIENTED_EDGE('',*,*,#14621,.T.);
#20522=ORIENTED_EDGE('',*,*,#14618,.T.);
#20523=ORIENTED_EDGE('',*,*,#14615,.T.);
#20524=ORIENTED_EDGE('',*,*,#14612,.T.);
#20525=ORIENTED_EDGE('',*,*,#14609,.T.);
#20526=ORIENTED_EDGE('',*,*,#14606,.T.);
#20527=ORIENTED_EDGE('',*,*,#14603,.T.);
#20528=ORIENTED_EDGE('',*,*,#14600,.T.);
#20529=ORIENTED_EDGE('',*,*,#14597,.T.);
#20530=ORIENTED_EDGE('',*,*,#14594,.T.);
#20531=ORIENTED_EDGE('',*,*,#14591,.T.);
#20532=ORIENTED_EDGE('',*,*,#14588,.T.);
#20533=ORIENTED_EDGE('',*,*,#14585,.T.);
#20534=ORIENTED_EDGE('',*,*,#14582,.T.);
#20535=ORIENTED_EDGE('',*,*,#14579,.T.);
#20536=ORIENTED_EDGE('',*,*,#14576,.T.);
#20537=ORIENTED_EDGE('',*,*,#14573,.T.);
#20538=ORIENTED_EDGE('',*,*,#14570,.T.);
#20539=ORIENTED_EDGE('',*,*,#14567,.T.);
#20540=ORIENTED_EDGE('',*,*,#14564,.T.);
#20541=ORIENTED_EDGE('',*,*,#14561,.T.);
#20542=ORIENTED_EDGE('',*,*,#14558,.T.);
#20543=ORIENTED_EDGE('',*,*,#14555,.T.);
#20544=ORIENTED_EDGE('',*,*,#14552,.T.);
#20545=ORIENTED_EDGE('',*,*,#14549,.T.);
#20546=ORIENTED_EDGE('',*,*,#14546,.T.);
#20547=ORIENTED_EDGE('',*,*,#14543,.T.);
#20548=ORIENTED_EDGE('',*,*,#14540,.T.);
#20549=ORIENTED_EDGE('',*,*,#14537,.T.);
#20550=ORIENTED_EDGE('',*,*,#14534,.T.);
#20551=ORIENTED_EDGE('',*,*,#14715,.T.);
#20552=ORIENTED_EDGE('',*,*,#14726,.F.);
#20553=ORIENTED_EDGE('',*,*,#14721,.F.);
#20554=ORIENTED_EDGE('',*,*,#14727,.T.);
#20555=ORIENTED_EDGE('',*,*,#14728,.F.);
#20556=ORIENTED_EDGE('',*,*,#14529,.F.);
#20557=ORIENTED_EDGE('',*,*,#14532,.F.);
#20558=ORIENTED_EDGE('',*,*,#14536,.F.);
#20559=ORIENTED_EDGE('',*,*,#14539,.F.);
#20560=ORIENTED_EDGE('',*,*,#14542,.F.);
#20561=ORIENTED_EDGE('',*,*,#14545,.F.);
#20562=ORIENTED_EDGE('',*,*,#14548,.F.);
#20563=ORIENTED_EDGE('',*,*,#14551,.F.);
#20564=ORIENTED_EDGE('',*,*,#14554,.F.);
#20565=ORIENTED_EDGE('',*,*,#14557,.F.);
#20566=ORIENTED_EDGE('',*,*,#14560,.F.);
#20567=ORIENTED_EDGE('',*,*,#14563,.F.);
#20568=ORIENTED_EDGE('',*,*,#14566,.F.);
#20569=ORIENTED_EDGE('',*,*,#14569,.F.);
#20570=ORIENTED_EDGE('',*,*,#14572,.F.);
#20571=ORIENTED_EDGE('',*,*,#14575,.F.);
#20572=ORIENTED_EDGE('',*,*,#14578,.F.);
#20573=ORIENTED_EDGE('',*,*,#14581,.F.);
#20574=ORIENTED_EDGE('',*,*,#14584,.F.);
#20575=ORIENTED_EDGE('',*,*,#14587,.F.);
#20576=ORIENTED_EDGE('',*,*,#14590,.F.);
#20577=ORIENTED_EDGE('',*,*,#14593,.F.);
#20578=ORIENTED_EDGE('',*,*,#14596,.F.);
#20579=ORIENTED_EDGE('',*,*,#14599,.F.);
#20580=ORIENTED_EDGE('',*,*,#14602,.F.);
#20581=ORIENTED_EDGE('',*,*,#14605,.F.);
#20582=ORIENTED_EDGE('',*,*,#14608,.F.);
#20583=ORIENTED_EDGE('',*,*,#14611,.F.);
#20584=ORIENTED_EDGE('',*,*,#14614,.F.);
#20585=ORIENTED_EDGE('',*,*,#14617,.F.);
#20586=ORIENTED_EDGE('',*,*,#14620,.F.);
#20587=ORIENTED_EDGE('',*,*,#14623,.F.);
#20588=ORIENTED_EDGE('',*,*,#14626,.F.);
#20589=ORIENTED_EDGE('',*,*,#14629,.F.);
#20590=ORIENTED_EDGE('',*,*,#14632,.F.);
#20591=ORIENTED_EDGE('',*,*,#14635,.F.);
#20592=ORIENTED_EDGE('',*,*,#14638,.F.);
#20593=ORIENTED_EDGE('',*,*,#14641,.F.);
#20594=ORIENTED_EDGE('',*,*,#14644,.F.);
#20595=ORIENTED_EDGE('',*,*,#14647,.F.);
#20596=ORIENTED_EDGE('',*,*,#14650,.F.);
#20597=ORIENTED_EDGE('',*,*,#14653,.F.);
#20598=ORIENTED_EDGE('',*,*,#14656,.F.);
#20599=ORIENTED_EDGE('',*,*,#14659,.F.);
#20600=ORIENTED_EDGE('',*,*,#14662,.F.);
#20601=ORIENTED_EDGE('',*,*,#14665,.F.);
#20602=ORIENTED_EDGE('',*,*,#14668,.F.);
#20603=ORIENTED_EDGE('',*,*,#14671,.F.);
#20604=ORIENTED_EDGE('',*,*,#14674,.F.);
#20605=ORIENTED_EDGE('',*,*,#14677,.F.);
#20606=ORIENTED_EDGE('',*,*,#14680,.F.);
#20607=ORIENTED_EDGE('',*,*,#14683,.F.);
#20608=ORIENTED_EDGE('',*,*,#14686,.F.);
#20609=ORIENTED_EDGE('',*,*,#14689,.F.);
#20610=ORIENTED_EDGE('',*,*,#14692,.F.);
#20611=ORIENTED_EDGE('',*,*,#14695,.F.);
#20612=ORIENTED_EDGE('',*,*,#14698,.F.);
#20613=ORIENTED_EDGE('',*,*,#14701,.F.);
#20614=ORIENTED_EDGE('',*,*,#14704,.F.);
#20615=ORIENTED_EDGE('',*,*,#14707,.F.);
#20616=ORIENTED_EDGE('',*,*,#14710,.F.);
#20617=ORIENTED_EDGE('',*,*,#14713,.F.);
#20618=ORIENTED_EDGE('',*,*,#14716,.F.);
#20619=ORIENTED_EDGE('',*,*,#14727,.F.);
#20620=ORIENTED_EDGE('',*,*,#14720,.F.);
#20621=ORIENTED_EDGE('',*,*,#14339,.F.);
#20622=ORIENTED_EDGE('',*,*,#14343,.F.);
#20623=ORIENTED_EDGE('',*,*,#14346,.F.);
#20624=ORIENTED_EDGE('',*,*,#14349,.F.);
#20625=ORIENTED_EDGE('',*,*,#14352,.F.);
#20626=ORIENTED_EDGE('',*,*,#14355,.F.);
#20627=ORIENTED_EDGE('',*,*,#14358,.F.);
#20628=ORIENTED_EDGE('',*,*,#14361,.F.);
#20629=ORIENTED_EDGE('',*,*,#14364,.F.);
#20630=ORIENTED_EDGE('',*,*,#14367,.F.);
#20631=ORIENTED_EDGE('',*,*,#14370,.F.);
#20632=ORIENTED_EDGE('',*,*,#14373,.F.);
#20633=ORIENTED_EDGE('',*,*,#14376,.F.);
#20634=ORIENTED_EDGE('',*,*,#14379,.F.);
#20635=ORIENTED_EDGE('',*,*,#14382,.F.);
#20636=ORIENTED_EDGE('',*,*,#14385,.F.);
#20637=ORIENTED_EDGE('',*,*,#14388,.F.);
#20638=ORIENTED_EDGE('',*,*,#14391,.F.);
#20639=ORIENTED_EDGE('',*,*,#14394,.F.);
#20640=ORIENTED_EDGE('',*,*,#14397,.F.);
#20641=ORIENTED_EDGE('',*,*,#14400,.F.);
#20642=ORIENTED_EDGE('',*,*,#14403,.F.);
#20643=ORIENTED_EDGE('',*,*,#14406,.F.);
#20644=ORIENTED_EDGE('',*,*,#14409,.F.);
#20645=ORIENTED_EDGE('',*,*,#14412,.F.);
#20646=ORIENTED_EDGE('',*,*,#14415,.F.);
#20647=ORIENTED_EDGE('',*,*,#14418,.F.);
#20648=ORIENTED_EDGE('',*,*,#14421,.F.);
#20649=ORIENTED_EDGE('',*,*,#14424,.F.);
#20650=ORIENTED_EDGE('',*,*,#14427,.F.);
#20651=ORIENTED_EDGE('',*,*,#14430,.F.);
#20652=ORIENTED_EDGE('',*,*,#14433,.F.);
#20653=ORIENTED_EDGE('',*,*,#14436,.F.);
#20654=ORIENTED_EDGE('',*,*,#14439,.F.);
#20655=ORIENTED_EDGE('',*,*,#14442,.F.);
#20656=ORIENTED_EDGE('',*,*,#14445,.F.);
#20657=ORIENTED_EDGE('',*,*,#14448,.F.);
#20658=ORIENTED_EDGE('',*,*,#14451,.F.);
#20659=ORIENTED_EDGE('',*,*,#14454,.F.);
#20660=ORIENTED_EDGE('',*,*,#14457,.F.);
#20661=ORIENTED_EDGE('',*,*,#14460,.F.);
#20662=ORIENTED_EDGE('',*,*,#14463,.F.);
#20663=ORIENTED_EDGE('',*,*,#14466,.F.);
#20664=ORIENTED_EDGE('',*,*,#14469,.F.);
#20665=ORIENTED_EDGE('',*,*,#14472,.F.);
#20666=ORIENTED_EDGE('',*,*,#14475,.F.);
#20667=ORIENTED_EDGE('',*,*,#14478,.F.);
#20668=ORIENTED_EDGE('',*,*,#14481,.F.);
#20669=ORIENTED_EDGE('',*,*,#14484,.F.);
#20670=ORIENTED_EDGE('',*,*,#14487,.F.);
#20671=ORIENTED_EDGE('',*,*,#14490,.F.);
#20672=ORIENTED_EDGE('',*,*,#14493,.F.);
#20673=ORIENTED_EDGE('',*,*,#14496,.F.);
#20674=ORIENTED_EDGE('',*,*,#14499,.F.);
#20675=ORIENTED_EDGE('',*,*,#14502,.F.);
#20676=ORIENTED_EDGE('',*,*,#14505,.F.);
#20677=ORIENTED_EDGE('',*,*,#14508,.F.);
#20678=ORIENTED_EDGE('',*,*,#14511,.F.);
#20679=ORIENTED_EDGE('',*,*,#14514,.F.);
#20680=ORIENTED_EDGE('',*,*,#14517,.F.);
#20681=ORIENTED_EDGE('',*,*,#14520,.F.);
#20682=ORIENTED_EDGE('',*,*,#14523,.F.);
#20683=ORIENTED_EDGE('',*,*,#14526,.F.);
#20684=ORIENTED_EDGE('',*,*,#14729,.F.);
#20685=ORIENTED_EDGE('',*,*,#14730,.F.);
#20686=ORIENTED_EDGE('',*,*,#14731,.T.);
#20687=ORIENTED_EDGE('',*,*,#14732,.F.);
#20688=ORIENTED_EDGE('',*,*,#14733,.F.);
#20689=ORIENTED_EDGE('',*,*,#14734,.F.);
#20690=ORIENTED_EDGE('',*,*,#14733,.T.);
#20691=ORIENTED_EDGE('',*,*,#14735,.T.);
#20692=ORIENTED_EDGE('',*,*,#14736,.T.);
#20693=ORIENTED_EDGE('',*,*,#14735,.F.);
#20694=ORIENTED_EDGE('',*,*,#14732,.T.);
#20695=ORIENTED_EDGE('',*,*,#14737,.T.);
#20696=ORIENTED_EDGE('',*,*,#14738,.F.);
#20697=ORIENTED_EDGE('',*,*,#14739,.F.);
#20698=ORIENTED_EDGE('',*,*,#14736,.F.);
#20699=ORIENTED_EDGE('',*,*,#14738,.T.);
#20700=ORIENTED_EDGE('',*,*,#14740,.T.);
#20701=ORIENTED_EDGE('',*,*,#14741,.F.);
#20702=ORIENTED_EDGE('',*,*,#14740,.F.);
#20703=ORIENTED_EDGE('',*,*,#14737,.F.);
#20704=ORIENTED_EDGE('',*,*,#14731,.F.);
#20705=ORIENTED_EDGE('',*,*,#14742,.F.);
#20706=ORIENTED_EDGE('',*,*,#14743,.T.);
#20707=ORIENTED_EDGE('',*,*,#14744,.F.);
#20708=ORIENTED_EDGE('',*,*,#14743,.F.);
#20709=ORIENTED_EDGE('',*,*,#14739,.T.);
#20710=ORIENTED_EDGE('',*,*,#14741,.T.);
#20711=ORIENTED_EDGE('',*,*,#14730,.T.);
#20712=ORIENTED_EDGE('',*,*,#14734,.T.);
#20713=ORIENTED_EDGE('',*,*,#14742,.T.);
#20714=ORIENTED_EDGE('',*,*,#14745,.F.);
#20715=ORIENTED_EDGE('',*,*,#14746,.T.);
#20716=ORIENTED_EDGE('',*,*,#14724,.T.);
#20717=ORIENTED_EDGE('',*,*,#14533,.T.);
#20718=ORIENTED_EDGE('',*,*,#14530,.T.);
#20719=ORIENTED_EDGE('',*,*,#14728,.T.);
#20720=ORIENTED_EDGE('',*,*,#14747,.F.);
#20721=ORIENTED_EDGE('',*,*,#14748,.T.);
#20722=ORIENTED_EDGE('',*,*,#14745,.T.);
#20723=ORIENTED_EDGE('',*,*,#14748,.F.);
#20724=ORIENTED_EDGE('',*,*,#14747,.T.);
#20725=ORIENTED_EDGE('',*,*,#14744,.T.);
#20726=ORIENTED_EDGE('',*,*,#14525,.T.);
#20727=ORIENTED_EDGE('',*,*,#14725,.T.);
#20728=ORIENTED_EDGE('',*,*,#14746,.F.);
#20729=ORIENTED_EDGE('',*,*,#14729,.T.);
#21500=CYLINDRICAL_SURFACE('',#26128,0.5941);
#21501=CYLINDRICAL_SURFACE('',#26130,0.5941);
#21502=CYLINDRICAL_SURFACE('',#26131,0.5941);
#21503=CYLINDRICAL_SURFACE('',#26132,0.5941);
#21504=CYLINDRICAL_SURFACE('',#26133,0.5941);
#21505=CYLINDRICAL_SURFACE('',#26134,0.5941);
#21506=CYLINDRICAL_SURFACE('',#26135,0.5941);
#21507=CYLINDRICAL_SURFACE('',#26136,0.5941);
#21508=CYLINDRICAL_SURFACE('',#26137,0.5941);
#21509=CYLINDRICAL_SURFACE('',#26138,0.5941);
#21510=CYLINDRICAL_SURFACE('',#26139,0.5941);
#21511=CYLINDRICAL_SURFACE('',#26140,0.5941);
#21512=CYLINDRICAL_SURFACE('',#26141,0.5941);
#21513=CYLINDRICAL_SURFACE('',#26142,0.5941);
#21514=CYLINDRICAL_SURFACE('',#26143,0.5941);
#21515=CYLINDRICAL_SURFACE('',#26144,0.5941);
#21516=CYLINDRICAL_SURFACE('',#26145,0.5941);
#21517=CYLINDRICAL_SURFACE('',#26146,0.5941);
#21518=CYLINDRICAL_SURFACE('',#26147,0.5941);
#21519=CYLINDRICAL_SURFACE('',#26148,0.5941);
#21520=CYLINDRICAL_SURFACE('',#26149,0.5941);
#21521=CYLINDRICAL_SURFACE('',#26150,0.5941);
#21522=CYLINDRICAL_SURFACE('',#26151,0.5941);
#21523=CYLINDRICAL_SURFACE('',#26152,0.5941);
#21524=CYLINDRICAL_SURFACE('',#26153,0.5941);
#21525=CYLINDRICAL_SURFACE('',#26154,0.5941);
#21526=CYLINDRICAL_SURFACE('',#26155,0.5941);
#21527=CYLINDRICAL_SURFACE('',#26156,0.5941);
#21528=CYLINDRICAL_SURFACE('',#26157,0.5941);
#21529=CYLINDRICAL_SURFACE('',#26158,0.5941);
#21530=CYLINDRICAL_SURFACE('',#26159,0.5941);
#21531=CYLINDRICAL_SURFACE('',#26160,0.5941);
#21532=CYLINDRICAL_SURFACE('',#26161,0.5941);
#21533=CYLINDRICAL_SURFACE('',#26162,0.5941);
#21534=CYLINDRICAL_SURFACE('',#26163,0.5941);
#21535=CYLINDRICAL_SURFACE('',#26164,0.5941);
#21536=CYLINDRICAL_SURFACE('',#26165,0.5941);
#21537=CYLINDRICAL_SURFACE('',#26166,0.5941);
#21538=CYLINDRICAL_SURFACE('',#26167,0.5941);
#21539=CYLINDRICAL_SURFACE('',#26168,0.5941);
#21540=CYLINDRICAL_SURFACE('',#26169,0.5941);
#21541=CYLINDRICAL_SURFACE('',#26170,0.5941);
#21542=CYLINDRICAL_SURFACE('',#26171,0.5941);
#21543=CYLINDRICAL_SURFACE('',#26172,0.5941);
#21544=CYLINDRICAL_SURFACE('',#26173,0.5941);
#21545=CYLINDRICAL_SURFACE('',#26174,0.5941);
#21546=CYLINDRICAL_SURFACE('',#26175,0.5941);
#21547=CYLINDRICAL_SURFACE('',#26176,0.5941);
#21548=CYLINDRICAL_SURFACE('',#26177,0.5941);
#21549=CYLINDRICAL_SURFACE('',#26178,0.5941);
#21550=CYLINDRICAL_SURFACE('',#26179,0.5941);
#21551=CYLINDRICAL_SURFACE('',#26180,0.5941);
#21552=CYLINDRICAL_SURFACE('',#26181,0.5941);
#21553=CYLINDRICAL_SURFACE('',#26182,0.5941);
#21554=CYLINDRICAL_SURFACE('',#26183,0.5941);
#21555=CYLINDRICAL_SURFACE('',#26184,0.5941);
#21556=CYLINDRICAL_SURFACE('',#26185,0.5941);
#21557=CYLINDRICAL_SURFACE('',#26186,0.5941);
#21558=CYLINDRICAL_SURFACE('',#26187,0.5941);
#21559=CYLINDRICAL_SURFACE('',#26188,0.5941);
#21560=CYLINDRICAL_SURFACE('',#26189,0.5941);
#21561=CYLINDRICAL_SURFACE('',#26190,0.5941);
#21562=CYLINDRICAL_SURFACE('',#26191,0.5941);
#21563=CYLINDRICAL_SURFACE('',#26192,0.415875);
#21564=CYLINDRICAL_SURFACE('',#26194,0.415875);
#21565=CYLINDRICAL_SURFACE('',#26196,0.415875);
#21566=CYLINDRICAL_SURFACE('',#26197,0.415875);
#21567=CYLINDRICAL_SURFACE('',#26198,0.415875);
#21568=CYLINDRICAL_SURFACE('',#26199,0.415875);
#21569=CYLINDRICAL_SURFACE('',#26200,0.415875);
#21570=CYLINDRICAL_SURFACE('',#26201,0.415875);
#21571=CYLINDRICAL_SURFACE('',#26202,0.415875);
#21572=CYLINDRICAL_SURFACE('',#26203,0.415875);
#21573=CYLINDRICAL_SURFACE('',#26204,0.415875);
#21574=CYLINDRICAL_SURFACE('',#26205,0.415875);
#21575=CYLINDRICAL_SURFACE('',#26206,0.415875);
#21576=CYLINDRICAL_SURFACE('',#26207,0.415875);
#21577=CYLINDRICAL_SURFACE('',#26208,0.415875);
#21578=CYLINDRICAL_SURFACE('',#26209,0.415875);
#21579=CYLINDRICAL_SURFACE('',#26210,0.415875);
#21580=CYLINDRICAL_SURFACE('',#26211,0.415875);
#21581=CYLINDRICAL_SURFACE('',#26212,0.415875);
#21582=CYLINDRICAL_SURFACE('',#26213,0.415875);
#21583=CYLINDRICAL_SURFACE('',#26214,0.415875);
#21584=CYLINDRICAL_SURFACE('',#26215,0.415875);
#21585=CYLINDRICAL_SURFACE('',#26216,0.415875);
#21586=CYLINDRICAL_SURFACE('',#26217,0.415875);
#21587=CYLINDRICAL_SURFACE('',#26218,0.415875);
#21588=CYLINDRICAL_SURFACE('',#26219,0.415875);
#21589=CYLINDRICAL_SURFACE('',#26220,0.415875);
#21590=CYLINDRICAL_SURFACE('',#26221,0.415875);
#21591=CYLINDRICAL_SURFACE('',#26222,0.415875);
#21592=CYLINDRICAL_SURFACE('',#26223,0.415875);
#21593=CYLINDRICAL_SURFACE('',#26224,0.415875);
#21594=CYLINDRICAL_SURFACE('',#26225,0.415875);
#21595=CYLINDRICAL_SURFACE('',#26226,0.415875);
#21596=CYLINDRICAL_SURFACE('',#26227,0.415875);
#21597=CYLINDRICAL_SURFACE('',#26228,0.415875);
#21598=CYLINDRICAL_SURFACE('',#26229,0.415875);
#21599=CYLINDRICAL_SURFACE('',#26230,0.415875);
#21600=CYLINDRICAL_SURFACE('',#26231,0.415875);
#21601=CYLINDRICAL_SURFACE('',#26232,0.415875);
#21602=CYLINDRICAL_SURFACE('',#26233,0.415875);
#21603=CYLINDRICAL_SURFACE('',#26234,0.415875);
#21604=CYLINDRICAL_SURFACE('',#26235,0.415875);
#21605=CYLINDRICAL_SURFACE('',#26236,0.415875);
#21606=CYLINDRICAL_SURFACE('',#26237,0.415875);
#21607=CYLINDRICAL_SURFACE('',#26238,0.415875);
#21608=CYLINDRICAL_SURFACE('',#26239,0.415875);
#21609=CYLINDRICAL_SURFACE('',#26240,0.415875);
#21610=CYLINDRICAL_SURFACE('',#26241,0.415875);
#21611=CYLINDRICAL_SURFACE('',#26242,0.415875);
#21612=CYLINDRICAL_SURFACE('',#26243,0.415875);
#21613=CYLINDRICAL_SURFACE('',#26244,0.415875);
#21614=CYLINDRICAL_SURFACE('',#26245,0.415875);
#21615=CYLINDRICAL_SURFACE('',#26246,0.415875);
#21616=CYLINDRICAL_SURFACE('',#26247,0.415875);
#21617=CYLINDRICAL_SURFACE('',#26248,0.415875);
#21618=CYLINDRICAL_SURFACE('',#26249,0.415875);
#21619=CYLINDRICAL_SURFACE('',#26250,0.415875);
#21620=CYLINDRICAL_SURFACE('',#26251,0.415875);
#21621=CYLINDRICAL_SURFACE('',#26252,0.415875);
#21622=CYLINDRICAL_SURFACE('',#26253,0.415875);
#21623=CYLINDRICAL_SURFACE('',#26254,0.415875);
#21624=CYLINDRICAL_SURFACE('',#26255,0.415875);
#21625=CYLINDRICAL_SURFACE('',#26256,0.415875);
#21626=CYLINDRICAL_SURFACE('',#26260,0.6);
#21627=CYLINDRICAL_SURFACE('',#26263,0.415875);
#21628=CYLINDRICAL_SURFACE('',#26271,1.);
#21629=CYLINDRICAL_SURFACE('',#26278,1.35);
#21630=CYLINDRICAL_SURFACE('',#26281,0.5941);
#22746=ADVANCED_FACE('',(#3965),#21500,.T.);
#22747=ADVANCED_FACE('',(#3966),#21501,.T.);
#22748=ADVANCED_FACE('',(#3967),#21502,.T.);
#22749=ADVANCED_FACE('',(#3968),#21503,.T.);
#22750=ADVANCED_FACE('',(#3969),#21504,.T.);
#22751=ADVANCED_FACE('',(#3970),#21505,.T.);
#22752=ADVANCED_FACE('',(#3971),#21506,.T.);
#22753=ADVANCED_FACE('',(#3972),#21507,.T.);
#22754=ADVANCED_FACE('',(#3973),#21508,.T.);
#22755=ADVANCED_FACE('',(#3974),#21509,.T.);
#22756=ADVANCED_FACE('',(#3975),#21510,.T.);
#22757=ADVANCED_FACE('',(#3976),#21511,.T.);
#22758=ADVANCED_FACE('',(#3977),#21512,.T.);
#22759=ADVANCED_FACE('',(#3978),#21513,.T.);
#22760=ADVANCED_FACE('',(#3979),#21514,.T.);
#22761=ADVANCED_FACE('',(#3980),#21515,.T.);
#22762=ADVANCED_FACE('',(#3981),#21516,.T.);
#22763=ADVANCED_FACE('',(#3982),#21517,.T.);
#22764=ADVANCED_FACE('',(#3983),#21518,.T.);
#22765=ADVANCED_FACE('',(#3984),#21519,.T.);
#22766=ADVANCED_FACE('',(#3985),#21520,.T.);
#22767=ADVANCED_FACE('',(#3986),#21521,.T.);
#22768=ADVANCED_FACE('',(#3987),#21522,.T.);
#22769=ADVANCED_FACE('',(#3988),#21523,.T.);
#22770=ADVANCED_FACE('',(#3989),#21524,.T.);
#22771=ADVANCED_FACE('',(#3990),#21525,.T.);
#22772=ADVANCED_FACE('',(#3991),#21526,.T.);
#22773=ADVANCED_FACE('',(#3992),#21527,.T.);
#22774=ADVANCED_FACE('',(#3993),#21528,.T.);
#22775=ADVANCED_FACE('',(#3994),#21529,.T.);
#22776=ADVANCED_FACE('',(#3995),#21530,.T.);
#22777=ADVANCED_FACE('',(#3996),#21531,.T.);
#22778=ADVANCED_FACE('',(#3997),#21532,.T.);
#22779=ADVANCED_FACE('',(#3998),#21533,.T.);
#22780=ADVANCED_FACE('',(#3999),#21534,.T.);
#22781=ADVANCED_FACE('',(#4000),#21535,.T.);
#22782=ADVANCED_FACE('',(#4001),#21536,.T.);
#22783=ADVANCED_FACE('',(#4002),#21537,.T.);
#22784=ADVANCED_FACE('',(#4003),#21538,.T.);
#22785=ADVANCED_FACE('',(#4004),#21539,.T.);
#22786=ADVANCED_FACE('',(#4005),#21540,.T.);
#22787=ADVANCED_FACE('',(#4006),#21541,.T.);
#22788=ADVANCED_FACE('',(#4007),#21542,.T.);
#22789=ADVANCED_FACE('',(#4008),#21543,.T.);
#22790=ADVANCED_FACE('',(#4009),#21544,.T.);
#22791=ADVANCED_FACE('',(#4010),#21545,.T.);
#22792=ADVANCED_FACE('',(#4011),#21546,.T.);
#22793=ADVANCED_FACE('',(#4012),#21547,.T.);
#22794=ADVANCED_FACE('',(#4013),#21548,.T.);
#22795=ADVANCED_FACE('',(#4014),#21549,.T.);
#22796=ADVANCED_FACE('',(#4015),#21550,.T.);
#22797=ADVANCED_FACE('',(#4016),#21551,.T.);
#22798=ADVANCED_FACE('',(#4017),#21552,.T.);
#22799=ADVANCED_FACE('',(#4018),#21553,.T.);
#22800=ADVANCED_FACE('',(#4019),#21554,.T.);
#22801=ADVANCED_FACE('',(#4020),#21555,.T.);
#22802=ADVANCED_FACE('',(#4021),#21556,.T.);
#22803=ADVANCED_FACE('',(#4022),#21557,.T.);
#22804=ADVANCED_FACE('',(#4023),#21558,.T.);
#22805=ADVANCED_FACE('',(#4024),#21559,.T.);
#22806=ADVANCED_FACE('',(#4025),#21560,.T.);
#22807=ADVANCED_FACE('',(#4026),#21561,.T.);
#22808=ADVANCED_FACE('',(#4027),#21562,.T.);
#22809=ADVANCED_FACE('',(#4028),#21563,.T.);
#22810=ADVANCED_FACE('',(#4029),#21564,.T.);
#22811=ADVANCED_FACE('',(#4030),#21565,.T.);
#22812=ADVANCED_FACE('',(#4031),#21566,.T.);
#22813=ADVANCED_FACE('',(#4032),#21567,.T.);
#22814=ADVANCED_FACE('',(#4033),#21568,.T.);
#22815=ADVANCED_FACE('',(#4034),#21569,.T.);
#22816=ADVANCED_FACE('',(#4035),#21570,.T.);
#22817=ADVANCED_FACE('',(#4036),#21571,.T.);
#22818=ADVANCED_FACE('',(#4037),#21572,.T.);
#22819=ADVANCED_FACE('',(#4038),#21573,.T.);
#22820=ADVANCED_FACE('',(#4039),#21574,.T.);
#22821=ADVANCED_FACE('',(#4040),#21575,.T.);
#22822=ADVANCED_FACE('',(#4041),#21576,.T.);
#22823=ADVANCED_FACE('',(#4042),#21577,.T.);
#22824=ADVANCED_FACE('',(#4043),#21578,.T.);
#22825=ADVANCED_FACE('',(#4044),#21579,.T.);
#22826=ADVANCED_FACE('',(#4045),#21580,.T.);
#22827=ADVANCED_FACE('',(#4046),#21581,.T.);
#22828=ADVANCED_FACE('',(#4047),#21582,.T.);
#22829=ADVANCED_FACE('',(#4048),#21583,.T.);
#22830=ADVANCED_FACE('',(#4049),#21584,.T.);
#22831=ADVANCED_FACE('',(#4050),#21585,.T.);
#22832=ADVANCED_FACE('',(#4051),#21586,.T.);
#22833=ADVANCED_FACE('',(#4052),#21587,.T.);
#22834=ADVANCED_FACE('',(#4053),#21588,.T.);
#22835=ADVANCED_FACE('',(#4054),#21589,.T.);
#22836=ADVANCED_FACE('',(#4055),#21590,.T.);
#22837=ADVANCED_FACE('',(#4056),#21591,.T.);
#22838=ADVANCED_FACE('',(#4057),#21592,.T.);
#22839=ADVANCED_FACE('',(#4058),#21593,.T.);
#22840=ADVANCED_FACE('',(#4059),#21594,.T.);
#22841=ADVANCED_FACE('',(#4060),#21595,.T.);
#22842=ADVANCED_FACE('',(#4061),#21596,.T.);
#22843=ADVANCED_FACE('',(#4062),#21597,.T.);
#22844=ADVANCED_FACE('',(#4063),#21598,.T.);
#22845=ADVANCED_FACE('',(#4064),#21599,.T.);
#22846=ADVANCED_FACE('',(#4065),#21600,.T.);
#22847=ADVANCED_FACE('',(#4066),#21601,.T.);
#22848=ADVANCED_FACE('',(#4067),#21602,.T.);
#22849=ADVANCED_FACE('',(#4068),#21603,.T.);
#22850=ADVANCED_FACE('',(#4069),#21604,.T.);
#22851=ADVANCED_FACE('',(#4070),#21605,.T.);
#22852=ADVANCED_FACE('',(#4071),#21606,.T.);
#22853=ADVANCED_FACE('',(#4072),#21607,.T.);
#22854=ADVANCED_FACE('',(#4073),#21608,.T.);
#22855=ADVANCED_FACE('',(#4074),#21609,.T.);
#22856=ADVANCED_FACE('',(#4075),#21610,.T.);
#22857=ADVANCED_FACE('',(#4076),#21611,.T.);
#22858=ADVANCED_FACE('',(#4077),#21612,.T.);
#22859=ADVANCED_FACE('',(#4078),#21613,.T.);
#22860=ADVANCED_FACE('',(#4079),#21614,.T.);
#22861=ADVANCED_FACE('',(#4080),#21615,.T.);
#22862=ADVANCED_FACE('',(#4081),#21616,.T.);
#22863=ADVANCED_FACE('',(#4082),#21617,.T.);
#22864=ADVANCED_FACE('',(#4083),#21618,.T.);
#22865=ADVANCED_FACE('',(#4084),#21619,.T.);
#22866=ADVANCED_FACE('',(#4085),#21620,.T.);
#22867=ADVANCED_FACE('',(#4086),#21621,.T.);
#22868=ADVANCED_FACE('',(#4087),#21622,.T.);
#22869=ADVANCED_FACE('',(#4088),#21623,.T.);
#22870=ADVANCED_FACE('',(#4089),#21624,.T.);
#22871=ADVANCED_FACE('',(#4090),#21625,.T.);
#22872=ADVANCED_FACE('',(#4091,#2272),#2809,.T.);
#22873=ADVANCED_FACE('',(#4092),#21626,.T.);
#22874=ADVANCED_FACE('',(#4093),#2810,.F.);
#22875=ADVANCED_FACE('',(#4094),#17,.F.);
#22876=ADVANCED_FACE('',(#4095),#21627,.T.);
#22877=ADVANCED_FACE('',(#4096),#18,.F.);
#22878=ADVANCED_FACE('',(#4097),#2811,.F.);
#22879=ADVANCED_FACE('',(#4098),#2812,.T.);
#22880=ADVANCED_FACE('',(#4099),#2813,.F.);
#22881=ADVANCED_FACE('',(#4100),#2814,.F.);
#22882=ADVANCED_FACE('',(#4101),#2815,.F.);
#22883=ADVANCED_FACE('',(#4102,#2273),#21628,.T.);
#22884=ADVANCED_FACE('',(#4103),#2816,.T.);
#22885=ADVANCED_FACE('',(#4104,#2274),#2817,.F.);
#22886=ADVANCED_FACE('',(#4105),#21629,.T.);
#22887=ADVANCED_FACE('',(#4106,#2275),#2818,.T.);
#22888=ADVANCED_FACE('',(#4107),#21630,.T.);
#23075=CLOSED_SHELL('',(#22746,#22747,#22748,#22749,#22750,#22751,#22752,
#22753,#22754,#22755,#22756,#22757,#22758,#22759,#22760,#22761,#22762,#22763,
#22764,#22765,#22766,#22767,#22768,#22769,#22770,#22771,#22772,#22773,#22774,
#22775,#22776,#22777,#22778,#22779,#22780,#22781,#22782,#22783,#22784,#22785,
#22786,#22787,#22788,#22789,#22790,#22791,#22792,#22793,#22794,#22795,#22796,
#22797,#22798,#22799,#22800,#22801,#22802,#22803,#22804,#22805,#22806,#22807,
#22808,#22809,#22810,#22811,#22812,#22813,#22814,#22815,#22816,#22817,#22818,
#22819,#22820,#22821,#22822,#22823,#22824,#22825,#22826,#22827,#22828,#22829,
#22830,#22831,#22832,#22833,#22834,#22835,#22836,#22837,#22838,#22839,#22840,
#22841,#22842,#22843,#22844,#22845,#22846,#22847,#22848,#22849,#22850,#22851,
#22852,#22853,#22854,#22855,#22856,#22857,#22858,#22859,#22860,#22861,#22862,
#22863,#22864,#22865,#22866,#22867,#22868,#22869,#22870,#22871,#22872,#22873,
#22874,#22875,#22876,#22877,#22878,#22879,#22880,#22881,#22882,#22883,#22884,
#22885,#22886,#22887,#22888));
#26127=AXIS2_PLACEMENT_3D('',#52622,#31962,#31963);
#26128=AXIS2_PLACEMENT_3D('',#52623,#31964,#31965);
#26129=AXIS2_PLACEMENT_3D('',#52648,#31967,#31968);
#26130=AXIS2_PLACEMENT_3D('',#52653,#31969,#31970);
#26131=AXIS2_PLACEMENT_3D('',#52740,#31972,#31973);
#26132=AXIS2_PLACEMENT_3D('',#52830,#31975,#31976);
#26133=AXIS2_PLACEMENT_3D('',#52917,#31978,#31979);
#26134=AXIS2_PLACEMENT_3D('',#53004,#31981,#31982);
#26135=AXIS2_PLACEMENT_3D('',#53091,#31984,#31985);
#26136=AXIS2_PLACEMENT_3D('',#53178,#31987,#31988);
#26137=AXIS2_PLACEMENT_3D('',#53265,#31990,#31991);
#26138=AXIS2_PLACEMENT_3D('',#53337,#31993,#31994);
#26139=AXIS2_PLACEMENT_3D('',#53388,#31996,#31997);
#26140=AXIS2_PLACEMENT_3D('',#53436,#31999,#32000);
#26141=AXIS2_PLACEMENT_3D('',#53484,#32002,#32003);
#26142=AXIS2_PLACEMENT_3D('',#53535,#32005,#32006);
#26143=AXIS2_PLACEMENT_3D('',#53586,#32008,#32009);
#26144=AXIS2_PLACEMENT_3D('',#53634,#32011,#32012);
#26145=AXIS2_PLACEMENT_3D('',#53685,#32014,#32015);
#26146=AXIS2_PLACEMENT_3D('',#53736,#32017,#32018);
#26147=AXIS2_PLACEMENT_3D('',#53784,#32020,#32021);
#26148=AXIS2_PLACEMENT_3D('',#53832,#32023,#32024);
#26149=AXIS2_PLACEMENT_3D('',#53883,#32026,#32027);
#26150=AXIS2_PLACEMENT_3D('',#53934,#32029,#32030);
#26151=AXIS2_PLACEMENT_3D('',#53982,#32032,#32033);
#26152=AXIS2_PLACEMENT_3D('',#54033,#32035,#32036);
#26153=AXIS2_PLACEMENT_3D('',#54084,#32038,#32039);
#26154=AXIS2_PLACEMENT_3D('',#54132,#32041,#32042);
#26155=AXIS2_PLACEMENT_3D('',#54180,#32044,#32045);
#26156=AXIS2_PLACEMENT_3D('',#54231,#32047,#32048);
#26157=AXIS2_PLACEMENT_3D('',#54282,#32050,#32051);
#26158=AXIS2_PLACEMENT_3D('',#54330,#32053,#32054);
#26159=AXIS2_PLACEMENT_3D('',#54381,#32056,#32057);
#26160=AXIS2_PLACEMENT_3D('',#54432,#32059,#32060);
#26161=AXIS2_PLACEMENT_3D('',#54480,#32062,#32063);
#26162=AXIS2_PLACEMENT_3D('',#54528,#32065,#32066);
#26163=AXIS2_PLACEMENT_3D('',#54579,#32068,#32069);
#26164=AXIS2_PLACEMENT_3D('',#54630,#32071,#32072);
#26165=AXIS2_PLACEMENT_3D('',#54678,#32074,#32075);
#26166=AXIS2_PLACEMENT_3D('',#54729,#32077,#32078);
#26167=AXIS2_PLACEMENT_3D('',#54780,#32080,#32081);
#26168=AXIS2_PLACEMENT_3D('',#54828,#32083,#32084);
#26169=AXIS2_PLACEMENT_3D('',#54876,#32086,#32087);
#26170=AXIS2_PLACEMENT_3D('',#54927,#32089,#32090);
#26171=AXIS2_PLACEMENT_3D('',#54978,#32092,#32093);
#26172=AXIS2_PLACEMENT_3D('',#55026,#32095,#32096);
#26173=AXIS2_PLACEMENT_3D('',#55077,#32098,#32099);
#26174=AXIS2_PLACEMENT_3D('',#55128,#32101,#32102);
#26175=AXIS2_PLACEMENT_3D('',#55176,#32104,#32105);
#26176=AXIS2_PLACEMENT_3D('',#55224,#32107,#32108);
#26177=AXIS2_PLACEMENT_3D('',#55275,#32110,#32111);
#26178=AXIS2_PLACEMENT_3D('',#55326,#32113,#32114);
#26179=AXIS2_PLACEMENT_3D('',#55374,#32116,#32117);
#26180=AXIS2_PLACEMENT_3D('',#55425,#32119,#32120);
#26181=AXIS2_PLACEMENT_3D('',#55476,#32122,#32123);
#26182=AXIS2_PLACEMENT_3D('',#55524,#32125,#32126);
#26183=AXIS2_PLACEMENT_3D('',#55572,#32128,#32129);
#26184=AXIS2_PLACEMENT_3D('',#55623,#32131,#32132);
#26185=AXIS2_PLACEMENT_3D('',#55689,#32134,#32135);
#26186=AXIS2_PLACEMENT_3D('',#55779,#32137,#32138);
#26187=AXIS2_PLACEMENT_3D('',#55866,#32140,#32141);
#26188=AXIS2_PLACEMENT_3D('',#55953,#32143,#32144);
#26189=AXIS2_PLACEMENT_3D('',#56040,#32146,#32147);
#26190=AXIS2_PLACEMENT_3D('',#56127,#32149,#32150);
#26191=AXIS2_PLACEMENT_3D('',#56214,#32152,#32153);
#26192=AXIS2_PLACEMENT_3D('',#56304,#32155,#32156);
#26193=AXIS2_PLACEMENT_3D('',#56313,#32158,#32159);
#26194=AXIS2_PLACEMENT_3D('',#56314,#32160,#32161);
#26195=AXIS2_PLACEMENT_3D('',#56336,#32163,#32164);
#26196=AXIS2_PLACEMENT_3D('',#56350,#32165,#32166);
#26197=AXIS2_PLACEMENT_3D('',#56388,#32168,#32169);
#26198=AXIS2_PLACEMENT_3D('',#56424,#32171,#32172);
#26199=AXIS2_PLACEMENT_3D('',#56462,#32174,#32175);
#26200=AXIS2_PLACEMENT_3D('',#56498,#32177,#32178);
#26201=AXIS2_PLACEMENT_3D('',#56536,#32180,#32181);
#26202=AXIS2_PLACEMENT_3D('',#56573,#32183,#32184);
#26203=AXIS2_PLACEMENT_3D('',#56608,#32186,#32187);
#26204=AXIS2_PLACEMENT_3D('',#56635,#32189,#32190);
#26205=AXIS2_PLACEMENT_3D('',#56659,#32192,#32193);
#26206=AXIS2_PLACEMENT_3D('',#56683,#32195,#32196);
#26207=AXIS2_PLACEMENT_3D('',#56707,#32198,#32199);
#26208=AXIS2_PLACEMENT_3D('',#56733,#32201,#32202);
#26209=AXIS2_PLACEMENT_3D('',#56757,#32204,#32205);
#26210=AXIS2_PLACEMENT_3D('',#56781,#32207,#32208);
#26211=AXIS2_PLACEMENT_3D('',#56807,#32210,#32211);
#26212=AXIS2_PLACEMENT_3D('',#56831,#32213,#32214);
#26213=AXIS2_PLACEMENT_3D('',#56855,#32216,#32217);
#26214=AXIS2_PLACEMENT_3D('',#56879,#32219,#32220);
#26215=AXIS2_PLACEMENT_3D('',#56905,#32222,#32223);
#26216=AXIS2_PLACEMENT_3D('',#56929,#32225,#32226);
#26217=AXIS2_PLACEMENT_3D('',#56953,#32228,#32229);
#26218=AXIS2_PLACEMENT_3D('',#56979,#32231,#32232);
#26219=AXIS2_PLACEMENT_3D('',#57003,#32234,#32235);
#26220=AXIS2_PLACEMENT_3D('',#57027,#32237,#32238);
#26221=AXIS2_PLACEMENT_3D('',#57051,#32240,#32241);
#26222=AXIS2_PLACEMENT_3D('',#57077,#32243,#32244);
#26223=AXIS2_PLACEMENT_3D('',#57101,#32246,#32247);
#26224=AXIS2_PLACEMENT_3D('',#57125,#32249,#32250);
#26225=AXIS2_PLACEMENT_3D('',#57151,#32252,#32253);
#26226=AXIS2_PLACEMENT_3D('',#57175,#32255,#32256);
#26227=AXIS2_PLACEMENT_3D('',#57199,#32258,#32259);
#26228=AXIS2_PLACEMENT_3D('',#57223,#32261,#32262);
#26229=AXIS2_PLACEMENT_3D('',#57249,#32264,#32265);
#26230=AXIS2_PLACEMENT_3D('',#57273,#32267,#32268);
#26231=AXIS2_PLACEMENT_3D('',#57297,#32270,#32271);
#26232=AXIS2_PLACEMENT_3D('',#57323,#32273,#32274);
#26233=AXIS2_PLACEMENT_3D('',#57347,#32276,#32277);
#26234=AXIS2_PLACEMENT_3D('',#57371,#32279,#32280);
#26235=AXIS2_PLACEMENT_3D('',#57395,#32282,#32283);
#26236=AXIS2_PLACEMENT_3D('',#57421,#32285,#32286);
#26237=AXIS2_PLACEMENT_3D('',#57445,#32288,#32289);
#26238=AXIS2_PLACEMENT_3D('',#57469,#32291,#32292);
#26239=AXIS2_PLACEMENT_3D('',#57495,#32294,#32295);
#26240=AXIS2_PLACEMENT_3D('',#57519,#32297,#32298);
#26241=AXIS2_PLACEMENT_3D('',#57543,#32300,#32301);
#26242=AXIS2_PLACEMENT_3D('',#57567,#32303,#32304);
#26243=AXIS2_PLACEMENT_3D('',#57593,#32306,#32307);
#26244=AXIS2_PLACEMENT_3D('',#57617,#32309,#32310);
#26245=AXIS2_PLACEMENT_3D('',#57641,#32312,#32313);
#26246=AXIS2_PLACEMENT_3D('',#57667,#32315,#32316);
#26247=AXIS2_PLACEMENT_3D('',#57691,#32318,#32319);
#26248=AXIS2_PLACEMENT_3D('',#57715,#32321,#32322);
#26249=AXIS2_PLACEMENT_3D('',#57740,#32324,#32325);
#26250=AXIS2_PLACEMENT_3D('',#57767,#32327,#32328);
#26251=AXIS2_PLACEMENT_3D('',#57804,#32330,#32331);
#26252=AXIS2_PLACEMENT_3D('',#57840,#32333,#32334);
#26253=AXIS2_PLACEMENT_3D('',#57878,#32336,#32337);
#26254=AXIS2_PLACEMENT_3D('',#57914,#32339,#32340);
#26255=AXIS2_PLACEMENT_3D('',#57952,#32342,#32343);
#26256=AXIS2_PLACEMENT_3D('',#57989,#32345,#32346);
#26257=AXIS2_PLACEMENT_3D('',#58026,#32348,#32349);
#26258=AXIS2_PLACEMENT_3D('',#58028,#32350,#32351);
#26259=AXIS2_PLACEMENT_3D('',#58105,#32352,#32353);
#26260=AXIS2_PLACEMENT_3D('',#58106,#32354,#32355);
#26261=AXIS2_PLACEMENT_3D('',#58109,#32357,#32358);
#26262=AXIS2_PLACEMENT_3D('',#58110,#32359,#32360);
#26263=AXIS2_PLACEMENT_3D('',#60184,#32361,#32362);
#26264=AXIS2_PLACEMENT_3D('',#62239,#32363,#32364);
#26265=AXIS2_PLACEMENT_3D('',#62248,#32369,#32370);
#26266=AXIS2_PLACEMENT_3D('',#62250,#32371,#32372);
#26267=AXIS2_PLACEMENT_3D('',#62254,#32375,#32376);
#26268=AXIS2_PLACEMENT_3D('',#62258,#32379,#32380);
#26269=AXIS2_PLACEMENT_3D('',#62262,#32383,#32384);
#26270=AXIS2_PLACEMENT_3D('',#62263,#32385,#32386);
#26271=AXIS2_PLACEMENT_3D('',#62264,#32387,#32388);
#26272=AXIS2_PLACEMENT_3D('',#62266,#32389,#32390);
#26273=AXIS2_PLACEMENT_3D('',#62269,#32392,#32393);
#26274=AXIS2_PLACEMENT_3D('',#62270,#32394,#32395);
#26275=AXIS2_PLACEMENT_3D('',#62271,#32396,#32397);
#26276=AXIS2_PLACEMENT_3D('',#62273,#32398,#32399);
#26277=AXIS2_PLACEMENT_3D('',#62274,#32400,#32401);
#26278=AXIS2_PLACEMENT_3D('',#62275,#32402,#32403);
#26279=AXIS2_PLACEMENT_3D('',#62277,#32404,#32405);
#26280=AXIS2_PLACEMENT_3D('',#62279,#32407,#32408);
#26281=AXIS2_PLACEMENT_3D('',#62280,#32409,#32410);
#31962=DIRECTION('axis',(0.,0.,1.));
#31963=DIRECTION('refdir',(1.,0.,0.));
#31964=DIRECTION('center_axis',(1.,0.,0.));
#31965=DIRECTION('ref_axis',(0.,0.975560628713931,0.219730425074181));
#31966=DIRECTION('',(-1.,0.,0.));
#31967=DIRECTION('center_axis',(-1.,0.,0.));
#31968=DIRECTION('ref_axis',(0.,0.,-1.));
#31969=DIRECTION('center_axis',(1.,0.,0.));
#31970=DIRECTION('ref_axis',(0.,0.,-1.));
#31971=DIRECTION('',(-1.,0.,0.));
#31972=DIRECTION('center_axis',(1.,0.,0.));
#31973=DIRECTION('ref_axis',(0.,0.,-1.));
#31974=DIRECTION('',(-1.,0.,0.));
#31975=DIRECTION('center_axis',(1.,0.,0.));
#31976=DIRECTION('ref_axis',(0.,0.,-1.));
#31977=DIRECTION('',(-1.,0.,0.));
#31978=DIRECTION('center_axis',(1.,0.,0.));
#31979=DIRECTION('ref_axis',(0.,0.,-1.));
#31980=DIRECTION('',(-1.,0.,0.));
#31981=DIRECTION('center_axis',(1.,0.,0.));
#31982=DIRECTION('ref_axis',(0.,0.,-1.));
#31983=DIRECTION('',(-1.,0.,0.));
#31984=DIRECTION('center_axis',(1.,0.,0.));
#31985=DIRECTION('ref_axis',(0.,0.,-1.));
#31986=DIRECTION('',(-1.,0.,0.));
#31987=DIRECTION('center_axis',(1.,0.,0.));
#31988=DIRECTION('ref_axis',(0.,0.,-1.));
#31989=DIRECTION('',(-1.,0.,0.));
#31990=DIRECTION('center_axis',(1.,0.,0.));
#31991=DIRECTION('ref_axis',(0.,0.,-1.));
#31992=DIRECTION('',(-1.,0.,0.));
#31993=DIRECTION('center_axis',(1.,0.,0.));
#31994=DIRECTION('ref_axis',(0.,0.,-1.));
#31995=DIRECTION('',(-1.,0.,0.));
#31996=DIRECTION('center_axis',(1.,0.,0.));
#31997=DIRECTION('ref_axis',(0.,0.,-1.));
#31998=DIRECTION('',(-1.,0.,0.));
#31999=DIRECTION('center_axis',(1.,0.,0.));
#32000=DIRECTION('ref_axis',(0.,0.,-1.));
#32001=DIRECTION('',(-1.,0.,0.));
#32002=DIRECTION('center_axis',(1.,0.,0.));
#32003=DIRECTION('ref_axis',(0.,0.,-1.));
#32004=DIRECTION('',(-1.,0.,0.));
#32005=DIRECTION('center_axis',(1.,0.,0.));
#32006=DIRECTION('ref_axis',(0.,0.,-1.));
#32007=DIRECTION('',(-1.,0.,0.));
#32008=DIRECTION('center_axis',(1.,0.,0.));
#32009=DIRECTION('ref_axis',(0.,0.,-1.));
#32010=DIRECTION('',(-1.,0.,0.));
#32011=DIRECTION('center_axis',(1.,0.,0.));
#32012=DIRECTION('ref_axis',(0.,0.,-1.));
#32013=DIRECTION('',(-1.,0.,0.));
#32014=DIRECTION('center_axis',(1.,0.,0.));
#32015=DIRECTION('ref_axis',(0.,0.,-1.));
#32016=DIRECTION('',(-1.,0.,0.));
#32017=DIRECTION('center_axis',(1.,0.,0.));
#32018=DIRECTION('ref_axis',(0.,0.,-1.));
#32019=DIRECTION('',(-1.,0.,0.));
#32020=DIRECTION('center_axis',(1.,0.,0.));
#32021=DIRECTION('ref_axis',(0.,0.,-1.));
#32022=DIRECTION('',(-1.,0.,0.));
#32023=DIRECTION('center_axis',(1.,0.,0.));
#32024=DIRECTION('ref_axis',(0.,0.,-1.));
#32025=DIRECTION('',(-1.,0.,0.));
#32026=DIRECTION('center_axis',(1.,0.,0.));
#32027=DIRECTION('ref_axis',(0.,0.,-1.));
#32028=DIRECTION('',(-1.,0.,0.));
#32029=DIRECTION('center_axis',(1.,0.,0.));
#32030=DIRECTION('ref_axis',(0.,0.,-1.));
#32031=DIRECTION('',(-1.,0.,0.));
#32032=DIRECTION('center_axis',(1.,0.,0.));
#32033=DIRECTION('ref_axis',(0.,0.,-1.));
#32034=DIRECTION('',(-1.,0.,0.));
#32035=DIRECTION('center_axis',(1.,0.,0.));
#32036=DIRECTION('ref_axis',(0.,0.,-1.));
#32037=DIRECTION('',(-1.,0.,0.));
#32038=DIRECTION('center_axis',(1.,0.,0.));
#32039=DIRECTION('ref_axis',(0.,0.,-1.));
#32040=DIRECTION('',(-1.,0.,0.));
#32041=DIRECTION('center_axis',(1.,0.,0.));
#32042=DIRECTION('ref_axis',(0.,0.,-1.));
#32043=DIRECTION('',(-1.,0.,0.));
#32044=DIRECTION('center_axis',(1.,0.,0.));
#32045=DIRECTION('ref_axis',(0.,0.,-1.));
#32046=DIRECTION('',(-1.,0.,0.));
#32047=DIRECTION('center_axis',(1.,0.,0.));
#32048=DIRECTION('ref_axis',(0.,0.,-1.));
#32049=DIRECTION('',(-1.,0.,0.));
#32050=DIRECTION('center_axis',(1.,0.,0.));
#32051=DIRECTION('ref_axis',(0.,0.,-1.));
#32052=DIRECTION('',(-1.,0.,0.));
#32053=DIRECTION('center_axis',(1.,0.,0.));
#32054=DIRECTION('ref_axis',(0.,0.,-1.));
#32055=DIRECTION('',(-1.,0.,0.));
#32056=DIRECTION('center_axis',(1.,0.,0.));
#32057=DIRECTION('ref_axis',(0.,0.,-1.));
#32058=DIRECTION('',(-1.,0.,0.));
#32059=DIRECTION('center_axis',(1.,0.,0.));
#32060=DIRECTION('ref_axis',(0.,0.,-1.));
#32061=DIRECTION('',(-1.,0.,0.));
#32062=DIRECTION('center_axis',(1.,0.,0.));
#32063=DIRECTION('ref_axis',(0.,0.,-1.));
#32064=DIRECTION('',(-1.,0.,0.));
#32065=DIRECTION('center_axis',(1.,0.,0.));
#32066=DIRECTION('ref_axis',(0.,0.,-1.));
#32067=DIRECTION('',(-1.,0.,0.));
#32068=DIRECTION('center_axis',(1.,0.,0.));
#32069=DIRECTION('ref_axis',(0.,0.,-1.));
#32070=DIRECTION('',(-1.,0.,0.));
#32071=DIRECTION('center_axis',(1.,0.,0.));
#32072=DIRECTION('ref_axis',(0.,0.,-1.));
#32073=DIRECTION('',(-1.,0.,0.));
#32074=DIRECTION('center_axis',(1.,0.,0.));
#32075=DIRECTION('ref_axis',(0.,0.,-1.));
#32076=DIRECTION('',(-1.,0.,0.));
#32077=DIRECTION('center_axis',(1.,0.,0.));
#32078=DIRECTION('ref_axis',(0.,0.,-1.));
#32079=DIRECTION('',(-1.,0.,0.));
#32080=DIRECTION('center_axis',(1.,0.,0.));
#32081=DIRECTION('ref_axis',(0.,0.,-1.));
#32082=DIRECTION('',(-1.,0.,0.));
#32083=DIRECTION('center_axis',(1.,0.,0.));
#32084=DIRECTION('ref_axis',(0.,0.,-1.));
#32085=DIRECTION('',(-1.,0.,0.));
#32086=DIRECTION('center_axis',(1.,0.,0.));
#32087=DIRECTION('ref_axis',(0.,0.,-1.));
#32088=DIRECTION('',(-1.,0.,0.));
#32089=DIRECTION('center_axis',(1.,0.,0.));
#32090=DIRECTION('ref_axis',(0.,0.,-1.));
#32091=DIRECTION('',(-1.,0.,0.));
#32092=DIRECTION('center_axis',(1.,0.,0.));
#32093=DIRECTION('ref_axis',(0.,0.,-1.));
#32094=DIRECTION('',(-1.,0.,0.));
#32095=DIRECTION('center_axis',(1.,0.,0.));
#32096=DIRECTION('ref_axis',(0.,0.,-1.));
#32097=DIRECTION('',(-1.,0.,0.));
#32098=DIRECTION('center_axis',(1.,0.,0.));
#32099=DIRECTION('ref_axis',(0.,0.,-1.));
#32100=DIRECTION('',(-1.,0.,0.));
#32101=DIRECTION('center_axis',(1.,0.,0.));
#32102=DIRECTION('ref_axis',(0.,0.,-1.));
#32103=DIRECTION('',(-1.,0.,0.));
#32104=DIRECTION('center_axis',(1.,0.,0.));
#32105=DIRECTION('ref_axis',(0.,0.,-1.));
#32106=DIRECTION('',(-1.,0.,0.));
#32107=DIRECTION('center_axis',(1.,0.,0.));
#32108=DIRECTION('ref_axis',(0.,0.,-1.));
#32109=DIRECTION('',(-1.,0.,0.));
#32110=DIRECTION('center_axis',(1.,0.,0.));
#32111=DIRECTION('ref_axis',(0.,0.,-1.));
#32112=DIRECTION('',(-1.,0.,0.));
#32113=DIRECTION('center_axis',(1.,0.,0.));
#32114=DIRECTION('ref_axis',(0.,0.,-1.));
#32115=DIRECTION('',(-1.,0.,0.));
#32116=DIRECTION('center_axis',(1.,0.,0.));
#32117=DIRECTION('ref_axis',(0.,0.,-1.));
#32118=DIRECTION('',(-1.,0.,0.));
#32119=DIRECTION('center_axis',(1.,0.,0.));
#32120=DIRECTION('ref_axis',(0.,0.,-1.));
#32121=DIRECTION('',(-1.,0.,0.));
#32122=DIRECTION('center_axis',(1.,0.,0.));
#32123=DIRECTION('ref_axis',(0.,0.,-1.));
#32124=DIRECTION('',(-1.,0.,0.));
#32125=DIRECTION('center_axis',(1.,0.,0.));
#32126=DIRECTION('ref_axis',(0.,0.,-1.));
#32127=DIRECTION('',(-1.,0.,0.));
#32128=DIRECTION('center_axis',(1.,0.,0.));
#32129=DIRECTION('ref_axis',(0.,0.,-1.));
#32130=DIRECTION('',(-1.,0.,0.));
#32131=DIRECTION('center_axis',(1.,0.,0.));
#32132=DIRECTION('ref_axis',(0.,0.,-1.));
#32133=DIRECTION('',(-1.,0.,0.));
#32134=DIRECTION('center_axis',(1.,0.,0.));
#32135=DIRECTION('ref_axis',(0.,0.,-1.));
#32136=DIRECTION('',(-1.,0.,0.));
#32137=DIRECTION('center_axis',(1.,0.,0.));
#32138=DIRECTION('ref_axis',(0.,0.,-1.));
#32139=DIRECTION('',(-1.,0.,0.));
#32140=DIRECTION('center_axis',(1.,0.,0.));
#32141=DIRECTION('ref_axis',(0.,0.,-1.));
#32142=DIRECTION('',(-1.,0.,0.));
#32143=DIRECTION('center_axis',(1.,0.,0.));
#32144=DIRECTION('ref_axis',(0.,0.,-1.));
#32145=DIRECTION('',(-1.,0.,0.));
#32146=DIRECTION('center_axis',(1.,0.,0.));
#32147=DIRECTION('ref_axis',(0.,0.,-1.));
#32148=DIRECTION('',(-1.,0.,0.));
#32149=DIRECTION('center_axis',(1.,0.,0.));
#32150=DIRECTION('ref_axis',(0.,0.,-1.));
#32151=DIRECTION('',(-1.,0.,0.));
#32152=DIRECTION('center_axis',(1.,0.,0.));
#32153=DIRECTION('ref_axis',(0.,0.,-1.));
#32154=DIRECTION('',(-1.,0.,0.));
#32155=DIRECTION('center_axis',(1.,0.,0.));
#32156=DIRECTION('ref_axis',(0.,-1.17203152359781E-12,-1.));
#32157=DIRECTION('',(1.,0.,0.));
#32158=DIRECTION('center_axis',(1.,0.,0.));
#32159=DIRECTION('ref_axis',(0.,-1.17203152359781E-12,-1.));
#32160=DIRECTION('center_axis',(1.,0.,0.));
#32161=DIRECTION('ref_axis',(0.,-1.17203152359781E-12,-1.));
#32162=DIRECTION('',(1.,0.,0.));
#32163=DIRECTION('center_axis',(1.,0.,0.));
#32164=DIRECTION('ref_axis',(0.,-1.17203152359781E-12,-1.));
#32165=DIRECTION('center_axis',(1.,0.,0.));
#32166=DIRECTION('ref_axis',(0.,-1.17203152359781E-12,-1.));
#32167=DIRECTION('',(1.,0.,0.));
#32168=DIRECTION('center_axis',(1.,0.,0.));
#32169=DIRECTION('ref_axis',(0.,-1.17203152359781E-12,-1.));
#32170=DIRECTION('',(1.,0.,0.));
#32171=DIRECTION('center_axis',(1.,0.,0.));
#32172=DIRECTION('ref_axis',(0.,-1.17203152359781E-12,-1.));
#32173=DIRECTION('',(1.,0.,0.));
#32174=DIRECTION('center_axis',(1.,0.,0.));
#32175=DIRECTION('ref_axis',(0.,-1.17203152359781E-12,-1.));
#32176=DIRECTION('',(1.,0.,0.));
#32177=DIRECTION('center_axis',(1.,0.,0.));
#32178=DIRECTION('ref_axis',(0.,-1.17203152359781E-12,-1.));
#32179=DIRECTION('',(1.,0.,0.));
#32180=DIRECTION('center_axis',(1.,0.,0.));
#32181=DIRECTION('ref_axis',(0.,-1.17203152359781E-12,-1.));
#32182=DIRECTION('',(1.,0.,0.));
#32183=DIRECTION('center_axis',(1.,0.,0.));
#32184=DIRECTION('ref_axis',(0.,-1.17203152359781E-12,-1.));
#32185=DIRECTION('',(1.,0.,0.));
#32186=DIRECTION('center_axis',(1.,0.,0.));
#32187=DIRECTION('ref_axis',(0.,-1.17203152359781E-12,-1.));
#32188=DIRECTION('',(1.,0.,0.));
#32189=DIRECTION('center_axis',(1.,0.,0.));
#32190=DIRECTION('ref_axis',(0.,-1.17203152359781E-12,-1.));
#32191=DIRECTION('',(1.,0.,0.));
#32192=DIRECTION('center_axis',(1.,0.,0.));
#32193=DIRECTION('ref_axis',(0.,-1.17203152359781E-12,-1.));
#32194=DIRECTION('',(1.,0.,0.));
#32195=DIRECTION('center_axis',(1.,0.,0.));
#32196=DIRECTION('ref_axis',(0.,-1.17203152359781E-12,-1.));
#32197=DIRECTION('',(1.,0.,0.));
#32198=DIRECTION('center_axis',(1.,0.,0.));
#32199=DIRECTION('ref_axis',(0.,-1.17203152359781E-12,-1.));
#32200=DIRECTION('',(1.,0.,0.));
#32201=DIRECTION('center_axis',(1.,0.,0.));
#32202=DIRECTION('ref_axis',(0.,-1.17203152359781E-12,-1.));
#32203=DIRECTION('',(1.,0.,0.));
#32204=DIRECTION('center_axis',(1.,0.,0.));
#32205=DIRECTION('ref_axis',(0.,-1.17203152359781E-12,-1.));
#32206=DIRECTION('',(1.,0.,0.));
#32207=DIRECTION('center_axis',(1.,0.,0.));
#32208=DIRECTION('ref_axis',(0.,-1.17203152359781E-12,-1.));
#32209=DIRECTION('',(1.,0.,0.));
#32210=DIRECTION('center_axis',(1.,0.,0.));
#32211=DIRECTION('ref_axis',(0.,-1.17203152359781E-12,-1.));
#32212=DIRECTION('',(1.,0.,0.));
#32213=DIRECTION('center_axis',(1.,0.,0.));
#32214=DIRECTION('ref_axis',(0.,-1.17203152359781E-12,-1.));
#32215=DIRECTION('',(1.,0.,0.));
#32216=DIRECTION('center_axis',(1.,0.,0.));
#32217=DIRECTION('ref_axis',(0.,-1.17203152359781E-12,-1.));
#32218=DIRECTION('',(1.,0.,0.));
#32219=DIRECTION('center_axis',(1.,0.,0.));
#32220=DIRECTION('ref_axis',(0.,-1.17203152359781E-12,-1.));
#32221=DIRECTION('',(1.,0.,0.));
#32222=DIRECTION('center_axis',(1.,0.,0.));
#32223=DIRECTION('ref_axis',(0.,-1.17203152359781E-12,-1.));
#32224=DIRECTION('',(1.,0.,0.));
#32225=DIRECTION('center_axis',(1.,0.,0.));
#32226=DIRECTION('ref_axis',(0.,-1.17203152359781E-12,-1.));
#32227=DIRECTION('',(1.,0.,0.));
#32228=DIRECTION('center_axis',(1.,0.,0.));
#32229=DIRECTION('ref_axis',(0.,-1.17203152359781E-12,-1.));
#32230=DIRECTION('',(1.,0.,0.));
#32231=DIRECTION('center_axis',(1.,0.,0.));
#32232=DIRECTION('ref_axis',(0.,-1.17203152359781E-12,-1.));
#32233=DIRECTION('',(1.,0.,0.));
#32234=DIRECTION('center_axis',(1.,0.,0.));
#32235=DIRECTION('ref_axis',(0.,-1.17203152359781E-12,-1.));
#32236=DIRECTION('',(1.,0.,0.));
#32237=DIRECTION('center_axis',(1.,0.,0.));
#32238=DIRECTION('ref_axis',(0.,-1.17203152359781E-12,-1.));
#32239=DIRECTION('',(1.,0.,0.));
#32240=DIRECTION('center_axis',(1.,0.,0.));
#32241=DIRECTION('ref_axis',(0.,-1.17203152359781E-12,-1.));
#32242=DIRECTION('',(1.,0.,0.));
#32243=DIRECTION('center_axis',(1.,0.,0.));
#32244=DIRECTION('ref_axis',(0.,-1.17203152359781E-12,-1.));
#32245=DIRECTION('',(1.,0.,0.));
#32246=DIRECTION('center_axis',(1.,0.,0.));
#32247=DIRECTION('ref_axis',(0.,-1.17203152359781E-12,-1.));
#32248=DIRECTION('',(1.,0.,0.));
#32249=DIRECTION('center_axis',(1.,0.,0.));
#32250=DIRECTION('ref_axis',(0.,-1.17203152359781E-12,-1.));
#32251=DIRECTION('',(1.,0.,0.));
#32252=DIRECTION('center_axis',(1.,0.,0.));
#32253=DIRECTION('ref_axis',(0.,-1.17203152359781E-12,-1.));
#32254=DIRECTION('',(1.,0.,0.));
#32255=DIRECTION('center_axis',(1.,0.,0.));
#32256=DIRECTION('ref_axis',(0.,-1.17203152359781E-12,-1.));
#32257=DIRECTION('',(1.,0.,0.));
#32258=DIRECTION('center_axis',(1.,0.,0.));
#32259=DIRECTION('ref_axis',(0.,-1.17203152359781E-12,-1.));
#32260=DIRECTION('',(1.,0.,0.));
#32261=DIRECTION('center_axis',(1.,0.,0.));
#32262=DIRECTION('ref_axis',(0.,-1.17203152359781E-12,-1.));
#32263=DIRECTION('',(1.,0.,0.));
#32264=DIRECTION('center_axis',(1.,0.,0.));
#32265=DIRECTION('ref_axis',(0.,-1.17203152359781E-12,-1.));
#32266=DIRECTION('',(1.,0.,0.));
#32267=DIRECTION('center_axis',(1.,0.,0.));
#32268=DIRECTION('ref_axis',(0.,-1.17203152359781E-12,-1.));
#32269=DIRECTION('',(1.,0.,0.));
#32270=DIRECTION('center_axis',(1.,0.,0.));
#32271=DIRECTION('ref_axis',(0.,-1.17203152359781E-12,-1.));
#32272=DIRECTION('',(1.,0.,0.));
#32273=DIRECTION('center_axis',(1.,0.,0.));
#32274=DIRECTION('ref_axis',(0.,-1.17203152359781E-12,-1.));
#32275=DIRECTION('',(1.,0.,0.));
#32276=DIRECTION('center_axis',(1.,0.,0.));
#32277=DIRECTION('ref_axis',(0.,-1.17203152359781E-12,-1.));
#32278=DIRECTION('',(1.,0.,0.));
#32279=DIRECTION('center_axis',(1.,0.,0.));
#32280=DIRECTION('ref_axis',(0.,-1.17203152359781E-12,-1.));
#32281=DIRECTION('',(1.,0.,0.));
#32282=DIRECTION('center_axis',(1.,0.,0.));
#32283=DIRECTION('ref_axis',(0.,-1.17203152359781E-12,-1.));
#32284=DIRECTION('',(1.,0.,0.));
#32285=DIRECTION('center_axis',(1.,0.,0.));
#32286=DIRECTION('ref_axis',(0.,-1.17203152359781E-12,-1.));
#32287=DIRECTION('',(1.,0.,0.));
#32288=DIRECTION('center_axis',(1.,0.,0.));
#32289=DIRECTION('ref_axis',(0.,-1.17203152359781E-12,-1.));
#32290=DIRECTION('',(1.,0.,0.));
#32291=DIRECTION('center_axis',(1.,0.,0.));
#32292=DIRECTION('ref_axis',(0.,-1.17203152359781E-12,-1.));
#32293=DIRECTION('',(1.,0.,0.));
#32294=DIRECTION('center_axis',(1.,0.,0.));
#32295=DIRECTION('ref_axis',(0.,-1.17203152359781E-12,-1.));
#32296=DIRECTION('',(1.,0.,0.));
#32297=DIRECTION('center_axis',(1.,0.,0.));
#32298=DIRECTION('ref_axis',(0.,-1.17203152359781E-12,-1.));
#32299=DIRECTION('',(1.,0.,0.));
#32300=DIRECTION('center_axis',(1.,0.,0.));
#32301=DIRECTION('ref_axis',(0.,-1.17203152359781E-12,-1.));
#32302=DIRECTION('',(1.,0.,0.));
#32303=DIRECTION('center_axis',(1.,0.,0.));
#32304=DIRECTION('ref_axis',(0.,-1.17203152359781E-12,-1.));
#32305=DIRECTION('',(1.,0.,0.));
#32306=DIRECTION('center_axis',(1.,0.,0.));
#32307=DIRECTION('ref_axis',(0.,-1.17203152359781E-12,-1.));
#32308=DIRECTION('',(1.,0.,0.));
#32309=DIRECTION('center_axis',(1.,0.,0.));
#32310=DIRECTION('ref_axis',(0.,-1.17203152359781E-12,-1.));
#32311=DIRECTION('',(1.,0.,0.));
#32312=DIRECTION('center_axis',(1.,0.,0.));
#32313=DIRECTION('ref_axis',(0.,-1.17203152359781E-12,-1.));
#32314=DIRECTION('',(1.,0.,0.));
#32315=DIRECTION('center_axis',(1.,0.,0.));
#32316=DIRECTION('ref_axis',(0.,-1.17203152359781E-12,-1.));
#32317=DIRECTION('',(1.,0.,0.));
#32318=DIRECTION('center_axis',(1.,0.,0.));
#32319=DIRECTION('ref_axis',(0.,-1.17203152359781E-12,-1.));
#32320=DIRECTION('',(1.,0.,0.));
#32321=DIRECTION('center_axis',(1.,0.,0.));
#32322=DIRECTION('ref_axis',(0.,-1.17203152359781E-12,-1.));
#32323=DIRECTION('',(1.,0.,0.));
#32324=DIRECTION('center_axis',(1.,0.,0.));
#32325=DIRECTION('ref_axis',(0.,-1.17203152359781E-12,-1.));
#32326=DIRECTION('',(1.,0.,0.));
#32327=DIRECTION('center_axis',(1.,0.,0.));
#32328=DIRECTION('ref_axis',(0.,-1.17203152359781E-12,-1.));
#32329=DIRECTION('',(1.,0.,0.));
#32330=DIRECTION('center_axis',(1.,0.,0.));
#32331=DIRECTION('ref_axis',(0.,-1.17203152359781E-12,-1.));
#32332=DIRECTION('',(1.,0.,0.));
#32333=DIRECTION('center_axis',(1.,0.,0.));
#32334=DIRECTION('ref_axis',(0.,-1.17203152359781E-12,-1.));
#32335=DIRECTION('',(1.,0.,0.));
#32336=DIRECTION('center_axis',(1.,0.,0.));
#32337=DIRECTION('ref_axis',(0.,-1.17203152359781E-12,-1.));
#32338=DIRECTION('',(1.,0.,0.));
#32339=DIRECTION('center_axis',(1.,0.,0.));
#32340=DIRECTION('ref_axis',(0.,-1.17203152359781E-12,-1.));
#32341=DIRECTION('',(1.,0.,0.));
#32342=DIRECTION('center_axis',(1.,0.,0.));
#32343=DIRECTION('ref_axis',(0.,-1.17203152359781E-12,-1.));
#32344=DIRECTION('',(1.,0.,0.));
#32345=DIRECTION('center_axis',(1.,0.,0.));
#32346=DIRECTION('ref_axis',(0.,-1.17203152359781E-12,-1.));
#32347=DIRECTION('',(1.,0.,0.));
#32348=DIRECTION('center_axis',(1.,0.,0.));
#32349=DIRECTION('ref_axis',(0.,0.,-1.));
#32350=DIRECTION('center_axis',(1.,0.,0.));
#32351=DIRECTION('ref_axis',(0.,0.,-1.));
#32352=DIRECTION('center_axis',(-1.,0.,0.));
#32353=DIRECTION('ref_axis',(0.,-1.17203152359781E-12,-1.));
#32354=DIRECTION('center_axis',(1.,0.,0.));
#32355=DIRECTION('ref_axis',(0.,0.,-1.));
#32356=DIRECTION('',(-1.,0.,0.));
#32357=DIRECTION('center_axis',(1.,0.,0.));
#32358=DIRECTION('ref_axis',(0.,0.,-1.));
#32359=DIRECTION('center_axis',(1.,0.,0.));
#32360=DIRECTION('ref_axis',(0.,0.,-1.));
#32361=DIRECTION('center_axis',(1.,0.,0.));
#32362=DIRECTION('ref_axis',(0.,-1.17203152359781E-12,-1.));
#32363=DIRECTION('center_axis',(0.,1.,0.));
#32364=DIRECTION('ref_axis',(0.,0.,1.));
#32365=DIRECTION('',(-1.,0.,0.));
#32366=DIRECTION('',(0.,0.,1.));
#32367=DIRECTION('',(1.,0.,0.));
#32368=DIRECTION('',(0.,0.,1.));
#32369=DIRECTION('center_axis',(1.,0.,0.));
#32370=DIRECTION('ref_axis',(0.,0.,-1.));
#32371=DIRECTION('center_axis',(-1.,0.,0.));
#32372=DIRECTION('ref_axis',(0.,0.,-1.));
#32373=DIRECTION('',(0.,-1.,0.));
#32374=DIRECTION('',(0.,0.,-1.));
#32375=DIRECTION('center_axis',(0.,0.,1.));
#32376=DIRECTION('ref_axis',(0.,-1.,0.));
#32377=DIRECTION('',(0.,-1.,0.));
#32378=DIRECTION('',(1.,0.,0.));
#32379=DIRECTION('center_axis',(0.,-1.,0.));
#32380=DIRECTION('ref_axis',(0.,0.,-1.));
#32381=DIRECTION('',(1.,0.,0.));
#32382=DIRECTION('',(0.,0.,-1.));
#32383=DIRECTION('center_axis',(1.,0.,0.));
#32384=DIRECTION('ref_axis',(0.,0.,-1.));
#32385=DIRECTION('center_axis',(1.,0.,0.));
#32386=DIRECTION('ref_axis',(0.,0.,-1.));
#32387=DIRECTION('center_axis',(1.,0.,0.));
#32388=DIRECTION('ref_axis',(0.,0.,-1.));
#32389=DIRECTION('center_axis',(1.,0.,0.));
#32390=DIRECTION('ref_axis',(0.,0.,-1.));
#32391=DIRECTION('',(-1.,0.,0.));
#32392=DIRECTION('center_axis',(-1.,0.,0.));
#32393=DIRECTION('ref_axis',(0.,0.,-1.));
#32394=DIRECTION('center_axis',(1.,0.,0.));
#32395=DIRECTION('ref_axis',(0.,0.,-1.));
#32396=DIRECTION('center_axis',(1.,0.,0.));
#32397=DIRECTION('ref_axis',(0.,0.,-1.));
#32398=DIRECTION('center_axis',(1.,0.,0.));
#32399=DIRECTION('ref_axis',(0.,0.,-1.));
#32400=DIRECTION('center_axis',(-1.,0.,0.));
#32401=DIRECTION('ref_axis',(0.,0.,-1.));
#32402=DIRECTION('center_axis',(1.,0.,0.));
#32403=DIRECTION('ref_axis',(0.,0.,-1.));
#32404=DIRECTION('center_axis',(1.,0.,0.));
#32405=DIRECTION('ref_axis',(0.,0.,-1.));
#32406=DIRECTION('',(-1.,0.,0.));
#32407=DIRECTION('center_axis',(1.,0.,0.));
#32408=DIRECTION('ref_axis',(0.,0.,-1.));
#32409=DIRECTION('center_axis',(1.,0.,0.));
#32410=DIRECTION('ref_axis',(0.,0.,-1.));
#52622=CARTESIAN_POINT('',(0.,0.,0.));
#52623=CARTESIAN_POINT('Origin',(4.,0.,4.));
#52624=CARTESIAN_POINT('',(4.12884541125756,8.40637486662632E-6,4.59405635738975));
#52625=CARTESIAN_POINT('',(4.02115458874249,-9.26662433349265E-6,4.59413599269206));
#52626=CARTESIAN_POINT('',(4.,-7.27562663373442E-17,4.5941));
#52627=CARTESIAN_POINT('',(4.,0.254721014554615,3.46322028700965));
#52628=CARTESIAN_POINT('Ctrl Pts',(4.12884541125756,8.40637486662632E-6,
4.59405635738975));
#52629=CARTESIAN_POINT('Ctrl Pts',(4.12564700130467,0.0398130654959074,
4.59407663624518));
#52630=CARTESIAN_POINT('Ctrl Pts',(4.12244859135178,0.079613792300143,4.59013569217808));
#52631=CARTESIAN_POINT('Ctrl Pts',(4.11925018139889,0.118599576779877,4.58219388355888));
#52632=CARTESIAN_POINT('Ctrl Pts',(4.11129754205509,0.215535206692688,4.56244709042845));
#52633=CARTESIAN_POINT('Ctrl Pts',(4.10334490271129,0.30743256945264,4.51796551073728));
#52634=CARTESIAN_POINT('Ctrl Pts',(4.09539226336748,0.383054411795556,4.45418672179759));
#52635=CARTESIAN_POINT('Ctrl Pts',(4.08743962402367,0.458676254138472,4.3904079328579));
#52636=CARTESIAN_POINT('Ctrl Pts',(4.07948698467986,0.518022576064352,4.30733193466969));
#52637=CARTESIAN_POINT('Ctrl Pts',(4.07153434533606,0.553840407547632,4.21511760274296));
#52638=CARTESIAN_POINT('Ctrl Pts',(4.06358170599225,0.589658239030912,4.12290327081622));
#52639=CARTESIAN_POINT('Ctrl Pts',(4.05562906664845,0.601947580071592,4.02155060515096));
#52640=CARTESIAN_POINT('Ctrl Pts',(4.04767642730464,0.589200356533535,3.92344812692479));
#52641=CARTESIAN_POINT('Ctrl Pts',(4.03972378796084,0.576453132995478,3.82534564869861));
#52642=CARTESIAN_POINT('Ctrl Pts',(4.03177114861703,0.538669344878685,3.73049335791153));
#52643=CARTESIAN_POINT('Ctrl Pts',(4.02381850927322,0.480479105222089,3.65049437695417));
#52644=CARTESIAN_POINT('Ctrl Pts',(4.01587900618215,0.422384984811151,3.57062753914914));
#52645=CARTESIAN_POINT('Ctrl Pts',(4.00793950309107,0.343951772361455,3.50556498199611));
#52646=CARTESIAN_POINT('Ctrl Pts',(4.,0.254721014554615,3.46322028700965));
#52647=CARTESIAN_POINT('',(4.,0.254694598474614,4.53673594206822));
#52648=CARTESIAN_POINT('Origin',(4.,0.,4.));
#52649=CARTESIAN_POINT('Ctrl Pts',(3.99999999999998,0.254694598474614,4.53673594206822));
#52650=CARTESIAN_POINT('Ctrl Pts',(4.00705152958082,0.175425736340139,4.5743509952638));
#52651=CARTESIAN_POINT('Ctrl Pts',(4.01410305916165,0.0876996967667308,
4.59405101338575));
#52652=CARTESIAN_POINT('Ctrl Pts',(4.02115458874249,-9.26662433349265E-6,
4.59413599269206));
#52653=CARTESIAN_POINT('Origin',(4.,0.,4.));
#52654=CARTESIAN_POINT('',(4.42884541125756,-2.46302091461148E-6,4.59415045696459));
#52655=CARTESIAN_POINT('',(4.32115458874249,3.58587963140688E-6,4.59404994535016));
#52656=CARTESIAN_POINT('',(4.,-7.27562663373442E-17,4.5941));
#52657=CARTESIAN_POINT('Ctrl Pts',(4.42884541125756,-2.46302091461148E-6,
4.59415045696459));
#52658=CARTESIAN_POINT('Ctrl Pts',(4.42107867343035,0.0966117732708647,
4.59412799973471));
#52659=CARTESIAN_POINT('Ctrl Pts',(4.41331193560314,0.193236775309615,4.57009608476161));
#52660=CARTESIAN_POINT('Ctrl Pts',(4.40554519777592,0.278573173318151,4.52479781884576));
#52661=CARTESIAN_POINT('Ctrl Pts',(4.39759255843212,0.36595214906825,4.47841531183407));
#52662=CARTESIAN_POINT('Ctrl Pts',(4.38963991908831,0.441495654419193,4.40973622444741));
#52663=CARTESIAN_POINT('Ctrl Pts',(4.3816872797445,0.495967466205845,4.32715751007026));
#52664=CARTESIAN_POINT('Ctrl Pts',(4.3737346404007,0.550439277992498,4.24457879569311));
#52665=CARTESIAN_POINT('Ctrl Pts',(4.36578200105689,0.58383939621486,4.14810045432546));
#52666=CARTESIAN_POINT('Ctrl Pts',(4.35782936171309,0.59208420294366,4.04951827803692));
#52667=CARTESIAN_POINT('Ctrl Pts',(4.34987672236928,0.600329009672459,3.95093610174838));
#52668=CARTESIAN_POINT('Ctrl Pts',(4.34192408302547,0.583418504907695,3.85025009053894));
#52669=CARTESIAN_POINT('Ctrl Pts',(4.33397144368167,0.54342022548472,3.75977047903001));
#52670=CARTESIAN_POINT('Ctrl Pts',(4.32601880433786,0.503421946061746,3.66929086752108));
#52671=CARTESIAN_POINT('Ctrl Pts',(4.31806616499406,0.440335891980562,3.58901765571266));
#52672=CARTESIAN_POINT('Ctrl Pts',(4.31011352565025,0.361875197644003,3.52876534000234));
#52673=CARTESIAN_POINT('Ctrl Pts',(4.30216088630644,0.283414503307443,3.46851302429202));
#52674=CARTESIAN_POINT('Ctrl Pts',(4.29420824696263,0.189579168715509,3.4282816046798));
#52675=CARTESIAN_POINT('Ctrl Pts',(4.28625560761883,0.0918418319479975,
3.41298991457491));
#52676=CARTESIAN_POINT('Ctrl Pts',(4.27830296827502,-0.00589550481951406,
3.39769822447003));
#52677=CARTESIAN_POINT('Ctrl Pts',(4.27035032893122,-0.107534843762603,
3.4073462638725));
#52678=CARTESIAN_POINT('Ctrl Pts',(4.26239768958741,-0.200649373295791,
3.44075443909651));
#52679=CARTESIAN_POINT('Ctrl Pts',(4.25444505024361,-0.293763902828979,
3.47416261432052));
#52680=CARTESIAN_POINT('Ctrl Pts',(4.24649241089979,-0.378353622952266,
3.53133092536608));
#52681=CARTESIAN_POINT('Ctrl Pts',(4.23853977155599,-0.444076322467606,
3.60526974769923));
#52682=CARTESIAN_POINT('Ctrl Pts',(4.23058713221218,-0.509799021982947,
3.67920857003239));
#52683=CARTESIAN_POINT('Ctrl Pts',(4.22263449286838,-0.556654700890342,
3.76991790365313));
#52684=CARTESIAN_POINT('Ctrl Pts',(4.21468185352458,-0.578914549750806,
3.86630733464992));
#52685=CARTESIAN_POINT('Ctrl Pts',(4.20672921418077,-0.601174398611269,
3.96269676564671));
#52686=CARTESIAN_POINT('Ctrl Pts',(4.19877657483696,-0.598838417424802,
4.06476629401955));
#52687=CARTESIAN_POINT('Ctrl Pts',(4.19082393549315,-0.5721923335546,4.16003645884502));
#52688=CARTESIAN_POINT('Ctrl Pts',(4.18287129614934,-0.545546249684398,
4.25530662367048));
#52689=CARTESIAN_POINT('Ctrl Pts',(4.17491865680554,-0.494590063130461,
4.34377742494856));
#52690=CARTESIAN_POINT('Ctrl Pts',(4.16696601746173,-0.425553631634784,
4.41463223618795));
#52691=CARTESIAN_POINT('Ctrl Pts',(4.15901337811793,-0.356517200139107,
4.48548704742733));
#52692=CARTESIAN_POINT('Ctrl Pts',(4.15106073877413,-0.269400523701689,
4.53872586862801));
#52693=CARTESIAN_POINT('Ctrl Pts',(4.14310809943032,-0.174855236950146,
4.56783927594351));
#52694=CARTESIAN_POINT('Ctrl Pts',(4.1383538700394,-0.118334381217266,4.5852437891806));
#52695=CARTESIAN_POINT('Ctrl Pts',(4.13359964064848,-0.0591586432141876,
4.59402621418361));
#52696=CARTESIAN_POINT('Ctrl Pts',(4.12884541125756,8.40637486662632E-6,
4.59405635738975));
#52697=CARTESIAN_POINT('Ctrl Pts',(4.02115458874249,-9.26662433349265E-6,
4.59413599269206));
#52698=CARTESIAN_POINT('Ctrl Pts',(4.02205569850546,-0.0112175303500608,
4.59414685213492));
#52699=CARTESIAN_POINT('Ctrl Pts',(4.02295680826843,-0.0224255152200988,
4.5938373961197));
#52700=CARTESIAN_POINT('Ctrl Pts',(4.0238579180314,-0.0336155370699344,
4.59320407706013));
#52701=CARTESIAN_POINT('Ctrl Pts',(4.03181055737521,-0.132371772633995,
4.58761479340425));
#52702=CARTESIAN_POINT('Ctrl Pts',(4.03976319671902,-0.229728915328813,
4.55680066053817));
#52703=CARTESIAN_POINT('Ctrl Pts',(4.04771583606282,-0.31374319278985,4.50455967689729));
#52704=CARTESIAN_POINT('Ctrl Pts',(4.05566847540663,-0.397757470250888,
4.4523186932564));
#52705=CARTESIAN_POINT('Ctrl Pts',(4.06362111475043,-0.468428882478145,
4.37865085884071));
#52706=CARTESIAN_POINT('Ctrl Pts',(4.07157375409424,-0.517135915630147,
4.29254879227412));
#52707=CARTESIAN_POINT('Ctrl Pts',(4.07952639343804,-0.565842948782149,
4.20644672570752));
#52708=CARTESIAN_POINT('Ctrl Pts',(4.08747903278185,-0.592585602858896,
4.10791042699003));
#52709=CARTESIAN_POINT('Ctrl Pts',(4.09543167212566,-0.594084460855775,
4.00899459728238));
#52710=CARTESIAN_POINT('Ctrl Pts',(4.10338431146947,-0.595583318852653,
3.91007876757474));
#52711=CARTESIAN_POINT('Ctrl Pts',(4.11133695081327,-0.571838380769662,
3.81078340687695));
#52712=CARTESIAN_POINT('Ctrl Pts',(4.11928959015708,-0.525757920758293,
3.72324489380985));
#52713=CARTESIAN_POINT('Ctrl Pts',(4.12724222950088,-0.479677460746923,
3.63570638074275));
#52714=CARTESIAN_POINT('Ctrl Pts',(4.13519486884469,-0.411261478807175,
3.55992471530633));
#52715=CARTESIAN_POINT('Ctrl Pts',(4.1431475081885,-0.328872047298013,3.50516726345229));
#52716=CARTESIAN_POINT('Ctrl Pts',(4.1511001475323,-0.246482615788851,3.45040981159825));
#52717=CARTESIAN_POINT('Ctrl Pts',(4.15905278687611,-0.150119734710276,
3.41667657332659));
#52718=CARTESIAN_POINT('Ctrl Pts',(4.16700542621992,-0.0515665150750243,
3.40809082437526));
#52719=CARTESIAN_POINT('Ctrl Pts',(4.17495806556372,0.0469867045602276,
3.39950507542393));
#52720=CARTESIAN_POINT('Ctrl Pts',(4.18291070490753,0.147730262752155,3.41606681579293));
#52721=CARTESIAN_POINT('Ctrl Pts',(4.19086334425134,0.238347648045887,3.45575171487277));
#52722=CARTESIAN_POINT('Ctrl Pts',(4.19881598359514,0.32896503333962,3.49543661395261));
#52723=CARTESIAN_POINT('Ctrl Pts',(4.20676862293895,0.409456245735157,3.55824467174328));
#52724=CARTESIAN_POINT('Ctrl Pts',(4.21472126228276,0.469979735422806,3.63649644709345));
#52725=CARTESIAN_POINT('Ctrl Pts',(4.22267390162656,0.530503225110456,3.71474822244363));
#52726=CARTESIAN_POINT('Ctrl Pts',(4.23062654097037,0.571058992090217,3.80844371535332));
#52727=CARTESIAN_POINT('Ctrl Pts',(4.23857918031417,0.586688754827568,3.90612753493601));
#52728=CARTESIAN_POINT('Ctrl Pts',(4.24653181965798,0.602318517564919,4.0038113545187));
#52729=CARTESIAN_POINT('Ctrl Pts',(4.25448445900178,0.593022276059861,4.10548350077438));
#52730=CARTESIAN_POINT('Ctrl Pts',(4.26243709834559,0.559936509464549,4.19871308474845));
#52731=CARTESIAN_POINT('Ctrl Pts',(4.2703897376894,0.526850742869238,4.29194266872251));
#52732=CARTESIAN_POINT('Ctrl Pts',(4.27834237703321,0.469975451183674,4.37672969041494));
#52733=CARTESIAN_POINT('Ctrl Pts',(4.28629501637701,0.396264473279151,4.44270782630825));
#52734=CARTESIAN_POINT('Ctrl Pts',(4.29424765572082,0.322553495374627,4.50868596220156));
#52735=CARTESIAN_POINT('Ctrl Pts',(4.30220029506462,0.232006831251144,4.55585521229574));
#52736=CARTESIAN_POINT('Ctrl Pts',(4.31015293440843,0.135695012128791,4.57844846968215));
#52737=CARTESIAN_POINT('Ctrl Pts',(4.31382015251978,0.0912825306677821,
4.58886694826517));
#52738=CARTESIAN_POINT('Ctrl Pts',(4.31748737063114,0.0456441298716245,
4.59405951624442));
#52739=CARTESIAN_POINT('Ctrl Pts',(4.32115458874249,3.58587963140688E-6,
4.59404994535016));
#52740=CARTESIAN_POINT('Origin',(4.,0.,4.));
#52741=CARTESIAN_POINT('',(4.72884541125756,-4.67700812217808E-6,4.59405084457266));
#52742=CARTESIAN_POINT('',(4.62115458874249,3.7232086238465E-6,4.59414939806979));
#52743=CARTESIAN_POINT('',(4.,-7.27562663373442E-17,4.5941));
#52744=CARTESIAN_POINT('Ctrl Pts',(4.72884541125756,-4.67700812217808E-6,
4.59405084457266));
#52745=CARTESIAN_POINT('Ctrl Pts',(4.72446298489983,0.0545367878429411,
4.59403588702548));
#52746=CARTESIAN_POINT('Ctrl Pts',(4.7200805585421,0.10908225468116,4.58659074407712));
#52747=CARTESIAN_POINT('Ctrl Pts',(4.71569813218437,0.16154350694756,4.57176871113812));
#52748=CARTESIAN_POINT('Ctrl Pts',(4.70774549284056,0.256743148594298,4.54487167450041));
#52749=CARTESIAN_POINT('Ctrl Pts',(4.69979285349676,0.345079446524661,4.4936824501733));
#52750=CARTESIAN_POINT('Ctrl Pts',(4.69184021415295,0.415752085200636,4.42445961801412));
#52751=CARTESIAN_POINT('Ctrl Pts',(4.68388757480915,0.486424723876611,4.35523678585494));
#52752=CARTESIAN_POINT('Ctrl Pts',(4.67593493546534,0.539433703298198,4.26798034586369));
#52753=CARTESIAN_POINT('Ctrl Pts',(4.66798229612153,0.568297953762936,4.17335858623793));
#52754=CARTESIAN_POINT('Ctrl Pts',(4.66002965677773,0.597162204227674,4.07873682661218));
#52755=CARTESIAN_POINT('Ctrl Pts',(4.65207701743392,0.601881725735563,3.97674974735193));
#52756=CARTESIAN_POINT('Ctrl Pts',(4.64412437809011,0.581879492504365,3.87986665793328));
#52757=CARTESIAN_POINT('Ctrl Pts',(4.63617173874631,0.561877259273167,3.78298356851463));
#52758=CARTESIAN_POINT('Ctrl Pts',(4.6282190994025,0.517153271302883,3.69120446893757));
#52759=CARTESIAN_POINT('Ctrl Pts',(4.6202664600587,0.453175645250056,3.61575060413089));
#52760=CARTESIAN_POINT('Ctrl Pts',(4.61231382071489,0.389198019197228,3.5402967393242));
#52761=CARTESIAN_POINT('Ctrl Pts',(4.60436118137108,0.305966755061857,3.48116810928789));
#52762=CARTESIAN_POINT('Ctrl Pts',(4.59640854202727,0.213658008474022,3.4455939943611));
#52763=CARTESIAN_POINT('Ctrl Pts',(4.58845590268347,0.121349261886187,3.41001987943431));
#52764=CARTESIAN_POINT('Ctrl Pts',(4.58050326333966,0.0199630328458878,
3.39800027961704));
#52765=CARTESIAN_POINT('Ctrl Pts',(4.57255062399586,-0.0781048312986516,
3.41100475468789));
#52766=CARTESIAN_POINT('Ctrl Pts',(4.56459798465205,-0.17617269544319,3.42400922975875));
#52767=CARTESIAN_POINT('Ctrl Pts',(4.55664534530825,-0.270922194691968,
3.46203777971774));
#52768=CARTESIAN_POINT('Ctrl Pts',(4.54869270596444,-0.350768912290741,
3.52044089639904));
#52769=CARTESIAN_POINT('Ctrl Pts',(4.54074006662063,-0.430615629889515,
3.57884401308035));
#52770=CARTESIAN_POINT('Ctrl Pts',(4.53278742727683,-0.495559565838284,
3.65762169648397));
#52771=CARTESIAN_POINT('Ctrl Pts',(4.52483478793302,-0.537660439465301,
3.74714230187364));
#52772=CARTESIAN_POINT('Ctrl Pts',(4.51688214858921,-0.579761313092318,
3.8366629072633));
#52773=CARTESIAN_POINT('Ctrl Pts',(4.50892950924541,-0.599019124397585,
3.936926434639));
#52774=CARTESIAN_POINT('Ctrl Pts',(4.5009768699016,-0.593079343631488,4.03567430223551));
#52775=CARTESIAN_POINT('Ctrl Pts',(4.49302423055779,-0.587139562865391,
4.13442216983203));
#52776=CARTESIAN_POINT('Ctrl Pts',(4.48507159121399,-0.556002190027932,
4.23165437764937));
#52777=CARTESIAN_POINT('Ctrl Pts',(4.47711895187018,-0.503474193090318,
4.31548296397124));
#52778=CARTESIAN_POINT('Ctrl Pts',(4.46916631252638,-0.450946196152703,
4.39931155029312));
#52779=CARTESIAN_POINT('Ctrl Pts',(4.46121367318257,-0.377027575114933,
4.46973651511953));
#52780=CARTESIAN_POINT('Ctrl Pts',(4.45326103383876,-0.290755888038263,
4.51814744739689));
#52781=CARTESIAN_POINT('Ctrl Pts',(4.44530839449495,-0.204484200961595,
4.56655837967425));
#52782=CARTESIAN_POINT('Ctrl Pts',(4.43735575515115,-0.105859447846027,
4.59295527940255));
#52783=CARTESIAN_POINT('Ctrl Pts',(4.42940311580734,-0.00693984821361558,
4.59411076594835));
#52784=CARTESIAN_POINT('Ctrl Pts',(4.42921721429075,-0.0046274959494805,
4.59413777669183));
#52785=CARTESIAN_POINT('Ctrl Pts',(4.42903131277416,-0.00231498256911503,
4.59415099449182));
#52786=CARTESIAN_POINT('Ctrl Pts',(4.42884541125756,-2.46302091461148E-6,
4.59415045696459));
#52787=CARTESIAN_POINT('Ctrl Pts',(4.32115458874249,3.58587963140688E-6,
4.59404994535016));
#52788=CARTESIAN_POINT('Ctrl Pts',(4.32544000997495,-0.0533308355660028,
4.59403876103764));
#52789=CARTESIAN_POINT('Ctrl Pts',(4.3297254312074,-0.106668183692779,4.58692369872924));
#52790=CARTESIAN_POINT('Ctrl Pts',(4.33401085243985,-0.158055593105036,
4.57274269264177));
#52791=CARTESIAN_POINT('Ctrl Pts',(4.34196349178366,-0.253417405095285,
4.54642639353635));
#52792=CARTESIAN_POINT('Ctrl Pts',(4.34991613112746,-0.342064054954561,
4.49577653064689));
#52793=CARTESIAN_POINT('Ctrl Pts',(4.35786877047127,-0.413157291282808,
4.42698573291487));
#52794=CARTESIAN_POINT('Ctrl Pts',(4.36582140981507,-0.484250527611055,
4.35819493518285));
#52795=CARTESIAN_POINT('Ctrl Pts',(4.37377404915888,-0.537790350408272,
4.27126320260829));
#52796=CARTESIAN_POINT('Ctrl Pts',(4.38172668850269,-0.567230782432438,
4.17681912699824));
#52797=CARTESIAN_POINT('Ctrl Pts',(4.3896793278465,-0.596671214456604,4.0823750513882));
#52798=CARTESIAN_POINT('Ctrl Pts',(4.3976319671903,-0.602012255707717,3.98041863274268));
#52799=CARTESIAN_POINT('Ctrl Pts',(4.40558460653411,-0.582600893642323,
3.88341542999892));
#52800=CARTESIAN_POINT('Ctrl Pts',(4.41353724587791,-0.563189531576929,
3.78641222725516));
#52801=CARTESIAN_POINT('Ctrl Pts',(4.42148988522172,-0.519025766195027,
3.69436224041317));
#52802=CARTESIAN_POINT('Ctrl Pts',(4.42944252456553,-0.455509217992651,
3.61851983504546));
#52803=CARTESIAN_POINT('Ctrl Pts',(4.43739516390933,-0.391992669790276,
3.54267742967776));
#52804=CARTESIAN_POINT('Ctrl Pts',(4.44534780325314,-0.309123338767427,
3.48304260578434));
#52805=CARTESIAN_POINT('Ctrl Pts',(4.45330044259694,-0.217033129998519,
3.44690653227429));
#52806=CARTESIAN_POINT('Ctrl Pts',(4.46125308194075,-0.12494292122961,3.41077045876423));
#52807=CARTESIAN_POINT('Ctrl Pts',(4.46920572128456,-0.0236318347146405,
3.39813313563753));
#52808=CARTESIAN_POINT('Ctrl Pts',(4.47715836062837,0.074513469760962,3.41053964803971));
#52809=CARTESIAN_POINT('Ctrl Pts',(4.48511099997217,0.172658774236564,3.42294616044189));
#52810=CARTESIAN_POINT('Ctrl Pts',(4.49306363931598,0.2676382966728,3.46039650837296));
#52811=CARTESIAN_POINT('Ctrl Pts',(4.50101627865978,0.34783949666059,3.51831187658845));
#52812=CARTESIAN_POINT('Ctrl Pts',(4.50896891800359,0.428040696648381,3.57622724480394));
#52813=CARTESIAN_POINT('Ctrl Pts',(4.51692155734739,0.493463574187728,3.65460763330386));
#52814=CARTESIAN_POINT('Ctrl Pts',(4.5248741966912,0.536109291561612,3.74386997215216));
#52815=CARTESIAN_POINT('Ctrl Pts',(4.53282683603501,0.578755008935497,3.83313231100046));
#52816=CARTESIAN_POINT('Ctrl Pts',(4.54077947537881,0.598623566143919,3.93327660019715));
#52817=CARTESIAN_POINT('Ctrl Pts',(4.54873211472262,0.593285761408823,4.03205883640902));
#52818=CARTESIAN_POINT('Ctrl Pts',(4.55668475406643,0.587947956673727,4.1308410726209));
#52819=CARTESIAN_POINT('Ctrl Pts',(4.56463739341024,0.557403789995114,4.22826125584796));
#52820=CARTESIAN_POINT('Ctrl Pts',(4.57259003275404,0.505387701781775,4.31240844187621));
#52821=CARTESIAN_POINT('Ctrl Pts',(4.58054267209785,0.453371613568435,4.39655562790445));
#52822=CARTESIAN_POINT('Ctrl Pts',(4.58849531144165,0.37988360382037,4.46742981673387));
#52823=CARTESIAN_POINT('Ctrl Pts',(4.59644795078546,0.293908582600447,4.51636567348148));
#52824=CARTESIAN_POINT('Ctrl Pts',(4.60440059012926,0.207933561380525,4.56530153022909));
#52825=CARTESIAN_POINT('Ctrl Pts',(4.61235322947307,0.109471528688745,4.59229905489488));
#52826=CARTESIAN_POINT('Ctrl Pts',(4.62030586881688,0.01056080905581,4.59405743239568));
#52827=CARTESIAN_POINT('Ctrl Pts',(4.62058877545875,0.00704216595801619,
4.59411998479525));
#52828=CARTESIAN_POINT('Ctrl Pts',(4.62087168210062,0.00352295504485493,
4.59415059693914));
#52829=CARTESIAN_POINT('Ctrl Pts',(4.62115458874249,3.7232086238465E-6,
4.59414939806979));
#52830=CARTESIAN_POINT('Origin',(4.,0.,4.));
#52831=CARTESIAN_POINT('',(5.02884541125756,1.1583539301252E-5,4.59413174414479));
#52832=CARTESIAN_POINT('',(4.92115458874249,-9.52916733652962E-6,4.59405847898621));
#52833=CARTESIAN_POINT('',(4.,-7.27562663373442E-17,4.5941));
#52834=CARTESIAN_POINT('Ctrl Pts',(5.02884541125756,1.1583539301252E-5,
4.59413174414479));
#52835=CARTESIAN_POINT('Ctrl Pts',(5.02784729636931,0.0124287555737821,
4.59414271605904));
#52836=CARTESIAN_POINT('Ctrl Pts',(5.02684918148107,0.024845254523583,4.59376142828251));
#52837=CARTESIAN_POINT('Ctrl Pts',(5.02585106659282,0.0372368329321061,
4.59298328977014));
#52838=CARTESIAN_POINT('Ctrl Pts',(5.01789842724901,0.135968707532707,4.58678334723719));
#52839=CARTESIAN_POINT('Ctrl Pts',(5.00994578790521,0.233118536601742,4.55538989360237));
#52840=CARTESIAN_POINT('Ctrl Pts',(5.0019931485614,0.316808430381418,4.50264120614281));
#52841=CARTESIAN_POINT('Ctrl Pts',(4.9940405092176,0.400498324161095,4.44989251868324));
#52842=CARTESIAN_POINT('Ctrl Pts',(4.98608786987379,0.470728282651411,4.37578859739892));
#52843=CARTESIAN_POINT('Ctrl Pts',(4.97813523052998,0.518911736914097,4.289389655942));
#52844=CARTESIAN_POINT('Ctrl Pts',(4.97018259118617,0.567095191176782,4.20299071448508));
#52845=CARTESIAN_POINT('Ctrl Pts',(4.96222995184237,0.593232141211837,4.10429675285556));
#52846=CARTESIAN_POINT('Ctrl Pts',(4.95427731249856,0.594126988899363,4.00537445204741));
#52847=CARTESIAN_POINT('Ctrl Pts',(4.94632467315476,0.595021836586889,3.90645215123927));
#52848=CARTESIAN_POINT('Ctrl Pts',(4.93837203381095,0.570674581926886,3.80730151125251));
#52849=CARTESIAN_POINT('Ctrl Pts',(4.93041939446714,0.524062008404491,3.72004504823011));
#52850=CARTESIAN_POINT('Ctrl Pts',(4.92246675512334,0.477449434882097,3.6327885852077));
#52851=CARTESIAN_POINT('Ctrl Pts',(4.91451411577953,0.408571542497308,3.55742629914966));
#52852=CARTESIAN_POINT('Ctrl Pts',(4.90656147643572,0.325849591692228,3.50317225594031));
#52853=CARTESIAN_POINT('Ctrl Pts',(4.89860883709192,0.243127640887147,3.44891821273095));
#52854=CARTESIAN_POINT('Ctrl Pts',(4.89065619774811,0.146561631661773,3.41577241237029));
#52855=CARTESIAN_POINT('Ctrl Pts',(4.88270355840431,0.0479580738465473,
3.40778738038914));
#52856=CARTESIAN_POINT('Ctrl Pts',(4.8747509190605,-0.0506454839686783,
3.39980234840799));
#52857=CARTESIAN_POINT('Ctrl Pts',(4.86679827971669,-0.151286590373755,
3.41697808480634));
#52858=CARTESIAN_POINT('Ctrl Pts',(4.85884564037289,-0.241660499406316,
3.45721462188069));
#52859=CARTESIAN_POINT('Ctrl Pts',(4.85089300102908,-0.332034408438876,
3.49745115895503));
#52860=CARTESIAN_POINT('Ctrl Pts',(4.84294036168527,-0.41214112009892,3.56074849670536));
#52861=CARTESIAN_POINT('Ctrl Pts',(4.83498772234147,-0.472186497854497,
3.63936767349926));
#52862=CARTESIAN_POINT('Ctrl Pts',(4.82703508299766,-0.532231875610076,
3.71798685029316));
#52863=CARTESIAN_POINT('Ctrl Pts',(4.81908244365386,-0.572215919461187,
3.81192786613063));
#52864=CARTESIAN_POINT('Ctrl Pts',(4.81112980431005,-0.587250035475296,
3.9097051523746));
#52865=CARTESIAN_POINT('Ctrl Pts',(4.80317716496624,-0.602284151489406,
4.00748243861856));
#52866=CARTESIAN_POINT('Ctrl Pts',(4.79522452562244,-0.592368339666514,
4.10909599526903));
#52867=CARTESIAN_POINT('Ctrl Pts',(4.78727188627863,-0.558714943052599,
4.20212218107662));
#52868=CARTESIAN_POINT('Ctrl Pts',(4.77931924693482,-0.525061546438685,
4.2951483668842));
#52869=CARTESIAN_POINT('Ctrl Pts',(4.77136660759101,-0.467670565033749,
4.37958718184891));
#52870=CARTESIAN_POINT('Ctrl Pts',(4.76341396824721,-0.393558827964045,
4.44511483080773));
#52871=CARTESIAN_POINT('Ctrl Pts',(4.7554613289034,-0.319447090894342,4.51064247976655));
#52872=CARTESIAN_POINT('Ctrl Pts',(4.7475086895596,-0.228614598159871,4.55725896271948));
#52873=CARTESIAN_POINT('Ctrl Pts',(4.73955605021579,-0.13216685911108,4.5792647797218));
#52874=CARTESIAN_POINT('Ctrl Pts',(4.73598583722972,-0.0888681559330128,
4.58914394690572));
#52875=CARTESIAN_POINT('Ctrl Pts',(4.73241562424364,-0.0444377444908,4.59406302997518));
#52876=CARTESIAN_POINT('Ctrl Pts',(4.72884541125756,-4.67700812217808E-6,
4.59405084457266));
#52877=CARTESIAN_POINT('Ctrl Pts',(4.62115458874249,3.7232086238465E-6,
4.59414939806979));
#52878=CARTESIAN_POINT('Ctrl Pts',(4.62882432144443,-0.0954043143036648,
4.59411689615543));
#52879=CARTESIAN_POINT('Ctrl Pts',(4.63649405414636,-0.190827729806029,
4.57070400848325));
#52880=CARTESIAN_POINT('Ctrl Pts',(4.6441637868483,-0.275369369969159,4.52648596729292));
#52881=CARTESIAN_POINT('Ctrl Pts',(4.65211642619211,-0.363029422787103,
4.48063689435358));
#52882=CARTESIAN_POINT('Ctrl Pts',(4.66006906553591,-0.438990121848901,
4.4124195181391));
#52883=CARTESIAN_POINT('Ctrl Pts',(4.66802170487971,-0.493964237128006,
4.33017434199545));
#52884=CARTESIAN_POINT('Ctrl Pts',(4.67597434422352,-0.548938352407109,
4.24792916585179));
#52885=CARTESIAN_POINT('Ctrl Pts',(4.68392698356733,-0.582925883903521,
4.15165618977896));
#52886=CARTESIAN_POINT('Ctrl Pts',(4.69187962291114,-0.591771392992132,
4.05312609631255));
#52887=CARTESIAN_POINT('Ctrl Pts',(4.69983226225494,-0.600616902080743,
3.95459600284613));
#52888=CARTESIAN_POINT('Ctrl Pts',(4.70778490159875,-0.584320388761555,
3.85380879198612));
#52889=CARTESIAN_POINT('Ctrl Pts',(4.71573754094256,-0.544874323741249,
3.76308707295491));
#52890=CARTESIAN_POINT('Ctrl Pts',(4.72369018028636,-0.505428258720944,
3.6723653539237));
#52891=CARTESIAN_POINT('Ctrl Pts',(4.73164281963017,-0.442832641999522,
3.59170912672127));
#52892=CARTESIAN_POINT('Ctrl Pts',(4.73959545897397,-0.364740640256699,
3.53097971363863));
#52893=CARTESIAN_POINT('Ctrl Pts',(4.74754809831778,-0.286648638513876,
3.47025030055599));
#52894=CARTESIAN_POINT('Ctrl Pts',(4.75550073766158,-0.193060251749651,
3.42944770159313));
#52895=CARTESIAN_POINT('Ctrl Pts',(4.76345337700539,-0.095417934894009,
3.41356059019365));
#52896=CARTESIAN_POINT('Ctrl Pts',(4.7714060163492,0.00222438196163176,
3.39767347879416));
#52897=CARTESIAN_POINT('Ctrl Pts',(4.77935865569301,0.10392062890869,3.40670185495805));
#52898=CARTESIAN_POINT('Ctrl Pts',(4.78731129503681,0.19723705468272,3.43954187673519));
#52899=CARTESIAN_POINT('Ctrl Pts',(4.79526393438062,0.290553480456751,3.47238189851233));
#52900=CARTESIAN_POINT('Ctrl Pts',(4.80321657372443,0.375490085057754,3.52903356590271));
#52901=CARTESIAN_POINT('Ctrl Pts',(4.81116921306823,0.441662211759978,3.60257044098769));
#52902=CARTESIAN_POINT('Ctrl Pts',(4.81912185241204,0.507834338462201,3.67610731607267));
#52903=CARTESIAN_POINT('Ctrl Pts',(4.82707449175584,0.555241987265645,3.76652939885225));
#52904=CARTESIAN_POINT('Ctrl Pts',(4.83502713109965,0.57808892742485,3.86278135818256));
#52905=CARTESIAN_POINT('Ctrl Pts',(4.84297977044346,0.600935867584054,3.95903331751286));
#52906=CARTESIAN_POINT('Ctrl Pts',(4.85093240978726,0.599222099099018,4.0611151533939));
#52907=CARTESIAN_POINT('Ctrl Pts',(4.85888504913107,0.573157153508111,4.15654597106253));
#52908=CARTESIAN_POINT('Ctrl Pts',(4.86683768847488,0.547092207917203,4.25197678873116));
#52909=CARTESIAN_POINT('Ctrl Pts',(4.87479032781868,0.496676085220424,4.34075658818739));
#52910=CARTESIAN_POINT('Ctrl Pts',(4.88274296716249,0.428072843071251,4.41203082979109));
#52911=CARTESIAN_POINT('Ctrl Pts',(4.89069560650629,0.359469600922078,4.48330507139479));
#52912=CARTESIAN_POINT('Ctrl Pts',(4.8986482458501,0.272679239320511,4.53707375514596));
#52913=CARTESIAN_POINT('Ctrl Pts',(4.90660088519391,0.178313062033339,4.56676292714126));
#52914=CARTESIAN_POINT('Ctrl Pts',(4.9114521197101,0.120748216373203,4.58487378690922));
#52915=CARTESIAN_POINT('Ctrl Pts',(4.9163033542263,0.0603642649825261,4.59402420038378));
#52916=CARTESIAN_POINT('Ctrl Pts',(4.92115458874249,-9.52916733652962E-6,
4.59405847898621));
#52917=CARTESIAN_POINT('Origin',(4.,0.,4.));
#52918=CARTESIAN_POINT('',(5.32884541125756,-1.45357002139801E-5,4.59407911932661));
#52919=CARTESIAN_POINT('',(5.22115458874249,1.46139895546772E-5,4.59411444380891));
#52920=CARTESIAN_POINT('',(4.,-7.27562663373442E-17,4.5941));
#52921=CARTESIAN_POINT('Ctrl Pts',(5.32884541125756,-1.45357002139801E-5,
4.59407911932661));
#52922=CARTESIAN_POINT('Ctrl Pts',(5.32327896849499,0.0692531541268509,
4.59401614001471));
#52923=CARTESIAN_POINT('Ctrl Pts',(5.31771252573242,0.138542285837495,4.5819075943171));
#52924=CARTESIAN_POINT('Ctrl Pts',(5.31214608296985,0.203593590158122,4.55818044906639));
#52925=CARTESIAN_POINT('Ctrl Pts',(5.30419344362604,0.296530782575621,4.5242820624512));
#52926=CARTESIAN_POINT('Ctrl Pts',(5.29624080428224,0.380818089806801,4.46666879957728));
#52927=CARTESIAN_POINT('Ctrl Pts',(5.28828816493843,0.446150240572578,4.39238466650784));
#52928=CARTESIAN_POINT('Ctrl Pts',(5.28033552559462,0.511482391338355,4.3181005334384));
#52929=CARTESIAN_POINT('Ctrl Pts',(5.27238288625081,0.557859385638729,4.22714553017344));
#52930=CARTESIAN_POINT('Ctrl Pts',(5.26443024690701,0.579611004278495,4.13064014464439));
#52931=CARTESIAN_POINT('Ctrl Pts',(5.2564776075632,0.601362622918262,4.03413475911534));
#52932=CARTESIAN_POINT('Ctrl Pts',(5.2485249682194,0.598488865897423,3.93207899132219));
#52933=CARTESIAN_POINT('Ctrl Pts',(5.24057232887559,0.571341089151559,3.8369505488493));
#52934=CARTESIAN_POINT('Ctrl Pts',(5.23261968953179,0.544193312405696,3.74182210637642));
#52935=CARTESIAN_POINT('Ctrl Pts',(5.22466705018798,0.492771515934809,3.65362098922379));
#52936=CARTESIAN_POINT('Ctrl Pts',(5.21671441084417,0.423362714708271,3.58313098523844));
#52937=CARTESIAN_POINT('Ctrl Pts',(5.20876177150037,0.353953913481732,3.51264098125308));
#52938=CARTESIAN_POINT('Ctrl Pts',(5.20080913215656,0.266558107499543,3.45986209043499));
#52939=CARTESIAN_POINT('Ctrl Pts',(5.19285649281275,0.171860624350003,3.43124725102074));
#52940=CARTESIAN_POINT('Ctrl Pts',(5.18490385346895,0.0771631412004631,
3.40263241160649));
#52941=CARTESIAN_POINT('Ctrl Pts',(5.17695121412514,-0.0248360191164267,
3.39818162359609));
#52942=CARTESIAN_POINT('Ctrl Pts',(5.16899857478133,-0.121666070051256,
3.41843905644231));
#52943=CARTESIAN_POINT('Ctrl Pts',(5.16104593543753,-0.218496120986084,
3.43869648928852));
#52944=CARTESIAN_POINT('Ctrl Pts',(5.15309329609372,-0.310157062538852,
3.48366214299137));
#52945=CARTESIAN_POINT('Ctrl Pts',(5.14514065674991,-0.385442096207774,
3.54783835396576));
#52946=CARTESIAN_POINT('Ctrl Pts',(5.13718801740611,-0.460727129876697,
3.61201456494015));
#52947=CARTESIAN_POINT('Ctrl Pts',(5.1292353780623,-0.519636255661773,3.6954013331861));
#52948=CARTESIAN_POINT('Ctrl Pts',(5.1212827387185,-0.554967030609594,3.78780349058054));
#52949=CARTESIAN_POINT('Ctrl Pts',(5.11333009937469,-0.590297805557415,
3.88020564797498));
#52950=CARTESIAN_POINT('Ctrl Pts',(5.10537746003088,-0.60205022966798,3.98162319451792));
#52951=CARTESIAN_POINT('Ctrl Pts',(5.09742482068708,-0.588787409028971,
4.07965645386523));
#52952=CARTESIAN_POINT('Ctrl Pts',(5.08947218134327,-0.575524588389962,
4.17768971321255));
#52953=CARTESIAN_POINT('Ctrl Pts',(5.08151954199946,-0.537246523001379,
4.27233868536424));
#52954=CARTESIAN_POINT('Ctrl Pts',(5.07356690265566,-0.47863322769376,4.35203124438164));
#52955=CARTESIAN_POINT('Ctrl Pts',(5.06561426331185,-0.42001993238614,4.43172380339905));
#52956=CARTESIAN_POINT('Ctrl Pts',(5.05766162396805,-0.341071407159484,
4.49645994928216));
#52957=CARTESIAN_POINT('Ctrl Pts',(5.04970898462424,-0.251440184480074,
4.53832480650817));
#52958=CARTESIAN_POINT('Ctrl Pts',(5.04275446016868,-0.1730583412759,4.5749353153996));
#52959=CARTESIAN_POINT('Ctrl Pts',(5.03579993571312,-0.0865070403179845,
4.59405529558476));
#52960=CARTESIAN_POINT('Ctrl Pts',(5.02884541125756,1.1583539301252E-5,
4.59413174414479));
#52961=CARTESIAN_POINT('Ctrl Pts',(4.92115458874249,-9.52916733652962E-6,
4.59405847898621));
#52962=CARTESIAN_POINT('Ctrl Pts',(4.9242559935701,-0.0386066277022544,
4.59408039337166));
#52963=CARTESIAN_POINT('Ctrl Pts',(4.92735739839772,-0.0771995748988638,
4.59037647703175));
#52964=CARTESIAN_POINT('Ctrl Pts',(4.93045880322533,-0.115049119822012,
4.58290605049323));
#52965=CARTESIAN_POINT('Ctrl Pts',(4.93841144256913,-0.212103131417409,
4.56375034161047));
#52966=CARTESIAN_POINT('Ctrl Pts',(4.94636408191294,-0.304269161635426,
4.51982926360553));
#52967=CARTESIAN_POINT('Ctrl Pts',(4.95431672125675,-0.380278658005779,
4.45651276645759));
#52968=CARTESIAN_POINT('Ctrl Pts',(4.96226936060055,-0.456288154376132,
4.39319626930964));
#52969=CARTESIAN_POINT('Ctrl Pts',(4.97022199994436,-0.516141116898821,
4.31048435301868));
#52970=CARTESIAN_POINT('Ctrl Pts',(4.97817463928816,-0.552519705724467,
4.21848967586497));
#52971=CARTESIAN_POINT('Ctrl Pts',(4.98612727863197,-0.588898294550112,
4.12649499871126));
#52972=CARTESIAN_POINT('Ctrl Pts',(4.99407991797578,-0.601802509678713,
4.0252175606948));
#52973=CARTESIAN_POINT('Ctrl Pts',(5.00203255731958,-0.589654635058918,
3.92703990798411));
#52974=CARTESIAN_POINT('Ctrl Pts',(5.00998519666339,-0.577506760439122,
3.82886225527341));
#52975=CARTESIAN_POINT('Ctrl Pts',(5.0179378360072,-0.540306796070929,3.73378438786847));
#52976=CARTESIAN_POINT('Ctrl Pts',(5.025890475351,-0.482602944251693,3.65343086999412));
#52977=CARTESIAN_POINT('Ctrl Pts',(5.03384311469481,-0.424899092432456,
3.57307735211977));
#52978=CARTESIAN_POINT('Ctrl Pts',(5.04179575403862,-0.346691353162178,
3.50744818377599));
#52979=CARTESIAN_POINT('Ctrl Pts',(5.04974839338242,-0.257541687734669,
3.46456742464414));
#52980=CARTESIAN_POINT('Ctrl Pts',(5.05770103272623,-0.16839202230716,3.42168666551229));
#52981=CARTESIAN_POINT('Ctrl Pts',(5.06565367207003,-0.0683004307224215,
3.40155431559236));
#52982=CARTESIAN_POINT('Ctrl Pts',(5.07360631141384,0.0304955267282049,
3.40663182885918));
#52983=CARTESIAN_POINT('Ctrl Pts',(5.08155895075765,0.129291484178831,3.41170934212599));
#52984=CARTESIAN_POINT('Ctrl Pts',(5.08951159010146,0.226791807495345,3.44199671857955));
#52985=CARTESIAN_POINT('Ctrl Pts',(5.09746422944526,0.311075754224562,3.49379091394262));
#52986=CARTESIAN_POINT('Ctrl Pts',(5.10541686878907,0.395359700953779,3.54558510930568));
#52987=CARTESIAN_POINT('Ctrl Pts',(5.11336950813287,0.466427271095698,3.61888612357825));
#52988=CARTESIAN_POINT('Ctrl Pts',(5.12132214747668,0.515589486279599,3.70473190942573));
#52989=CARTESIAN_POINT('Ctrl Pts',(5.12927478682048,0.564751701463499,3.79057769527322));
#52990=CARTESIAN_POINT('Ctrl Pts',(5.13722742616429,0.592008561689381,3.88896825269562));
#52991=CARTESIAN_POINT('Ctrl Pts',(5.1451800655081,0.594027544563649,3.98787399599556));
#52992=CARTESIAN_POINT('Ctrl Pts',(5.1531327048519,0.596046527437917,4.0867797392955));
#52993=CARTESIAN_POINT('Ctrl Pts',(5.16108534419571,0.572827632960568,4.18620066847299));
#52994=CARTESIAN_POINT('Ctrl Pts',(5.16903798353952,0.527209687216453,4.2739812208502));
#52995=CARTESIAN_POINT('Ctrl Pts',(5.17699062288332,0.481591741472338,4.3617617732274));
#52996=CARTESIAN_POINT('Ctrl Pts',(5.18494326222713,0.413574744461461,4.43790194880433));
#52997=CARTESIAN_POINT('Ctrl Pts',(5.19289590157094,0.331474700441294,4.49309257410834));
#52998=CARTESIAN_POINT('Ctrl Pts',(5.20084854091474,0.24937465642113,4.54828319941234));
#52999=CARTESIAN_POINT('Ctrl Pts',(5.20880118025855,0.153191565391677,4.58252427444343));
#53000=CARTESIAN_POINT('Ctrl Pts',(5.21675381960235,0.0546851202186884,
4.59162936142496));
#53001=CARTESIAN_POINT('Ctrl Pts',(5.21822074264906,0.0365148790664279,
4.59330886194775));
#53002=CARTESIAN_POINT('Ctrl Pts',(5.21968766569578,0.018265586889787,4.59413312238171));
#53003=CARTESIAN_POINT('Ctrl Pts',(5.22115458874249,1.46139895546772E-5,
4.59411444380891));
#53004=CARTESIAN_POINT('Origin',(4.,0.,4.));
#53005=CARTESIAN_POINT('',(5.62884541125756,1.52328526200479E-5,4.59408648697874));
#53006=CARTESIAN_POINT('',(5.52115458874249,-1.55733839743342E-5,4.59409663347568));
#53007=CARTESIAN_POINT('',(4.,-7.27562663373442E-17,4.5941));
#53008=CARTESIAN_POINT('Ctrl Pts',(5.62884541125756,1.52328526200479E-5,
4.59408648697874));
#53009=CARTESIAN_POINT('Ctrl Pts',(5.62666327996447,0.0271682673899915,
4.59411287463303));
#53010=CARTESIAN_POINT('Ctrl Pts',(5.62448114867138,0.054317778225707,4.59228554395034));
#53011=CARTESIAN_POINT('Ctrl Pts',(5.62229901737829,0.0812075234320336,
4.58857548522516));
#53012=CARTESIAN_POINT('Ctrl Pts',(5.61434637803449,0.179205497408217,4.57505441109036));
#53013=CARTESIAN_POINT('Ctrl Pts',(5.60639373869068,0.273753285393806,4.53652709601604));
#53014=CARTESIAN_POINT('Ctrl Pts',(5.59844109934688,0.353291132582354,4.47770402899113));
#53015=CARTESIAN_POINT('Ctrl Pts',(5.59048846000307,0.432828979770902,4.41888096196622));
#53016=CARTESIAN_POINT('Ctrl Pts',(5.58253582065927,0.497356886162411,4.33976214299073));
#53017=CARTESIAN_POINT('Ctrl Pts',(5.57458318131546,0.538985436353474,4.25002092526659));
#53018=CARTESIAN_POINT('Ctrl Pts',(5.56663054197165,0.580613986544537,4.16027970754245));
#53019=CARTESIAN_POINT('Ctrl Pts',(5.55867790262784,0.599343180535155,4.05991609106967));
#53020=CARTESIAN_POINT('Ctrl Pts',(5.55072526328404,0.592883119270616,3.96120089488413));
#53021=CARTESIAN_POINT('Ctrl Pts',(5.54277262394023,0.586423058006077,3.86248569869858));
#53022=CARTESIAN_POINT('Ctrl Pts',(5.53481998459642,0.554773741486382,3.76541892280029));
#53023=CARTESIAN_POINT('Ctrl Pts',(5.52686734525262,0.501804729712613,3.68186830256729));
#53024=CARTESIAN_POINT('Ctrl Pts',(5.51891470590881,0.448835717938844,3.5983176823343));
#53025=CARTESIAN_POINT('Ctrl Pts',(5.51096206656501,0.374547010911001,3.52828321776661));
#53026=CARTESIAN_POINT('Ctrl Pts',(5.5030094272212,0.288021414854312,3.48032757600706));
#53027=CARTESIAN_POINT('Ctrl Pts',(5.4950567878774,0.201495818797622,3.4323719342475));
#53028=CARTESIAN_POINT('Ctrl Pts',(5.48710414853359,0.102733333712086,3.40649511529609));
#53029=CARTESIAN_POINT('Ctrl Pts',(5.47915150918978,0.00380901851787326,
3.40586091270526));
#53030=CARTESIAN_POINT('Ctrl Pts',(5.47119886984597,-0.0951152966763399,
3.40522671011442));
#53031=CARTESIAN_POINT('Ctrl Pts',(5.46324623050217,-0.194201441979227,
3.42983512388417));
#53032=CARTESIAN_POINT('Ctrl Pts',(5.45529359115836,-0.281334786601535,
3.47667744027106));
#53033=CARTESIAN_POINT('Ctrl Pts',(5.44734095181456,-0.368468131223842,
3.52351975665794));
#53034=CARTESIAN_POINT('Ctrl Pts',(5.43938831247075,-0.443648675165568,
3.59259597566196));
#53035=CARTESIAN_POINT('Ctrl Pts',(5.43143567312694,-0.497684572991269,
3.67546058871077));
#53036=CARTESIAN_POINT('Ctrl Pts',(5.42348303378314,-0.551720470816969,
3.75832520175959));
#53037=CARTESIAN_POINT('Ctrl Pts',(5.41553039443933,-0.584611722526643,
3.85497820885321));
#53038=CARTESIAN_POINT('Ctrl Pts',(5.40757775509553,-0.592336924628993,
3.95360246348684));
#53039=CARTESIAN_POINT('Ctrl Pts',(5.39962511575172,-0.600062126731343,
4.05222671812048));
#53040=CARTESIAN_POINT('Ctrl Pts',(5.39167247640791,-0.582621279226368,
4.15282222029412));
#53041=CARTESIAN_POINT('Ctrl Pts',(5.3837198370641,-0.542146763261091,4.24308979978386));
#53042=CARTESIAN_POINT('Ctrl Pts',(5.3757671977203,-0.501672247295815,4.3333573792736));
#53043=CARTESIAN_POINT('Ctrl Pts',(5.36781455837649,-0.438164062870237,
4.41329703607943));
#53044=CARTESIAN_POINT('Ctrl Pts',(5.35986191903269,-0.359386950494509,
4.47313505840055));
#53045=CARTESIAN_POINT('Ctrl Pts',(5.35190927968888,-0.28060983811878,4.53297308072167));
#53046=CARTESIAN_POINT('Ctrl Pts',(5.34395664034507,-0.1865637977929,4.57270946855809));
#53047=CARTESIAN_POINT('Ctrl Pts',(5.33600400100126,-0.0887472388280498,
4.58748590729807));
#53048=CARTESIAN_POINT('Ctrl Pts',(5.33361780442003,-0.0593972924141157,
4.59191959101989));
#53049=CARTESIAN_POINT('Ctrl Pts',(5.3312316078388,-0.0297078841644672,
4.59410611700271));
#53050=CARTESIAN_POINT('Ctrl Pts',(5.32884541125756,-1.45357002139801E-5,
4.59407911932661));
#53051=CARTESIAN_POINT('Ctrl Pts',(5.22115458874249,1.46139895546772E-5,
4.59411444380891));
#53052=CARTESIAN_POINT('Ctrl Pts',(5.22764030503958,-0.0806785298274998,
4.59403186011492));
#53053=CARTESIAN_POINT('Ctrl Pts',(5.23412602133668,-0.161404528346198,
4.57747154641029));
#53054=CARTESIAN_POINT('Ctrl Pts',(5.24061173763377,-0.235476461490165,
4.54549665421293));
#53055=CARTESIAN_POINT('Ctrl Pts',(5.24856437697758,-0.32630179870949,4.50628976108741));
#53056=CARTESIAN_POINT('Ctrl Pts',(5.25651701632139,-0.407122673831612,
4.44390687590439));
#53057=CARTESIAN_POINT('Ctrl Pts',(5.26446965566519,-0.468057634114636,
4.36597515601533));
#53058=CARTESIAN_POINT('Ctrl Pts',(5.272422295009,-0.52899259439766,4.28804343612627));
#53059=CARTESIAN_POINT('Ctrl Pts',(5.28037493435281,-0.570041639841584,
4.19456288153117));
#53060=CARTESIAN_POINT('Ctrl Pts',(5.28832757369661,-0.586185965564114,
4.09696276320888));
#53061=CARTESIAN_POINT('Ctrl Pts',(5.29628021304042,-0.602330291286644,
3.99936264488659));
#53062=CARTESIAN_POINT('Ctrl Pts',(5.30423285238423,-0.59356989728778,3.89764296283709));
#53063=CARTESIAN_POINT('Ctrl Pts',(5.31218549172803,-0.560975861048054,
3.80424033358521));
#53064=CARTESIAN_POINT('Ctrl Pts',(5.32013813107184,-0.528381824808328,
3.71083770433334));
#53065=CARTESIAN_POINT('Ctrl Pts',(5.32809077041564,-0.471954146327742,
3.62575212787907));
#53066=CARTESIAN_POINT('Ctrl Pts',(5.33604340975945,-0.398591877830097,
3.55938647478623));
#53067=CARTESIAN_POINT('Ctrl Pts',(5.34399604910326,-0.325229609332449,
3.49302082169338));
#53068=CARTESIAN_POINT('Ctrl Pts',(5.35194868844707,-0.234932750817741,
3.44537509196196));
#53069=CARTESIAN_POINT('Ctrl Pts',(5.35990132779087,-0.138741323057917,
3.42227462497344));
#53070=CARTESIAN_POINT('Ctrl Pts',(5.36785396713468,-0.042549895298095,
3.39917415798493));
#53071=CARTESIAN_POINT('Ctrl Pts',(5.37580660647848,0.059536101706843,3.40061895373932));
#53072=CARTESIAN_POINT('Ctrl Pts',(5.38375924582229,0.155035264439678,3.42643236627792));
#53073=CARTESIAN_POINT('Ctrl Pts',(5.39171188516609,0.250534427172515,3.45224577881651));
#53074=CARTESIAN_POINT('Ctrl Pts',(5.3996645245099,0.339446755633248,3.5024278081393));
#53075=CARTESIAN_POINT('Ctrl Pts',(5.40761716385371,0.41090150670596,3.57084301769608));
#53076=CARTESIAN_POINT('Ctrl Pts',(5.41556980319751,0.482356257778672,3.63925822725286));
#53077=CARTESIAN_POINT('Ctrl Pts',(5.42352244254132,0.536353431463363,3.72590661704362));
#53078=CARTESIAN_POINT('Ctrl Pts',(5.43147508188513,0.566291137850326,3.82019424128906));
#53079=CARTESIAN_POINT('Ctrl Pts',(5.43942772122893,0.596228844237288,3.91448186553449));
#53080=CARTESIAN_POINT('Ctrl Pts',(5.44738036057274,0.602107083326521,4.01640872423458));
#53081=CARTESIAN_POINT('Ctrl Pts',(5.45533299991655,0.583207160329387,4.11351287069736));
#53082=CARTESIAN_POINT('Ctrl Pts',(5.46328563926035,0.564307237332252,4.21061701716013));
#53083=CARTESIAN_POINT('Ctrl Pts',(5.47123827860416,0.520629152248751,4.30289845138559));
#53084=CARTESIAN_POINT('Ctrl Pts',(5.47919091794796,0.457513145863858,4.37907451119169));
#53085=CARTESIAN_POINT('Ctrl Pts',(5.48714355729177,0.394397139478966,4.45525057099779));
#53086=CARTESIAN_POINT('Ctrl Pts',(5.49509619663558,0.311843211792683,4.51532125638452));
#53087=CARTESIAN_POINT('Ctrl Pts',(5.50304883597938,0.219944704826683,4.5519421079172));
#53088=CARTESIAN_POINT('Ctrl Pts',(5.50908408690042,0.150203009669811,4.5797336395568));
#53089=CARTESIAN_POINT('Ctrl Pts',(5.51511933782146,0.0750795109720808,
4.59401975858331));
#53090=CARTESIAN_POINT('Ctrl Pts',(5.52115458874249,-1.55733839743342E-5,
4.59409663347568));
#53091=CARTESIAN_POINT('Origin',(4.,0.,4.));
#53092=CARTESIAN_POINT('',(5.92884541125757,-1.3134308860685E-5,4.59412454375027));
#53093=CARTESIAN_POINT('',(5.82115458874249,1.31105368646138E-5,4.59407040741879));
#53094=CARTESIAN_POINT('',(4.,-7.27562663373442E-17,4.5941));
#53095=CARTESIAN_POINT('Ctrl Pts',(5.92884541125757,-1.3134308860685E-5,
4.59412454375027));
#53096=CARTESIAN_POINT('Ctrl Pts',(5.92209495209015,0.0839697382976411,
4.5940436242297));
#53097=CARTESIAN_POINT('Ctrl Pts',(5.91534449292274,0.16798613900316,4.57606223573506));
#53098=CARTESIAN_POINT('Ctrl Pts',(5.90859403375532,0.244517407380453,4.54150437939301));
#53099=CARTESIAN_POINT('Ctrl Pts',(5.90064139441152,0.334678026211646,4.50079216098422));
#53100=CARTESIAN_POINT('Ctrl Pts',(5.89268875506771,0.41445008323119,4.43707358099086));
#53101=CARTESIAN_POINT('Ctrl Pts',(5.8847361157239,0.474080337065587,4.35813908232779));
#53102=CARTESIAN_POINT('Ctrl Pts',(5.8767834763801,0.533710590899983,4.27920458366471));
#53103=CARTESIAN_POINT('Ctrl Pts',(5.86883083703629,0.573199041549232,4.18505416633191));
#53104=CARTESIAN_POINT('Ctrl Pts',(5.86087819769249,0.587717699183782,4.08719901244189));
#53105=CARTESIAN_POINT('Ctrl Pts',(5.85292555834868,0.602236356818331,3.98934385855186));
#53106=CARTESIAN_POINT('Ctrl Pts',(5.84497291900487,0.591785221438181,3.88778396810461));
#53107=CARTESIAN_POINT('Ctrl Pts',(5.83702027966107,0.557642080814915,3.79493641494568));
#53108=CARTESIAN_POINT('Ctrl Pts',(5.82906764031726,0.523498940191649,3.70208886178675));
#53109=CARTESIAN_POINT('Ctrl Pts',(5.82111500097346,0.465663794325265,3.61795364591614));
#53110=CARTESIAN_POINT('Ctrl Pts',(5.81316236162965,0.391207780605707,3.55281744653948));
#53111=CARTESIAN_POINT('Ctrl Pts',(5.80520972228584,0.31675176688615,3.48768124716281));
#53112=CARTESIAN_POINT('Ctrl Pts',(5.79725708294203,0.225674885313418,3.44154406428009));
#53113=CARTESIAN_POINT('Ctrl Pts',(5.78930444359823,0.129112523455512,3.42004679519738));
#53114=CARTESIAN_POINT('Ctrl Pts',(5.78135180425442,0.0325501615976049,
3.39854952611466));
#53115=CARTESIAN_POINT('Ctrl Pts',(5.77339916491062,-0.0694976805454773,
3.40169217083197));
#53116=CARTESIAN_POINT('Ctrl Pts',(5.76544652556681,-0.164554263536051,
3.42909049911887));
#53117=CARTESIAN_POINT('Ctrl Pts',(5.75749388622301,-0.259610846526622,
3.45648882740576));
#53118=CARTESIAN_POINT('Ctrl Pts',(5.7495412468792,-0.347676170364685,3.50814283926225));
#53119=CARTESIAN_POINT('Ctrl Pts',(5.74158860753539,-0.417983050247216,
3.57773712775495));
#53120=CARTESIAN_POINT('Ctrl Pts',(5.73363596819158,-0.488289930129746,
3.64733141624764));
#53121=CARTESIAN_POINT('Ctrl Pts',(5.72568332884778,-0.540838366056745,
3.73486598137654));
#53122=CARTESIAN_POINT('Ctrl Pts',(5.71773068950397,-0.569203595796233,
3.82963853060694));
#53123=CARTESIAN_POINT('Ctrl Pts',(5.70977805016017,-0.597568825535722,
3.92441107983734));
#53124=CARTESIAN_POINT('Ctrl Pts',(5.70182541081636,-0.6017508490877,4.02642161316923));
#53125=CARTESIAN_POINT('Ctrl Pts',(5.69387277147255,-0.581238357244447,
4.12319795341528));
#53126=CARTESIAN_POINT('Ctrl Pts',(5.68592013212875,-0.560725865401195,
4.21997429366132));
#53127=CARTESIAN_POINT('Ctrl Pts',(5.67796749278494,-0.515518858162713,
4.31151644082153));
#53128=CARTESIAN_POINT('Ctrl Pts',(5.67001485344113,-0.451144507802385,
4.38663212069642));
#53129=CARTESIAN_POINT('Ctrl Pts',(5.66206221409732,-0.386770157442057,
4.46174780057131));
#53130=CARTESIAN_POINT('Ctrl Pts',(5.65410957475352,-0.303228463959881,
4.52043701316089));
#53131=CARTESIAN_POINT('Ctrl Pts',(5.64615693540972,-0.210733537235404,
4.55552420285805));
#53132=CARTESIAN_POINT('Ctrl Pts',(5.640386427359,-0.143618370026196,4.5809837895275));
#53133=CARTESIAN_POINT('Ctrl Pts',(5.63461591930828,-0.07178924788396,4.59401670649762));
#53134=CARTESIAN_POINT('Ctrl Pts',(5.62884541125756,1.52328526200479E-5,
4.59408648697874));
#53135=CARTESIAN_POINT('Ctrl Pts',(5.52115458874249,-1.55733839743342E-5,
4.59409663347568));
#53136=CARTESIAN_POINT('Ctrl Pts',(5.52307197716526,-0.0238731473664388,
4.59412105649149));
#53137=CARTESIAN_POINT('Ctrl Pts',(5.52498936558803,-0.0477278534282068,
4.59271130989713));
#53138=CARTESIAN_POINT('Ctrl Pts',(5.5269067540108,-0.0714062077139717,
4.58984482465595));
#53139=CARTESIAN_POINT('Ctrl Pts',(5.53485939335461,-0.169615527042917,
4.57795567218339));
#53140=CARTESIAN_POINT('Ctrl Pts',(5.54281203269841,-0.264791079455087,
4.54100634955965));
#53141=CARTESIAN_POINT('Ctrl Pts',(5.55076467204222,-0.345296357402727,
4.48351441471562));
#53142=CARTESIAN_POINT('Ctrl Pts',(5.55871731138603,-0.425801635350366,
4.4260224798716));
#53143=CARTESIAN_POINT('Ctrl Pts',(5.56666995072984,-0.491636638833473,
4.34798793280729));
#53144=CARTESIAN_POINT('Ctrl Pts',(5.57462259007364,-0.534752142022197,
4.2589515597096));
#53145=CARTESIAN_POINT('Ctrl Pts',(5.58257522941745,-0.577867645210921,
4.16991518661191));
#53146=CARTESIAN_POINT('Ctrl Pts',(5.59052786876125,-0.598263648105263,
4.06987698748084));
#53147=CARTESIAN_POINT('Ctrl Pts',(5.59848050810506,-0.59344646156208,3.97106799465478));
#53148=CARTESIAN_POINT('Ctrl Pts',(5.60643314744886,-0.588629275018896,
3.87225900182873));
#53149=CARTESIAN_POINT('Ctrl Pts',(5.61438578679267,-0.558598899038186,
3.77467921530768));
#53150=CARTESIAN_POINT('Ctrl Pts',(5.62233842613648,-0.50702695609161,3.69025909300064));
#53151=CARTESIAN_POINT('Ctrl Pts',(5.63029106548029,-0.455455013145033,
3.6058389706936));
#53152=CARTESIAN_POINT('Ctrl Pts',(5.63824370482409,-0.382341503232591,
3.53457851260056));
#53153=CARTESIAN_POINT('Ctrl Pts',(5.6461963441679,-0.296625548722353,3.48519028027742));
#53154=CARTESIAN_POINT('Ctrl Pts',(5.6541489835117,-0.210909594212113,3.43580204795428));
#53155=CARTESIAN_POINT('Ctrl Pts',(5.66210162285551,-0.112591195104077,
3.40828604140104));
#53156=CARTESIAN_POINT('Ctrl Pts',(5.67005426219932,-0.0136911147678568,
3.40600646716786));
#53157=CARTESIAN_POINT('Ctrl Pts',(5.67800690154312,0.0852089655683624,
3.40372689293467));
#53158=CARTESIAN_POINT('Ctrl Pts',(5.68595954088693,0.184690727132768,3.42668375102154));
#53159=CARTESIAN_POINT('Ctrl Pts',(5.69391218023074,0.272591169676606,3.47207025288287));
#53160=CARTESIAN_POINT('Ctrl Pts',(5.70186481957454,0.360491612220445,3.51745675474419));
#53161=CARTESIAN_POINT('Ctrl Pts',(5.70981745891835,0.436810735743714,3.58527290037998));
#53162=CARTESIAN_POINT('Ctrl Pts',(5.71777009826216,0.492217487918224,3.667227242308));
#53163=CARTESIAN_POINT('Ctrl Pts',(5.72572273760596,0.547624240092733,3.74918158423602));
#53164=CARTESIAN_POINT('Ctrl Pts',(5.73367537694977,0.582118620918482,3.84527412245626));
#53165=CARTESIAN_POINT('Ctrl Pts',(5.74162801629357,0.591483222595687,3.94375623549444));
#53166=CARTESIAN_POINT('Ctrl Pts',(5.74958065563738,0.600847824272892,4.04223834853263));
#53167=CARTESIAN_POINT('Ctrl Pts',(5.75753329498119,0.585082646801554,4.14311003638875));
#53168=CARTESIAN_POINT('Ctrl Pts',(5.76548593432499,0.546115197731279,4.23403836123177));
#53169=CARTESIAN_POINT('Ctrl Pts',(5.7734385736688,0.507147748661005,4.32496668607478));
#53170=CARTESIAN_POINT('Ctrl Pts',(5.78139121301261,0.444978027991796,4.4059516479047));
#53171=CARTESIAN_POINT('Ctrl Pts',(5.78934385235641,0.367207131024688,4.46709173242012));
#53172=CARTESIAN_POINT('Ctrl Pts',(5.79729649170022,0.28943623405758,4.52823181693554));
#53173=CARTESIAN_POINT('Ctrl Pts',(5.80524913104403,0.196064160792572,4.56952702413646));
#53174=CARTESIAN_POINT('Ctrl Pts',(5.81320177038783,0.0985069184831505,
4.58592845199323));
#53175=CARTESIAN_POINT('Ctrl Pts',(5.81585270983939,0.0659871057213339,
4.59139571767544));
#53176=CARTESIAN_POINT('Ctrl Pts',(5.81850364929094,0.0330022532417819,
4.59409688335147));
#53177=CARTESIAN_POINT('Ctrl Pts',(5.82115458874249,1.31105368646138E-5,
4.59407040741879));
#53178=CARTESIAN_POINT('Origin',(4.,0.,4.));
#53179=CARTESIAN_POINT('',(6.22884541125756,-1.27841859475647E-5,4.5940334609955));
#53180=CARTESIAN_POINT('',(6.12115458874249,-9.50793186244619E-6,4.59413936148612));
#53181=CARTESIAN_POINT('',(4.,-7.27562663373442E-17,4.5941));
#53182=CARTESIAN_POINT('Ctrl Pts',(6.22884541125756,-1.27841859475647E-5,
4.5940334609955));
#53183=CARTESIAN_POINT('Ctrl Pts',(6.22547926355963,0.0418951881409122,
4.59406590912705));
#53184=CARTESIAN_POINT('Ctrl Pts',(6.2221131158617,0.0838018877146867,4.58971510200585));
#53185=CARTESIAN_POINT('Ctrl Pts',(6.21874696816377,0.124749109322564,4.58093223526196));
#53186=CARTESIAN_POINT('Ctrl Pts',(6.21079432881996,0.22148832423537,4.56018241146135));
#53187=CARTESIAN_POINT('Ctrl Pts',(6.20284168947616,0.31287214740051,4.51469474440412));
#53188=CARTESIAN_POINT('Ctrl Pts',(6.19488905013236,0.387808805213989,4.4501133836823));
#53189=CARTESIAN_POINT('Ctrl Pts',(6.18693641078855,0.462745463027469,4.38553202296047));
#53190=CARTESIAN_POINT('Ctrl Pts',(6.17898377144474,0.521234955489287,4.30185696857405));
#53191=CARTESIAN_POINT('Ctrl Pts',(6.17103113210093,0.556083161424236,4.20927485003939));
#53192=CARTESIAN_POINT('Ctrl Pts',(6.16307849275713,0.590931367359184,4.11669273150472));
#53193=CARTESIAN_POINT('Ctrl Pts',(6.15512585341332,0.602138286767263,4.0152035488218));
#53194=CARTESIAN_POINT('Ctrl Pts',(6.14717321406952,0.588356486924291,3.9172389266648));
#53195=CARTESIAN_POINT('Ctrl Pts',(6.13922057472571,0.574574687081318,3.81927430450779));
#53196=CARTESIAN_POINT('Ctrl Pts',(6.1312679353819,0.535804167987293,3.7248342428767));
#53197=CARTESIAN_POINT('Ctrl Pts',(6.12331529603809,0.476773096629474,3.64545304401991));
#53198=CARTESIAN_POINT('Ctrl Pts',(6.11536265669429,0.417742025271657,3.56607184516312));
#53199=CARTESIAN_POINT('Ctrl Pts',(6.10741001735048,0.338450401650047,3.50174950908064));
#53200=CARTESIAN_POINT('Ctrl Pts',(6.09945737800668,0.248599092144812,3.46035682177302));
#53201=CARTESIAN_POINT('Ctrl Pts',(6.09150473866287,0.158747782639575,3.41896413446539));
#53202=CARTESIAN_POINT('Ctrl Pts',(6.08355209931906,0.0583367872507115,
3.40050109593262));
#53203=CARTESIAN_POINT('Ctrl Pts',(6.07559945997526,-0.0403606640336046,
3.40722161935946));
#53204=CARTESIAN_POINT('Ctrl Pts',(6.06764682063145,-0.139058115317921,
3.4139421427863));
#53205=CARTESIAN_POINT('Ctrl Pts',(6.05969418128764,-0.23604202249769,3.44584622817275));
#53206=CARTESIAN_POINT('Ctrl Pts',(6.05174154194384,-0.319452991027635,
3.49903499090221));
#53207=CARTESIAN_POINT('Ctrl Pts',(6.04378890260003,-0.40286395955758,3.55222375363166));
#53208=CARTESIAN_POINT('Ctrl Pts',(6.03583626325623,-0.472701989437702,
3.62669719370411));
#53209=CARTESIAN_POINT('Ctrl Pts',(6.02788362391242,-0.520429378860104,
3.71334895258148));
#53210=CARTESIAN_POINT('Ctrl Pts',(6.01993098456861,-0.568156768282506,
3.80000071145885));
#53211=CARTESIAN_POINT('Ctrl Pts',(6.0119783452248,-0.593773517247188,3.89883078914114));
#53212=CARTESIAN_POINT('Ctrl Pts',(6.004025705881,-0.594147126960238,3.99775637428654));
#53213=CARTESIAN_POINT('Ctrl Pts',(5.99607306653719,-0.594520736673288,
4.09668195943193));
#53214=CARTESIAN_POINT('Ctrl Pts',(5.98812042719339,-0.569651207134705,
4.19570305204043));
#53215=CARTESIAN_POINT('Ctrl Pts',(5.98016778784958,-0.52257944308796,4.28271270390554));
#53216=CARTESIAN_POINT('Ctrl Pts',(5.97221514850578,-0.475507679041215,
4.36972235577065));
#53217=CARTESIAN_POINT('Ctrl Pts',(5.96426250916196,-0.406233680486307,
4.44472056689237));
#53218=CARTESIAN_POINT('Ctrl Pts',(5.95630986981816,-0.323226996343023,
4.49853792802592));
#53219=CARTESIAN_POINT('Ctrl Pts',(5.94835723047435,-0.240220312199739,
4.55235528915947));
#53220=CARTESIAN_POINT('Ctrl Pts',(5.94040459113055,-0.143480942468078,
4.58499180030486));
#53221=CARTESIAN_POINT('Ctrl Pts',(5.93245195178675,-0.0448366672808267,
4.59245712746544));
#53222=CARTESIAN_POINT('Ctrl Pts',(5.93124977161035,-0.0299248641651563,
4.59358564190382));
#53223=CARTESIAN_POINT('Ctrl Pts',(5.93004759143396,-0.0149695309183627,
4.59413895459864));
#53224=CARTESIAN_POINT('Ctrl Pts',(5.92884541125757,-1.3134308860685E-5,
4.59412454375027));
#53225=CARTESIAN_POINT('Ctrl Pts',(5.82115458874249,1.31105368646138E-5,
4.59407040741879));
#53226=CARTESIAN_POINT('Ctrl Pts',(5.82645628863475,-0.0659629472043463,
4.59401745734129));
#53227=CARTESIAN_POINT('Ctrl Pts',(5.831757988527,-0.131956164688202,4.58305467757793));
#53228=CARTESIAN_POINT('Ctrl Pts',(5.83705968841925,-0.194280919321303,
4.56148970414564));
#53229=CARTESIAN_POINT('Ctrl Pts',(5.84501232776306,-0.287769103462499,
4.52914187992864));
#53230=CARTESIAN_POINT('Ctrl Pts',(5.85296496710686,-0.373003060391055,
4.47293858298203));
#53231=CARTESIAN_POINT('Ctrl Pts',(5.86091760645067,-0.439561779454174,
4.39975142997742));
#53232=CARTESIAN_POINT('Ctrl Pts',(5.86887024579447,-0.506120498517293,
4.32656427697281));
#53233=CARTESIAN_POINT('Ctrl Pts',(5.87682288513828,-0.554003979714975,
4.2363932679102));
#53234=CARTESIAN_POINT('Ctrl Pts',(5.88477552448209,-0.577357812582609,
4.14026304025204));
#53235=CARTESIAN_POINT('Ctrl Pts',(5.8927281638259,-0.600711645450243,4.04413281259387));
#53236=CARTESIAN_POINT('Ctrl Pts',(5.9006808031697,-0.59953582998783,3.94204336634015));
#53237=CARTESIAN_POINT('Ctrl Pts',(5.90863344251351,-0.573974130801472,
3.84647652011691));
#53238=CARTESIAN_POINT('Ctrl Pts',(5.91658608185731,-0.548412431615114,
3.75090967389367));
#53239=CARTESIAN_POINT('Ctrl Pts',(5.92453872120112,-0.498464848704808,
3.66186542770092));
#53240=CARTESIAN_POINT('Ctrl Pts',(5.93249136054493,-0.430238144626613,
3.59023066587279));
#53241=CARTESIAN_POINT('Ctrl Pts',(5.94044399988873,-0.362011440548417,
3.51859590404466));
#53242=CARTESIAN_POINT('Ctrl Pts',(5.94839663923254,-0.275505615302329,
3.46437062658116));
#53243=CARTESIAN_POINT('Ctrl Pts',(5.95634927857635,-0.181297202577209,
3.43418458862315));
#53244=CARTESIAN_POINT('Ctrl Pts',(5.96430191792015,-0.087088789852092,
3.40399855066514));
#53245=CARTESIAN_POINT('Ctrl Pts',(5.97225455726396,0.0148222103520573,
3.39785175221263));
#53246=CARTESIAN_POINT('Ctrl Pts',(5.98020719660777,0.111975824940657,3.41649576758492));
#53247=CARTESIAN_POINT('Ctrl Pts',(5.98815983595157,0.209129439529257,3.43513978295721));
#53248=CARTESIAN_POINT('Ctrl Pts',(5.99611247529537,0.301525668502307,3.47857461215431));
#53249=CARTESIAN_POINT('Ctrl Pts',(6.00406511463918,0.377867748972965,3.54148967172874));
#53250=CARTESIAN_POINT('Ctrl Pts',(6.01201775398299,0.454209829443624,3.60440473130317));
#53251=CARTESIAN_POINT('Ctrl Pts',(6.0199703933268,0.514497761411887,3.68680002125492));
#53252=CARTESIAN_POINT('Ctrl Pts',(6.02792303267061,0.551360647735685,3.77860175380959));
#53253=CARTESIAN_POINT('Ctrl Pts',(6.03587567201441,0.588223534059482,3.87040348636426));
#53254=CARTESIAN_POINT('Ctrl Pts',(6.04382831135821,0.601661374738811,3.97161166152184));
#53255=CARTESIAN_POINT('Ctrl Pts',(6.05178095070202,0.590030977261751,4.06985190192822));
#53256=CARTESIAN_POINT('Ctrl Pts',(6.05973359004583,0.578400579784692,4.16809214233459));
#53257=CARTESIAN_POINT('Ctrl Pts',(6.06768622938964,0.541701944151245,4.26336444798975));
#53258=CARTESIAN_POINT('Ctrl Pts',(6.07563886873345,0.484422419230229,4.3440210474869));
#53259=CARTESIAN_POINT('Ctrl Pts',(6.08359150807725,0.427142894309213,4.42467764698404));
#53260=CARTESIAN_POINT('Ctrl Pts',(6.09154414742105,0.349282480100627,4.49071854032316));
#53261=CARTESIAN_POINT('Ctrl Pts',(6.09949678676486,0.26035984028865,4.53406826097581));
#53262=CARTESIAN_POINT('Ctrl Pts',(6.10671605409073,0.179637418414302,4.5734203814938));
#53263=CARTESIAN_POINT('Ctrl Pts',(6.11393532141662,0.0897989573399868,
4.59407340590587));
#53264=CARTESIAN_POINT('Ctrl Pts',(6.12115458874249,-9.50793186244619E-6,
4.59413936148612));
#53265=CARTESIAN_POINT('Origin',(4.,0.,4.));
#53266=CARTESIAN_POINT('',(6.52884541125757,2.61457539729726E-5,4.59508370962656));
#53267=CARTESIAN_POINT('',(6.42115458874249,-0.000630941829811112,4.59394485456974));
#53268=CARTESIAN_POINT('',(4.,-7.27562663373442E-17,4.5941));
#53269=CARTESIAN_POINT('Ctrl Pts',(6.52884541125757,2.61457539729726E-5,
4.59508370962656));
#53270=CARTESIAN_POINT('Ctrl Pts',(6.5129582963415,0.196771080344787,4.59506033873941));
#53271=CARTESIAN_POINT('Ctrl Pts',(6.49707118142544,0.393450480974957,4.48779253427891));
#53272=CARTESIAN_POINT('Ctrl Pts',(6.48118406650938,0.500111739713094,4.32240987211318));
#53273=CARTESIAN_POINT('Ctrl Pts',(6.46527878782176,0.606894944490356,4.15683812760557));
#53274=CARTESIAN_POINT('Ctrl Pts',(6.44937350913416,0.623454053851315,3.93301856375293));
#53275=CARTESIAN_POINT('Ctrl Pts',(6.43346823044654,0.541809843535619,3.75368369989414));
#53276=CARTESIAN_POINT('Ctrl Pts',(6.41756295175893,0.460165633219924,3.57434883603535));
#53277=CARTESIAN_POINT('Ctrl Pts',(6.40165767307132,0.280318103227576,3.43949867217041));
#53278=CARTESIAN_POINT('Ctrl Pts',(6.3857523943837,0.085604811340831,3.41110814665827));
#53279=CARTESIAN_POINT('Ctrl Pts',(6.36984711569609,-0.109108480545914,
3.38271762114613));
#53280=CARTESIAN_POINT('Ctrl Pts',(6.35394183700848,-0.318687534327053,
3.46078673398678));
#53281=CARTESIAN_POINT('Ctrl Pts',(6.33803655832087,-0.448733343985475,
3.60951691634857));
#53282=CARTESIAN_POINT('Ctrl Pts',(6.33008391897706,-0.513756248814686,
3.68388200752946));
#53283=CARTESIAN_POINT('Ctrl Pts',(6.32213127963325,-0.558895842613217,
3.77591236609064));
#53284=CARTESIAN_POINT('Ctrl Pts',(6.31417864028945,-0.579995970841135,
3.87270290659392));
#53285=CARTESIAN_POINT('Ctrl Pts',(6.30622600094564,-0.601096099069052,
3.9694934470972));
#53286=CARTESIAN_POINT('Ctrl Pts',(6.29827336160184,-0.598156761726356,
4.07104416954258));
#53287=CARTESIAN_POINT('Ctrl Pts',(6.29032072225803,-0.570614590620327,
4.16591643177432));
#53288=CARTESIAN_POINT('Ctrl Pts',(6.28236808291422,-0.543072419514299,
4.26078869400605));
#53289=CARTESIAN_POINT('Ctrl Pts',(6.27441544357042,-0.490927414644939,
4.34898249602413));
#53290=CARTESIAN_POINT('Ctrl Pts',(6.26646280422661,-0.421087730399527,
4.41916768405122));
#53291=CARTESIAN_POINT('Ctrl Pts',(6.2585101648828,-0.351248046154114,4.48935287207832));
#53292=CARTESIAN_POINT('Ctrl Pts',(6.250557525539,-0.263713682532649,4.54152944611444));
#53293=CARTESIAN_POINT('Ctrl Pts',(6.24260488619519,-0.168899197391682,
4.5696117428605));
#53294=CARTESIAN_POINT('Ctrl Pts',(6.23801839454932,-0.114217245248871,
4.58580752565092));
#53295=CARTESIAN_POINT('Ctrl Pts',(6.23343190290344,-0.0571138332845632,
4.59398924930378));
#53296=CARTESIAN_POINT('Ctrl Pts',(6.22884541125756,-1.27841859475647E-5,
4.5940334609955));
#53297=CARTESIAN_POINT('Ctrl Pts',(6.12115458874249,-9.50793186244619E-6,
4.59413936148612));
#53298=CARTESIAN_POINT('Ctrl Pts',(6.12188796076042,-0.00913273504488762,
4.59414606160884));
#53299=CARTESIAN_POINT('Ctrl Pts',(6.12262133277835,-0.0182556526135436,
4.59394031163173));
#53300=CARTESIAN_POINT('Ctrl Pts',(6.12335470479628,-0.0273686726716501,
4.59352013235631));
#53301=CARTESIAN_POINT('Ctrl Pts',(6.13130734414009,-0.126189680404606,
4.58896373511797));
#53302=CARTESIAN_POINT('Ctrl Pts',(6.13925998348389,-0.223846830455152,
4.55919239267511));
#53303=CARTESIAN_POINT('Ctrl Pts',(6.14721262282769,-0.308403173896691,
4.50784224986958));
#53304=CARTESIAN_POINT('Ctrl Pts',(6.1551652621715,-0.392959517338232,4.45649210706404));
#53305=CARTESIAN_POINT('Ctrl Pts',(6.16311790151532,-0.464415054170765,
4.38356316389581));
#53306=CARTESIAN_POINT('Ctrl Pts',(6.17107054085912,-0.514027768136376,
4.29797916579711));
#53307=CARTESIAN_POINT('Ctrl Pts',(6.17902318020293,-0.563640482101988,
4.2123951676984));
#53308=CARTESIAN_POINT('Ctrl Pts',(6.18697581954673,-0.591410373200678,
4.11415611466921));
#53309=CARTESIAN_POINT('Ctrl Pts',(6.19492845889053,-0.593952774873424,
4.0152594949342));
#53310=CARTESIAN_POINT('Ctrl Pts',(6.20288109823434,-0.59649517654617,3.9163628751992));
#53311=CARTESIAN_POINT('Ctrl Pts',(6.21083373757815,-0.573810088792972,
3.81680868875837));
#53312=CARTESIAN_POINT('Ctrl Pts',(6.21878637692196,-0.528651094032059,
3.72879442104321));
#53313=CARTESIAN_POINT('Ctrl Pts',(6.22673901626577,-0.483492099271145,
3.64078015332805));
#53314=CARTESIAN_POINT('Ctrl Pts',(6.23469165560957,-0.415859197502516,
3.56430580433857));
#53315=CARTESIAN_POINT('Ctrl Pts',(6.24264429495337,-0.334059153459168,
3.50867301156809));
#53316=CARTESIAN_POINT('Ctrl Pts',(6.25059693429718,-0.252259109415819,
3.45304021879761));
#53317=CARTESIAN_POINT('Ctrl Pts',(6.25854957364099,-0.156291923097747,
3.41824898224614));
#53318=CARTESIAN_POINT('Ctrl Pts',(6.2665022129848,-0.057819682214149,3.40864436538418));
#53319=CARTESIAN_POINT('Ctrl Pts',(6.2744548523286,0.0406525586694487,3.39903974852221));
#53320=CARTESIAN_POINT('Ctrl Pts',(6.28240749167241,0.141629854118573,3.41462175134974));
#53321=CARTESIAN_POINT('Ctrl Pts',(6.29036013101621,0.232632044389671,3.453312878872));
#53322=CARTESIAN_POINT('Ctrl Pts',(6.29831277036002,0.323634234660771,3.49200400639426));
#53323=CARTESIAN_POINT('Ctrl Pts',(6.30626540970382,0.404661319753841,3.55380425861124));
#53324=CARTESIAN_POINT('Ctrl Pts',(6.31421804904763,0.466059055789261,3.63148218419904));
#53325=CARTESIAN_POINT('Ctrl Pts',(6.32217068839144,0.527456791824679,3.70916010978684));
#53326=CARTESIAN_POINT('Ctrl Pts',(6.33012332773525,0.569225178802449,3.80271570874544));
#53327=CARTESIAN_POINT('Ctrl Pts',(6.33807596707905,0.585790493249255,3.90010619949006));
#53328=CARTESIAN_POINT('Ctrl Pts',(6.34602860642286,0.602355807696062,3.99749669023468));
#53329=CARTESIAN_POINT('Ctrl Pts',(6.35398124576666,0.593718049611903,4.09872207276531));
#53330=CARTESIAN_POINT('Ctrl Pts',(6.36193388511047,0.56173881546021,4.19248215342453));
#53331=CARTESIAN_POINT('Ctrl Pts',(6.36988652445427,0.529759581308516,4.28624223408375));
#53332=CARTESIAN_POINT('Ctrl Pts',(6.37783916379808,0.474438871089287,4.37253701287156));
#53333=CARTESIAN_POINT('Ctrl Pts',(6.38579180314189,0.401374624788453,4.4390182948332));
#53334=CARTESIAN_POINT('Ctrl Pts',(6.39757939834209,0.293077024234899,4.53755846574697));
#53335=CARTESIAN_POINT('Ctrl Pts',(6.40936699354229,0.145797072855576,4.59256860517148));
#53336=CARTESIAN_POINT('Ctrl Pts',(6.42115458874249,-0.000630941829811112,
4.59394485456974));
#53337=CARTESIAN_POINT('Origin',(4.,0.,4.));
#53338=CARTESIAN_POINT('',(6.82884541125756,0.000528213615369061,4.5937871332276));
#53339=CARTESIAN_POINT('',(6.72115458874249,0.000109070110168276,4.59505938903171));
#53340=CARTESIAN_POINT('',(4.,-7.27562663373442E-17,4.5941));
#53341=CARTESIAN_POINT('Ctrl Pts',(6.82884541125756,0.000528213615369061,
4.5937871332276));
#53342=CARTESIAN_POINT('Ctrl Pts',(6.82429524715479,0.0572034606387535,
4.59426930340541));
#53343=CARTESIAN_POINT('Ctrl Pts',(6.81974508305202,0.113754426020979,4.58681959872387));
#53344=CARTESIAN_POINT('Ctrl Pts',(6.81519491894924,0.167823213394864,4.57092612439125));
#53345=CARTESIAN_POINT('Ctrl Pts',(6.79928964026163,0.356822799356826,4.51536985589957));
#53346=CARTESIAN_POINT('Ctrl Pts',(6.78338436157403,0.515493156338912,4.35664088088147));
#53347=CARTESIAN_POINT('Ctrl Pts',(6.76747908288642,0.570983871223461,4.16762126762428));
#53348=CARTESIAN_POINT('Ctrl Pts',(6.7515738041988,0.626474586108011,3.97860165436708));
#53349=CARTESIAN_POINT('Ctrl Pts',(6.73566852551118,0.578785658895023,3.75929140287077));
#53350=CARTESIAN_POINT('Ctrl Pts',(6.71976324682357,0.449805704301045,3.61038767491097));
#53351=CARTESIAN_POINT('Ctrl Pts',(6.70385796813595,0.320825749707067,3.46148394695116));
#53352=CARTESIAN_POINT('Ctrl Pts',(6.68795268944834,0.110554767732096,3.38298674252784));
#53353=CARTESIAN_POINT('Ctrl Pts',(6.67204741076073,-0.0844443642884844,
3.4109402193496));
#53354=CARTESIAN_POINT('Ctrl Pts',(6.65614213207312,-0.279443496309066,
3.43889369617135));
#53355=CARTESIAN_POINT('Ctrl Pts',(6.64023685338551,-0.459170778375258,
3.57329785423817));
#53356=CARTESIAN_POINT('Ctrl Pts',(6.6243315746979,-0.541132009270427,3.75243704050979));
#53357=CARTESIAN_POINT('Ctrl Pts',(6.60842629601029,-0.623093240165596,
3.9315762267814));
#53358=CARTESIAN_POINT('Ctrl Pts',(6.59252101732267,-0.60728841988974,4.15545044125781));
#53359=CARTESIAN_POINT('Ctrl Pts',(6.57661573863506,-0.500919754058047,
4.32127168369798));
#53360=CARTESIAN_POINT('Ctrl Pts',(6.56069229617589,-0.394429615589227,
4.48728229340579));
#53361=CARTESIAN_POINT('Ctrl Pts',(6.54476885371673,-0.197168666623305,
4.59510713395368));
#53362=CARTESIAN_POINT('Ctrl Pts',(6.52884541125757,2.61457539729726E-5,
4.59508370962656));
#53363=CARTESIAN_POINT('Ctrl Pts',(6.42115458874249,-0.000630941829811112,
4.59394485456974));
#53364=CARTESIAN_POINT('Ctrl Pts',(6.4252722722299,-0.0517816819022344,
4.59442561076518));
#53365=CARTESIAN_POINT('Ctrl Pts',(6.42938995571731,-0.102828462800867,
4.58836159088269));
#53366=CARTESIAN_POINT('Ctrl Pts',(6.43350763920472,-0.152073274319339,
4.5753220992581));
#53367=CARTESIAN_POINT('Ctrl Pts',(6.44941291789233,-0.342290043897387,
4.52495476314113));
#53368=CARTESIAN_POINT('Ctrl Pts',(6.46531819657995,-0.5056209461254,4.37051151428857));
#53369=CARTESIAN_POINT('Ctrl Pts',(6.48122347526756,-0.56632363157735,4.18304963962536));
#53370=CARTESIAN_POINT('Ctrl Pts',(6.49712875395518,-0.627026317029301,
3.99558776496215));
#53371=CARTESIAN_POINT('Ctrl Pts',(6.51303403264279,-0.58510078570519,3.77510726448829));
#53372=CARTESIAN_POINT('Ctrl Pts',(6.5289393113304,-0.460166914262479,3.62276494217392));
#53373=CARTESIAN_POINT('Ctrl Pts',(6.54484459001801,-0.335233042819767,
3.47042261985956));
#53374=CARTESIAN_POINT('Ctrl Pts',(6.56074986870563,-0.127290831258456,
3.38621847570468));
#53375=CARTESIAN_POINT('Ctrl Pts',(6.57665514739324,0.068373869747762,3.4088573345089));
#53376=CARTESIAN_POINT('Ctrl Pts',(6.59256042608085,0.26403857075398,3.43149619331313));
#53377=CARTESIAN_POINT('Ctrl Pts',(6.60846570476847,0.447425761205104,3.56097805507645));
#53378=CARTESIAN_POINT('Ctrl Pts',(6.62437098345608,0.534230294511761,3.73782813427527));
#53379=CARTESIAN_POINT('Ctrl Pts',(6.64027626214369,0.621034827818418,3.91467821347409));
#53380=CARTESIAN_POINT('Ctrl Pts',(6.65618154083131,0.611256703980608,4.1388965101084));
#53381=CARTESIAN_POINT('Ctrl Pts',(6.67208681951892,0.509439333868548,4.30754322537844));
#53382=CARTESIAN_POINT('Ctrl Pts',(6.68799209820653,0.40762196375649,4.47618994064847));
#53383=CARTESIAN_POINT('Ctrl Pts',(6.70389737689414,0.213765347370184,4.58926507455422));
#53384=CARTESIAN_POINT('Ctrl Pts',(6.71980265558175,0.016851802420978,4.59484308232941));
#53385=CARTESIAN_POINT('Ctrl Pts',(6.72025329996867,0.0112726493937942,
4.59500112406784));
#53386=CARTESIAN_POINT('Ctrl Pts',(6.72070394435558,0.00569104238866241,
4.59507287148453));
#53387=CARTESIAN_POINT('Ctrl Pts',(6.72115458874249,0.000109070110168276,
4.59505938903171));
#53388=CARTESIAN_POINT('Origin',(4.,0.,4.));
#53389=CARTESIAN_POINT('',(7.12884541125757,-0.000233413975479213,4.59320261234329));
#53390=CARTESIAN_POINT('',(7.02115458874249,0.000491936389841303,4.5936290357477));
#53391=CARTESIAN_POINT('',(4.,-7.27562663373442E-17,4.5941));
#53392=CARTESIAN_POINT('Ctrl Pts',(7.12884541125757,-0.000233413975479213,
4.59320261234329));
#53393=CARTESIAN_POINT('Ctrl Pts',(7.11972691928047,0.113624805666132,4.59280158872514));
#53394=CARTESIAN_POINT('Ctrl Pts',(7.11060842730338,0.227688545642871,4.56127879346404));
#53395=CARTESIAN_POINT('Ctrl Pts',(7.10148993532628,0.322592019514134,4.50005536307953));
#53396=CARTESIAN_POINT('Ctrl Pts',(7.08558465663867,0.488131036726243,4.39326405099382));
#53397=CARTESIAN_POINT('Ctrl Pts',(7.06967937795105,0.595374147168556,4.19610732087965));
#53398=CARTESIAN_POINT('Ctrl Pts',(7.05377409926343,0.595079946532544,3.99911121186167));
#53399=CARTESIAN_POINT('Ctrl Pts',(7.03786882057582,0.594785745896532,3.80211510284369));
#53400=CARTESIAN_POINT('Ctrl Pts',(7.02196354188821,0.486954234182196,3.60527961492189));
#53401=CARTESIAN_POINT('Ctrl Pts',(7.0060582632006,0.321096900356496,3.49898325846904));
#53402=CARTESIAN_POINT('Ctrl Pts',(6.99015298451299,0.155239566530797,3.3926869020162));
#53403=CARTESIAN_POINT('Ctrl Pts',(6.97424770582538,-0.0686435894062663,
3.37692967703231));
#53404=CARTESIAN_POINT('Ctrl Pts',(6.95834242713776,-0.247754555527299,
3.45894666907189));
#53405=CARTESIAN_POINT('Ctrl Pts',(6.94243714845015,-0.426865521648332,
3.54096366111146));
#53406=CARTESIAN_POINT('Ctrl Pts',(6.92653186976253,-0.561204297953336,
3.72075487017451));
#53407=CARTESIAN_POINT('Ctrl Pts',(6.91062659107492,-0.589088840804576,
3.91576771430201));
#53408=CARTESIAN_POINT('Ctrl Pts',(6.89472131238731,-0.616973383655816,
4.11078055842951));
#53409=CARTESIAN_POINT('Ctrl Pts',(6.8788160336997,-0.538403693053295,4.32101503762147));
#53410=CARTESIAN_POINT('Ctrl Pts',(6.86291075501209,-0.389454440281117,
4.44994049623482));
#53411=CARTESIAN_POINT('Ctrl Pts',(6.85155564042725,-0.283116420949728,
4.54198310574898));
#53412=CARTESIAN_POINT('Ctrl Pts',(6.8402005258424,-0.140907108175025,4.59258385846765));
#53413=CARTESIAN_POINT('Ctrl Pts',(6.82884541125756,0.000528213615369061,
4.5937871332276));
#53414=CARTESIAN_POINT('Ctrl Pts',(6.72115458874249,0.000109070110168276,
4.59505938903171));
#53415=CARTESIAN_POINT('Ctrl Pts',(6.73660922304319,-0.191322006690816,
4.59459701474307));
#53416=CARTESIAN_POINT('Ctrl Pts',(6.75206385734389,-0.38318268672033,4.49389457135631));
#53417=CARTESIAN_POINT('Ctrl Pts',(6.76751849164459,-0.49122657597837,4.33588597251985));
#53418=CARTESIAN_POINT('Ctrl Pts',(6.78342377033221,-0.60242093591639,4.17326997329048));
#53419=CARTESIAN_POINT('Ctrl Pts',(6.79932904901982,-0.624839182280325,
3.94995709318712));
#53420=CARTESIAN_POINT('Ctrl Pts',(6.81523432770743,-0.548195780923551,
3.76848141254984));
#53421=CARTESIAN_POINT('Ctrl Pts',(6.83113960639504,-0.471552379566775,
3.58700573191256));
#53422=CARTESIAN_POINT('Ctrl Pts',(6.84704488508266,-0.295847330489284,
3.44736725074137));
#53423=CARTESIAN_POINT('Ctrl Pts',(6.86295016377027,-0.101752734572189,
3.41368297698799));
#53424=CARTESIAN_POINT('Ctrl Pts',(6.87885544245788,0.0923418613449005,
3.37999870323461));
#53425=CARTESIAN_POINT('Ctrl Pts',(6.8947607211455,0.304826004101594,3.45226863689903));
#53426=CARTESIAN_POINT('Ctrl Pts',(6.91066599983311,0.438133727661537,3.59730899203965));
#53427=CARTESIAN_POINT('Ctrl Pts',(6.92657127852072,0.571441451221483,3.74234934718029));
#53428=CARTESIAN_POINT('Ctrl Pts',(6.94247655720833,0.625572755584675,3.96016012379713));
#53429=CARTESIAN_POINT('Ctrl Pts',(6.95838183589594,0.57567402069499,4.15073208753033));
#53430=CARTESIAN_POINT('Ctrl Pts',(6.97428711458356,0.525775285805305,4.34130405126353));
#53431=CARTESIAN_POINT('Ctrl Pts',(6.99019239327118,0.371846511662747,4.5046372021131));
#53432=CARTESIAN_POINT('Ctrl Pts',(7.00609767195879,0.184564651688987,4.56573572985967));
#53433=CARTESIAN_POINT('Ctrl Pts',(7.01111664422002,0.125467135782336,4.58501560681028));
#53434=CARTESIAN_POINT('Ctrl Pts',(7.01613561648126,0.0630485115161635,
4.59411554829291));
#53435=CARTESIAN_POINT('Ctrl Pts',(7.02115458874249,0.000491936389841303,
4.5936290357477));
#53436=CARTESIAN_POINT('Origin',(4.,0.,4.));
#53437=CARTESIAN_POINT('',(7.42884541125756,-0.000438237927964824,4.59464495791636));
#53438=CARTESIAN_POINT('',(7.32115458874249,-0.000317338366111653,4.59328419319629));
#53439=CARTESIAN_POINT('',(4.,-7.27562663373442E-17,4.5941));
#53440=CARTESIAN_POINT('Ctrl Pts',(7.42884541125756,-0.000438237927964824,
4.59464495791636));
#53441=CARTESIAN_POINT('Ctrl Pts',(7.41515859140615,0.169409178821721,4.5932420274804));
#53442=CARTESIAN_POINT('Ctrl Pts',(7.40147177155473,0.340360224580004,4.51673272682389));
#53443=CARTESIAN_POINT('Ctrl Pts',(7.38778495170331,0.450965110664874,4.38826722161738));
#53444=CARTESIAN_POINT('Ctrl Pts',(7.37187967301569,0.579497637321094,4.23897909740477));
#53445=CARTESIAN_POINT('Ctrl Pts',(7.35597439432808,0.626535888751401,4.01952688559808));
#53446=CARTESIAN_POINT('Ctrl Pts',(7.34006911564046,0.570481892017836,3.83067375781486));
#53447=CARTESIAN_POINT('Ctrl Pts',(7.32416383695285,0.51442789528427,3.64182063003164));
#53448=CARTESIAN_POINT('Ctrl Pts',(7.30825855826524,0.355281650386831,3.48356658627189));
#53449=CARTESIAN_POINT('Ctrl Pts',(7.29235327957763,0.166116376105148,3.42857518785077));
#53450=CARTESIAN_POINT('Ctrl Pts',(7.27644800089002,-0.023048898176535,
3.37358378942964));
#53451=CARTESIAN_POINT('Ctrl Pts',(7.2605427222024,-0.242233201842457,3.42185503634715));
#53452=CARTESIAN_POINT('Ctrl Pts',(7.24463744351479,-0.390796368104757,
3.5512248149675));
#53453=CARTESIAN_POINT('Ctrl Pts',(7.22873216482718,-0.539359534367058,
3.68059459358785));
#53454=CARTESIAN_POINT('Ctrl Pts',(7.21282688613957,-0.617301563225728,
3.89106290391106));
#53455=CARTESIAN_POINT('Ctrl Pts',(7.19692160745195,-0.588834786584626,
4.08599160058025));
#53456=CARTESIAN_POINT('Ctrl Pts',(7.18101632876434,-0.560368009943526,
4.28092029724944));
#53457=CARTESIAN_POINT('Ctrl Pts',(7.16511105007672,-0.425492427802657,
4.46030938026461));
#53458=CARTESIAN_POINT('Ctrl Pts',(7.14920577138911,-0.24613717474127,4.54179097474357));
#53459=CARTESIAN_POINT('Ctrl Pts',(7.1424189846786,-0.169606239833077,4.57655919310821));
#53460=CARTESIAN_POINT('Ctrl Pts',(7.13563219796808,-0.0849767524450092,
4.59350108952231));
#53461=CARTESIAN_POINT('Ctrl Pts',(7.12884541125757,-0.000233413975479213,
4.59320261234329));
#53462=CARTESIAN_POINT('Ctrl Pts',(7.02115458874249,0.000491936389841303,
4.5936290357477));
#53463=CARTESIAN_POINT('Ctrl Pts',(7.03204089516887,-0.135195214358064,
4.59257377495492));
#53464=CARTESIAN_POINT('Ctrl Pts',(7.04292720159524,-0.271531381894462,
4.54641716720817));
#53465=CARTESIAN_POINT('Ctrl Pts',(7.05381350802162,-0.376033620593693,
4.46121547122365));
#53466=CARTESIAN_POINT('Ctrl Pts',(7.06971878670923,-0.528715087097646,
4.33673278019746));
#53467=CARTESIAN_POINT('Ctrl Pts',(7.08562406539685,-0.613443074300594,
4.1289034935015));
#53468=CARTESIAN_POINT('Ctrl Pts',(7.10152934408446,-0.591314251018945,
3.93315398851514));
#53469=CARTESIAN_POINT('Ctrl Pts',(7.11743462277207,-0.569185427737295,
3.73740448352876));
#53470=CARTESIAN_POINT('Ctrl Pts',(7.13333990145968,-0.440199793971044,
3.55373476025198));
#53471=CARTESIAN_POINT('Ctrl Pts',(7.14924518014729,-0.263582002606135,
3.46647820559892));
#53472=CARTESIAN_POINT('Ctrl Pts',(7.16515045883491,-0.0869642112412332,
3.37922165094586));
#53473=CARTESIAN_POINT('Ctrl Pts',(7.18105573752253,0.137285737722324,3.38837826491652));
#53474=CARTESIAN_POINT('Ctrl Pts',(7.19696101621014,0.306201705590428,3.48974370695041));
#53475=CARTESIAN_POINT('Ctrl Pts',(7.21286629489775,0.47511767345854,3.59110914898431));
#53476=CARTESIAN_POINT('Ctrl Pts',(7.22877157358536,0.588699660231196,3.78468341908144));
#53477=CARTESIAN_POINT('Ctrl Pts',(7.24467685227297,0.594795648982816,3.98158540759));
#53478=CARTESIAN_POINT('Ctrl Pts',(7.26058213096058,0.600891637734436,4.17848739609855));
#53479=CARTESIAN_POINT('Ctrl Pts',(7.2764874096482,0.499501628465021,4.37871710301853));
#53480=CARTESIAN_POINT('Ctrl Pts',(7.29239268833581,0.337179610128186,4.49033751492072));
#53481=CARTESIAN_POINT('Ctrl Pts',(7.30197998847137,0.239335998647354,4.5576194790522));
#53482=CARTESIAN_POINT('Ctrl Pts',(7.31156728860693,0.119353510611835,4.59270637405629));
#53483=CARTESIAN_POINT('Ctrl Pts',(7.32115458874249,-0.000317338366111653,
4.59328419319629));
#53484=CARTESIAN_POINT('Origin',(4.,0.,4.));
#53485=CARTESIAN_POINT('',(7.72884541125757,0.000455182276646732,4.59460030787683));
#53486=CARTESIAN_POINT('',(7.62115458874249,-0.000367422317862595,4.59479267874092));
#53487=CARTESIAN_POINT('',(4.,-7.27562663373442E-17,4.5941));
#53488=CARTESIAN_POINT('Ctrl Pts',(7.72884541125757,0.000455182276646732,
4.59460030787683));
#53489=CARTESIAN_POINT('Ctrl Pts',(7.72649554221944,0.0296217258780686,
4.59484761241511));
#53490=CARTESIAN_POINT('Ctrl Pts',(7.72414567318131,0.0587549042441869,
4.59288776399295));
#53491=CARTESIAN_POINT('Ctrl Pts',(7.72179580414318,0.0875427725731367,
4.58860617484604));
#53492=CARTESIAN_POINT('Ctrl Pts',(7.70589052545556,0.282395788279217,4.55962589232715));
#53493=CARTESIAN_POINT('Ctrl Pts',(7.68998524676794,0.461428877889185,4.42427810603975));
#53494=CARTESIAN_POINT('Ctrl Pts',(7.67407996808033,0.542437620895056,4.24470879335187));
#53495=CARTESIAN_POINT('Ctrl Pts',(7.65817468939272,0.623446363900926,4.065139480664));
#53496=CARTESIAN_POINT('Ctrl Pts',(7.64226941070511,0.606430760302702,3.84134864157567));
#53497=CARTESIAN_POINT('Ctrl Pts',(7.6263641320175,0.499203655448083,3.67609156159133));
#53498=CARTESIAN_POINT('Ctrl Pts',(7.61045885332988,0.391976550593464,3.51083448160699));
#53499=CARTESIAN_POINT('Ctrl Pts',(7.59455357464227,0.19453794448245,3.40411116072664));
#53500=CARTESIAN_POINT('Ctrl Pts',(7.57864829595466,-0.00245670798462758,
3.40492443279829));
#53501=CARTESIAN_POINT('Ctrl Pts',(7.56274301726704,-0.199451360451705,
3.40573770486994));
#53502=CARTESIAN_POINT('Ctrl Pts',(7.54683773857943,-0.396002059274846,
3.5140875698936));
#53503=CARTESIAN_POINT('Ctrl Pts',(7.53093245989182,-0.50186103876401,3.68022435377194));
#53504=CARTESIAN_POINT('Ctrl Pts',(7.51502718120421,-0.607720018253171,
3.84636113765028));
#53505=CARTESIAN_POINT('Ctrl Pts',(7.4991219025166,-0.622887278408357,4.07028484038331));
#53506=CARTESIAN_POINT('Ctrl Pts',(7.48321662382898,-0.540398655351294,
4.24917917107494));
#53507=CARTESIAN_POINT('Ctrl Pts',(7.46731134514137,-0.45791003229423,4.42807350176658));
#53508=CARTESIAN_POINT('Ctrl Pts',(7.45140606645375,-0.277765526024924,
4.56193846041682));
#53509=CARTESIAN_POINT('Ctrl Pts',(7.43550078776614,-0.0826798719492015,
4.58930892143267));
#53510=CARTESIAN_POINT('Ctrl Pts',(7.43328232892995,-0.0554694406452989,
4.59312653709876));
#53511=CARTESIAN_POINT('Ctrl Pts',(7.43106387009376,-0.0279683367079049,
4.5948723550368));
#53512=CARTESIAN_POINT('Ctrl Pts',(7.42884541125756,-0.000438237927964824,
4.59464495791636));
#53513=CARTESIAN_POINT('Ctrl Pts',(7.32115458874249,-0.000317338366111653,
4.59328419319629));
#53514=CARTESIAN_POINT('Ctrl Pts',(7.32747256729455,-0.0791797758050172,
4.59366497286126));
#53515=CARTESIAN_POINT('Ctrl Pts',(7.3337905458466,-0.157906876560309,4.57905936436794));
#53516=CARTESIAN_POINT('Ctrl Pts',(7.34010852439865,-0.230073660466993,
4.54880513582638));
#53517=CARTESIAN_POINT('Ctrl Pts',(7.35601380308626,-0.411750885321067,
4.47264122794544));
#53518=CARTESIAN_POINT('Ctrl Pts',(7.37191908177388,-0.551851307624962,
4.29730229529918));
#53519=CARTESIAN_POINT('Ctrl Pts',(7.38782436046149,-0.586046744500155,
4.10329655692985));
#53520=CARTESIAN_POINT('Ctrl Pts',(7.4037296391491,-0.620242181375348,3.90929081856053));
#53521=CARTESIAN_POINT('Ctrl Pts',(7.41963491783671,-0.548532632821828,
3.69661827446815));
#53522=CARTESIAN_POINT('Ctrl Pts',(7.43554019652432,-0.403844087697925,
3.56292915991696));
#53523=CARTESIAN_POINT('Ctrl Pts',(7.45144547521194,-0.259155542574025,
3.42924004536577));
#53524=CARTESIAN_POINT('Ctrl Pts',(7.46735075389955,-0.0414880008797467,
3.37453436035576));
#53525=CARTESIAN_POINT('Ctrl Pts',(7.48325603258717,0.149214809903968,3.42393064079835));
#53526=CARTESIAN_POINT('Ctrl Pts',(7.49916131127478,0.339917620687686,3.47332692124094));
#53527=CARTESIAN_POINT('Ctrl Pts',(7.51506658996239,0.50365570056084,3.62682516713614));
#53528=CARTESIAN_POINT('Ctrl Pts',(7.53097186865001,0.56524745100941,3.81394547807041));
#53529=CARTESIAN_POINT('Ctrl Pts',(7.54687714733762,0.626839201457978,4.00106578900469));
#53530=CARTESIAN_POINT('Ctrl Pts',(7.56278242602523,0.58628462248197,4.22180816497804));
#53531=CARTESIAN_POINT('Ctrl Pts',(7.57868770471284,0.462204660718925,4.3748170457164));
#53532=CARTESIAN_POINT('Ctrl Pts',(7.59284333272272,0.351774041004839,4.51099427596058));
#53533=CARTESIAN_POINT('Ctrl Pts',(7.60699896073261,0.175183620117616,4.59352033541115));
#53534=CARTESIAN_POINT('Ctrl Pts',(7.62115458874249,-0.000367422317862596,
4.59479267874092));
#53535=CARTESIAN_POINT('Origin',(4.,0.,4.));
#53536=CARTESIAN_POINT('',(8.02884541125756,0.000208508845897126,4.59318438507865));
#53537=CARTESIAN_POINT('',(7.92115458874249,0.000504499356536197,4.59443266285439));
#53538=CARTESIAN_POINT('',(4.,-7.27562663373442E-17,4.5941));
#53539=CARTESIAN_POINT('Ctrl Pts',(8.02884541125756,0.000208508845897126,
4.59318438507865));
#53540=CARTESIAN_POINT('Ctrl Pts',(8.02192721434511,0.0865993248636432,
4.5934556945658));
#53541=CARTESIAN_POINT('Ctrl Pts',(8.01500901743265,0.17288466952141,4.57582457789876));
#53542=CARTESIAN_POINT('Ctrl Pts',(8.0080908205202,0.250602156771344,4.53974023855861));
#53543=CARTESIAN_POINT('Ctrl Pts',(7.99218554183259,0.42927852421987,4.4567805482338));
#53544=CARTESIAN_POINT('Ctrl Pts',(7.97628026314498,0.562668370741438,4.27628395749428));
#53545=CARTESIAN_POINT('Ctrl Pts',(7.96037498445736,0.589524722071826,4.08112686462655));
#53546=CARTESIAN_POINT('Ctrl Pts',(7.94446970576975,0.616381073402214,3.88596977175883));
#53547=CARTESIAN_POINT('Ctrl Pts',(7.92856442708213,0.536703929541425,3.67615217676291));
#53548=CARTESIAN_POINT('Ctrl Pts',(7.91265914839452,0.387077664089382,3.54801344261061));
#53549=CARTESIAN_POINT('Ctrl Pts',(7.89675386970691,0.237451398637336,3.41987470845831));
#53550=CARTESIAN_POINT('Ctrl Pts',(7.88084859101929,0.0178760115940344,
3.37341483514963));
#53551=CARTESIAN_POINT('Ctrl Pts',(7.86494331233168,-0.170828768780714,
3.42996623095257));
#53552=CARTESIAN_POINT('Ctrl Pts',(7.84903803364407,-0.359533549155462,
3.48651762675552));
#53553=CARTESIAN_POINT('Ctrl Pts',(7.83313275495647,-0.517367722861657,
3.64608029167009));
#53554=CARTESIAN_POINT('Ctrl Pts',(7.81722747626885,-0.571860514742998,
3.83538980050754));
#53555=CARTESIAN_POINT('Ctrl Pts',(7.80132219758124,-0.626353306624339,
4.02469930934499));
#53556=CARTESIAN_POINT('Ctrl Pts',(7.78541691889362,-0.577504716680827,
4.24375566210532));
#53557=CARTESIAN_POINT('Ctrl Pts',(7.769511640206,-0.447743950807975,4.3919774491103));
#53558=CARTESIAN_POINT('Ctrl Pts',(7.75595623055652,-0.337154229471824,
4.51830073342946));
#53559=CARTESIAN_POINT('Ctrl Pts',(7.74240082090705,-0.16779438404434,4.593173711641));
#53560=CARTESIAN_POINT('Ctrl Pts',(7.72884541125757,0.000455182276646732,
4.59460030787683));
#53561=CARTESIAN_POINT('Ctrl Pts',(7.62115458874249,-0.000367422317862596,
4.59479267874092));
#53562=CARTESIAN_POINT('Ctrl Pts',(7.62290423942022,-0.022065717876263,
4.59494994172972));
#53563=CARTESIAN_POINT('Ctrl Pts',(7.62465389009795,-0.043748134618359,
4.59386587358433));
#53564=CARTESIAN_POINT('Ctrl Pts',(7.62640354077568,-0.0652877816099521,
4.59148835294282));
#53565=CARTESIAN_POINT('Ctrl Pts',(7.64230881946329,-0.261094917625702,
4.56987539392751));
#53566=CARTESIAN_POINT('Ctrl Pts',(7.6582140981509,-0.445103845107109,4.44137409039354));
#53567=CARTESIAN_POINT('Ctrl Pts',(7.67411937683852,-0.532825449416136,
4.2649868044631));
#53568=CARTESIAN_POINT('Ctrl Pts',(7.69002465552613,-0.620547053725161,
4.08859951853267));
#53569=CARTESIAN_POINT('Ctrl Pts',(7.70592993421374,-0.611981334861803,
3.86432625020577));
#53570=CARTESIAN_POINT('Ctrl Pts',(7.72183521290136,-0.511061308497056,
3.69514379608856));
#53571=CARTESIAN_POINT('Ctrl Pts',(7.73774049158897,-0.410141282132307,
3.52596134197134));
#53572=CARTESIAN_POINT('Ctrl Pts',(7.75364577027658,-0.216866948266163,
3.4118697020638));
#53573=CARTESIAN_POINT('Ctrl Pts',(7.76955104896419,-0.0199817042712483,
3.40525493058698));
#53574=CARTESIAN_POINT('Ctrl Pts',(7.78545632765181,0.176903539723664,3.39864015911017));
#53575=CARTESIAN_POINT('Ctrl Pts',(7.80136160633942,0.377399693847348,3.49950225606407));
#53576=CARTESIAN_POINT('Ctrl Pts',(7.81726688502703,0.489447406431712,3.66152961365368));
#53577=CARTESIAN_POINT('Ctrl Pts',(7.83317216371464,0.601495119016078,3.82355697124329));
#53578=CARTESIAN_POINT('Ctrl Pts',(7.84907744240226,0.625094390061116,4.04674958946861));
#53579=CARTESIAN_POINT('Ctrl Pts',(7.86498272108987,0.549409432699027,4.22862686054007));
#53580=CARTESIAN_POINT('Ctrl Pts',(7.88088799977748,0.473724475336938,4.41050413161152));
#53581=CARTESIAN_POINT('Ctrl Pts',(7.89679327846509,0.298755289567731,4.55106605552911));
#53582=CARTESIAN_POINT('Ctrl Pts',(7.91269855715271,0.104840323164387,4.58577254351526));
#53583=CARTESIAN_POINT('Ctrl Pts',(7.9155172343493,0.0704753991278659,4.59192310448195));
#53584=CARTESIAN_POINT('Ctrl Pts',(7.91833591154589,0.0355154700816755,
4.59474920414003));
#53585=CARTESIAN_POINT('Ctrl Pts',(7.92115458874249,0.000504499356536197,
4.59443266285439));
#53586=CARTESIAN_POINT('Origin',(4.,0.,4.));
#53587=CARTESIAN_POINT('',(8.32884541125757,-0.000534402448739424,4.5938336238991));
#53588=CARTESIAN_POINT('',(8.2211545887425,0.000116005647334215,4.59313666129657));
#53589=CARTESIAN_POINT('',(4.,-7.27562663373442E-17,4.5941));
#53590=CARTESIAN_POINT('Ctrl Pts',(8.32884541125757,-0.000534402448739424,
4.5938336238991));
#53591=CARTESIAN_POINT('Ctrl Pts',(8.31735888647079,0.142509087977489,4.59259298046846));
#53592=CARTESIAN_POINT('Ctrl Pts',(8.30587236168401,0.286359812054371,4.54070236535691));
#53593=CARTESIAN_POINT('Ctrl Pts',(8.29438583689723,0.393155811111917,4.44670960845581));
#53594=CARTESIAN_POINT('Ctrl Pts',(8.27848055820962,0.541035187969857,4.31655875596735));
#53595=CARTESIAN_POINT('Ctrl Pts',(8.262575279522,0.617867056310918,4.10568264439756));
#53596=CARTESIAN_POINT('Ctrl Pts',(8.24667000083439,0.588373472681163,3.91090666274675));
#53597=CARTESIAN_POINT('Ctrl Pts',(8.23076472214677,0.558879889051408,3.71613068109593));
#53598=CARTESIAN_POINT('Ctrl Pts',(8.21485944345917,0.423060853450833,3.53745482936408));
#53599=CARTESIAN_POINT('Ctrl Pts',(8.19895416477155,0.243278720997716,3.45691949951456));
#53600=CARTESIAN_POINT('Ctrl Pts',(8.18304888608394,0.0634965885445972,
3.37638416966503));
#53601=CARTESIAN_POINT('Ctrl Pts',(8.16714360739632,-0.160248640761069,
3.39398936169784));
#53602=CARTESIAN_POINT('Ctrl Pts',(8.15123832870871,-0.325222623502191,
3.50165151624576));
#53603=CARTESIAN_POINT('Ctrl Pts',(8.1353330500211,-0.490196606243315,3.60931367079368));
#53604=CARTESIAN_POINT('Ctrl Pts',(8.11942777133349,-0.59639934241989,3.80703278785672));
#53605=CARTESIAN_POINT('Ctrl Pts',(8.10352249264588,-0.595067028646789,
4.00402461368555));
#53606=CARTESIAN_POINT('Ctrl Pts',(8.08761721395827,-0.593734714873688,
4.20101643951437));
#53607=CARTESIAN_POINT('Ctrl Pts',(8.07171193527065,-0.484867351150922,
4.39728097410898));
#53608=CARTESIAN_POINT('Ctrl Pts',(8.05580665658303,-0.3184522251018,4.50270184645125));
#53609=CARTESIAN_POINT('Ctrl Pts',(8.04681957480788,-0.224421408301879,
4.56226861162124));
#53610=CARTESIAN_POINT('Ctrl Pts',(8.03783249303272,-0.112017456676448,
4.59283194056482));
#53611=CARTESIAN_POINT('Ctrl Pts',(8.02884541125756,0.000208508845897126,
4.59318438507865));
#53612=CARTESIAN_POINT('Ctrl Pts',(7.92115458874249,0.000504499356536197,
4.59443266285439));
#53613=CARTESIAN_POINT('Ctrl Pts',(7.93424119023351,-0.162045019349314,
4.59296301969496));
#53614=CARTESIAN_POINT('Ctrl Pts',(7.94732779172453,-0.325694779556815,
4.52375140444135));
#53615=CARTESIAN_POINT('Ctrl Pts',(7.96041439321555,-0.436005268305889,
4.40499428651169));
#53616=CARTESIAN_POINT('Ctrl Pts',(7.97631967190316,-0.570075146335334,
4.26065848946726));
#53617=CARTESIAN_POINT('Ctrl Pts',(7.99222495059077,-0.625354155356748,
4.04313584332371));
#53618=CARTESIAN_POINT('Ctrl Pts',(8.00813022927838,-0.576460513088508,
3.85230354456612));
#53619=CARTESIAN_POINT('Ctrl Pts',(8.024035507966,-0.527566870820267,3.66147124580852));
#53620=CARTESIAN_POINT('Ctrl Pts',(8.03994078665361,-0.374500577262366,
3.49732929443689));
#53621=CARTESIAN_POINT('Ctrl Pts',(8.05584606534123,-0.187543198716277,
3.43524473024767));
#53622=CARTESIAN_POINT('Ctrl Pts',(8.07175134402884,-0.000585820170193818,
3.37316016605846));
#53623=CARTESIAN_POINT('Ctrl Pts',(8.08765662271645,0.220262643364076,3.41313298905166));
#53624=CARTESIAN_POINT('Ctrl Pts',(8.10356190140406,0.37359792075985,3.53680937001953));
#53625=CARTESIAN_POINT('Ctrl Pts',(8.11946718009167,0.526933198155627,3.66048575098741));
#53626=CARTESIAN_POINT('Ctrl Pts',(8.13537245877928,0.612755289412907,3.86786568992997));
#53627=CARTESIAN_POINT('Ctrl Pts',(8.1512777374669,0.591658321059451,4.06372909240644));
#53628=CARTESIAN_POINT('Ctrl Pts',(8.16718301615451,0.570561352705995,4.2595924948829));
#53629=CARTESIAN_POINT('Ctrl Pts',(8.18308829484212,0.44254532474181,4.44393936089328));
#53630=CARTESIAN_POINT('Ctrl Pts',(8.19899357352974,0.266389781296621,4.53212540863836));
#53631=CARTESIAN_POINT('Ctrl Pts',(8.20638057860065,0.184576572093718,4.57308230066594));
#53632=CARTESIAN_POINT('Ctrl Pts',(8.21376758367158,0.0923795717789203,
4.59329710918813));
#53633=CARTESIAN_POINT('Ctrl Pts',(8.2211545887425,0.000116005647334215,
4.59313666129657));
#53634=CARTESIAN_POINT('Origin',(4.,0.,4.));
#53635=CARTESIAN_POINT('',(8.62884541125757,3.48566139269993E-5,4.59507810043999));
#53636=CARTESIAN_POINT('',(8.5211545887425,-0.000547905086566465,4.594005652201));
#53637=CARTESIAN_POINT('',(4.,-7.27562663373442E-17,4.5941));
#53638=CARTESIAN_POINT('Ctrl Pts',(8.62884541125757,3.48566139269993E-5,
4.59507810043999));
#53639=CARTESIAN_POINT('Ctrl Pts',(8.62869583728408,0.00188744051982823,
4.59507966949126));
#53640=CARTESIAN_POINT('Ctrl Pts',(8.62854626331059,0.00374001065808006,
4.59507176912216));
#53641=CARTESIAN_POINT('Ctrl Pts',(8.6283966893371,0.00559249142073073,
4.59505435897699));
#53642=CARTESIAN_POINT('Ctrl Pts',(8.61249141064948,0.202580123064263,4.59320301275402));
#53643=CARTESIAN_POINT('Ctrl Pts',(8.59658613196187,0.398557131004382,4.48381890612783));
#53644=CARTESIAN_POINT('Ctrl Pts',(8.58068085327426,0.503539164298441,4.31712659320126));
#53645=CARTESIAN_POINT('Ctrl Pts',(8.56477557458664,0.608521197592498,4.15043428027469));
#53646=CARTESIAN_POINT('Ctrl Pts',(8.54887029589904,0.622508256240502,3.92643376104774));
#53647=CARTESIAN_POINT('Ctrl Pts',(8.53296501721142,0.539078074654942,3.74797659726896));
#53648=CARTESIAN_POINT('Ctrl Pts',(8.51705973852381,0.455647893069379,3.56951943349019));
#53649=CARTESIAN_POINT('Ctrl Pts',(8.50115445983619,0.274800471250253,3.43660562515959));
#53650=CARTESIAN_POINT('Ctrl Pts',(8.48524918114857,0.0795732942734406,
3.41026356994308));
#53651=CARTESIAN_POINT('Ctrl Pts',(8.46934390246096,-0.115653882703369,
3.38392151472657));
#53652=CARTESIAN_POINT('Ctrl Pts',(8.45343862377335,-0.32526081483786,3.46415121262414));
#53653=CARTESIAN_POINT('Ctrl Pts',(8.43753334508574,-0.453004866631874,
3.61411458059983));
#53654=CARTESIAN_POINT('Ctrl Pts',(8.42162806639813,-0.580748918425883,
3.76407794857552));
#53655=CARTESIAN_POINT('Ctrl Pts',(8.40572278771052,-0.626630089879422,
3.98377498662932));
#53656=CARTESIAN_POINT('Ctrl Pts',(8.3898175090229,-0.569581688133314,4.17233010950212));
#53657=CARTESIAN_POINT('Ctrl Pts',(8.37391223033529,-0.512533286387202,
4.36088523237493));
#53658=CARTESIAN_POINT('Ctrl Pts',(8.35800695164768,-0.352555311441432,
4.51829844006673));
#53659=CARTESIAN_POINT('Ctrl Pts',(8.34210167296007,-0.163102881281137,
4.57229224720906));
#53660=CARTESIAN_POINT('Ctrl Pts',(8.33768291905923,-0.110469810133188,
4.58729263485501));
#53661=CARTESIAN_POINT('Ctrl Pts',(8.3332641651584,-0.0555618361628184,
4.59431088730997));
#53662=CARTESIAN_POINT('Ctrl Pts',(8.32884541125757,-0.000534402448739424,
4.5938336238991));
#53663=CARTESIAN_POINT('Ctrl Pts',(8.2211545887425,0.000116005647334215,
4.59313666129657));
#53664=CARTESIAN_POINT('Ctrl Pts',(8.22967286235919,-0.106277085140544,
4.59295164192424));
#53665=CARTESIAN_POINT('Ctrl Pts',(8.23819113597589,-0.212758691085218,
4.56567285125378));
#53666=CARTESIAN_POINT('Ctrl Pts',(8.24670940959258,-0.303508593564514,
4.51186277431583));
#53667=CARTESIAN_POINT('Ctrl Pts',(8.26261468828019,-0.472956366054245,
4.41138886276846));
#53668=CARTESIAN_POINT('Ctrl Pts',(8.2785199669678,-0.587556852107514,4.21841581019395));
#53669=CARTESIAN_POINT('Ctrl Pts',(8.29442524565541,-0.594690356875377,
4.02154867831793));
#53670=CARTESIAN_POINT('Ctrl Pts',(8.31033052434302,-0.60182386164324,3.82468154644191));
#53671=CARTESIAN_POINT('Ctrl Pts',(8.32623580303064,-0.501490385125681,
3.62392033526436));
#53672=CARTESIAN_POINT('Ctrl Pts',(8.34214108171825,-0.339758814980244,
3.51144609945163));
#53673=CARTESIAN_POINT('Ctrl Pts',(8.35804636040587,-0.178027244834812,
3.3989718636389));
#53674=CARTESIAN_POINT('Ctrl Pts',(8.37395163909348,0.0451024189384938,
3.37478460319097));
#53675=CARTESIAN_POINT('Ctrl Pts',(8.38985691778109,0.227178474572579,3.44999008482693));
#53676=CARTESIAN_POINT('Ctrl Pts',(8.4057621964687,0.40925453020667,3.5251955664629));
#53677=CARTESIAN_POINT('Ctrl Pts',(8.42166747515631,0.550276977701535,3.69979379018275));
#53678=CARTESIAN_POINT('Ctrl Pts',(8.43757275384392,0.585494275335268,3.89361663829603));
#53679=CARTESIAN_POINT('Ctrl Pts',(8.45347803253154,0.620711572969,4.0874394864093));
#53680=CARTESIAN_POINT('Ctrl Pts',(8.46938331121915,0.550123720741606,4.30048695891599));
#53681=CARTESIAN_POINT('Ctrl Pts',(8.48528858990677,0.406141674070155,4.4349366697363));
#53682=CARTESIAN_POINT('Ctrl Pts',(8.49724392285201,0.297916389879728,4.53599689564107));
#53683=CARTESIAN_POINT('Ctrl Pts',(8.50919925579725,0.148224117540273,4.59265016978245));
#53684=CARTESIAN_POINT('Ctrl Pts',(8.5211545887425,-0.000547905086566465,
4.594005652201));
#53685=CARTESIAN_POINT('Origin',(4.,0.,4.));
#53686=CARTESIAN_POINT('',(8.92884541125757,0.000516595407308196,4.59372894893997));
#53687=CARTESIAN_POINT('',(8.82115458874249,0.000142235148737217,4.59503945166131));
#53688=CARTESIAN_POINT('',(4.,-7.27562663373442E-17,4.5941));
#53689=CARTESIAN_POINT('Ctrl Pts',(8.92884541125757,0.000516595407308196,
4.59372894893997));
#53690=CARTESIAN_POINT('Ctrl Pts',(8.92412750940976,0.0592956068199462,
4.59421507565108));
#53691=CARTESIAN_POINT('Ctrl Pts',(8.91940960756194,0.117944888069788,4.58619493689145));
#53692=CARTESIAN_POINT('Ctrl Pts',(8.91469170571413,0.17383025386194,4.56912565303288));
#53693=CARTESIAN_POINT('Ctrl Pts',(8.89878642702651,0.362234410233906,4.51158064138869));
#53694=CARTESIAN_POINT('Ctrl Pts',(8.8828811483389,0.519225559109383,4.35118846702123));
#53695=CARTESIAN_POINT('Ctrl Pts',(8.86697586965128,0.572720006672535,4.16159443076672));
#53696=CARTESIAN_POINT('Ctrl Pts',(8.85107059096367,0.626214454235688,3.97200039451221));
#53697=CARTESIAN_POINT('Ctrl Pts',(8.83516531227606,0.576212200486512,3.75320449637065));
#53698=CARTESIAN_POINT('Ctrl Pts',(8.81926003358845,0.445672164925724,3.60566855627755));
#53699=CARTESIAN_POINT('Ctrl Pts',(8.80335475490084,0.315132129364936,3.45813261618446));
#53700=CARTESIAN_POINT('Ctrl Pts',(8.78744947621322,0.104054311992536,3.38185663413984));
#53701=CARTESIAN_POINT('Ctrl Pts',(8.77154419752561,-0.0906432834200916,
3.41186331412789));
#53702=CARTESIAN_POINT('Ctrl Pts',(8.755638918838,-0.285340878832719,3.44186999411594));
#53703=CARTESIAN_POINT('Ctrl Pts',(8.73973364015038,-0.463658252285575,
3.57815933613666));
#53704=CARTESIAN_POINT('Ctrl Pts',(8.72382836146277,-0.543719609875046,
3.75815304026071));
#53705=CARTESIAN_POINT('Ctrl Pts',(8.70792308277515,-0.623780967464517,
3.93814674438476));
#53706=CARTESIAN_POINT('Ctrl Pts',(8.69201780408754,-0.605586309190603,
4.16184481061213));
#53707=CARTESIAN_POINT('Ctrl Pts',(8.67611252539993,-0.497489852380174,
4.32653455081593));
#53708=CARTESIAN_POINT('Ctrl Pts',(8.66035682068581,-0.390409939629295,
4.48967554111606));
#53709=CARTESIAN_POINT('Ctrl Pts',(8.64460111597169,-0.195111159088962,
4.59491282095998));
#53710=CARTESIAN_POINT('Ctrl Pts',(8.62884541125757,3.48566139269993E-5,
4.59507810043999));
#53711=CARTESIAN_POINT('Ctrl Pts',(8.5211545887425,-0.000547905086566465,
4.594005652201));
#53712=CARTESIAN_POINT('Ctrl Pts',(8.52510453448487,-0.0497009834700827,
4.59445349267793));
#53713=CARTESIAN_POINT('Ctrl Pts',(8.52905448022724,-0.0987536084630192,
4.58886509038946));
#53714=CARTESIAN_POINT('Ctrl Pts',(8.53300442596961,-0.146177075786514,
4.57684766499685));
#53715=CARTESIAN_POINT('Ctrl Pts',(8.54890970465722,-0.337137537856201,
4.52845700030318));
#53716=CARTESIAN_POINT('Ctrl Pts',(8.56481498334483,-0.501682220880061,
4.37582372178193));
#53717=CARTESIAN_POINT('Ctrl Pts',(8.58072026203244,-0.564259167724997,
4.18903057354857));
#53718=CARTESIAN_POINT('Ctrl Pts',(8.59662554072005,-0.626836114569933,
4.00223742531521));
#53719=CARTESIAN_POINT('Ctrl Pts',(8.61253081940767,-0.587445325235947,
3.78128440736974));
#53720=CARTESIAN_POINT('Ctrl Pts',(8.62843609809528,-0.464173383698336,
3.62762379780141));
#53721=CARTESIAN_POINT('Ctrl Pts',(8.6443413767829,-0.340901442160722,3.47396318823307));
#53722=CARTESIAN_POINT('Ctrl Pts',(8.66024665547051,-0.133748348419481,
3.38759498704188));
#53723=CARTESIAN_POINT('Ctrl Pts',(8.67615193415812,0.0621699608040676,
3.40817581827756));
#53724=CARTESIAN_POINT('Ctrl Pts',(8.69205721284573,0.25808827002761,3.42875664951325));
#53725=CARTESIAN_POINT('Ctrl Pts',(8.70796249153334,0.44277179473346,3.55628651317581));
#53726=CARTESIAN_POINT('Ctrl Pts',(8.72386777022095,0.531421673692279,3.73220909121499));
#53727=CARTESIAN_POINT('Ctrl Pts',(8.73977304890857,0.620071552651101,3.90813166925417));
#53728=CARTESIAN_POINT('Ctrl Pts',(8.75567832759618,0.612687785862888,4.13244696166997));
#53729=CARTESIAN_POINT('Ctrl Pts',(8.7715836062838,0.512660686655375,4.30215887618246));
#53730=CARTESIAN_POINT('Ctrl Pts',(8.78748888497141,0.412633587447865,4.47187079069495));
#53731=CARTESIAN_POINT('Ctrl Pts',(8.80339416365902,0.21996315582106,4.58697932730413));
#53732=CARTESIAN_POINT('Ctrl Pts',(8.81929944234663,0.0231155027642346,
4.59463151583965));
#53733=CARTESIAN_POINT('Ctrl Pts',(8.81991782447859,0.0154622529370322,
4.59492902566351));
#53734=CARTESIAN_POINT('Ctrl Pts',(8.82053620661054,0.00780268890311657,
4.59506410656044));
#53735=CARTESIAN_POINT('Ctrl Pts',(8.82115458874249,0.000142235148737217,
4.59503945166131));
#53736=CARTESIAN_POINT('Origin',(4.,0.,4.));
#53737=CARTESIAN_POINT('',(9.22884541125756,-0.000264402795292107,4.59322887297718));
#53738=CARTESIAN_POINT('',(9.12115458874249,0.000475196148639644,4.59357609051269));
#53739=CARTESIAN_POINT('',(4.,-7.27562663373442E-17,4.5941));
#53740=CARTESIAN_POINT('Ctrl Pts',(9.22884541125756,-0.000264402795292107,
4.59322887297718));
#53741=CARTESIAN_POINT('Ctrl Pts',(9.21955918153543,0.115675446261185,4.59276508993807));
#53742=CARTESIAN_POINT('Ctrl Pts',(9.21027295181329,0.231857423975292,4.55999255403315));
#53743=CARTESIAN_POINT('Ctrl Pts',(9.20098672209116,0.327844211240712,4.49662776730038));
#53744=CARTESIAN_POINT('Ctrl Pts',(9.18508144340355,0.492248565587605,4.38809775866155));
#53745=CARTESIAN_POINT('Ctrl Pts',(9.16917616471593,0.597407924103304,4.18982173958679));
#53746=CARTESIAN_POINT('Ctrl Pts',(9.15327088602831,0.595037558282966,3.99283966966863));
#53747=CARTESIAN_POINT('Ctrl Pts',(9.1373656073407,0.592667192462628,3.79585759975047));
#53748=CARTESIAN_POINT('Ctrl Pts',(9.12146032865309,0.482767102306254,3.60016947898891));
#53749=CARTESIAN_POINT('Ctrl Pts',(9.10555504996548,0.315798759724268,3.49562701355602));
#53750=CARTESIAN_POINT('Ctrl Pts',(9.08964977127787,0.148830417142278,3.39108454812312));
#53751=CARTESIAN_POINT('Ctrl Pts',(9.07374449259025,-0.0752061778653251,
3.37768773801888));
#53752=CARTESIAN_POINT('Ctrl Pts',(9.05783921390264,-0.253442899077741,
3.46158783167087));
#53753=CARTESIAN_POINT('Ctrl Pts',(9.04193393521502,-0.431679620290152,
3.54548792532286));
#53754=CARTESIAN_POINT('Ctrl Pts',(9.02602865652741,-0.56411646770738,3.72668492273107));
#53755=CARTESIAN_POINT('Ctrl Pts',(9.0101233778398,-0.589944043936388,3.92198082849844));
#53756=CARTESIAN_POINT('Ctrl Pts',(8.99421809915219,-0.615771620165397,
4.11727673426582));
#53757=CARTESIAN_POINT('Ctrl Pts',(8.97831282046457,-0.534989925206181,
4.32667154839236));
#53758=CARTESIAN_POINT('Ctrl Pts',(8.96240754177696,-0.384690495792338,
4.45402003099517));
#53759=CARTESIAN_POINT('Ctrl Pts',(8.95122016493716,-0.278973620993485,
4.54359378149875));
#53760=CARTESIAN_POINT('Ctrl Pts',(8.94003278809737,-0.138863784294423,
4.59257621560968));
#53761=CARTESIAN_POINT('Ctrl Pts',(8.92884541125757,0.000516595407308196,
4.59372894893997));
#53762=CARTESIAN_POINT('Ctrl Pts',(8.82115458874249,0.000142235148737217,
4.59503945166131));
#53763=CARTESIAN_POINT('Ctrl Pts',(8.83644148529816,-0.189230254871984,
4.59442996300828));
#53764=CARTESIAN_POINT('Ctrl Pts',(8.85172838185382,-0.379146468724227,
4.49620311855542));
#53765=CARTESIAN_POINT('Ctrl Pts',(8.86701527840948,-0.487657002993039,
4.34104488491935));
#53766=CARTESIAN_POINT('Ctrl Pts',(8.88292055709709,-0.600556981206626,
4.17961022500168));
#53767=CARTESIAN_POINT('Ctrl Pts',(8.89882583578469,-0.62533206314696,3.95654506470448));
#53768=CARTESIAN_POINT('Ctrl Pts',(8.91473111447231,-0.550606579334316,
3.77427148852754));
#53769=CARTESIAN_POINT('Ctrl Pts',(8.93063639315992,-0.47588109552167,3.5919979123506));
#53770=CARTESIAN_POINT('Ctrl Pts',(8.94654167184753,-0.301655045956043,
3.45051592029392));
#53771=CARTESIAN_POINT('Ctrl Pts',(8.96244695053515,-0.107925661701669,
3.41478805750048));
#53772=CARTESIAN_POINT('Ctrl Pts',(8.97835222922276,0.0858037225526985,
3.37906019470703));
#53773=CARTESIAN_POINT('Ctrl Pts',(8.99425750791037,0.299036441495806,3.4490864611768));
#53774=CARTESIAN_POINT('Ctrl Pts',(9.01016278659798,0.433865051721373,3.5927137579139));
#53775=CARTESIAN_POINT('Ctrl Pts',(9.0260680652856,0.568693661946943,3.736341054651));
#53776=CARTESIAN_POINT('Ctrl Pts',(9.04197334397321,0.625118163454969,3.95356938165542));
#53777=CARTESIAN_POINT('Ctrl Pts',(9.05787862266082,0.577230812276762,4.14465668133936));
#53778=CARTESIAN_POINT('Ctrl Pts',(9.07378390134844,0.529343461098555,4.3357439810233));
#53779=CARTESIAN_POINT('Ctrl Pts',(9.08968918003605,0.377144257234124,4.50069025338676));
#53780=CARTESIAN_POINT('Ctrl Pts',(9.10559445872366,0.190516636080703,4.56375914846174));
#53781=CARTESIAN_POINT('Ctrl Pts',(9.11078116872994,0.129657384941762,4.58432590969837));
#53782=CARTESIAN_POINT('Ctrl Pts',(9.11596787873622,0.0651369761893139,
4.59405891310139));
#53783=CARTESIAN_POINT('Ctrl Pts',(9.12115458874249,0.000475196148639644,
4.59357609051269));
#53784=CARTESIAN_POINT('Origin',(4.,0.,4.));
#53785=CARTESIAN_POINT('',(9.52884541125756,-0.000414715089906426,4.59470005288553));
#53786=CARTESIAN_POINT('',(9.4211545887425,-0.000345133784900094,4.59331940772745));
#53787=CARTESIAN_POINT('',(4.,-7.27562663373442E-17,4.5941));
#53788=CARTESIAN_POINT('Ctrl Pts',(9.52884541125756,-0.000414715089906426,
4.59470005288553));
#53789=CARTESIAN_POINT('Ctrl Pts',(9.5149908536611,0.17147269131647,4.59333531965569));
#53790=CARTESIAN_POINT('Ctrl Pts',(9.50113629606464,0.344448366351018,4.51470554290992));
#53791=CARTESIAN_POINT('Ctrl Pts',(9.48728173846818,0.455032043431697,4.38349290156166));
#53792=CARTESIAN_POINT('Ctrl Pts',(9.47137645978057,0.581984072756561,4.23285845412795));
#53793=CARTESIAN_POINT('Ctrl Pts',(9.45547118109296,0.626706888961734,4.01292269047354));
#53794=CARTESIAN_POINT('Ctrl Pts',(9.43956590240535,0.56866566691212,3.82467080855373));
#53795=CARTESIAN_POINT('Ctrl Pts',(9.42366062371773,0.510624444862503,3.63641892663391));
#53796=CARTESIAN_POINT('Ctrl Pts',(9.40775534503012,0.349819184558098,3.47985092644869));
#53797=CARTESIAN_POINT('Ctrl Pts',(9.39185006634251,0.160084858421151,3.42685620983728));
#53798=CARTESIAN_POINT('Ctrl Pts',(9.37594478765489,-0.0296494677157886,
3.37386149322587));
#53799=CARTESIAN_POINT('Ctrl Pts',(9.36003950896728,-0.248312859685263,
3.42444006018826));
#53800=CARTESIAN_POINT('Ctrl Pts',(9.34413423027966,-0.395504338780113,
3.55536837257802));
#53801=CARTESIAN_POINT('Ctrl Pts',(9.32822895159205,-0.542695817874971,
3.6862966849678));
#53802=CARTESIAN_POINT('Ctrl Pts',(9.31232367290444,-0.618415384095196,
3.89757474278496));
#53803=CARTESIAN_POINT('Ctrl Pts',(9.29641839421683,-0.587895816063128,
4.09219260031737));
#53804=CARTESIAN_POINT('Ctrl Pts',(9.28051311552922,-0.55737624803106,4.28681045784976));
#53805=CARTESIAN_POINT('Ctrl Pts',(9.26460783684159,-0.42061754574671,4.4647681150974));
#53806=CARTESIAN_POINT('Ctrl Pts',(9.24870255815398,-0.240413519515492,
4.54435494461976));
#53807=CARTESIAN_POINT('Ctrl Pts',(9.24208350918851,-0.165420852186184,
4.57747534017911));
#53808=CARTESIAN_POINT('Ctrl Pts',(9.23546446022304,-0.0829041350566004,
4.59355944875842));
#53809=CARTESIAN_POINT('Ctrl Pts',(9.22884541125756,-0.000264402795292107,
4.59322887297718));
#53810=CARTESIAN_POINT('Ctrl Pts',(9.12115458874249,0.000475196148639644,
4.59357609051269));
#53811=CARTESIAN_POINT('Ctrl Pts',(9.13187315742383,-0.133151270259641,
4.59257831599443));
#53812=CARTESIAN_POINT('Ctrl Pts',(9.14259172610516,-0.267381477949042,
4.54795275857003));
#53813=CARTESIAN_POINT('Ctrl Pts',(9.1533102947865,-0.371151898503526,4.46515291500219));
#53814=CARTESIAN_POINT('Ctrl Pts',(9.16921557347411,-0.525136773491911,
4.34228626868117));
#53815=CARTESIAN_POINT('Ctrl Pts',(9.18512085216173,-0.612050485026272,
4.13536145825263));
#53816=CARTESIAN_POINT('Ctrl Pts',(9.20102613084934,-0.591985933785934,
3.93938960239856));
#53817=CARTESIAN_POINT('Ctrl Pts',(9.21693140953695,-0.571921382545595,
3.74341774654449));
#53818=CARTESIAN_POINT('Ctrl Pts',(9.23283668822456,-0.444878568530549,
3.55839884526489));
#53819=CARTESIAN_POINT('Ctrl Pts',(9.24874196691217,-0.269190177198291,
3.46928575052316));
#53820=CARTESIAN_POINT('Ctrl Pts',(9.26464724559978,-0.0935017858660342,
3.38017265578144));
#53821=CARTESIAN_POINT('Ctrl Pts',(9.28055252428739,0.130832182783434,3.38696536757758));
#53822=CARTESIAN_POINT('Ctrl Pts',(9.29645780297501,0.300807061133818,3.48654496003073));
#53823=CARTESIAN_POINT('Ctrl Pts',(9.31236308166262,0.470781939484206,3.58612455248389));
#53824=CARTESIAN_POINT('Ctrl Pts',(9.32826836035024,0.586397727535503,3.77849102559406));
#53825=CARTESIAN_POINT('Ctrl Pts',(9.34417363903785,0.594568546715174,3.97531783326339));
#53826=CARTESIAN_POINT('Ctrl Pts',(9.36007891772546,0.602739365894845,4.17214464093271));
#53827=CARTESIAN_POINT('Ctrl Pts',(9.37598419641307,0.503465216202894,4.37343178316119));
#53828=CARTESIAN_POINT('Ctrl Pts',(9.39188947510069,0.342328587234952,4.48675671999422));
#53829=CARTESIAN_POINT('Ctrl Pts',(9.40164451298129,0.243500144778355,4.55626125828842));
#53830=CARTESIAN_POINT('Ctrl Pts',(9.41139955086189,0.121401365174849,4.59267772446372));
#53831=CARTESIAN_POINT('Ctrl Pts',(9.4211545887425,-0.000345133784900094,
4.59331940772745));
#53832=CARTESIAN_POINT('Origin',(4.,0.,4.));
#53833=CARTESIAN_POINT('',(9.82884541125756,0.000474857175501747,4.59454166667424));
#53834=CARTESIAN_POINT('',(9.7211545887425,-0.000338423355870402,4.59484023865297));
#53835=CARTESIAN_POINT('',(4.,-7.27562663373442E-17,4.5941));
#53836=CARTESIAN_POINT('Ctrl Pts',(9.82884541125756,0.000474857175501747,
4.59454166667424));
#53837=CARTESIAN_POINT('Ctrl Pts',(9.82632780447438,0.0317313679687054,
4.59481419231428));
#53838=CARTESIAN_POINT('Ctrl Pts',(9.82381019769121,0.0629485386443197,
4.59256288124703));
#53839=CARTESIAN_POINT('Ctrl Pts',(9.82129259090804,0.093741277189286,4.58765086492638));
#53840=CARTESIAN_POINT('Ctrl Pts',(9.80538731222043,0.288278045752977,4.55661862072519));
#53841=CARTESIAN_POINT('Ctrl Pts',(9.78948203353282,0.465874751366426,4.41939150759219));
#53842=CARTESIAN_POINT('Ctrl Pts',(9.77357675484521,0.54498650030893,4.23897841027765));
#53843=CARTESIAN_POINT('Ctrl Pts',(9.7576714761576,0.624098249251433,4.05856531296313));
#53844=CARTESIAN_POINT('Ctrl Pts',(9.74176619746998,0.604725041522997,3.83496623146707));
#53845=CARTESIAN_POINT('Ctrl Pts',(9.72586091878237,0.495762234499694,3.67084840431546));
#53846=CARTESIAN_POINT('Ctrl Pts',(9.70995564009475,0.386799427476386,3.50673057716384));
#53847=CARTESIAN_POINT('Ctrl Pts',(9.69405036140714,0.188247021158209,3.40209400435668));
#53848=CARTESIAN_POINT('Ctrl Pts',(9.67814508271953,-0.00872811953311764,
3.40498337331868));
#53849=CARTESIAN_POINT('Ctrl Pts',(9.66223980403192,-0.205703260224436,
3.40787274228067));
#53850=CARTESIAN_POINT('Ctrl Pts',(9.6463345253443,-0.4011011352889,3.51828805301183));
#53851=CARTESIAN_POINT('Ctrl Pts',(9.63042924665669,-0.505203307099277,
3.68553126611098));
#53852=CARTESIAN_POINT('Ctrl Pts',(9.61452396796908,-0.609305478909656,
3.85277447921013));
#53853=CARTESIAN_POINT('Ctrl Pts',(9.59861868928147,-0.622111947465945,
4.07684559467727));
#53854=CARTESIAN_POINT('Ctrl Pts',(9.58271341059386,-0.537742524204099,
4.25486063595701));
#53855=CARTESIAN_POINT('Ctrl Pts',(9.56680813190624,-0.453373100942255,
4.43287567723675));
#53856=CARTESIAN_POINT('Ctrl Pts',(9.55090285321863,-0.271827785862281,
4.5648346443291));
#53857=CARTESIAN_POINT('Ctrl Pts',(9.53499757453102,-0.0764645071000137,
4.59014756226876));
#53858=CARTESIAN_POINT('Ctrl Pts',(9.53294685343987,-0.0512756623106346,
4.5934112419387));
#53859=CARTESIAN_POINT('Ctrl Pts',(9.53089613234871,-0.025857110284879,
4.59490205769144));
#53860=CARTESIAN_POINT('Ctrl Pts',(9.52884541125756,-0.000414715089906426,
4.59470005288553));
#53861=CARTESIAN_POINT('Ctrl Pts',(9.4211545887425,-0.000345133784900094,
4.59331940772745));
#53862=CARTESIAN_POINT('Ctrl Pts',(9.42730482954951,-0.0771024252662454,
4.59372396859559));
#53863=CARTESIAN_POINT('Ctrl Pts',(9.43345507035652,-0.153719688677923,
4.57990840728947));
#53864=CARTESIAN_POINT('Ctrl Pts',(9.43960531116353,-0.224276981305518,
4.55119942103951));
#53865=CARTESIAN_POINT('Ctrl Pts',(9.45551058985114,-0.406746812634079,
4.47695445381419));
#53866=CARTESIAN_POINT('Ctrl Pts',(9.47141586853875,-0.548687367047265,
4.30310178792596));
#53867=CARTESIAN_POINT('Ctrl Pts',(9.48732114722636,-0.58492554696818,4.10946721245096));
#53868=CARTESIAN_POINT('Ctrl Pts',(9.50322642591398,-0.621163726889096,
3.91583263697596));
#53869=CARTESIAN_POINT('Ctrl Pts',(9.5191317046016,-0.55169953231774,3.70241615191419));
#53870=CARTESIAN_POINT('Ctrl Pts',(9.53503698328921,-0.408427982613559,
3.56720957829912));
#53871=CARTESIAN_POINT('Ctrl Pts',(9.55094226197682,-0.265156432909381,
3.43200300468405));
#53872=CARTESIAN_POINT('Ctrl Pts',(9.56684754066442,-0.0480775280723801,
3.37500634251568));
#53873=CARTESIAN_POINT('Ctrl Pts',(9.58275281935204,0.14313528264739,3.42239004773181));
#53874=CARTESIAN_POINT('Ctrl Pts',(9.59865809803965,0.334348093367161,3.46977375294793));
#53875=CARTESIAN_POINT('Ctrl Pts',(9.61456337672728,0.499694809969701,3.62153782554855));
#53876=CARTESIAN_POINT('Ctrl Pts',(9.63046865541489,0.563255215433827,3.80799862400389));
#53877=CARTESIAN_POINT('Ctrl Pts',(9.6463739341025,0.626815620897955,3.99445942245922));
#53878=CARTESIAN_POINT('Ctrl Pts',(9.6622792127901,0.588589715223662,4.21561694676927));
#53879=CARTESIAN_POINT('Ctrl Pts',(9.67818449147771,0.466129217091882,4.36992501817411));
#53880=CARTESIAN_POINT('Ctrl Pts',(9.69250785723264,0.355848439261942,4.50888586187125));
#53881=CARTESIAN_POINT('Ctrl Pts',(9.70683122298757,0.177255492135987,4.59363345408847));
#53882=CARTESIAN_POINT('Ctrl Pts',(9.7211545887425,-0.000338423355870402,
4.59484023865297));
#53883=CARTESIAN_POINT('Origin',(4.,0.,4.));
#53884=CARTESIAN_POINT('',(10.1288454112576,0.000175993811045716,4.59316417414361));
#53885=CARTESIAN_POINT('',(10.0211545887425,0.000517772199431355,4.59437035498519));
#53886=CARTESIAN_POINT('',(4.,-7.27562663373442E-17,4.5941));
#53887=CARTESIAN_POINT('Ctrl Pts',(10.1288454112576,0.000175993811045716,
4.59316417414361));
#53888=CARTESIAN_POINT('Ctrl Pts',(10.1217594766001,0.0886689559287146,
4.59339827721605));
#53889=CARTESIAN_POINT('Ctrl Pts',(10.1146735419426,0.177068724884878,4.57486525982572));
#53890=CARTESIAN_POINT('Ctrl Pts',(10.1075876072851,0.256276603526552,4.53706914692868));
#53891=CARTESIAN_POINT('Ctrl Pts',(10.0916823285975,0.434068729046268,4.45223097977176));
#53892=CARTESIAN_POINT('Ctrl Pts',(10.0757770499098,0.565548899719798,4.27033860735548));
#53893=CARTESIAN_POINT('Ctrl Pts',(10.0598717712222,0.590346983641159,4.0749093118617));
#53894=CARTESIAN_POINT('Ctrl Pts',(10.0439664925346,0.61514506756252,3.87948001636793));
#53895=CARTESIAN_POINT('Ctrl Pts',(10.028061213847,0.533261064731712,3.67051379779667));
#53896=CARTESIAN_POINT('Ctrl Pts',(10.0121559351594,0.382292645022166,3.5439591030842));
#53897=CARTESIAN_POINT('Ctrl Pts',(9.99625065647179,0.231324225312614,3.41740440837173));
#53898=CARTESIAN_POINT('Ctrl Pts',(9.98034537778417,0.011271388724311,3.37326123751805));
#53899=CARTESIAN_POINT('Ctrl Pts',(9.96444009909655,-0.17682691184915,3.43179826703564));
#53900=CARTESIAN_POINT('Ctrl Pts',(9.94853482040894,-0.364925212422603,
3.49033529655323));
#53901=CARTESIAN_POINT('Ctrl Pts',(9.93262954172133,-0.521068976981223,
3.65155252644206));
#53902=CARTESIAN_POINT('Ctrl Pts',(9.91672426303372,-0.573563594737602,
3.84142582527571));
#53903=CARTESIAN_POINT('Ctrl Pts',(9.90081898434611,-0.626058212493981,
4.03129912410937));
#53904=CARTESIAN_POINT('Ctrl Pts',(9.8849137056585,-0.574903683448118,4.24982849188785));
#53905=CARTESIAN_POINT('Ctrl Pts',(9.86900842697089,-0.443588003168223,
4.39667448814241));
#53906=CARTESIAN_POINT('Ctrl Pts',(9.85562075506645,-0.333057953489513,
4.52027659892262));
#53907=CARTESIAN_POINT('Ctrl Pts',(9.842233083162,-0.165735336637852,4.59309247934331));
#53908=CARTESIAN_POINT('Ctrl Pts',(9.82884541125756,0.000474857175501747,
4.59454166667424));
#53909=CARTESIAN_POINT('Ctrl Pts',(9.7211545887425,-0.000338423355870402,
4.59484023865297));
#53910=CARTESIAN_POINT('Ctrl Pts',(9.72273650167518,-0.0199523965301825,
4.59497351934566));
#53911=CARTESIAN_POINT('Ctrl Pts',(9.72431841460787,-0.0395541838993478,
4.59408780127083));
#53912=CARTESIAN_POINT('Ctrl Pts',(9.72590032754056,-0.0590504136254521,
4.592143576127));
#53913=CARTESIAN_POINT('Ctrl Pts',(9.74180560622817,-0.255074455621757,
4.57259544417541));
#53914=CARTESIAN_POINT('Ctrl Pts',(9.75771088491579,-0.4404274490251,4.4460405617726));
#53915=CARTESIAN_POINT('Ctrl Pts',(9.7736161636034,-0.530003140903138,4.2705875768224));
#53916=CARTESIAN_POINT('Ctrl Pts',(9.78952144229101,-0.619578832781174,
4.0951345918722));
#53917=CARTESIAN_POINT('Ctrl Pts',(9.80542672097862,-0.61337722313391,3.87078350437461));
#53918=CARTESIAN_POINT('Ctrl Pts',(9.82133199966623,-0.514245828742901,
3.70054684219675));
#53919=CARTESIAN_POINT('Ctrl Pts',(9.83723727835384,-0.41511443435189,3.53031018001889));
#53920=CARTESIAN_POINT('Ctrl Pts',(9.85314255704146,-0.223053255217129,
3.41418794316076));
#53921=CARTESIAN_POINT('Ctrl Pts',(9.86904783572907,-0.0262486593588972,
3.40549855006092));
#53922=CARTESIAN_POINT('Ctrl Pts',(9.88495311441669,0.170555936499329,3.39680915696108));
#53923=CARTESIAN_POINT('Ctrl Pts',(9.9008583931043,0.372103949081026,3.49555260761951));
#53924=CARTESIAN_POINT('Ctrl Pts',(9.91676367179191,0.485853057801912,3.65639008698476));
#53925=CARTESIAN_POINT('Ctrl Pts',(9.93266895047952,0.5996021665228,3.81722756635002));
#53926=CARTESIAN_POINT('Ctrl Pts',(9.94857422916713,0.625552371382872,4.04015907442209));
#53927=CARTESIAN_POINT('Ctrl Pts',(9.96447950785475,0.551788436173011,4.22282389414861));
#53928=CARTESIAN_POINT('Ctrl Pts',(9.98038478654236,0.478024500963153,4.40548871387512));
#53929=CARTESIAN_POINT('Ctrl Pts',(9.99629006522997,0.304546425683368,4.54788684525607));
#53930=CARTESIAN_POINT('Ctrl Pts',(10.0121953439176,0.111008003250015,4.58463509072946));
#53931=CARTESIAN_POINT('Ctrl Pts',(10.0151817588592,0.0746687445744621,
4.59153503329043));
#53932=CARTESIAN_POINT('Ctrl Pts',(10.0181681738009,0.0376222632219309,
4.59471031472953));
#53933=CARTESIAN_POINT('Ctrl Pts',(10.0211545887425,0.000517772199431355,
4.59437035498519));
#53934=CARTESIAN_POINT('Origin',(4.,0.,4.));
#53935=CARTESIAN_POINT('',(10.4288454112576,-0.000541293539476018,4.59389423388278));
#53936=CARTESIAN_POINT('',(10.3211545887425,8.19078234495683E-5,4.59312629593825));
#53937=CARTESIAN_POINT('',(4.,-7.27562663373442E-17,4.5941));
#53938=CARTESIAN_POINT('Ctrl Pts',(10.4288454112576,-0.000541293539476018,
4.59389423388278));
#53939=CARTESIAN_POINT('Ctrl Pts',(10.4171911487257,0.144553461780974,4.59260897165526));
#53940=CARTESIAN_POINT('Ctrl Pts',(10.4055368861939,0.290497422953868,4.53904330389552));
#53941=CARTESIAN_POINT('Ctrl Pts',(10.3938826236621,0.397841883685798,4.4425412994096));
#53942=CARTESIAN_POINT('Ctrl Pts',(10.3779773449745,0.544341377656434,4.31083916286766));
#53943=CARTESIAN_POINT('Ctrl Pts',(10.3620720662869,0.618946539098701,4.09916502578488));
#53944=CARTESIAN_POINT('Ctrl Pts',(10.3461667875993,0.587401834162399,3.90471069671543));
#53945=CARTESIAN_POINT('Ctrl Pts',(10.3302615089117,0.555857129226098,3.710256367646));
#53946=CARTESIAN_POINT('Ctrl Pts',(10.314356230224,0.418162557911234,3.5330218465899));
#53947=CARTESIAN_POINT('Ctrl Pts',(10.2984509515364,0.237541641988682,3.45438572744188));
#53948=CARTESIAN_POINT('Ctrl Pts',(10.2825456728488,0.0569207260661262,
3.37574960829385));
#53949=CARTESIAN_POINT('Ctrl Pts',(10.2666403941612,-0.16662653446412,3.3957118910539));
#53950=CARTESIAN_POINT('Ctrl Pts',(10.2507351154736,-0.330456695071223,
3.50510674001315));
#53951=CARTESIAN_POINT('Ctrl Pts',(10.234829836786,-0.494286855678321,3.61450158897239));
#53952=CARTESIAN_POINT('Ctrl Pts',(10.2189245580984,-0.59839991636228,3.81332900413083));
#53953=CARTESIAN_POINT('Ctrl Pts',(10.2030192794108,-0.594991564317383,
4.01029584814195));
#53954=CARTESIAN_POINT('Ctrl Pts',(10.1871140007231,-0.591583212272486,
4.20726269215308));
#53955=CARTESIAN_POINT('Ctrl Pts',(10.1712087220355,-0.480653447498727,
4.40236896501689));
#53956=CARTESIAN_POINT('Ctrl Pts',(10.1553034433479,-0.313136524928893,
4.50603012050002));
#53957=CARTESIAN_POINT('Ctrl Pts',(10.1464840993178,-0.220249792163878,
4.56350936438632));
#53958=CARTESIAN_POINT('Ctrl Pts',(10.1376647552877,-0.109964716607974,
4.59287280319057));
#53959=CARTESIAN_POINT('Ctrl Pts',(10.1288454112576,0.000175993811045716,
4.59316417414361));
#53960=CARTESIAN_POINT('Ctrl Pts',(10.0211545887425,0.000517772199431355,
4.59437035498519));
#53961=CARTESIAN_POINT('Ctrl Pts',(10.0340734524885,-0.159991692577292,
4.59289973094197));
#53962=CARTESIAN_POINT('Ctrl Pts',(10.0469923162344,-0.321586704601994,
4.52564765365589));
#53963=CARTESIAN_POINT('Ctrl Pts',(10.0599111799804,-0.431712787135162,
4.40956688772629));
#53964=CARTESIAN_POINT('Ctrl Pts',(10.075816458668,-0.567296385500051,4.2666520796839));
#53965=CARTESIAN_POINT('Ctrl Pts',(10.0917217373556,-0.624864812642908,
4.04972410403331));
#53966=CARTESIAN_POINT('Ctrl Pts',(10.1076270160433,-0.577985082339038,
3.85838710972745));
#53967=CARTESIAN_POINT('Ctrl Pts',(10.1235322947309,-0.531105352035168,
3.6670501154216));
#53968=CARTESIAN_POINT('Ctrl Pts',(10.1394375734185,-0.379777464284567,
3.50130410246047));
#53969=CARTESIAN_POINT('Ctrl Pts',(10.1553428521061,-0.193484782987353,
3.43725262786029));
#53970=CARTESIAN_POINT('Ctrl Pts',(10.1712481307937,-0.00719210169012799,
3.37320115326011));
#53971=CARTESIAN_POINT('Ctrl Pts',(10.1871534094813,0.214065373153706,3.41084421702088));
#53972=CARTESIAN_POINT('Ctrl Pts',(10.2030586881689,0.368695569727689,3.53289771681035));
#53973=CARTESIAN_POINT('Ctrl Pts',(10.2189639668565,0.523325766301663,3.65495121659981));
#53974=CARTESIAN_POINT('Ctrl Pts',(10.2348692455442,0.611328684605784,3.86141515241798));
#53975=CARTESIAN_POINT('Ctrl Pts',(10.2507745242318,0.592297107651237,4.05749001970593));
#53976=CARTESIAN_POINT('Ctrl Pts',(10.2666798029194,0.573265530696689,4.25356488699388));
#53977=CARTESIAN_POINT('Ctrl Pts',(10.282585081607,0.447199458483466,4.43925068575162));
#53978=CARTESIAN_POINT('Ctrl Pts',(10.2984903602946,0.271983097956201,4.5292883529079));
#53979=CARTESIAN_POINT('Ctrl Pts',(10.3060451031106,0.188758241169316,4.57205474716445));
#53980=CARTESIAN_POINT('Ctrl Pts',(10.3135998459265,0.0944446272328244,
4.59324204311815));
#53981=CARTESIAN_POINT('Ctrl Pts',(10.3211545887425,8.19078234495684E-5,
4.59312629593825));
#53982=CARTESIAN_POINT('Origin',(4.,0.,4.));
#53983=CARTESIAN_POINT('',(10.7288454112576,7.37317986114466E-5,4.59506942345298));
#53984=CARTESIAN_POINT('',(10.6211545887425,-0.000548317120500629,4.59406879148573));
#53985=CARTESIAN_POINT('',(4.,-7.27562663373442E-17,4.5941));
#53986=CARTESIAN_POINT('Ctrl Pts',(10.7288454112576,7.37317986114466E-5,
4.59506942345298));
#53987=CARTESIAN_POINT('Ctrl Pts',(10.728528099539,0.00400402563557926,
4.59507627971693));
#53988=CARTESIAN_POINT('Ctrl Pts',(10.7282107878205,0.00793419209028873,
4.59504072157671));
#53989=CARTESIAN_POINT('Ctrl Pts',(10.727893476102,0.0118635052742893,4.59496237136513));
#53990=CARTESIAN_POINT('Ctrl Pts',(10.7119881974144,0.208820685209451,4.59103505989901));
#53991=CARTESIAN_POINT('Ctrl Pts',(10.6960829187267,0.403634001393415,4.47959161118634));
#53992=CARTESIAN_POINT('Ctrl Pts',(10.6801776400391,0.506853420906232,4.31180214209248));
#53993=CARTESIAN_POINT('Ctrl Pts',(10.6642723613515,0.610072840419052,4.14401267299861));
#53994=CARTESIAN_POINT('Ctrl Pts',(10.6483670826639,0.621698363260717,3.91987718352354));
#53995=CARTESIAN_POINT('Ctrl Pts',(10.6324618039763,0.536392041177647,3.74230920804366));
#53996=CARTESIAN_POINT('Ctrl Pts',(10.6165565252887,0.451085719094577,3.56474123256377));
#53997=CARTESIAN_POINT('Ctrl Pts',(10.6006512466011,0.26884755208677,3.43374077107907));
#53998=CARTESIAN_POINT('Ctrl Pts',(10.5847459679135,0.0733535965831807,
3.40945769333085));
#53999=CARTESIAN_POINT('Ctrl Pts',(10.5688406892258,-0.122140358920403,
3.38517461558263));
#54000=CARTESIAN_POINT('Ctrl Pts',(10.5529354105382,-0.33089010291977,3.46760892157089));
#54001=CARTESIAN_POINT('Ctrl Pts',(10.5370301318506,-0.457046584443773,
3.61891026549369));
#54002=CARTESIAN_POINT('Ctrl Pts',(10.521124853163,-0.583203065967777,3.7702116094165));
#54003=CARTESIAN_POINT('Ctrl Pts',(10.5052195744754,-0.626766285016417,
3.99037999127385));
#54004=CARTESIAN_POINT('Ctrl Pts',(10.4893142957878,-0.567733854410369,
4.17832340467295));
#54005=CARTESIAN_POINT('Ctrl Pts',(10.4734090171002,-0.508701423804317,
4.36626681807206));
#54006=CARTESIAN_POINT('Ctrl Pts',(10.4575037384126,-0.347073343543565,
4.52198526301292));
#54007=CARTESIAN_POINT('Ctrl Pts',(10.4415984597249,-0.157062390163684,
4.57397941748279));
#54008=CARTESIAN_POINT('Ctrl Pts',(10.4373474435692,-0.106278015462724,
4.58787593542499));
#54009=CARTESIAN_POINT('Ctrl Pts',(10.4330964274134,-0.0534661480554494,
4.59436304694399));
#54010=CARTESIAN_POINT('Ctrl Pts',(10.4288454112576,-0.000541293539476018,
4.59389423388278));
#54011=CARTESIAN_POINT('Ctrl Pts',(10.3211545887425,8.19078234495684E-5,
4.59312629593825));
#54012=CARTESIAN_POINT('Ctrl Pts',(10.3295051246142,-0.104220686264852,
4.59299835631127));
#54013=CARTESIAN_POINT('Ctrl Pts',(10.3378556604858,-0.208583275928277,
4.56684300569277));
#54014=CARTESIAN_POINT('Ctrl Pts',(10.3462061963575,-0.298097175589899,
4.5150330474864));
#54015=CARTESIAN_POINT('Ctrl Pts',(10.3621114750451,-0.468594439767441,
4.41635053935381));
#54016=CARTESIAN_POINT('Ctrl Pts',(10.3780167537327,-0.585222319281217,
4.22459598753381));
#54017=CARTESIAN_POINT('Ctrl Pts',(10.3939220324203,-0.594430225977177,
4.02781496975607));
#54018=CARTESIAN_POINT('Ctrl Pts',(10.4098273111079,-0.603638132673137,
3.83103395197833));
#54019=CARTESIAN_POINT('Ctrl Pts',(10.4257325897955,-0.505426066551287,
3.62922646824286));
#54020=CARTESIAN_POINT('Ctrl Pts',(10.4416378684831,-0.344888853364916,
3.51505397731042));
#54021=CARTESIAN_POINT('Ctrl Pts',(10.4575431471707,-0.184351640178541,
3.40088148637798));
#54022=CARTESIAN_POINT('Ctrl Pts',(10.4734484258584,0.0385107200723601,
3.37434398824859));
#54023=CARTESIAN_POINT('Ctrl Pts',(10.489353704546,0.221369260089487,3.4476263793543));
#54024=CARTESIAN_POINT('Ctrl Pts',(10.5052589832336,0.40422780010661,3.52090877046001));
#54025=CARTESIAN_POINT('Ctrl Pts',(10.5211642619212,0.54708251988996,3.69401105080081));
#54026=CARTESIAN_POINT('Ctrl Pts',(10.5370695406088,0.584340575799814,3.88745197659776));
#54027=CARTESIAN_POINT('Ctrl Pts',(10.5529748192964,0.621598631709669,4.08089290239472));
#54028=CARTESIAN_POINT('Ctrl Pts',(10.568880097984,0.55326002374602,4.29467247364782));
#54029=CARTESIAN_POINT('Ctrl Pts',(10.5847853766716,0.4107029495177,4.43063215550545));
#54030=CARTESIAN_POINT('Ctrl Pts',(10.5969084473619,0.302045344566967,4.53426120008624));
#54031=CARTESIAN_POINT('Ctrl Pts',(10.6090315180522,0.150270129189204,4.59268036842864));
#54032=CARTESIAN_POINT('Ctrl Pts',(10.6211545887425,-0.000548317120500629,
4.59406879148573));
#54033=CARTESIAN_POINT('Origin',(4.,0.,4.));
#54034=CARTESIAN_POINT('',(11.0288454112576,0.000503618959454472,4.59367252935801));
#54035=CARTESIAN_POINT('',(10.9211545887425,0.000179316795020235,4.59501533910171));
#54036=CARTESIAN_POINT('',(4.,-7.27562663373442E-17,4.5941));
#54037=CARTESIAN_POINT('Ctrl Pts',(11.0288454112576,0.000503618959454472,
4.59367252935801));
#54038=CARTESIAN_POINT('Ctrl Pts',(11.0239597716647,0.0613870506829751,
4.59415995979602));
#54039=CARTESIAN_POINT('Ctrl Pts',(11.0190741320719,0.122135879976345,4.58554712933309));
#54040=CARTESIAN_POINT('Ctrl Pts',(11.014188492479,0.179818659528701,4.56726203449827));
#54041=CARTESIAN_POINT('Ctrl Pts',(10.9982832137914,0.36760588100072,4.50773461262244));
#54042=CARTESIAN_POINT('Ctrl Pts',(10.9823779351038,0.52289792528528,4.34569680405454));
#54043=CARTESIAN_POINT('Ctrl Pts',(10.9664726564162,0.574391255511512,4.15554951523459));
#54044=CARTESIAN_POINT('Ctrl Pts',(10.9505673777285,0.625884585737745,3.96540222641464));
#54045=CARTESIAN_POINT('Ctrl Pts',(10.9346620990409,0.573579201905647,3.74714545734266));
#54046=CARTESIAN_POINT('Ctrl Pts',(10.9187568203533,0.441491523412615,3.60099348269406));
#54047=CARTESIAN_POINT('Ctrl Pts',(10.9028515416657,0.309403844919578,3.45484150804546));
#54048=CARTESIAN_POINT('Ctrl Pts',(10.8869462629781,0.0975338717655902,
3.38079432782024));
#54049=CARTESIAN_POINT('Ctrl Pts',(10.8710409842905,-0.0968366678563846,
3.41285127449999));
#54050=CARTESIAN_POINT('Ctrl Pts',(10.8551357056029,-0.291207207478354,
3.44490822117975));
#54051=CARTESIAN_POINT('Ctrl Pts',(10.8392304269153,-0.468078313568319,
3.58306929476445));
#54052=CARTESIAN_POINT('Ctrl Pts',(10.8233251482276,-0.546238257009186,
3.76389677537701));
#54053=CARTESIAN_POINT('Ctrl Pts',(10.80741986954,-0.624398200450053,3.94472425598957));
#54054=CARTESIAN_POINT('Ctrl Pts',(10.7915145908524,-0.603846981241821,
4.16821814362997));
#54055=CARTESIAN_POINT('Ctrl Pts',(10.7756093121648,-0.494020849794526,
4.33175950034039));
#54056=CARTESIAN_POINT('Ctrl Pts',(10.7600213451957,-0.386385759396791,
4.49203819249975));
#54057=CARTESIAN_POINT('Ctrl Pts',(10.7444333782267,-0.193002309618558,
4.59473260886404));
#54058=CARTESIAN_POINT('Ctrl Pts',(10.7288454112576,7.37317986114466E-5,
4.59506942345298));
#54059=CARTESIAN_POINT('Ctrl Pts',(10.6211545887425,-0.000548317120500629,
4.59406879148573));
#54060=CARTESIAN_POINT('Ctrl Pts',(10.6249367967398,-0.0476013079303647,
4.5945019577127));
#54061=CARTESIAN_POINT('Ctrl Pts',(10.6287190047372,-0.0945611723716044,
4.58938408097059));
#54062=CARTESIAN_POINT('Ctrl Pts',(10.6325012127345,-0.140089514783682,
4.57835619988505));
#54063=CARTESIAN_POINT('Ctrl Pts',(10.6484064914221,-0.331549364363767,
4.53198076994489));
#54064=CARTESIAN_POINT('Ctrl Pts',(10.6643117701097,-0.497693523030948,
4.38109011760241));
#54065=CARTESIAN_POINT('Ctrl Pts',(10.6802170487973,-0.562235622104956,
4.19496684675621));
#54066=CARTESIAN_POINT('Ctrl Pts',(10.6961223274849,-0.626777721178965,
4.00884357591002));
#54067=CARTESIAN_POINT('Ctrl Pts',(10.7120276061725,-0.589717760659791,
3.78748768656011));
#54068=CARTESIAN_POINT('Ctrl Pts',(10.7279328848602,-0.468072106540212,
3.63253643830059));
#54069=CARTESIAN_POINT('Ctrl Pts',(10.7438381635478,-0.346426452420629,
3.47758519004106));
#54070=CARTESIAN_POINT('Ctrl Pts',(10.7597434422354,-0.140195104700642,
3.38903858287192));
#54071=CARTESIAN_POINT('Ctrl Pts',(10.775648720923,0.0559292266755373,3.40755347270721));
#54072=CARTESIAN_POINT('Ctrl Pts',(10.7915539996106,0.252053558051711,3.4260683625425));
#54073=CARTESIAN_POINT('Ctrl Pts',(10.8074592782982,0.438070873084069,3.55164474938222));
#54074=CARTESIAN_POINT('Ctrl Pts',(10.8233645569858,0.528569890453362,3.72662326908837));
#54075=CARTESIAN_POINT('Ctrl Pts',(10.8392698356734,0.619068907822657,3.90160178879453));
#54076=CARTESIAN_POINT('Ctrl Pts',(10.8551751143611,0.614049627528876,4.12598244136713));
#54077=CARTESIAN_POINT('Ctrl Pts',(10.8710803930487,0.515816690734684,4.29673912390739));
#54078=CARTESIAN_POINT('Ctrl Pts',(10.8869856717363,0.417583753940498,4.46749580644764));
#54079=CARTESIAN_POINT('Ctrl Pts',(10.9028909504239,0.226137160645921,4.58462851895556));
#54080=CARTESIAN_POINT('Ctrl Pts',(10.9187962291115,0.0293810870543861,
4.59435487532392));
#54081=CARTESIAN_POINT('Ctrl Pts',(10.9195823489885,0.0196563998352688,
4.59483560139116));
#54082=CARTESIAN_POINT('Ctrl Pts',(10.9203684688655,0.00991874240631306,
4.5950539509358));
#54083=CARTESIAN_POINT('Ctrl Pts',(10.9211545887425,0.000179316795020235,
4.59501533910171));
#54084=CARTESIAN_POINT('Origin',(4.,0.,4.));
#54085=CARTESIAN_POINT('',(11.3288454112576,-0.000294350894641693,4.59325842069974));
#54086=CARTESIAN_POINT('',(11.2211545887425,0.000456638431143918,4.59352536526061));
#54087=CARTESIAN_POINT('',(4.,-7.27562663373442E-17,4.5941));
#54088=CARTESIAN_POINT('Ctrl Pts',(11.3288454112576,-0.000294350894641693,
4.59325842069974));
#54089=CARTESIAN_POINT('Ctrl Pts',(11.3193914437904,0.117725031793324,4.59273125875086));
#54090=CARTESIAN_POINT('Ctrl Pts',(11.3099374763232,0.236024696118704,4.55868066117597));
#54091=CARTESIAN_POINT('Ctrl Pts',(11.300483508856,0.333060002447629,4.49314500997921));
#54092=CARTESIAN_POINT('Ctrl Pts',(11.2845782301684,0.496311419914153,4.38288835848583));
#54093=CARTESIAN_POINT('Ctrl Pts',(11.2686729514808,0.599375291650127,4.18351506848348));
#54094=CARTESIAN_POINT('Ctrl Pts',(11.2527676727932,0.594929048027223,3.98656891995295));
#54095=CARTESIAN_POINT('Ctrl Pts',(11.2368623941056,0.59048280440432,3.78962277142242));
#54096=CARTESIAN_POINT('Ctrl Pts',(11.220957115418,0.478526445422532,3.5951037643637));
#54097=CARTESIAN_POINT('Ctrl Pts',(11.2050518367303,0.310465594643358,3.49232679739763));
#54098=CARTESIAN_POINT('Ctrl Pts',(11.1891465580427,0.142404743864184,3.38954983043155));
#54099=CARTESIAN_POINT('Ctrl Pts',(11.1732412793551,-0.0817605987123653,
3.37851490355812));
#54100=CARTESIAN_POINT('Ctrl Pts',(11.1573360006675,-0.259103191428711,
3.46428878834836));
#54101=CARTESIAN_POINT('Ctrl Pts',(11.1414307219799,-0.436445784145052,
3.5500626731386));
#54102=CARTESIAN_POINT('Ctrl Pts',(11.1255254432923,-0.566965627001181,
3.73264536959251));
#54103=CARTESIAN_POINT('Ctrl Pts',(11.1096201646047,-0.590733529996744,
3.92820262793532));
#54104=CARTESIAN_POINT('Ctrl Pts',(11.0937148859171,-0.614501432992307,
4.12375988627813));
#54105=CARTESIAN_POINT('Ctrl Pts',(11.0778096072294,-0.531517396127296,
4.33229170650985));
#54106=CARTESIAN_POINT('Ctrl Pts',(11.0619043285418,-0.379884178365051,
4.45804909903384));
#54107=CARTESIAN_POINT('Ctrl Pts',(11.0508846894471,-0.274828280424841,
4.54517747360242));
#54108=CARTESIAN_POINT('Ctrl Pts',(11.0398650503523,-0.136819945681758,
4.59257312212411));
#54109=CARTESIAN_POINT('Ctrl Pts',(11.0288454112576,0.000503618959454472,
4.59367252935801));
#54110=CARTESIAN_POINT('Ctrl Pts',(10.9211545887425,0.000179316795020235,
4.59501533910171));
#54111=CARTESIAN_POINT('Ctrl Pts',(10.9362737475531,-0.187135527734918,
4.59427273168419));
#54112=CARTESIAN_POINT('Ctrl Pts',(10.9513929063637,-0.375104412928531,
4.49848156101044));
#54113=CARTESIAN_POINT('Ctrl Pts',(10.9665120651743,-0.484035620954107,
4.34616539940523));
#54114=CARTESIAN_POINT('Ctrl Pts',(10.982417343862,-0.598630701482551,4.1859295668894));
#54115=CARTESIAN_POINT('Ctrl Pts',(10.9983226225496,-0.625755308650954,
3.96313790162893));
#54116=CARTESIAN_POINT('Ctrl Pts',(11.0142279012372,-0.55295497039508,3.7800869107734));
#54117=CARTESIAN_POINT('Ctrl Pts',(11.0301331799248,-0.480154632139201,
3.59703591991786));
#54118=CARTESIAN_POINT('Ctrl Pts',(11.0460384586124,-0.307429348459053,
3.45372560346725));
#54119=CARTESIAN_POINT('Ctrl Pts',(11.0619437373,-0.114087262216405,3.41595799577618));
#54120=CARTESIAN_POINT('Ctrl Pts',(11.0778490159876,0.0792548240262376,
3.37819038808511));
#54121=CARTESIAN_POINT('Ctrl Pts',(11.0937542946752,0.293213712831377,3.4459654891536));
#54122=CARTESIAN_POINT('Ctrl Pts',(11.1096595733629,0.429548534313776,3.58816383989905));
#54123=CARTESIAN_POINT('Ctrl Pts',(11.1255648520505,0.565883355796175,3.7303621906445));
#54124=CARTESIAN_POINT('Ctrl Pts',(11.1414701307381,0.624594109955846,3.94698379106692));
#54125=CARTESIAN_POINT('Ctrl Pts',(11.1573754094257,0.578723302329844,4.13856516675647));
#54126=CARTESIAN_POINT('Ctrl Pts',(11.1732806881133,0.53285249470384,4.33014654244603));
#54127=CARTESIAN_POINT('Ctrl Pts',(11.1891859668009,0.382400125292158,4.49668769340272));
#54128=CARTESIAN_POINT('Ctrl Pts',(11.2050912454885,0.196447557013804,4.56171996888228));
#54129=CARTESIAN_POINT('Ctrl Pts',(11.2104456932399,0.133847376870746,4.58361282144047));
#54130=CARTESIAN_POINT('Ctrl Pts',(11.2158001409912,0.0672239414478651,
4.5940016224088));
#54131=CARTESIAN_POINT('Ctrl Pts',(11.2211545887425,0.000456638431143918,
4.59352536526061));
#54132=CARTESIAN_POINT('Origin',(4.,0.,4.));
#54133=CARTESIAN_POINT('',(11.6288454112576,-0.000389145320547679,4.59475273347735));
#54134=CARTESIAN_POINT('',(11.5211545887425,-0.0003715675665865,4.59335763259963));
#54135=CARTESIAN_POINT('',(4.,-7.27562663373442E-17,4.5941));
#54136=CARTESIAN_POINT('Ctrl Pts',(11.6288454112576,-0.000389145320547679,
4.59475273347735));
#54137=CARTESIAN_POINT('Ctrl Pts',(11.6148231159161,0.173538999407471,4.59343557735163));
#54138=CARTESIAN_POINT('Ctrl Pts',(11.6008008205746,0.348531733704351,4.51264940831536));
#54139=CARTESIAN_POINT('Ctrl Pts',(11.586778525233,0.459048433726307,4.37867598496766));
#54140=CARTESIAN_POINT('Ctrl Pts',(11.5708732465454,0.584405864209301,4.22671194604376));
#54141=CARTESIAN_POINT('Ctrl Pts',(11.5549679678578,0.626808276394098,4.00631705984067));
#54142=CARTESIAN_POINT('Ctrl Pts',(11.5390626891702,0.566786276503563,3.81868733396413));
#54143=CARTESIAN_POINT('Ctrl Pts',(11.5231574104826,0.506764276613028,3.6310576080876));
#54144=CARTESIAN_POINT('Ctrl Pts',(11.507252131795,0.344317864647159,3.47619304253762));
#54145=CARTESIAN_POINT('Ctrl Pts',(11.4913468531074,0.154035560439752,3.4252008940353));
#54146=CARTESIAN_POINT('Ctrl Pts',(11.4754415744198,-0.0362467437676612,
3.37420874553297));
#54147=CARTESIAN_POINT('Ctrl Pts',(11.4595362957322,-0.254364940216614,
3.4270890140783));
#54148=CARTESIAN_POINT('Ctrl Pts',(11.4436310170445,-0.400168380917644,
3.55956131753494));
#54149=CARTESIAN_POINT('Ctrl Pts',(11.4277257383569,-0.545971821618673,
3.69203362099157));
#54150=CARTESIAN_POINT('Ctrl Pts',(11.4118204596693,-0.619460506571779,
3.90409795935952));
#54151=CARTESIAN_POINT('Ctrl Pts',(11.3959151809817,-0.586891540696359,
4.09838336016249));
#54152=CARTESIAN_POINT('Ctrl Pts',(11.3800099022941,-0.554322574820941,
4.29266876096545));
#54153=CARTESIAN_POINT('Ctrl Pts',(11.3641046236065,-0.415695958117004,
4.46917522420345));
#54154=CARTESIAN_POINT('Ctrl Pts',(11.3481993449189,-0.234663168166497,
4.54685844933023));
#54155=CARTESIAN_POINT('Ctrl Pts',(11.3417480336984,-0.161234786808821,
4.57836740127901));
#54156=CARTESIAN_POINT('Ctrl Pts',(11.335296722478,-0.080829826651965,4.59361815176584));
#54157=CARTESIAN_POINT('Ctrl Pts',(11.3288454112576,-0.000294350894641693,
4.59325842069974));
#54158=CARTESIAN_POINT('Ctrl Pts',(11.2211545887425,0.000456638431143918,
4.59352536526061));
#54159=CARTESIAN_POINT('Ctrl Pts',(11.2317054196788,-0.131106980996848,
4.59258691018808));
#54160=CARTESIAN_POINT('Ctrl Pts',(11.2422562506151,-0.263229208150973,
4.54946171071576));
#54161=CARTESIAN_POINT('Ctrl Pts',(11.2528070815514,-0.366229002642205,
4.4690386804108));
#54162=CARTESIAN_POINT('Ctrl Pts',(11.268712360239,-0.521500226874852,4.34780171645731));
#54163=CARTESIAN_POINT('Ctrl Pts',(11.2846176389266,-0.610589908195122,
4.1418043885479));
#54164=CARTESIAN_POINT('Ctrl Pts',(11.3005229176142,-0.592591834014348,
3.94563195463032));
#54165=CARTESIAN_POINT('Ctrl Pts',(11.3164281963018,-0.574593759833574,
3.74945952071274));
#54166=CARTESIAN_POINT('Ctrl Pts',(11.3323334749894,-0.449507930151742,
3.56311198078699));
#54167=CARTESIAN_POINT('Ctrl Pts',(11.3482387536771,-0.274768466013715,
3.47215224147272));
#54168=CARTESIAN_POINT('Ctrl Pts',(11.3641440323647,-0.100029001875688,
3.38119250215845));
#54169=CARTESIAN_POINT('Ctrl Pts',(11.3800493110523,0.12436409671854,3.38562056345565));
#54170=CARTESIAN_POINT('Ctrl Pts',(11.3959545897399,0.295379012183608,3.48340324695247));
#54171=CARTESIAN_POINT('Ctrl Pts',(11.4118598684275,0.466393927648671,3.5811859304493));
#54172=CARTESIAN_POINT('Ctrl Pts',(11.4277651471151,0.584030659984583,3.77232323614575));
#54173=CARTESIAN_POINT('Ctrl Pts',(11.4436704258027,0.594275398502411,3.96905299961855));
#54174=CARTESIAN_POINT('Ctrl Pts',(11.4595757044903,0.60452013702024,4.16578276309136));
#54175=CARTESIAN_POINT('Ctrl Pts',(11.475480983178,0.507372881719984,4.36810498434052));
#54176=CARTESIAN_POINT('Ctrl Pts',(11.4913862618656,0.34743954227408,4.48312185891572));
#54177=CARTESIAN_POINT('Ctrl Pts',(11.5013090374912,0.247662438486696,4.55487707062799));
#54178=CARTESIAN_POINT('Ctrl Pts',(11.5112318131169,0.123448374926332,4.59265218509947));
#54179=CARTESIAN_POINT('Ctrl Pts',(11.5211545887425,-0.0003715675665865,
4.59335763259963));
#54180=CARTESIAN_POINT('Origin',(4.,0.,4.));
#54181=CARTESIAN_POINT('',(11.9288454112576,0.000492284285450728,4.5944814532616));
#54182=CARTESIAN_POINT('',(11.8211545887425,-0.000307672146732893,4.59488449882539));
#54183=CARTESIAN_POINT('',(4.,-7.27562663373442E-17,4.5941));
#54184=CARTESIAN_POINT('Ctrl Pts',(11.9288454112576,0.000492284285450728,
4.5944814532616));
#54185=CARTESIAN_POINT('Ctrl Pts',(11.9261600667293,0.0338400408399785,
4.59477876231094));
#54186=CARTESIAN_POINT('Ctrl Pts',(11.9234747222011,0.0671420792079604,
4.59221542322669));
#54187=CARTESIAN_POINT('Ctrl Pts',(11.9207893776729,0.0999293694653808,
4.5866302815369));
#54188=CARTESIAN_POINT('Ctrl Pts',(11.9048840989853,0.294128282668868,4.55354952256816));
#54189=CARTESIAN_POINT('Ctrl Pts',(11.8889788202977,0.470268877700486,4.41445832512751));
#54190=CARTESIAN_POINT('Ctrl Pts',(11.8730735416101,0.547474845215755,4.2332214826164));
#54191=CARTESIAN_POINT('Ctrl Pts',(11.8571682629225,0.624680812731027,4.05198464010529));
#54192=CARTESIAN_POINT('Ctrl Pts',(11.8412629842349,0.602952152729945,3.82860215252373));
#54193=CARTESIAN_POINT('Ctrl Pts',(11.8253577055472,0.492265746621211,3.66564180763548));
#54194=CARTESIAN_POINT('Ctrl Pts',(11.8094524268596,0.38157934051248,3.50268146274723));
#54195=CARTESIAN_POINT('Ctrl Pts',(11.793547148172,0.181935188296101,3.40014326055229));
#54196=CARTESIAN_POINT('Ctrl Pts',(11.7776418694844,-0.0149985615777061,
3.40510840546499));
#54197=CARTESIAN_POINT('Ctrl Pts',(11.7617365907968,-0.211932311451519,
3.41007355037768));
#54198=CARTESIAN_POINT('Ctrl Pts',(11.7458313121092,-0.406155658982761,
3.52254204239802));
#54199=CARTESIAN_POINT('Ctrl Pts',(11.7299260334216,-0.508489459897291,
3.69087310813977));
#54200=CARTESIAN_POINT('Ctrl Pts',(11.714020754734,-0.610823260811815,3.8592041738815));
#54201=CARTESIAN_POINT('Ctrl Pts',(11.6981154760463,-0.621267515109637,
4.08339781334463));
#54202=CARTESIAN_POINT('Ctrl Pts',(11.6822101973587,-0.53502666307716,4.26051379213839));
#54203=CARTESIAN_POINT('Ctrl Pts',(11.6663049186711,-0.448785811044678,
4.43762977093217));
#54204=CARTESIAN_POINT('Ctrl Pts',(11.6503996399835,-0.265859852681883,
4.56766808905658));
#54205=CARTESIAN_POINT('Ctrl Pts',(11.6344943612959,-0.070240649109886,
4.59092065229643));
#54206=CARTESIAN_POINT('Ctrl Pts',(11.6326113779498,-0.0470818155087989,
4.59367346098309));
#54207=CARTESIAN_POINT('Ctrl Pts',(11.6307283946037,-0.0237450789937817,
4.59492960773286));
#54208=CARTESIAN_POINT('Ctrl Pts',(11.6288454112576,-0.000389145320547679,
4.59475273347735));
#54209=CARTESIAN_POINT('Ctrl Pts',(11.5211545887425,-0.0003715675665865,
4.59335763259963));
#54210=CARTESIAN_POINT('Ctrl Pts',(11.5271370918045,-0.0750233800274846,
4.5937829512795));
#54211=CARTESIAN_POINT('Ctrl Pts',(11.5331195948664,-0.149531931096223,
4.58073359799715));
#54212=CARTESIAN_POINT('Ctrl Pts',(11.5391020979284,-0.218455391669058,
4.55353248138526));
#54213=CARTESIAN_POINT('Ctrl Pts',(11.555007376616,-0.40169756257477,4.48121470137836));
#54214=CARTESIAN_POINT('Ctrl Pts',(11.5709126553036,-0.545462480794654,
4.3088676134633));
#54215=CARTESIAN_POINT('Ctrl Pts',(11.5868179339912,-0.583739378074245,
4.1156257090067));
#54216=CARTESIAN_POINT('Ctrl Pts',(11.6027232126789,-0.622016275353834,
3.92238380455011));
#54217=CARTESIAN_POINT('Ctrl Pts',(11.6186284913665,-0.554805151693135,
3.70824708355197));
#54218=CARTESIAN_POINT('Ctrl Pts',(11.6345337700541,-0.412966511608993,
3.57153806891708));
#54219=CARTESIAN_POINT('Ctrl Pts',(11.6504390487417,-0.271127871524847,
3.43482905428217));
#54220=CARTESIAN_POINT('Ctrl Pts',(11.6663443274293,-0.0546617150172531,
3.37554774601052));
#54221=CARTESIAN_POINT('Ctrl Pts',(11.6822496061169,0.137039856773353,3.42091361287512));
#54222=CARTESIAN_POINT('Ctrl Pts',(11.6981548848045,0.328741428563947,3.46627947973972));
#54223=CARTESIAN_POINT('Ctrl Pts',(11.7140601634921,0.495678415637556,3.61629252174057));
#54224=CARTESIAN_POINT('Ctrl Pts',(11.7299654421798,0.56120041605148,3.80207309651931));
#54225=CARTESIAN_POINT('Ctrl Pts',(11.7458707208674,0.626722416465409,3.98785367129807));
#54226=CARTESIAN_POINT('Ctrl Pts',(11.761775999555,0.590829430219633,4.20940177885472));
#54227=CARTESIAN_POINT('Ctrl Pts',(11.7776812782426,0.470001998091193,4.36499190112672));
#54228=CARTESIAN_POINT('Ctrl Pts',(11.7921723817426,0.359917612963646,4.5067481450567));
#54229=CARTESIAN_POINT('Ctrl Pts',(11.8066634852425,0.179330777996457,4.59375393408315));
#54230=CARTESIAN_POINT('Ctrl Pts',(11.8211545887425,-0.000307672146732893,
4.59488449882539));
#54231=CARTESIAN_POINT('Origin',(4.,0.,4.));
#54232=CARTESIAN_POINT('',(12.2288454112576,0.000142795628640946,4.59314744373127));
#54233=CARTESIAN_POINT('',(12.1211545887425,0.00052868291625318,4.59430727435519));
#54234=CARTESIAN_POINT('',(4.,-7.27562663373442E-17,4.5941));
#54235=CARTESIAN_POINT('Ctrl Pts',(12.2288454112576,0.000142795628640946,
4.59314744373127));
#54236=CARTESIAN_POINT('Ctrl Pts',(12.221591738855,0.0907369315914116,4.59334157666405));
#54237=CARTESIAN_POINT('Ctrl Pts',(12.2143380664525,0.181251971066953,4.57388161006077));
#54238=CARTESIAN_POINT('Ctrl Pts',(12.2070843940499,0.261922584292681,4.53433840020651));
#54239=CARTESIAN_POINT('Ctrl Pts',(12.1911791153623,0.438810719578057,4.44763117963851));
#54240=CARTESIAN_POINT('Ctrl Pts',(12.1752738366747,0.56836661021043,4.26436322928705));
#54241=CARTESIAN_POINT('Ctrl Pts',(12.1593685579871,0.591103672269137,4.06868343852597));
#54242=CARTESIAN_POINT('Ctrl Pts',(12.1434632792995,0.613840734327844,3.87300364776488));
#54243=CARTESIAN_POINT('Ctrl Pts',(12.1275580006119,0.529758967812885,3.66491201659415));
#54244=CARTESIAN_POINT('Ctrl Pts',(12.1116527219243,0.377465162701742,3.53995541841648));
#54245=CARTESIAN_POINT('Ctrl Pts',(12.0957474432367,0.225171357590603,3.41499882023882));
#54246=CARTESIAN_POINT('Ctrl Pts',(12.0798421645491,0.00466551388328543,
3.37317725505421));
#54247=CARTESIAN_POINT('Ctrl Pts',(12.0639368858614,-0.182805413822737,
3.43369341627091));
#54248=CARTESIAN_POINT('Ctrl Pts',(12.0480316071738,-0.37027634152876,3.49420957748762));
#54249=CARTESIAN_POINT('Ctrl Pts',(12.0321263284862,-0.524712353233489,
3.65706346510565));
#54250=CARTESIAN_POINT('Ctrl Pts',(12.0162210497986,-0.575202966010955,
3.84747946371059));
#54251=CARTESIAN_POINT('Ctrl Pts',(12.000315771111,-0.625693578788423,4.03789546231555));
#54252=CARTESIAN_POINT('Ctrl Pts',(11.9844104924234,-0.572238792638624,
4.25587357190742));
#54253=CARTESIAN_POINT('Ctrl Pts',(11.9685052137358,-0.439382783876041,
4.40132746645495));
#54254=CARTESIAN_POINT('Ctrl Pts',(11.9552852795764,-0.328957325572706,
4.52222386487166));
#54255=CARTESIAN_POINT('Ctrl Pts',(11.942065345417,-0.163678510702966,4.59301780268865));
#54256=CARTESIAN_POINT('Ctrl Pts',(11.9288454112576,0.000492284285450728,
4.5944814532616));
#54257=CARTESIAN_POINT('Ctrl Pts',(11.8211545887425,-0.000307672146732893,
4.59488449882539));
#54258=CARTESIAN_POINT('Ctrl Pts',(11.8225687639301,-0.0178384446610953,
4.59499482973335));
#54259=CARTESIAN_POINT('Ctrl Pts',(11.8239829391178,-0.035360185088601,
4.59428731490513));
#54260=CARTESIAN_POINT('Ctrl Pts',(11.8253971143054,-0.0528064866265509,
4.59273302680715));
#54261=CARTESIAN_POINT('Ctrl Pts',(11.8413023929931,-0.249025661204777,
4.57525189322826));
#54262=CARTESIAN_POINT('Ctrl Pts',(11.8572076716807,-0.435702132350142,
4.45065748908313));
#54263=CARTESIAN_POINT('Ctrl Pts',(11.8731129503683,-0.527121962142897,
4.27615829360067));
#54264=CARTESIAN_POINT('Ctrl Pts',(11.8890182290559,-0.618541791935657,
4.10165909811819));
#54265=CARTESIAN_POINT('Ctrl Pts',(11.9049235077435,-0.614704980375792,
3.87725511129838));
#54266=CARTESIAN_POINT('Ctrl Pts',(11.9208287864311,-0.517373229009482,
3.70598315013913));
#54267=CARTESIAN_POINT('Ctrl Pts',(11.9367340651187,-0.420041477643178,
3.53471118897989));
#54268=CARTESIAN_POINT('Ctrl Pts',(11.9526393438063,-0.229214786470442,
3.41657125348121));
#54269=CARTESIAN_POINT('Ctrl Pts',(11.9685446224939,-0.0325126988662629,
3.4058082039356));
#54270=CARTESIAN_POINT('Ctrl Pts',(11.9844499011816,0.164189388737916,3.39504515438998));
#54271=CARTESIAN_POINT('Ctrl Pts',(12.0003551798692,0.366766872773537,3.49165899079743));
#54272=CARTESIAN_POINT('Ctrl Pts',(12.0162604585568,0.482204742918021,3.65128872687397));
#54273=CARTESIAN_POINT('Ctrl Pts',(12.0321657372444,0.597642613062508,3.81091846295053));
#54274=CARTESIAN_POINT('Ctrl Pts',(12.048071015932,0.625940869315854,4.03356409869619));
#54275=CARTESIAN_POINT('Ctrl Pts',(12.0639762946196,0.554106149607013,4.21699617753661));
#54276=CARTESIAN_POINT('Ctrl Pts',(12.0798815733072,0.482271429898174,4.40042825637702));
#54277=CARTESIAN_POINT('Ctrl Pts',(12.0957868519948,0.310303734227154,4.5446467783122));
#54278=CARTESIAN_POINT('Ctrl Pts',(12.1116921306825,0.117163353092859,4.583432699452));
#54279=CARTESIAN_POINT('Ctrl Pts',(12.1148462833691,0.0788619649798074,
4.59112427906975));
#54280=CARTESIAN_POINT('Ctrl Pts',(12.1180004360558,0.0397279339241207,
4.59466958677844));
#54281=CARTESIAN_POINT('Ctrl Pts',(12.1211545887425,0.00052868291625318,
4.59430727435519));
#54282=CARTESIAN_POINT('Origin',(4.,0.,4.));
#54283=CARTESIAN_POINT('',(12.5288454112576,-0.000545899910317726,4.59395595168017));
#54284=CARTESIAN_POINT('',(12.4211545887425,4.74932194801069E-5,4.59311952367199));
#54285=CARTESIAN_POINT('',(4.,-7.27562663373442E-17,4.5941));
#54286=CARTESIAN_POINT('Ctrl Pts',(12.5288454112576,-0.000545899910317726,
4.59395595168017));
#54287=CARTESIAN_POINT('Ctrl Pts',(12.5170234109807,0.14659828900878,4.5926299020853));
#54288=CARTESIAN_POINT('Ctrl Pts',(12.5052014107038,0.29463204299547,4.53735693360054));
#54289=CARTESIAN_POINT('Ctrl Pts',(12.493379410427,0.402483765871145,4.43832383497591));
#54290=CARTESIAN_POINT('Ctrl Pts',(12.4774741317394,0.547587104485886,4.30508504322883));
#54291=CARTESIAN_POINT('Ctrl Pts',(12.4615688530518,0.619957272242066,4.09263639239171));
#54292=CARTESIAN_POINT('Ctrl Pts',(12.4456635743641,0.586364949835353,3.89852531496775));
#54293=CARTESIAN_POINT('Ctrl Pts',(12.4297582956765,0.55277262742864,3.7044142375438));
#54294=CARTESIAN_POINT('Ctrl Pts',(12.4138530169889,0.41321781485904,3.52864073353302));
#54295=CARTESIAN_POINT('Ctrl Pts',(12.3979477383013,0.231778177981285,3.45191255961345));
#54296=CARTESIAN_POINT('Ctrl Pts',(12.3820424596137,0.0503385411035255,
3.37518438569388));
#54297=CARTESIAN_POINT('Ctrl Pts',(12.3661371809261,-0.172985920082391,
3.39750154186552));
#54298=CARTESIAN_POINT('Ctrl Pts',(12.3502319022385,-0.335654061078685,
3.50861693417539));
#54299=CARTESIAN_POINT('Ctrl Pts',(12.3343266235509,-0.498322202074975,
3.61973232648525));
#54300=CARTESIAN_POINT('Ctrl Pts',(12.3184213448632,-0.600334022881645,
3.81964595493332));
#54301=CARTESIAN_POINT('Ctrl Pts',(12.3025160661756,-0.594850011148503,
4.0165659389844));
#54302=CARTESIAN_POINT('Ctrl Pts',(12.286610787488,-0.58936599941536,4.21348592303547));
#54303=CARTESIAN_POINT('Ctrl Pts',(12.2707055088004,-0.476386155142398,
4.40741226268955));
#54304=CARTESIAN_POINT('Ctrl Pts',(12.2548002301128,-0.307786043036728,
4.50930218712431));
#54305=CARTESIAN_POINT('Ctrl Pts',(12.2461486238277,-0.216076754679914,
4.564724762732));
#54306=CARTESIAN_POINT('Ctrl Pts',(12.2374970175426,-0.107910718865932,
4.59291589733543));
#54307=CARTESIAN_POINT('Ctrl Pts',(12.2288454112576,0.000142795628640946,
4.59314744373127));
#54308=CARTESIAN_POINT('Ctrl Pts',(12.1211545887425,0.00052868291625318,
4.59430727435519));
#54309=CARTESIAN_POINT('Ctrl Pts',(12.1339057147434,-0.157940052872902,
4.59284257311225));
#54310=CARTESIAN_POINT('Ctrl Pts',(12.1466568407444,-0.317474678016714,
4.52751565545538));
#54311=CARTESIAN_POINT('Ctrl Pts',(12.1594079667453,-0.427372353356377,
4.41409399619463));
#54312=CARTESIAN_POINT('Ctrl Pts',(12.1753132454329,-0.564454612073754,
4.27261605145303));
#54313=CARTESIAN_POINT('Ctrl Pts',(12.1912185241205,-0.62430606291093,4.0563068416254));
#54314=CARTESIAN_POINT('Ctrl Pts',(12.2071238028081,-0.579445451749542,
3.8644864045766));
#54315=CARTESIAN_POINT('Ctrl Pts',(12.2230290814957,-0.534584840588155,
3.6726659675278));
#54316=CARTESIAN_POINT('Ctrl Pts',(12.2389343601834,-0.38501216742821,3.50533430325784));
#54317=CARTESIAN_POINT('Ctrl Pts',(12.254839638871,-0.199404875886796,3.43932303278057));
#54318=CARTESIAN_POINT('Ctrl Pts',(12.2707449175586,-0.0137975843453769,
3.37331176230329));
#54319=CARTESIAN_POINT('Ctrl Pts',(12.2866501962462,0.207844325577514,3.40862088561871));
#54320=CARTESIAN_POINT('Ctrl Pts',(12.3025554749338,0.363752265741203,3.52903794710619));
#54321=CARTESIAN_POINT('Ctrl Pts',(12.3184607536214,0.519660205904889,3.64945500859368));
#54322=CARTESIAN_POINT('Ctrl Pts',(12.334366032309,0.609834176309377,3.85498000825323));
#54323=CARTESIAN_POINT('Ctrl Pts',(12.3502713109967,0.592870104691008,4.05124456128685));
#54324=CARTESIAN_POINT('Ctrl Pts',(12.3661765896843,0.575906033072638,4.24750911432049));
#54325=CARTESIAN_POINT('Ctrl Pts',(12.3820818683719,0.451803919431404,4.4345132207282));
#54326=CARTESIAN_POINT('Ctrl Pts',(12.3979871470595,0.277546204023914,4.52639250633888));
#54327=CARTESIAN_POINT('Ctrl Pts',(12.4057096276205,0.192938958450368,4.57100260157974));
#54328=CARTESIAN_POINT('Ctrl Pts',(12.4134321081815,0.0965080911524262,
4.59318808505049));
#54329=CARTESIAN_POINT('Ctrl Pts',(12.4211545887425,4.74932194801069E-5,
4.59311952367199));
#54330=CARTESIAN_POINT('Origin',(4.,0.,4.));
#54331=CARTESIAN_POINT('',(12.8288454112576,0.000112157221815526,4.59505491513413));
#54332=CARTESIAN_POINT('',(12.7211545887425,-0.000546355209092884,4.59413239245978));
#54333=CARTESIAN_POINT('',(4.,-7.27562663373442E-17,4.5941));
#54334=CARTESIAN_POINT('Ctrl Pts',(12.8288454112576,0.000112157221815526,
4.59505491513413));
#54335=CARTESIAN_POINT('Ctrl Pts',(12.828360361794,0.00612048155630211,
4.59507046002904));
#54336=CARTESIAN_POINT('Ctrl Pts',(12.8278753123304,0.0121283652366354,
4.59498736156652));
#54337=CARTESIAN_POINT('Ctrl Pts',(12.8273902628668,0.0181332013859869,
4.59480429815638));
#54338=CARTESIAN_POINT('Ctrl Pts',(12.8114849841792,0.215038052543873,4.58880145767424));
#54339=CARTESIAN_POINT('Ctrl Pts',(12.7955797054916,0.408666038032992,4.47531104548453));
#54340=CARTESIAN_POINT('Ctrl Pts',(12.779674426804,0.510111378641258,4.30644305748136));
#54341=CARTESIAN_POINT('Ctrl Pts',(12.7637691481164,0.611556719249521,4.1375750694782));
#54342=CARTESIAN_POINT('Ctrl Pts',(12.7478638694288,0.620819414976937,3.9133295056616));
#54343=CARTESIAN_POINT('Ctrl Pts',(12.7319585907412,0.533646427817818,3.7366704418887));
#54344=CARTESIAN_POINT('Ctrl Pts',(12.7160533120536,0.446473440658691,3.56001137811579));
#54345=CARTESIAN_POINT('Ctrl Pts',(12.700148033366,0.26286477061301,3.43093881438659));
#54346=CARTESIAN_POINT('Ctrl Pts',(12.6842427546783,0.0671257511235207,
3.4087174113557));
#54347=CARTESIAN_POINT('Ctrl Pts',(12.6683374759907,-0.128613268365957,
3.38649600832481));
#54348=CARTESIAN_POINT('Ctrl Pts',(12.6524321973031,-0.336482637299241,
3.47112576599221));
#54349=CARTESIAN_POINT('Ctrl Pts',(12.6365269186155,-0.461037535689932,
3.62374828002683));
#54350=CARTESIAN_POINT('Ctrl Pts',(12.6206216399279,-0.585592434080627,
3.77637079406146));
#54351=CARTESIAN_POINT('Ctrl Pts',(12.6047163612403,-0.626832861928724,
3.9969860644633));
#54352=CARTESIAN_POINT('Ctrl Pts',(12.5888110825527,-0.565822959504995,
4.18429689252621));
#54353=CARTESIAN_POINT('Ctrl Pts',(12.5729058038651,-0.504813057081268,
4.37160772058911));
#54354=CARTESIAN_POINT('Ctrl Pts',(12.5570005251774,-0.341552824385721,
4.52561410631309));
#54355=CARTESIAN_POINT('Ctrl Pts',(12.5410952464898,-0.151004453301302,
4.57560283284656));
#54356=CARTESIAN_POINT('Ctrl Pts',(12.5370119680791,-0.102085973774189,
4.58843617527608));
#54357=CARTESIAN_POINT('Ctrl Pts',(12.5329286896683,-0.0513689988622793,
4.59441396466913));
#54358=CARTESIAN_POINT('Ctrl Pts',(12.5288454112576,-0.000545899910317726,
4.59395595168017));
#54359=CARTESIAN_POINT('Ctrl Pts',(12.4211545887425,4.74932194801069E-5,
4.59311952367199));
#54360=CARTESIAN_POINT('Ctrl Pts',(12.4293373868691,-0.102162877376194,
4.59304687552285));
#54361=CARTESIAN_POINT('Ctrl Pts',(12.4375201849957,-0.204406628577491,
4.5679880979308));
#54362=CARTESIAN_POINT('Ctrl Pts',(12.4457029831223,-0.292652646395614,
4.51814611323009));
#54363=CARTESIAN_POINT('Ctrl Pts',(12.4616082618099,-0.46418046423393,4.42126596969699));
#54364=CARTESIAN_POINT('Ctrl Pts',(12.4775135404976,-0.582822782736806,
4.23075121781716));
#54365=CARTESIAN_POINT('Ctrl Pts',(12.4934188191852,-0.594104068590283,
4.03407817163935));
#54366=CARTESIAN_POINT('Ctrl Pts',(12.5093240978728,-0.605385354443759,
3.83740512546155));
#54367=CARTESIAN_POINT('Ctrl Pts',(12.5252293765604,-0.509305607647849,
3.63457378498577));
#54368=CARTESIAN_POINT('Ctrl Pts',(12.541134655248,-0.34998058313236,3.51871572067214));
#54369=CARTESIAN_POINT('Ctrl Pts',(12.5570399339356,-0.19065555861687,3.4028576563585));
#54370=CARTESIAN_POINT('Ctrl Pts',(12.5729452126232,0.031914743618199,3.37397286820701));
#54371=CARTESIAN_POINT('Ctrl Pts',(12.5888504913108,0.215535456959467,3.44532402892222));
#54372=CARTESIAN_POINT('Ctrl Pts',(12.6047557699985,0.399156170300736,3.51667518963742));
#54373=CARTESIAN_POINT('Ctrl Pts',(12.6206610486861,0.543827294748204,3.68826229921932));
#54374=CARTESIAN_POINT('Ctrl Pts',(12.6365663273737,0.583121970486127,3.88129981619987));
#54375=CARTESIAN_POINT('Ctrl Pts',(12.6524716060613,0.622416646224052,4.07433733318042));
#54376=CARTESIAN_POINT('Ctrl Pts',(12.6683768847489,0.556334873252426,4.28882525755962));
#54377=CARTESIAN_POINT('Ctrl Pts',(12.6842821634365,0.415218606030559,4.42627980869829));
#54378=CARTESIAN_POINT('Ctrl Pts',(12.6965729718718,0.306170972122536,4.53249785050629));
#54379=CARTESIAN_POINT('Ctrl Pts',(12.7088637803072,0.152317016475741,4.59271595401221));
#54380=CARTESIAN_POINT('Ctrl Pts',(12.7211545887425,-0.000546355209092884,
4.59413239245978));
#54381=CARTESIAN_POINT('Origin',(4.,0.,4.));
#54382=CARTESIAN_POINT('',(13.1288454112576,0.000488576923893258,4.59361798633976));
#54383=CARTESIAN_POINT('',(13.0211545887425,0.000215375668158819,4.59498635240753));
#54384=CARTESIAN_POINT('',(4.,-7.27562663373442E-17,4.5941));
#54385=CARTESIAN_POINT('Ctrl Pts',(13.1288454112576,0.000488576923893258,
4.59361798633976));
#54386=CARTESIAN_POINT('Ctrl Pts',(13.1237920339197,0.0634769139372694,
4.59410397103046));
#54387=CARTESIAN_POINT('Ctrl Pts',(13.1187386565818,0.126326538027094,4.58487602541266));
#54388=CARTESIAN_POINT('Ctrl Pts',(13.1136852792439,0.185787091792062,4.56533540718874));
#54389=CARTESIAN_POINT('Ctrl Pts',(13.0977800005563,0.372936519850693,4.50383218710482));
#54390=CARTESIAN_POINT('Ctrl Pts',(13.0818747218686,0.526512210440984,4.34016674272733));
#54391=CARTESIAN_POINT('Ctrl Pts',(13.065969443181,0.575998703695535,4.14948732200047));
#54392=CARTESIAN_POINT('Ctrl Pts',(13.0500641644934,0.625485196950086,3.9588079012736));
#54393=CARTESIAN_POINT('Ctrl Pts',(13.0341588858058,0.570882492868891,3.74111450419737));
#54394=CARTESIAN_POINT('Ctrl Pts',(13.0182536071182,0.437261843116128,3.59636272886105));
#54395=CARTESIAN_POINT('Ctrl Pts',(13.0023483284306,0.303641193363369,3.45161095352474));
#54396=CARTESIAN_POINT('Ctrl Pts',(12.986443049743,0.0910025979390456,3.37980079992835));
#54397=CARTESIAN_POINT('Ctrl Pts',(12.9705377710554,-0.10301929613509,3.41390445256627));
#54398=CARTESIAN_POINT('Ctrl Pts',(12.9546324923678,-0.297041190209231,
3.4480081052042));
#54399=CARTESIAN_POINT('Ctrl Pts',(12.9387272136801,-0.472446382933184,
3.58802556407645));
#54400=CARTESIAN_POINT('Ctrl Pts',(12.9228219349925,-0.54869623058984,3.76966673571907));
#54401=CARTESIAN_POINT('Ctrl Pts',(12.9069166563049,-0.624946078246494,
3.95130790736168));
#54402=CARTESIAN_POINT('Ctrl Pts',(12.8910113776173,-0.602040580835857,
4.17457279177466));
#54403=CARTESIAN_POINT('Ctrl Pts',(12.8751060989297,-0.490496973717212,
4.33694759959386));
#54404=CARTESIAN_POINT('Ctrl Pts',(12.8596858697056,-0.382355015061345,
4.49437060399126));
#54405=CARTESIAN_POINT('Ctrl Pts',(12.8442656404816,-0.190898750836606,
4.59456072668396));
#54406=CARTESIAN_POINT('Ctrl Pts',(12.8288454112576,0.000112157221815526,
4.59505491513413));
#54407=CARTESIAN_POINT('Ctrl Pts',(12.7211545887425,-0.000546355209092884,
4.59413239245978));
#54408=CARTESIAN_POINT('Ctrl Pts',(12.7247690589948,-0.0455002825709059,
4.59454893744622));
#54409=CARTESIAN_POINT('Ctrl Pts',(12.7283835292471,-0.0903685417208244,
4.58988016539195));
#54410=CARTESIAN_POINT('Ctrl Pts',(12.7319979994994,-0.13398639330236,4.5798004937111));
#54411=CARTESIAN_POINT('Ctrl Pts',(12.747903278187,-0.325924363941296,4.53544544968711));
#54412=CARTESIAN_POINT('Ctrl Pts',(12.7638085568746,-0.493649543747071,
4.38631418374101));
#54413=CARTESIAN_POINT('Ctrl Pts',(12.7797138355622,-0.560149626020051,
4.20088146397168));
#54414=CARTESIAN_POINT('Ctrl Pts',(12.7956191142498,-0.626649708293032,
4.01544874420235));
#54415=CARTESIAN_POINT('Ctrl Pts',(12.8115243929374,-0.591924693033219,
3.79371457060979));
#54416=CARTESIAN_POINT('Ctrl Pts',(12.827429671625,-0.471918838153678,3.63748989490844));
#54417=CARTESIAN_POINT('Ctrl Pts',(12.8433349503126,-0.351912983274129,
3.48126521920708));
#54418=CARTESIAN_POINT('Ctrl Pts',(12.8592402290002,-0.146626288774854,
3.39055004139693));
#54419=CARTESIAN_POINT('Ctrl Pts',(12.8751455076879,0.0496822801939141,
3.40699693328572));
#54420=CARTESIAN_POINT('Ctrl Pts',(12.8910507863755,0.245990849162665,3.42344382517451));
#54421=CARTESIAN_POINT('Ctrl Pts',(12.9069560650631,0.433321292600904,3.54705278676224));
#54422=CARTESIAN_POINT('Ctrl Pts',(12.9228613437507,0.525659396179275,3.72106781235173));
#54423=CARTESIAN_POINT('Ctrl Pts',(12.9387666224383,0.617997499757654,3.89508283794124));
#54424=CARTESIAN_POINT('Ctrl Pts',(12.9546719011259,0.615343263476151,4.11950392753251));
#54425=CARTESIAN_POINT('Ctrl Pts',(12.9705771798135,0.518915400343756,4.29128641125856));
#54426=CARTESIAN_POINT('Ctrl Pts',(12.9864824585012,0.422487537211366,4.46306889498459));
#54427=CARTESIAN_POINT('Ctrl Pts',(13.0023877371888,0.232286047228094,4.58221277284539));
#54428=CARTESIAN_POINT('Ctrl Pts',(13.0182930158764,0.0356434078328121,
4.59401221668908));
#54429=CARTESIAN_POINT('Ctrl Pts',(13.0192468734984,0.0238505254767134,
4.59471984273368));
#54430=CARTESIAN_POINT('Ctrl Pts',(13.0202007311205,0.0120344772878951,
4.59504140054066));
#54431=CARTESIAN_POINT('Ctrl Pts',(13.0211545887425,0.000215375668158819,
4.59498635240753));
#54432=CARTESIAN_POINT('Origin',(4.,0.,4.));
#54433=CARTESIAN_POINT('',(13.4288454112576,-0.000323145728561625,4.59329116515504));
#54434=CARTESIAN_POINT('',(13.3211545887425,0.000436239896754628,4.59347700091179));
#54435=CARTESIAN_POINT('',(4.,-7.27562663373442E-17,4.5941));
#54436=CARTESIAN_POINT('Ctrl Pts',(13.4288454112576,-0.000323145728561625,
4.59329116515504));
#54437=CARTESIAN_POINT('Ctrl Pts',(13.4192237060453,0.11977362227264,4.59270025156928));
#54438=CARTESIAN_POINT('Ctrl Pts',(13.4096020008331,0.240190260834984,4.55734300206483));
#54439=CARTESIAN_POINT('Ctrl Pts',(13.3999802956209,0.338238798929947,4.48960747645051));
#54440=CARTESIAN_POINT('Ctrl Pts',(13.3840750169333,0.500319146323361,4.37763642888821));
#54441=CARTESIAN_POINT('Ctrl Pts',(13.3681697382457,0.601276083433826,4.17718801339723));
#54442=CARTESIAN_POINT('Ctrl Pts',(13.3522644595581,0.594754455875995,3.9802996620979));
#54443=CARTESIAN_POINT('Ctrl Pts',(13.3363591808704,0.588232828318166,3.78341131079859));
#54444=CARTESIAN_POINT('Ctrl Pts',(13.3204539021828,0.474232636092054,3.59008302369095));
#54445=CARTESIAN_POINT('Ctrl Pts',(13.3045486234952,0.305097944517489,3.48908297116948));
#54446=CARTESIAN_POINT('Ctrl Pts',(13.2886433448076,0.135963252942929,3.388082918648));
#54447=CARTESIAN_POINT('Ctrl Pts',(13.27273806612,-0.0883059379800925,3.3794111007127));
#54448=CARTESIAN_POINT('Ctrl Pts',(13.2568327874324,-0.264734703826722,
3.46704924928509));
#54449=CARTESIAN_POINT('Ctrl Pts',(13.2409275087448,-0.441163469673367,
3.55468739785749));
#54450=CARTESIAN_POINT('Ctrl Pts',(13.2250222300572,-0.569751810443623,
3.7386355129376));
#54451=CARTESIAN_POINT('Ctrl Pts',(13.2091169513696,-0.591457400179852,
3.9344324022836));
#54452=CARTESIAN_POINT('Ctrl Pts',(13.1932116726819,-0.613162989916079,
4.1302292916296));
#54453=CARTESIAN_POINT('Ctrl Pts',(13.1773063939943,-0.527985828618295,
4.33787495524147));
#54454=CARTESIAN_POINT('Ctrl Pts',(13.1614011153067,-0.375035665205916,
4.46202728915223));
#54455=CARTESIAN_POINT('Ctrl Pts',(13.150549213957,-0.270680367988337,4.54673431669939));
#54456=CARTESIAN_POINT('Ctrl Pts',(13.1396973126073,-0.134776053786733,
4.59257435599745));
#54457=CARTESIAN_POINT('Ctrl Pts',(13.1288454112576,0.000488576923893258,
4.59361798633976));
#54458=CARTESIAN_POINT('Ctrl Pts',(13.0211545887425,0.000215375668158819,
4.59498635240753));
#54459=CARTESIAN_POINT('Ctrl Pts',(13.0361060098081,-0.185045360160338,
4.59412349007018));
#54460=CARTESIAN_POINT('Ctrl Pts',(13.0510574308736,-0.371056311319581,
4.5007301079696));
#54461=CARTESIAN_POINT('Ctrl Pts',(13.0660088519392,-0.480360474535337,
4.35124746348123));
#54462=CARTESIAN_POINT('Ctrl Pts',(13.0819141306268,-0.596637928700896,
4.19222825660313));
#54463=CARTESIAN_POINT('Ctrl Pts',(13.0978194093145,-0.626109048224722,
3.96973483302036));
#54464=CARTESIAN_POINT('Ctrl Pts',(13.1137246880021,-0.555241941841719,
3.78592675992164));
#54465=CARTESIAN_POINT('Ctrl Pts',(13.1296299666897,-0.484374835458714,
3.60211868682292));
#54466=CARTESIAN_POINT('Ctrl Pts',(13.1455352453773,-0.313169503168878,
3.45699596420825));
#54467=CARTESIAN_POINT('Ctrl Pts',(13.1614405240649,-0.120236190459409,
3.4171928066662));
#54468=CARTESIAN_POINT('Ctrl Pts',(13.1773458027525,0.0726971222500488,
3.37738964912416));
#54469=CARTESIAN_POINT('Ctrl Pts',(13.1932510814401,0.287358415379145,3.44290605665475));
#54470=CARTESIAN_POINT('Ctrl Pts',(13.2091563601277,0.425184304693362,3.58365966669054));
#54471=CARTESIAN_POINT('Ctrl Pts',(13.2250616388154,0.563010194007583,3.72441327672633));
#54472=CARTESIAN_POINT('Ctrl Pts',(13.240966917503,0.624000679506934,3.94040408926733));
#54473=CARTESIAN_POINT('Ctrl Pts',(13.2568721961906,0.580151510544767,4.13245826101242));
#54474=CARTESIAN_POINT('Ctrl Pts',(13.2727774748782,0.536302341582597,4.32451243275751));
#54475=CARTESIAN_POINT('Ctrl Pts',(13.2886827535658,0.387613518158899,4.49262996370669));
#54476=CARTESIAN_POINT('Ctrl Pts',(13.3045880322534,0.202356657484476,4.55961839611428));
#54477=CARTESIAN_POINT('Ctrl Pts',(13.3101102177498,0.13803695776657,4.58287624384712));
#54478=CARTESIAN_POINT('Ctrl Pts',(13.3156324032461,0.0693092633201986,
4.59394375907155));
#54479=CARTESIAN_POINT('Ctrl Pts',(13.3211545887425,0.000436239896754628,
4.59347700091179));
#54480=CARTESIAN_POINT('Origin',(4.,0.,4.));
#54481=CARTESIAN_POINT('',(13.7288454112576,-0.000361622974213827,4.59480268714608));
#54482=CARTESIAN_POINT('',(13.6211545887425,-0.000396530615921017,4.59339874939382));
#54483=CARTESIAN_POINT('',(4.,-7.27562663373442E-17,4.5941));
#54484=CARTESIAN_POINT('Ctrl Pts',(13.7288454112576,-0.000361622974213827,
4.59480268714608));
#54485=CARTESIAN_POINT('Ctrl Pts',(13.714655378171,0.175608319374377,4.59354294412002));
#54486=CARTESIAN_POINT('Ctrl Pts',(13.7004653450845,0.352610168065205,4.51056419690263));
#54487=CARTESIAN_POINT('Ctrl Pts',(13.6862753119979,0.463013835099274,4.37381700684221));
#54488=CARTESIAN_POINT('Ctrl Pts',(13.6703700333103,0.586762742631886,4.22054025587244));
#54489=CARTESIAN_POINT('Ctrl Pts',(13.6544647546227,0.626840040937572,3.99971072753873));
#54490=CARTESIAN_POINT('Ctrl Pts',(13.6385594759351,0.564843930165024,3.81272399872504));
#54491=CARTESIAN_POINT('Ctrl Pts',(13.6226541972475,0.502847819392478,3.62573726991136));
#54492=CARTESIAN_POINT('Ctrl Pts',(13.6067489185599,0.338778299541704,3.4725933406177));
#54493=CARTESIAN_POINT('Ctrl Pts',(13.5908436398723,0.147969152919217,3.42360942419035));
#54494=CARTESIAN_POINT('Ctrl Pts',(13.5749383611846,-0.0428399937032757,
3.37462550776301));
#54495=CARTESIAN_POINT('Ctrl Pts',(13.559033082497,-0.260388767097474,3.42980160420198));
#54496=CARTESIAN_POINT('Ctrl Pts',(13.5431278038094,-0.404787974250376,
3.56380318433064));
#54497=CARTESIAN_POINT('Ctrl Pts',(13.5272225251218,-0.549187181403275,
3.6978047644593));
#54498=CARTESIAN_POINT('Ctrl Pts',(13.5113172464342,-0.620436822314871,
3.91063182827765));
#54499=CARTESIAN_POINT('Ctrl Pts',(13.4954119677466,-0.585822076202281,
4.10456319205082));
#54500=CARTESIAN_POINT('Ctrl Pts',(13.479506689059,-0.551207330089691,4.298494555824));
#54501=CARTESIAN_POINT('Ctrl Pts',(13.4636014103714,-0.410728196952908,
4.47353021955202));
#54502=CARTESIAN_POINT('Ctrl Pts',(13.4476961316837,-0.228886751546343,
4.54930121159921));
#54503=CARTESIAN_POINT('Ctrl Pts',(13.4414125582084,-0.15704808052867,4.57923546205676));
#54504=CARTESIAN_POINT('Ctrl Pts',(13.435128984733,-0.0787538239969463,
4.5936770685736));
#54505=CARTESIAN_POINT('Ctrl Pts',(13.4288454112576,-0.000323145728561625,
4.59329116515504));
#54506=CARTESIAN_POINT('Ctrl Pts',(13.3211545887425,0.000436239896754628,
4.59347700091179));
#54507=CARTESIAN_POINT('Ctrl Pts',(13.3315376819337,-0.129062311182503,
4.59259937855127));
#54508=CARTESIAN_POINT('Ctrl Pts',(13.341920775125,-0.259074650003773,4.55094414667863));
#54509=CARTESIAN_POINT('Ctrl Pts',(13.3523038683163,-0.361265427801182,
4.47287234722855));
#54510=CARTESIAN_POINT('Ctrl Pts',(13.3682091470039,-0.517805754487323,
4.35327853206923));
#54511=CARTESIAN_POINT('Ctrl Pts',(13.3841144256915,-0.609061509934468,
4.14823156788458));
#54512=CARTESIAN_POINT('Ctrl Pts',(13.4000197043791,-0.593131911953917,
3.95188034580653));
#54513=CARTESIAN_POINT('Ctrl Pts',(13.4159249830667,-0.577202313973367,
3.75552912372848));
#54514=CARTESIAN_POINT('Ctrl Pts',(13.4318302617543,-0.454087362565127,
3.56787364375704));
#54515=CARTESIAN_POINT('Ctrl Pts',(13.4477355404419,-0.280316234851803,
3.47507736324643));
#54516=CARTESIAN_POINT('Ctrl Pts',(13.4636408191295,-0.106545107138479,
3.38228108273583));
#54517=CARTESIAN_POINT('Ctrl Pts',(13.4795460978172,0.117882196879929,3.38434400168606));
#54518=CARTESIAN_POINT('Ctrl Pts',(13.4954513765048,0.2899181539344,3.48031891499009));
#54519=CARTESIAN_POINT('Ctrl Pts',(13.5113566551924,0.461954110988876,3.57629382829412));
#54520=CARTESIAN_POINT('Ctrl Pts',(13.52726193388,0.581598721079409,3.76618073595195));
#54521=CARTESIAN_POINT('Ctrl Pts',(13.5431672125676,0.593916240998451,3.96279160341967));
#54522=CARTESIAN_POINT('Ctrl Pts',(13.5590724912552,0.606233760917493,4.15940247088739));
#54523=CARTESIAN_POINT('Ctrl Pts',(13.5749777699428,0.511224190665043,4.362737298165));
#54524=CARTESIAN_POINT('Ctrl Pts',(13.5908830486304,0.352511905377589,4.47943333495374));
#54525=CARTESIAN_POINT('Ctrl Pts',(13.6009735620011,0.251822790258117,4.55346680161908));
#54526=CARTESIAN_POINT('Ctrl Pts',(13.6110640753718,0.125494626822297,4.59262991567553));
#54527=CARTESIAN_POINT('Ctrl Pts',(13.6211545887425,-0.000396530615921017,
4.59339874939382));
#54528=CARTESIAN_POINT('Origin',(4.,0.,4.));
#54529=CARTESIAN_POINT('',(14.0288454112576,0.000507412974116619,4.59441995931617));
#54530=CARTESIAN_POINT('',(13.9211545887425,-0.000275297881949146,4.59492513410986));
#54531=CARTESIAN_POINT('',(4.,-7.27562663373442E-17,4.5941));
#54532=CARTESIAN_POINT('Ctrl Pts',(14.0288454112576,0.000507412974116619,
4.59441995931617));
#54533=CARTESIAN_POINT('Ctrl Pts',(14.0259923289843,0.0359476882196221,
4.59474138052009));
#54534=CARTESIAN_POINT('Ctrl Pts',(14.0231392467111,0.0713355155074759,
4.59184535342408));
#54535=CARTESIAN_POINT('Ctrl Pts',(14.0202861644378,0.106106362061302,4.58554453803953));
#54536=CARTESIAN_POINT('Ctrl Pts',(14.0043808857502,0.299945849210873,4.55041893875697));
#54537=CARTESIAN_POINT('Ctrl Pts',(13.9884756070626,0.474610768799237,4.40947910659883));
#54538=CARTESIAN_POINT('Ctrl Pts',(13.972570328375,0.549902379214768,4.22743864981956));
#54539=CARTESIAN_POINT('Ctrl Pts',(13.9566650496873,0.625193989630293,4.04539819304031));
#54540=CARTESIAN_POINT('Ctrl Pts',(13.9407597709997,0.601112290873006,3.82225711163994));
#54541=CARTESIAN_POINT('Ctrl Pts',(13.9248544923121,0.488714580199595,3.66047234987686));
#54542=CARTESIAN_POINT('Ctrl Pts',(13.9089492136245,0.376316869526181,3.49868758811377));
#54543=CARTESIAN_POINT('Ctrl Pts',(13.8930439349369,0.175603146936639,3.39825914598798));
#54544=CARTESIAN_POINT('Ctrl Pts',(13.8771386562493,-0.0212673376532481,
3.40529951534663));
#54545=CARTESIAN_POINT('Ctrl Pts',(13.8612333775617,-0.218137822243141,
3.41233988470529));
#54546=CARTESIAN_POINT('Ctrl Pts',(13.8453280988741,-0.411165068833379,
3.52684906554841));
#54547=CARTESIAN_POINT('Ctrl Pts',(13.8294228201864,-0.511719132099071,
3.69624928651676));
#54548=CARTESIAN_POINT('Ctrl Pts',(13.8135175414988,-0.612273195364761,
3.8656495074851));
#54549=CARTESIAN_POINT('Ctrl Pts',(13.7976122628112,-0.62035407530591,4.08994076857866));
#54550=CARTESIAN_POINT('Ctrl Pts',(13.7817069841236,-0.532251373727382,
4.26613801168402));
#54551=CARTESIAN_POINT('Ctrl Pts',(13.765801705436,-0.44414867214885,4.44233525478938));
#54552=CARTESIAN_POINT('Ctrl Pts',(13.7498964267484,-0.259862389050636,
4.57043847990653));
#54553=CARTESIAN_POINT('Ctrl Pts',(13.7339911480608,-0.0640089891217576,
4.59162810566218));
#54554=CARTESIAN_POINT('Ctrl Pts',(13.7322759024597,-0.0428879079209441,
4.59391322201126));
#54555=CARTESIAN_POINT('Ctrl Pts',(13.7305606568586,-0.0216323041412813,
4.594954960835));
#54556=CARTESIAN_POINT('Ctrl Pts',(13.7288454112576,-0.000361622974213827,
4.59480268714608));
#54557=CARTESIAN_POINT('Ctrl Pts',(13.6211545887425,-0.000396530615921017,
4.59339874939382));
#54558=CARTESIAN_POINT('Ctrl Pts',(13.6269693540594,-0.0729426448807452,
4.59384179797573));
#54559=CARTESIAN_POINT('Ctrl Pts',(13.6327841193764,-0.145343639818557,
4.58153501668255));
#54560=CARTESIAN_POINT('Ctrl Pts',(13.6385988846933,-0.212609537044371,
4.5558040579697));
#54561=CARTESIAN_POINT('Ctrl Pts',(13.6545041633809,-0.396603693856438,
4.48542149789704));
#54562=CARTESIAN_POINT('Ctrl Pts',(13.6704094420685,-0.542177007158105,
4.31459913145184));
#54563=CARTESIAN_POINT('Ctrl Pts',(13.6863147207561,-0.582488370180261,
4.12177136240739));
#54564=CARTESIAN_POINT('Ctrl Pts',(13.7022199994437,-0.622799733202417,
3.92894359336294));
#54565=CARTESIAN_POINT('Ctrl Pts',(13.7181252781313,-0.557849145945042,
3.71411042171923));
#54566=CARTESIAN_POINT('Ctrl Pts',(13.734030556819,-0.417459170243993,3.57591415105311));
#54567=CARTESIAN_POINT('Ctrl Pts',(13.7499358355066,-0.277069194542941,
3.43771788038699));
#54568=CARTESIAN_POINT('Ctrl Pts',(13.7658411141942,-0.0612398303982075,
3.37615851069845));
#54569=CARTESIAN_POINT('Ctrl Pts',(13.7817463928818,0.130929209162332,3.41950150018632));
#54570=CARTESIAN_POINT('Ctrl Pts',(13.7976516715694,0.323098248722867,3.46284448967418));
#54571=CARTESIAN_POINT('Ctrl Pts',(13.813556950257,0.491606963699209,3.61108983833845));
#54572=CARTESIAN_POINT('Ctrl Pts',(13.8294622289446,0.559083281190044,3.79616955381596));
#54573=CARTESIAN_POINT('Ctrl Pts',(13.8453675076322,0.62655959868088,3.98124926929349));
#54574=CARTESIAN_POINT('Ctrl Pts',(13.8612727863198,0.593003518686204,4.20316335158427));
#54575=CARTESIAN_POINT('Ctrl Pts',(13.8771780650075,0.4738225734989,4.36001824251097));
#54576=CARTESIAN_POINT('Ctrl Pts',(13.8918369062525,0.363981395029584,4.50458099992985));
#54577=CARTESIAN_POINT('Ctrl Pts',(13.9064957474975,0.181409709145346,4.59388191268165));
#54578=CARTESIAN_POINT('Ctrl Pts',(13.9211545887425,-0.000275297881949146,
4.59492513410986));
#54579=CARTESIAN_POINT('Origin',(4.,0.,4.));
#54580=CARTESIAN_POINT('',(14.3288454112576,0.000109044058801022,4.5931342436645));
#54581=CARTESIAN_POINT('',(14.2211545887425,0.000537210645871958,4.59424369460725));
#54582=CARTESIAN_POINT('',(4.,-7.27562663373442E-17,4.5941));
#54583=CARTESIAN_POINT('Ctrl Pts',(14.3288454112576,0.000109044058801022,
4.5931342436645));
#54584=CARTESIAN_POINT('Ctrl Pts',(14.32142400111,0.0928032711674493,4.59328573107644));
#54585=CARTESIAN_POINT('Ctrl Pts',(14.3140025909624,0.185434358886594,4.57287353691408));
#54586=CARTESIAN_POINT('Ctrl Pts',(14.3065811808148,0.267539471941071,4.53154830171049));
#54587=CARTESIAN_POINT('Ctrl Pts',(14.2906759021272,0.443503969097433,4.44298165875801));
#54588=CARTESIAN_POINT('Ctrl Pts',(14.2747706234396,0.571121189235106,4.25835848700565));
#54589=CARTESIAN_POINT('Ctrl Pts',(14.258865344752,0.591794703906212,4.06244993615984));
#54590=CARTESIAN_POINT('Ctrl Pts',(14.2429600660644,0.612468218577319,3.86654138531401));
#54591=CARTESIAN_POINT('Ctrl Pts',(14.2270547873768,0.526198027781844,3.65934745537473));
#54592=CARTESIAN_POINT('Ctrl Pts',(14.2111495086891,0.372595753342289,3.53600283331781));
#54593=CARTESIAN_POINT('Ctrl Pts',(14.1952442300015,0.218993478902743,3.4126582112609));
#54594=CARTESIAN_POINT('Ctrl Pts',(14.1793389513139,-0.00194087918087354,
3.37316289708635));
#54595=CARTESIAN_POINT('Ctrl Pts',(14.1634336726263,-0.18876361063844,3.43565146815417));
#54596=CARTESIAN_POINT('Ctrl Pts',(14.1475283939387,-0.375586342096006,
3.49814003922198));
#54597=CARTESIAN_POINT('Ctrl Pts',(14.1316231152511,-0.528297446927522,
3.66261249553216));
#54598=CARTESIAN_POINT('Ctrl Pts',(14.1157178365635,-0.576778446468407,
3.85355004340287));
#54599=CARTESIAN_POINT('Ctrl Pts',(14.0998125578759,-0.625259446009293,
4.04448759127359));
#54600=CARTESIAN_POINT('Ctrl Pts',(14.0839072791882,-0.569510340259543,
4.26189023070484));
#54601=CARTESIAN_POINT('Ctrl Pts',(14.0680020005006,-0.435128760029281,
4.40593586721696));
#54602=CARTESIAN_POINT('Ctrl Pts',(14.0549498040863,-0.324852491748397,
4.52414265738481));
#54603=CARTESIAN_POINT('Ctrl Pts',(14.0418976076719,-0.161623710204441,
4.5929495310973));
#54604=CARTESIAN_POINT('Ctrl Pts',(14.0288454112576,0.000507412974116619,
4.59441995931617));
#54605=CARTESIAN_POINT('Ctrl Pts',(13.9211545887425,-0.000275297881949146,
4.59492513410986));
#54606=CARTESIAN_POINT('Ctrl Pts',(13.9224010261851,-0.015723926578741,
4.59501383895544));
#54607=CARTESIAN_POINT('Ctrl Pts',(13.9236474636277,-0.0311661445373128,
4.59446443570748));
#54608=CARTESIAN_POINT('Ctrl Pts',(13.9248939010703,-0.0465566941337027,
4.59325663951544));
#54609=CARTESIAN_POINT('Ctrl Pts',(13.9407991797579,-0.242949206199084,
4.5778444460306));
#54610=CARTESIAN_POINT('Ctrl Pts',(13.9567044584455,-0.430928419949921,
4.4552243594983));
#54611=CARTESIAN_POINT('Ctrl Pts',(13.9726097371331,-0.524182233176515,
4.28169833602613));
#54612=CARTESIAN_POINT('Ctrl Pts',(13.9885150158207,-0.617436046403107,
4.10817231255396));
#54613=CARTESIAN_POINT('Ctrl Pts',(14.0044202945084,-0.615964459105464,
3.88374035214192));
#54614=CARTESIAN_POINT('Ctrl Pts',(14.020325573196,-0.52044316191294,3.71145211607799));
#54615=CARTESIAN_POINT('Ctrl Pts',(14.0362308518836,-0.424921864720413,
3.53916388001405));
#54616=CARTESIAN_POINT('Ctrl Pts',(14.0521361305712,-0.235350857633014,
3.41901936829824));
#54617=CARTESIAN_POINT('Ctrl Pts',(14.0680414092588,-0.0387731270173405,
3.40618385781531));
#54618=CARTESIAN_POINT('Ctrl Pts',(14.0839466879464,0.157804603598333,3.39334834733239));
#54619=CARTESIAN_POINT('Ctrl Pts',(14.0998519666341,0.361389057742269,3.48782183808236));
#54620=CARTESIAN_POINT('Ctrl Pts',(14.1157572453217,0.478502867019537,3.64622609995664));
#54621=CARTESIAN_POINT('Ctrl Pts',(14.1316625240093,0.595616676296804,3.80463036183091));
#54622=CARTESIAN_POINT('Ctrl Pts',(14.1475678026969,0.626259840707404,4.02696539482948));
#54623=CARTESIAN_POINT('Ctrl Pts',(14.1634730813845,0.556362315559365,4.21114435801894));
#54624=CARTESIAN_POINT('Ctrl Pts',(14.1793783600721,0.486464790411328,4.3953233212084));
#54625=CARTESIAN_POINT('Ctrl Pts',(14.1952836387597,0.316026575704654,4.54134621458875));
#54626=CARTESIAN_POINT('Ctrl Pts',(14.2111889174473,0.123305688986428,4.58216550323889));
#54627=CARTESIAN_POINT('Ctrl Pts',(14.2145108078791,0.0830550475387342,
4.59069079896363));
#54628=CARTESIAN_POINT('Ctrl Pts',(14.2178326983108,0.0418324306113591,
4.59462708830176));
#54629=CARTESIAN_POINT('Ctrl Pts',(14.2211545887425,0.000537210645871958,
4.59424369460725));
#54630=CARTESIAN_POINT('Origin',(4.,0.,4.));
#54631=CARTESIAN_POINT('',(14.6288454112575,-0.000548182068839831,4.59401855345973));
#54632=CARTESIAN_POINT('',(14.5211545887425,1.28950532977596E-5,4.59311636453746));
#54633=CARTESIAN_POINT('',(4.,-7.27562663373442E-17,4.5941));
#54634=CARTESIAN_POINT('Ctrl Pts',(14.6288454112575,-0.000548182068839831,
4.59401855345973));
#54635=CARTESIAN_POINT('Ctrl Pts',(14.6168556732357,0.148643716013534,4.59265593252186));
#54636=CARTESIAN_POINT('Ctrl Pts',(14.6048659352138,0.29876355451001,4.53564313143304));
#54637=CARTESIAN_POINT('Ctrl Pts',(14.5928761971919,0.407080942069735,4.43405768361063));
#54638=CARTESIAN_POINT('Ctrl Pts',(14.5769709185042,0.55077200793829,4.29929703619113));
#54639=CARTESIAN_POINT('Ctrl Pts',(14.5610656398166,0.620899143473568,4.08609746938767));
#54640=CARTESIAN_POINT('Ctrl Pts',(14.545160361129,0.585262934872208,3.89235120454656));
#54641=CARTESIAN_POINT('Ctrl Pts',(14.5292550824414,0.549626726270847,3.69860493970543));
#54642=CARTESIAN_POINT('Ctrl Pts',(14.5133498037538,0.408227173532835,3.52431197682665));
#54643=CARTESIAN_POINT('Ctrl Pts',(14.4974445250662,0.225988969153725,3.44950027073699));
#54644=CARTESIAN_POINT('Ctrl Pts',(14.4815392463786,0.04375076477463,3.37468856464734));
#54645=CARTESIAN_POINT('Ctrl Pts',(14.465633967691,-0.179326091245555,3.39935811534679));
#54646=CARTESIAN_POINT('Ctrl Pts',(14.4497286890033,-0.340814144225853,
3.51218170883678));
#54647=CARTESIAN_POINT('Ctrl Pts',(14.4338234103157,-0.50230219720616,3.62500530232677));
#54648=CARTESIAN_POINT('Ctrl Pts',(14.4179181316281,-0.602201447146573,
3.82598293860731));
#54649=CARTESIAN_POINT('Ctrl Pts',(14.4020128529405,-0.594642384863179,
4.02283418976097));
#54650=CARTESIAN_POINT('Ctrl Pts',(14.3861075742529,-0.587083322579785,
4.21968544091462));
#54651=CARTESIAN_POINT('Ctrl Pts',(14.3702022955653,-0.47206594807259,4.4124103069414));
#54652=CARTESIAN_POINT('Ctrl Pts',(14.3542970168777,-0.302401373731467,
4.51251768287848));
#54653=CARTESIAN_POINT('Ctrl Pts',(14.3458131483376,-0.211902365642262,
4.565914912441));
#54654=CARTESIAN_POINT('Ctrl Pts',(14.3373292797976,-0.10585540495725,4.59296106912451));
#54655=CARTESIAN_POINT('Ctrl Pts',(14.3288454112576,0.000109044058801022,
4.5931342436645));
#54656=CARTESIAN_POINT('Ctrl Pts',(14.2211545887425,0.000537210645871958,
4.59424369460725));
#54657=CARTESIAN_POINT('Ctrl Pts',(14.2337379769984,-0.155889919212927,
4.59279139152499));
#54658=CARTESIAN_POINT('Ctrl Pts',(14.2463213652543,-0.313358837143528,
4.52935553548989));
#54659=CARTESIAN_POINT('Ctrl Pts',(14.2589047535102,-0.422984449084643,
4.4185751090669));
#54660=CARTESIAN_POINT('Ctrl Pts',(14.2748100321978,-0.561550141707708,
4.27854974232482));
#54661=CARTESIAN_POINT('Ctrl Pts',(14.2907153108854,-0.623677968224056,
4.06288332492072));
#54662=CARTESIAN_POINT('Ctrl Pts',(14.306620589573,-0.580841459108965,3.87060075163287));
#54663=CARTESIAN_POINT('Ctrl Pts',(14.3225258682606,-0.538004949993874,
3.67831817834502));
#54664=CARTESIAN_POINT('Ctrl Pts',(14.3384311469482,-0.390204105247342,
3.50941944917344));
#54665=CARTESIAN_POINT('Ctrl Pts',(14.3543364256359,-0.205302819838896,
3.44145571503774));
#54666=CARTESIAN_POINT('Ctrl Pts',(14.3702417043235,-0.0204015344304391,
3.37349198090203));
#54667=CARTESIAN_POINT('Ctrl Pts',(14.3861469830111,0.201600191639931,3.40646324180223));
#54668=CARTESIAN_POINT('Ctrl Pts',(14.4020522616987,0.358768557879186,3.52523048963197));
#54669=CARTESIAN_POINT('Ctrl Pts',(14.4179575403863,0.515936924118427,3.6439977374617));
#54670=CARTESIAN_POINT('Ctrl Pts',(14.4338628190739,0.608271930526566,3.84856097222098));
#54671=CARTESIAN_POINT('Ctrl Pts',(14.4497680977615,0.59337724853295,4.04499341086509));
#54672=CARTESIAN_POINT('Ctrl Pts',(14.4656733764491,0.578482566539332,4.2414258495092));
#54673=CARTESIAN_POINT('Ctrl Pts',(14.4815786551367,0.456358196143958,4.42972749203816));
#54674=CARTESIAN_POINT('Ctrl Pts',(14.4974839338244,0.283078481576349,4.52343819058819));
#54675=CARTESIAN_POINT('Ctrl Pts',(14.5053741521304,0.197118668938093,4.56992576768087));
#54676=CARTESIAN_POINT('Ctrl Pts',(14.5132643704364,0.0985699939877532,
4.59313537862966));
#54677=CARTESIAN_POINT('Ctrl Pts',(14.5211545887425,1.28950532977596E-5,
4.59311636453746));
#54678=CARTESIAN_POINT('Origin',(4.,0.,4.));
#54679=CARTESIAN_POINT('',(14.9288454112575,0.000149915246051877,4.59503491979621));
#54680=CARTESIAN_POINT('',(14.8211545887425,-0.000542004001680995,4.59419620878869));
#54681=CARTESIAN_POINT('',(4.,-7.27562663373442E-17,4.5941));
#54682=CARTESIAN_POINT('Ctrl Pts',(14.9288454112575,0.000149915246051877,
4.59503491979621));
#54683=CARTESIAN_POINT('Ctrl Pts',(14.9281926240489,0.00823674021970066,
4.59506221957623));
#54684=CARTESIAN_POINT('Ctrl Pts',(14.9275398368403,0.0163225255999611,
4.59491168338633));
#54685=CARTESIAN_POINT('Ctrl Pts',(14.9268870496317,0.0244008833477238,
4.59458015690877));
#54686=CARTESIAN_POINT('Ctrl Pts',(14.9109817709441,0.221231534471853,4.58650245417764));
#54687=CARTESIAN_POINT('Ctrl Pts',(14.8950764922565,0.413652681988333,4.47097768448731));
#54688=CARTESIAN_POINT('Ctrl Pts',(14.8791712135689,0.513312675625014,4.30104993462962));
#54689=CARTESIAN_POINT('Ctrl Pts',(14.8632659348813,0.612972669261697,4.13112218477192));
#54690=CARTESIAN_POINT('Ctrl Pts',(14.8473606561937,0.619871509018575,3.90679145474687));
#54691=CARTESIAN_POINT('Ctrl Pts',(14.831455377506,0.530841539545133,3.73106092513143));
#54692=CARTESIAN_POINT('Ctrl Pts',(14.8155500988184,0.441811570071688,3.55533039551599));
#54693=CARTESIAN_POINT('Ctrl Pts',(14.7996448201308,0.256852791367914,3.42820006631018));
#54694=CARTESIAN_POINT('Ctrl Pts',(14.7837395414432,0.0608904496539635,
3.40804280624462));
#54695=CARTESIAN_POINT('Ctrl Pts',(14.7678342627556,-0.135071892059981,
3.38788554617906));
#54696=CARTESIAN_POINT('Ctrl Pts',(14.751928984068,-0.342037796784102,3.47470135525375));
#54697=CARTESIAN_POINT('Ctrl Pts',(14.7360237053804,-0.464977277074429,
3.62862808681558));
#54698=CARTESIAN_POINT('Ctrl Pts',(14.7201184266927,-0.587916757364756,
3.78255481837741));
#54699=CARTESIAN_POINT('Ctrl Pts',(14.7042131480052,-0.62682981322129,4.00359247242638));
#54700=CARTESIAN_POINT('Ctrl Pts',(14.6883078693175,-0.56384921567034,4.19024990955517));
#54701=CARTESIAN_POINT('Ctrl Pts',(14.6724025906299,-0.500868618119389,
4.37690734668397));
#54702=CARTESIAN_POINT('Ctrl Pts',(14.6564973119423,-0.335994367160947,
4.52918456689258));
#54703=CARTESIAN_POINT('Ctrl Pts',(14.6405920332547,-0.144929743580805,
4.57716231297912));
#54704=CARTESIAN_POINT('Ctrl Pts',(14.636676492589,-0.097893704910838,4.5889734116427));
#54705=CARTESIAN_POINT('Ctrl Pts',(14.6327609519233,-0.0492704262804658,
4.59446355048005));
#54706=CARTESIAN_POINT('Ctrl Pts',(14.6288454112575,-0.000548182068839831,
4.59401855345973));
#54707=CARTESIAN_POINT('Ctrl Pts',(14.5211545887425,1.28950532977596E-5,
4.59311636453746));
#54708=CARTESIAN_POINT('Ctrl Pts',(14.5291696491241,-0.100103612291989,
4.59309704959697));
#54709=CARTESIAN_POINT('Ctrl Pts',(14.5371847095056,-0.200228812305367,
4.56910822985942));
#54710=CARTESIAN_POINT('Ctrl Pts',(14.5451997698872,-0.287175610734119,
4.52120162576233));
#54711=CARTESIAN_POINT('Ctrl Pts',(14.5611050485748,-0.459714929737158,
4.42613460781534));
#54712=CARTESIAN_POINT('Ctrl Pts',(14.5770103272624,-0.580358509003398,
4.23688081735026));
#54713=CARTESIAN_POINT('Ctrl Pts',(14.59291560595,-0.593711920942704,4.04033758828107));
#54714=CARTESIAN_POINT('Ctrl Pts',(14.6088208846377,-0.607065332882009,
3.84379435921188));
#54715=CARTESIAN_POINT('Ctrl Pts',(14.6247261633253,-0.513128577494387,
3.63996169153858));
#54716=CARTESIAN_POINT('Ctrl Pts',(14.6406314420129,-0.35503343871745,3.52243092280774));
#54717=CARTESIAN_POINT('Ctrl Pts',(14.6565367207005,-0.196938299940509,
3.40490015407689));
#54718=CARTESIAN_POINT('Ctrl Pts',(14.6724419993881,0.025315222225754,3.37367128428849));
#54719=CARTESIAN_POINT('Ctrl Pts',(14.6883472780757,0.209677713173688,3.44308328926485));
#54720=CARTESIAN_POINT('Ctrl Pts',(14.7042525567633,0.394040204121622,3.51249529424121));
#54721=CARTESIAN_POINT('Ctrl Pts',(14.720157835451,0.540511663851219,3.68254817398232));
#54722=CARTESIAN_POINT('Ctrl Pts',(14.7360631141386,0.581838594751101,3.87516084045512));
#54723=CARTESIAN_POINT('Ctrl Pts',(14.7519683928262,0.623165525650983,4.06777350692792));
#54724=CARTESIAN_POINT('Ctrl Pts',(14.7678736715138,0.559347927721136,4.2829459601324));
#54725=CARTESIAN_POINT('Ctrl Pts',(14.7837789502014,0.419688142031033,4.42188011275284));
#54726=CARTESIAN_POINT('Ctrl Pts',(14.7962374963817,0.310293146587505,4.53070672248707));
#54727=CARTESIAN_POINT('Ctrl Pts',(14.8086960425621,0.154364940471616,4.59275708529138));
#54728=CARTESIAN_POINT('Ctrl Pts',(14.8211545887425,-0.000542004001680995,
4.59419620878869));
#54729=CARTESIAN_POINT('Origin',(4.,0.,4.));
#54730=CARTESIAN_POINT('',(15.2288454112576,0.000471544078774977,4.59356550157774));
#54731=CARTESIAN_POINT('',(15.1211545887425,0.000250233060073018,4.59495282954609));
#54732=CARTESIAN_POINT('',(4.,-7.27562663373442E-17,4.5941));
#54733=CARTESIAN_POINT('Ctrl Pts',(15.2288454112576,0.000471544078774977,
4.59356550157774));
#54734=CARTESIAN_POINT('Ctrl Pts',(15.2236242961746,0.0655651715058866,
4.59404721416646));
#54735=CARTESIAN_POINT('Ctrl Pts',(15.2184031810917,0.130516835945995,4.58418155789741));
#54736=CARTESIAN_POINT('Ctrl Pts',(15.2131820660088,0.191734887706884,4.56334598510492));
#54737=CARTESIAN_POINT('Ctrl Pts',(15.1972767873211,0.378225734681762,4.49987379829874));
#54738=CARTESIAN_POINT('Ctrl Pts',(15.1813715086335,0.530068013118856,4.33459889729257));
#54739=CARTESIAN_POINT('Ctrl Pts',(15.1654662299459,0.577542172676889,4.143408524424));
#54740=CARTESIAN_POINT('Ctrl Pts',(15.1495609512583,0.625016332234921,3.95221815155542));
#54741=CARTESIAN_POINT('Ctrl Pts',(15.1336556725707,0.568122372913892,3.73511230682445));
#54742=CARTESIAN_POINT('Ctrl Pts',(15.1177503938831,0.432983593849097,3.59177680914072));
#54743=CARTESIAN_POINT('Ctrl Pts',(15.1018451151955,0.297844814784303,3.44844131145699));
#54744=CARTESIAN_POINT('Ctrl Pts',(15.0859398365078,0.0844612159757424,
3.37887616082051));
#54745=CARTESIAN_POINT('Ctrl Pts',(15.0700345578202,-0.109190481519281,
3.41502273134472));
#54746=CARTESIAN_POINT('Ctrl Pts',(15.0541292791326,-0.302842179014298,
3.45116930186893));
#54747=CARTESIAN_POINT('Ctrl Pts',(15.038224000445,-0.47676197519578,3.59302759355383));
#54748=CARTESIAN_POINT('Ctrl Pts',(15.0223187217574,-0.551093257596978,
3.77546228038711));
#54749=CARTESIAN_POINT('Ctrl Pts',(15.0064134430698,-0.625424539998176,
3.95789696722038));
#54750=CARTESIAN_POINT('Ctrl Pts',(14.9905081643822,-0.600167308619091,
4.18090804920204));
#54751=CARTESIAN_POINT('Ctrl Pts',(14.9746028856946,-0.486918615563658,
4.34209827230691));
#54752=CARTESIAN_POINT('Ctrl Pts',(14.9593503942156,-0.378317895025423,
4.49667289829699));
#54753=CARTESIAN_POINT('Ctrl Pts',(14.9440979027365,-0.188800216398263,
4.59439705548643));
#54754=CARTESIAN_POINT('Ctrl Pts',(14.9288454112575,0.000149915246051877,
4.59503491979621));
#54755=CARTESIAN_POINT('Ctrl Pts',(14.8211545887425,-0.000542004001680995,
4.59419620878869));
#54756=CARTESIAN_POINT('Ctrl Pts',(14.8246013212497,-0.0433979515083632,
4.5945943510493));
#54757=CARTESIAN_POINT('Ctrl Pts',(14.828048053757,-0.0861757330942537,
4.59035339483295));
#54758=CARTESIAN_POINT('Ctrl Pts',(14.8314947862642,-0.127868389248254,
4.58118038604969));
#54759=CARTESIAN_POINT('Ctrl Pts',(14.8474000649518,-0.320263161387096,
4.5388506546897));
#54760=CARTESIAN_POINT('Ctrl Pts',(14.8633053436395,-0.489550732214419,
4.39149533993331));
#54761=CARTESIAN_POINT('Ctrl Pts',(14.8792106223271,-0.558001411172811,
4.20677376822741));
#54762=CARTESIAN_POINT('Ctrl Pts',(14.8951159010147,-0.6264520901312,4.0220521965215));
#54763=CARTESIAN_POINT('Ctrl Pts',(14.9110211797023,-0.594065877220663,
3.79996436786608));
#54764=CARTESIAN_POINT('Ctrl Pts',(14.9269264583899,-0.475713151262041,
3.64248361741852));
#54765=CARTESIAN_POINT('Ctrl Pts',(14.9428317370775,-0.357360425303418,
3.48500286697096));
#54766=CARTESIAN_POINT('Ctrl Pts',(14.9587370157651,-0.153041186296697,
3.39212919473125));
#54767=CARTESIAN_POINT('Ctrl Pts',(14.9746422944528,0.0434298152403689,
3.40650626183085));
#54768=CARTESIAN_POINT('Ctrl Pts',(14.9905475731404,0.239900816777435,3.42088332893044));
#54769=CARTESIAN_POINT('Ctrl Pts',(15.006452851828,0.428523580844854,3.54251113536931));
#54770=CARTESIAN_POINT('Ctrl Pts',(15.0223581305156,0.522690514153935,3.71554333807889));
#54771=CARTESIAN_POINT('Ctrl Pts',(15.0382634092032,0.616857447463019,3.88857554078846));
#54772=CARTESIAN_POINT('Ctrl Pts',(15.0541686878908,0.616568550013756,4.11301213976874));
#54773=CARTESIAN_POINT('Ctrl Pts',(15.0700739665784,0.521956471292605,4.28580134389743));
#54774=CARTESIAN_POINT('Ctrl Pts',(15.085979245266,0.427344392571456,4.45859054802613));
#54775=CARTESIAN_POINT('Ctrl Pts',(15.1018845239536,0.238409132578427,4.57973235730324));
#54776=CARTESIAN_POINT('Ctrl Pts',(15.1177898026413,0.0419017695106382,
4.59360357799603));
#54777=CARTESIAN_POINT('Ctrl Pts',(15.1189113980083,0.0280446248267054,
4.59458173733358));
#54778=CARTESIAN_POINT('Ctrl Pts',(15.1200329933754,0.0141498265549413,
4.59502647517791));
#54779=CARTESIAN_POINT('Ctrl Pts',(15.1211545887425,0.000250233060073018,
4.59495282954609));
#54780=CARTESIAN_POINT('Origin',(4.,0.,4.));
#54781=CARTESIAN_POINT('',(15.5288454112575,-0.000350670266729247,4.59332700645389));
#54782=CARTESIAN_POINT('',(15.4211545887425,0.000414092275955974,4.59343115273787));
#54783=CARTESIAN_POINT('',(4.,-7.27562663373442E-17,4.5941));
#54784=CARTESIAN_POINT('Ctrl Pts',(15.5288454112575,-0.000350670266729247,
4.59332700645389));
#54785=CARTESIAN_POINT('Ctrl Pts',(15.5190559683003,0.121821298278883,4.59267222728074));
#54786=CARTESIAN_POINT('Ctrl Pts',(15.509266525343,0.244354036528086,4.55597946496206));
#54787=CARTESIAN_POINT('Ctrl Pts',(15.4994770823858,0.343380025451582,4.48601555964668));
#54788=CARTESIAN_POINT('Ctrl Pts',(15.4835718036982,0.504271299656008,4.37234255322809));
#54789=CARTESIAN_POINT('Ctrl Pts',(15.4676665250105,0.603110088323456,4.17084127710728));
#54790=CARTESIAN_POINT('Ctrl Pts',(15.4517612463229,0.594513801222153,3.97403259246294));
#54791=CARTESIAN_POINT('Ctrl Pts',(15.4358559676353,0.58591751412085,3.7772239078186));
#54792=CARTESIAN_POINT('Ctrl Pts',(15.4199506889477,0.469886151250777,3.58510781465072));
#54793=CARTESIAN_POINT('Ctrl Pts',(15.4040454102601,0.299696405559752,3.48589589518039));
#54794=CARTESIAN_POINT('Ctrl Pts',(15.3881401315725,0.129506659868722,3.38668397571006));
#54795=CARTESIAN_POINT('Ctrl Pts',(15.3722348528849,-0.0948414686432761,
3.38037622993726));
#54796=CARTESIAN_POINT('Ctrl Pts',(15.3563295741973,-0.270336810750117,
3.46986890786216));
#54797=CARTESIAN_POINT('Ctrl Pts',(15.3404242955096,-0.445832152856957,
3.55936158578705));
#54798=CARTESIAN_POINT('Ctrl Pts',(15.324519016822,-0.572474708558633,3.74465468740961));
#54799=CARTESIAN_POINT('Ctrl Pts',(15.3086137381344,-0.592115574081638,
3.94066945956945));
#54800=CARTESIAN_POINT('Ctrl Pts',(15.2927084594468,-0.611756439604643,
4.13668423172929));
#54801=CARTESIAN_POINT('Ctrl Pts',(15.2768031807592,-0.524395614948954,
4.3434206744264));
#54802=CARTESIAN_POINT('Ctrl Pts',(15.2608979020716,-0.370145494864779,
4.46595415947185));
#54803=CARTESIAN_POINT('Ctrl Pts',(15.2502137384669,-0.266529987624151,
4.54826443060822));
#54804=CARTESIAN_POINT('Ctrl Pts',(15.2395295748622,-0.13273198696893,4.59257975504152));
#54805=CARTESIAN_POINT('Ctrl Pts',(15.2288454112576,0.000471544078774977,
4.59356550157774));
#54806=CARTESIAN_POINT('Ctrl Pts',(15.1211545887425,0.000250233060073018,
4.59495282954609));
#54807=CARTESIAN_POINT('Ctrl Pts',(15.135938272063,-0.18295950063263,4.59398211075496));
#54808=CARTESIAN_POINT('Ctrl Pts',(15.1507219553836,-0.367002343096231,
4.50294888365168));
#54809=CARTESIAN_POINT('Ctrl Pts',(15.1655056387041,-0.476631971954554,
4.35629051265579));
#54810=CARTESIAN_POINT('Ctrl Pts',(15.1814109173917,-0.594578884209397,
4.19850559451431));
#54811=CARTESIAN_POINT('Ctrl Pts',(15.1973161960793,-0.626393242576541,
3.97633512612291));
#54812=CARTESIAN_POINT('Ctrl Pts',(15.2132214747669,-0.557467239648298,
3.79179038730953));
#54813=CARTESIAN_POINT('Ctrl Pts',(15.2291267534545,-0.488541236720055,
3.60724564849615));
#54814=CARTESIAN_POINT('Ctrl Pts',(15.2450320321422,-0.318874872496425,
3.46032663926078));
#54815=CARTESIAN_POINT('Ctrl Pts',(15.2609373108298,-0.126371763436977,
3.41849235301362));
#54816=CARTESIAN_POINT('Ctrl Pts',(15.2768425895174,0.0661313456224706,
3.37665806676646));
#54817=CARTESIAN_POINT('Ctrl Pts',(15.292747868205,0.281471199517752,3.4399085035075));
#54818=CARTESIAN_POINT('Ctrl Pts',(15.3086531468926,0.420772847618048,3.57920173859056));
#54819=CARTESIAN_POINT('Ctrl Pts',(15.3245584255802,0.560074495718348,3.71849497367363));
#54820=CARTESIAN_POINT('Ctrl Pts',(15.3404637042678,0.623337938023671,3.9338310070987));
#54821=CARTESIAN_POINT('Ctrl Pts',(15.3563689829554,0.581515278282945,4.12633664243329));
#54822=CARTESIAN_POINT('Ctrl Pts',(15.3722742616431,0.53969261854222,4.31884227776789));
#54823=CARTESIAN_POINT('Ctrl Pts',(15.3881795403307,0.392783856755445,4.48851751501199));
#54824=CARTESIAN_POINT('Ctrl Pts',(15.4040848190183,0.208243281137944,4.55745466359042));
#54825=CARTESIAN_POINT('Ctrl Pts',(15.4097747422597,0.142226097106806,4.58211610408423));
#54826=CARTESIAN_POINT('Ctrl Pts',(15.4154646655011,0.0713929250243718,
4.593885435962));
#54827=CARTESIAN_POINT('Ctrl Pts',(15.4211545887425,0.000414092275955974,
4.59343115273787));
#54828=CARTESIAN_POINT('Origin',(4.,0.,4.));
#54829=CARTESIAN_POINT('',(15.8288454112575,-0.000332254705457391,4.59484959654372));
#54830=CARTESIAN_POINT('',(15.7211545887425,-0.000419917270904514,4.59344262983929));
#54831=CARTESIAN_POINT('',(4.,-7.27562663373442E-17,4.5941));
#54832=CARTESIAN_POINT('Ctrl Pts',(15.8288454112575,-0.000332254705457391,
4.59484959654372));
#54833=CARTESIAN_POINT('Ctrl Pts',(15.814487640426,0.177680873019276,4.5936575613883));
#54834=CARTESIAN_POINT('Ctrl Pts',(15.8001298695944,0.356683508224643,4.50844978272675));
#54835=CARTESIAN_POINT('Ctrl Pts',(15.7857720987628,0.466927807092597,4.36891650689757));
#54836=CARTESIAN_POINT('Ctrl Pts',(15.7698668200752,0.589054446233417,4.21434406913608));
#54837=CARTESIAN_POINT('Ctrl Pts',(15.7539615413876,0.626802179063893,3.99310442736787));
#54838=CARTESIAN_POINT('Ctrl Pts',(15.7380562627,0.562838843643149,3.80678146521555));
#54839=CARTESIAN_POINT('Ctrl Pts',(15.7221509840123,0.498875508222402,3.62045850306322));
#54840=CARTESIAN_POINT('Ctrl Pts',(15.7062457053247,0.333201104550436,3.46905222052678));
#54841=CARTESIAN_POINT('Ctrl Pts',(15.6903404266371,0.141886309687413,3.42208197707538));
#54842=CARTESIAN_POINT('Ctrl Pts',(15.6744351479495,-0.0494284851756215,
3.37511173362399));
#54843=CARTESIAN_POINT('Ctrl Pts',(15.6585298692619,-0.266383671229707,
3.43257752925765));
#54844=CARTESIAN_POINT('Ctrl Pts',(15.6426245905743,-0.409362605655794,
3.5680935017987));
#54845=CARTESIAN_POINT('Ctrl Pts',(15.6267193118867,-0.552341540081869,
3.70360947433975));
#54846=CARTESIAN_POINT('Ctrl Pts',(15.6108140331991,-0.621344222879956,
3.9171756237882));
#54847=CARTESIAN_POINT('Ctrl Pts',(15.5949087545115,-0.584687541371933,
4.11073140955597));
#54848=CARTESIAN_POINT('Ctrl Pts',(15.5790034758238,-0.548030859863907,
4.30428719532377));
#54849=CARTESIAN_POINT('Ctrl Pts',(15.5630981971362,-0.405714814049763,
4.47783261741089));
#54850=CARTESIAN_POINT('Ctrl Pts',(15.5471929184486,-0.223084911271984,
4.55168296009627));
#54851=CARTESIAN_POINT('Ctrl Pts',(15.5410770827183,-0.152860773312716,
4.58007960584922));
#54852=CARTESIAN_POINT('Ctrl Pts',(15.5349612469879,-0.0766761255292402,
4.5937360717991));
#54853=CARTESIAN_POINT('Ctrl Pts',(15.5288454112575,-0.000350670266729247,
4.59332700645389));
#54854=CARTESIAN_POINT('Ctrl Pts',(15.4211545887425,0.000414092275955974,
4.59343115273787));
#54855=CARTESIAN_POINT('Ctrl Pts',(15.4313699441887,-0.12701715326484,4.59261555920332));
#54856=CARTESIAN_POINT('Ctrl Pts',(15.4415852996349,-0.254917899718674,
4.55240018390688));
#54857=CARTESIAN_POINT('Ctrl Pts',(15.4518006550811,-0.356261725310785,
4.47665348962993));
#54858=CARTESIAN_POINT('Ctrl Pts',(15.4677059337687,-0.514053766693778,
4.35871610717824));
#54859=CARTESIAN_POINT('Ctrl Pts',(15.4836112124564,-0.607465460011524,
4.15464228236211));
#54860=CARTESIAN_POINT('Ctrl Pts',(15.499516491144,-0.593606107615349,3.95813408188558));
#54861=CARTESIAN_POINT('Ctrl Pts',(15.5154217698316,-0.579746755219174,
3.76162588140906));
#54862=CARTESIAN_POINT('Ctrl Pts',(15.5313270485192,-0.458616357109098,
3.57268330527213));
#54863=CARTESIAN_POINT('Ctrl Pts',(15.5472323272068,-0.285832867492734,
3.47806079093568));
#54864=CARTESIAN_POINT('Ctrl Pts',(15.5631376058944,-0.113049377876356,
3.38343827659922));
#54865=CARTESIAN_POINT('Ctrl Pts',(15.579042884582,0.111387203246309,3.38313582406324));
#54866=CARTESIAN_POINT('Ctrl Pts',(15.5949481632696,0.284425092952457,3.47729230673655));
#54867=CARTESIAN_POINT('Ctrl Pts',(15.6108534419572,0.457462982658595,3.57144878940986));
#54868=CARTESIAN_POINT('Ctrl Pts',(15.6267587206449,0.579102180948212,3.76006420729246));
#54869=CARTESIAN_POINT('Ctrl Pts',(15.6426639993325,0.593491114096805,3.95653434015292));
#54870=CARTESIAN_POINT('Ctrl Pts',(15.6585692780201,0.607880047245398,4.15300447301339));
#54871=CARTESIAN_POINT('Ctrl Pts',(15.6744745567077,0.515018715252963,4.35732932085173));
#54872=CARTESIAN_POINT('Ctrl Pts',(15.6903798353953,0.357545113131455,4.47569155781202));
#54873=CARTESIAN_POINT('Ctrl Pts',(15.700638086511,0.255981111243369,4.55203033647815));
#54874=CARTESIAN_POINT('Ctrl Pts',(15.7108963376268,0.127540214881222,4.59261107697802));
#54875=CARTESIAN_POINT('Ctrl Pts',(15.7211545887425,-0.000419917270904514,
4.59344262983929));
#54876=CARTESIAN_POINT('Origin',(4.,0.,4.));
#54877=CARTESIAN_POINT('',(16.1288454112575,0.000520203518568921,4.59435747030618));
#54878=CARTESIAN_POINT('',(16.0211545887425,-0.00024144267326323,4.59496181546483));
#54879=CARTESIAN_POINT('',(4.,-7.27562663373442E-17,4.5941));
#54880=CARTESIAN_POINT('Ctrl Pts',(16.1288454112575,0.000520203518568921,
4.59435747030618));
#54881=CARTESIAN_POINT('Ctrl Pts',(16.1258245912393,0.0380542554257849,
4.59470210862833));
#54882=CARTESIAN_POINT('Ctrl Pts',(16.122803771221,0.0755288363057283,4.59145263304759));
#54883=CARTESIAN_POINT('Ctrl Pts',(16.1197829512027,0.112271568866026,4.58439375503351));
#54884=CARTESIAN_POINT('Ctrl Pts',(16.1038776725151,0.305730099191281,4.54722721702202));
#54885=CARTESIAN_POINT('Ctrl Pts',(16.0879723938275,0.478899942385972,4.40445440507416));
#54886=CARTESIAN_POINT('Ctrl Pts',(16.0720671151398,0.55226883266698,4.22163055421683));
#54887=CARTESIAN_POINT('Ctrl Pts',(16.0561618364522,0.625637722947984,4.03880670335952));
#54888=CARTESIAN_POINT('Ctrl Pts',(16.0402565577646,0.599205660315318,3.81593181359275));
#54889=CARTESIAN_POINT('Ctrl Pts',(16.024351279077,0.485109129681553,3.65534060523843));
#54890=CARTESIAN_POINT('Ctrl Pts',(16.0084460003894,0.371012599047788,3.4947493968841));
#54891=CARTESIAN_POINT('Ctrl Pts',(15.9925407217018,0.169251600412921,3.39644186994223));
#54892=CARTESIAN_POINT('Ctrl Pts',(15.9766354430142,-0.0275337514538456,
3.40555668173602));
#54893=CARTESIAN_POINT('Ctrl Pts',(15.9607301643265,-0.224319103320618,
3.41467149352982));
#54894=CARTESIAN_POINT('Ctrl Pts',(15.9448248856389,-0.416128808419276,
3.53120864405929));
#54895=CARTESIAN_POINT('Ctrl Pts',(15.9289196069513,-0.514891964967956,
3.70165920408156));
#54896=CARTESIAN_POINT('Ctrl Pts',(15.9130143282637,-0.613655121516638,
3.87210976410384));
#54897=CARTESIAN_POINT('Ctrl Pts',(15.8971090495761,-0.619371729515322,
4.09647373361892));
#54898=CARTESIAN_POINT('Ctrl Pts',(15.8812037708885,-0.52941696442075,4.27173266988224));
#54899=CARTESIAN_POINT('Ctrl Pts',(15.8652984922009,-0.439462199326184,
4.44699160614554));
#54900=CARTESIAN_POINT('Ctrl Pts',(15.8493932135132,-0.25383606113837,4.57314550915708));
#54901=CARTESIAN_POINT('Ctrl Pts',(15.8334879348256,-0.0577702193188812,
4.59226984378546));
#54902=CARTESIAN_POINT('Ctrl Pts',(15.8319404269696,-0.0386939468137543,
4.59413055045147));
#54903=CARTESIAN_POINT('Ctrl Pts',(15.8303929191136,-0.0195188482833839,
4.59497807636063));
#54904=CARTESIAN_POINT('Ctrl Pts',(15.8288454112575,-0.000332254705457391,
4.59484959654372));
#54905=CARTESIAN_POINT('Ctrl Pts',(15.7211545887425,-0.000419917270904514,
4.59344262983929));
#54906=CARTESIAN_POINT('Ctrl Pts',(15.7268016163144,-0.0708602278282204,
4.59390038836772));
#54907=CARTESIAN_POINT('Ctrl Pts',(15.7324486438863,-0.141154849878182,
4.58231274148771));
#54908=CARTESIAN_POINT('Ctrl Pts',(15.7380956714582,-0.206740066761224,
4.55801389847688));
#54909=CARTESIAN_POINT('Ctrl Pts',(15.7540009501458,-0.391465772281827,
4.48957437609924));
#54910=CARTESIAN_POINT('Ctrl Pts',(15.7699062288334,-0.538831311072463,
4.32029570526172));
#54911=CARTESIAN_POINT('Ctrl Pts',(15.785811507521,-0.58117266224226,4.12790349002296));
#54912=CARTESIAN_POINT('Ctrl Pts',(15.8017167862086,-0.62351401341206,3.93551127478418));
#54913=CARTESIAN_POINT('Ctrl Pts',(15.8176220648962,-0.560831176961022,
3.72000551514415));
#54914=CARTESIAN_POINT('Ctrl Pts',(15.8335273435838,-0.421905459495345,
3.58033733863277));
#54915=CARTESIAN_POINT('Ctrl Pts',(15.8494326222715,-0.282979742029676,
3.44066916212139));
#54916=CARTESIAN_POINT('Ctrl Pts',(15.8653379009591,-0.0678111435493865,
3.37683856873865));
#54917=CARTESIAN_POINT('Ctrl Pts',(15.8812431796467,0.124804018556085,3.41815386651619));
#54918=CARTESIAN_POINT('Ctrl Pts',(15.8971484583343,0.317419180661557,3.45946916429373));
#54919=CARTESIAN_POINT('Ctrl Pts',(15.9130537370219,0.487480906392202,3.60593035323155));
#54920=CARTESIAN_POINT('Ctrl Pts',(15.9289590157095,0.556904046010802,3.79028865163133));
#54921=CARTESIAN_POINT('Ctrl Pts',(15.9448642943971,0.6263271856294,3.9746469500311));
#54922=CARTESIAN_POINT('Ctrl Pts',(15.9607695730847,0.595111739135951,4.19690235789283));
#54923=CARTESIAN_POINT('Ctrl Pts',(15.9766748517723,0.477590518943614,4.35500459477727));
#54924=CARTESIAN_POINT('Ctrl Pts',(15.9915014307624,0.368039615220995,4.50238430120742));
#54925=CARTESIAN_POINT('Ctrl Pts',(16.0063280097524,0.18349252241573,4.59401752470064));
#54926=CARTESIAN_POINT('Ctrl Pts',(16.0211545887425,-0.00024144267326323,
4.59496181546483));
#54927=CARTESIAN_POINT('Origin',(4.,0.,4.));
#54928=CARTESIAN_POINT('',(16.4288454112575,7.48704377684928E-5,4.59312461313858));
#54929=CARTESIAN_POINT('',(16.3211545887425,0.000543344619121817,4.59417988242975));
#54930=CARTESIAN_POINT('',(4.,-7.27562663373442E-17,4.5941));
#54931=CARTESIAN_POINT('Ctrl Pts',(16.4288454112575,7.48704377684928E-5,
4.59312461313858));
#54932=CARTESIAN_POINT('Ctrl Pts',(16.4212562633649,0.0948679978941589,
4.5932308806522));
#54933=CARTESIAN_POINT('Ctrl Pts',(16.4136671154723,0.189615837117123,4.57184094704105));
#54934=CARTESIAN_POINT('Ctrl Pts',(16.4060779675797,0.273126642574496,4.52869916135151));
#54935=CARTESIAN_POINT('Ctrl Pts',(16.3901726888921,0.448147956300534,4.43828293357696));
#54936=CARTESIAN_POINT('Ctrl Pts',(16.3742674102045,0.573812330828296,4.25232504748949));
#54937=CARTESIAN_POINT('Ctrl Pts',(16.3583621315169,0.592420001795879,4.05620949715111));
#54938=CARTESIAN_POINT('Ctrl Pts',(16.3424568528292,0.611027672763462,3.86009394681272));
#54939=CARTESIAN_POINT('Ctrl Pts',(16.3265515741416,0.522578640170867,3.6538207322234));
#54940=CARTESIAN_POINT('Ctrl Pts',(16.310646295454,0.367684957814641,3.53210178682255));
#54941=CARTESIAN_POINT('Ctrl Pts',(16.2947410167664,0.212791275458425,3.4103828414217));
#54942=CARTESIAN_POINT('Ctrl Pts',(16.2788357380788,-0.00854705666138705,
3.3732181652093));
#54943=CARTESIAN_POINT('Ctrl Pts',(16.2629304593912,-0.19470084048803,3.43767220519428));
#54944=CARTESIAN_POINT('Ctrl Pts',(16.2470251807036,-0.380854624314662,
3.50212624517926));
#54945=CARTESIAN_POINT('Ctrl Pts',(16.231119902016,-0.531823859848111,3.66819900136163));
#54946=CARTESIAN_POINT('Ctrl Pts',(16.2152146233283,-0.578289861113055,
3.85963689006134));
#54947=CARTESIAN_POINT('Ctrl Pts',(16.1993093446407,-0.624755862378002,
4.05107477876107));
#54948=CARTESIAN_POINT('Ctrl Pts',(16.1834040659531,-0.566718629374431,
4.26787779997815));
#54949=CARTESIAN_POINT('Ctrl Pts',(16.1674987872655,-0.430826404144746,
4.41049917854914));
#54950=CARTESIAN_POINT('Ctrl Pts',(16.1546143285962,-0.320743594918802,
4.52603310245269));
#54951=CARTESIAN_POINT('Ctrl Pts',(16.1417298699269,-0.159570744489656,
4.592887512417));
#54952=CARTESIAN_POINT('Ctrl Pts',(16.1288454112575,0.000520203518568921,
4.59435747030618));
#54953=CARTESIAN_POINT('Ctrl Pts',(16.0211545887425,-0.00024144267326323,
4.59496181546483));
#54954=CARTESIAN_POINT('Ctrl Pts',(16.0222332884401,-0.0136089074611732,
4.59503051682625));
#54955=CARTESIAN_POINT('Ctrl Pts',(16.0233119881376,-0.0269720681925484,
4.59461918253551));
#54956=CARTESIAN_POINT('Ctrl Pts',(16.0243906878352,-0.0403017303441999,
4.59371435609144));
#54957=CARTESIAN_POINT('Ctrl Pts',(16.0402959665228,-0.236845765548457,
4.58037281461397));
#54958=CARTESIAN_POINT('Ctrl Pts',(16.0562012452104,-0.426106842065734,
4.45974066575184));
#54959=CARTESIAN_POINT('Ctrl Pts',(16.072106523898,-0.521184280535122,4.2872070887372));
#54960=CARTESIAN_POINT('Ctrl Pts',(16.0880118025856,-0.616261719004504,
4.11467351172257));
#54961=CARTESIAN_POINT('Ctrl Pts',(16.1039170812732,-0.61715551942601,3.89023850655542));
#54962=CARTESIAN_POINT('Ctrl Pts',(16.1198223599609,-0.523455286459661,
3.71695313254649));
#54963=CARTESIAN_POINT('Ctrl Pts',(16.1357276386485,-0.429755053493313,
3.54366775853756));
#54964=CARTESIAN_POINT('Ctrl Pts',(16.1516329173361,-0.241460787139106,
3.42153201568684));
#54965=CARTESIAN_POINT('Ctrl Pts',(16.1675381960237,-0.045029248433429,
3.40662546997421));
#54966=CARTESIAN_POINT('Ctrl Pts',(16.1834434747113,0.151402290272254,3.39171892426158));
#54967=CARTESIAN_POINT('Ctrl Pts',(16.1993487533989,0.355971101329402,3.48404157568705));
#54968=CARTESIAN_POINT('Ctrl Pts',(16.2152540320865,0.474747841293266,3.64120276856532));
#54969=CARTESIAN_POINT('Ctrl Pts',(16.2311593107741,0.593524581257127,3.79836396144359));
#54970=CARTESIAN_POINT('Ctrl Pts',(16.2470645894618,0.626509250127697,4.02036369577466));
#54971=CARTESIAN_POINT('Ctrl Pts',(16.2629698681494,0.558556683425868,4.20526908558792));
#54972=CARTESIAN_POINT('Ctrl Pts',(16.278875146837,0.490604116724039,4.39017447540119));
#54973=CARTESIAN_POINT('Ctrl Pts',(16.2947804255246,0.32171431444981,4.53798552069667));
#54974=CARTESIAN_POINT('Ctrl Pts',(16.3106857042122,0.129434328669215,4.58083364284428));
#54975=CARTESIAN_POINT('Ctrl Pts',(16.314175332389,0.0872479785030607,4.5902345478711));
#54976=CARTESIAN_POINT('Ctrl Pts',(16.3176649605657,0.0439357035691123,
4.5945828907904));
#54977=CARTESIAN_POINT('Ctrl Pts',(16.3211545887425,0.000543344619121817,
4.59417988242975));
#54978=CARTESIAN_POINT('Origin',(4.,0.,4.));
#54979=CARTESIAN_POINT('',(16.7288454112575,-0.000548108868865471,4.59408180714414));
#54980=CARTESIAN_POINT('',(16.6211545887425,-2.1752937549985E-5,4.5931168278739));
#54981=CARTESIAN_POINT('',(4.,-7.27562663373442E-17,4.5941));
#54982=CARTESIAN_POINT('Ctrl Pts',(16.7288454112575,-0.000548108868865471,
4.59408180714414));
#54983=CARTESIAN_POINT('Ctrl Pts',(16.7166879354906,0.15068989439403,4.59268722311157));
#54984=CARTESIAN_POINT('Ctrl Pts',(16.7045304597237,0.302891836883802,4.53390177381835));
#54985=CARTESIAN_POINT('Ctrl Pts',(16.6923729839567,0.411632901649024,4.42974331917764));
#54986=CARTESIAN_POINT('Ctrl Pts',(16.6764677052691,0.553895734249677,4.29347578465895));
#54987=CARTESIAN_POINT('Ctrl Pts',(16.6605624265815,0.621772048174623,4.07954898308531));
#54988=CARTESIAN_POINT('Ctrl Pts',(16.6446571478939,0.58409591167956,3.88618905124272));
#54989=CARTESIAN_POINT('Ctrl Pts',(16.6287518692063,0.546419775184499,3.69282911940014));
#54990=CARTESIAN_POINT('Ctrl Pts',(16.6128465905187,0.403191188269443,3.52003605728863));
#54991=CARTESIAN_POINT('Ctrl Pts',(16.596941311831,0.220174658543969,3.44714912875817));
#54992=CARTESIAN_POINT('Ctrl Pts',(16.5810360331434,0.0371581288184754,
3.37426220022769));
#54993=CARTESIAN_POINT('Ctrl Pts',(16.5651307544558,-0.185646343717467,
3.40128140527831));
#54994=CARTESIAN_POINT('Ctrl Pts',(16.5492254757682,-0.34593637135519,3.51580066803907));
#54995=CARTESIAN_POINT('Ctrl Pts',(16.5333201970806,-0.506226398992903,
3.63031993079982));
#54996=CARTESIAN_POINT('Ctrl Pts',(16.517414918393,-0.604001981732426,3.83233925127069));
#54997=CARTESIAN_POINT('Ctrl Pts',(16.5015096397054,-0.594368708523554,
4.02909990422408));
#54998=CARTESIAN_POINT('Ctrl Pts',(16.4856043610178,-0.584735435314682,
4.22586055717748));
#54999=CARTESIAN_POINT('Ctrl Pts',(16.4696990823301,-0.467693306157413,
4.4173625426134));
#55000=CARTESIAN_POINT('Ctrl Pts',(16.4537938036425,-0.296983115116624,
4.51567625060054));
#55001=CARTESIAN_POINT('Ctrl Pts',(16.4454776728475,-0.20772669247752,4.56707991793767));
#55002=CARTESIAN_POINT('Ctrl Pts',(16.4371615420525,-0.103798720846626,
4.59300816600183));
#55003=CARTESIAN_POINT('Ctrl Pts',(16.4288454112575,7.48704377684928E-5,
4.59312461313858));
#55004=CARTESIAN_POINT('Ctrl Pts',(16.3211545887425,0.000543344619121817,
4.59417988242975));
#55005=CARTESIAN_POINT('Ctrl Pts',(16.3335702392533,-0.153841115924154,
4.59274603025257));
#55006=CARTESIAN_POINT('Ctrl Pts',(16.3459858897642,-0.309239316255332,
4.53116741914846));
#55007=CARTESIAN_POINT('Ctrl Pts',(16.3584015402751,-0.418549561707542,
4.42300972860235));
#55008=CARTESIAN_POINT('Ctrl Pts',(16.3743068189627,-0.558583297016706,
4.28445249321304));
#55009=CARTESIAN_POINT('Ctrl Pts',(16.3902120976503,-0.622980598348072,
4.06945282343469));
#55010=CARTESIAN_POINT('Ctrl Pts',(16.4061173763379,-0.582172949355422,
3.87672947174358));
#55011=CARTESIAN_POINT('Ctrl Pts',(16.4220226550255,-0.541365300362771,
3.68400612005246));
#55012=CARTESIAN_POINT('Ctrl Pts',(16.4379279337131,-0.395352701046104,
3.5135590864486));
#55013=CARTESIAN_POINT('Ctrl Pts',(16.4538332124007,-0.211177959727979,
3.44365043774355));
#55014=CARTESIAN_POINT('Ctrl Pts',(16.4697384910883,-0.0270032184098532,
3.37374178903851));
#55015=CARTESIAN_POINT('Ctrl Pts',(16.485643769776,0.195333664909731,3.40437152523229));
#55016=CARTESIAN_POINT('Ctrl Pts',(16.5015490484636,0.353744999708243,3.52147576730199));
#55017=CARTESIAN_POINT('Ctrl Pts',(16.5174543271512,0.512156334506764,3.63858000937169));
#55018=CARTESIAN_POINT('Ctrl Pts',(16.5333596058388,0.606642120784206,3.84215875731731));
#55019=CARTESIAN_POINT('Ctrl Pts',(16.5492648845264,0.59381848284593,4.03873726278877));
#55020=CARTESIAN_POINT('Ctrl Pts',(16.565170163214,0.580994844907655,4.23531576826023));
#55021=CARTESIAN_POINT('Ctrl Pts',(16.5810754419016,0.460861782753675,4.42489403125753));
#55022=CARTESIAN_POINT('Ctrl Pts',(16.5969807205892,0.288579316114369,4.52042573380721));
#55023=CARTESIAN_POINT('Ctrl Pts',(16.6050386766403,0.201297315476928,4.56882414767653));
#55024=CARTESIAN_POINT('Ctrl Pts',(16.6130966326914,0.100630370301649,4.59308406930439));
#55025=CARTESIAN_POINT('Ctrl Pts',(16.6211545887425,-2.1752937549985E-5,
4.5931168278739));
#55026=CARTESIAN_POINT('Origin',(4.,0.,4.));
#55027=CARTESIAN_POINT('',(17.0288454112575,0.000186802344652959,4.59500977980842));
#55028=CARTESIAN_POINT('',(16.9211545887425,-0.000535257393875686,4.59425998651214));
#55029=CARTESIAN_POINT('',(4.,-7.27562663373442E-17,4.5941));
#55030=CARTESIAN_POINT('Ctrl Pts',(17.0288454112575,0.000186802344652959,
4.59500977980842));
#55031=CARTESIAN_POINT('Ctrl Pts',(17.0280248863039,0.0103527338555297,
4.59505157132578));
#55032=CARTESIAN_POINT('Ctrl Pts',(17.0272043613502,0.0205166685362397,
4.5948136789481));
#55033=CARTESIAN_POINT('Ctrl Pts',(17.0263838363966,0.0306658549750798,
4.59428997251885));
#55034=CARTESIAN_POINT('Ctrl Pts',(17.010478557709,0.227400443050786,4.58413830477164));
#55035=CARTESIAN_POINT('Ctrl Pts',(16.9945732790214,0.418593379366704,4.46659200952389));
#55036=CARTESIAN_POINT('Ctrl Pts',(16.9786680003338,0.516456956272638,4.29562337257973));
#55037=CARTESIAN_POINT('Ctrl Pts',(16.9627627216462,0.614320533178566,4.12465473563558));
#55038=CARTESIAN_POINT('Ctrl Pts',(16.9468574429585,0.618854750674521,3.90026375699502));
#55039=CARTESIAN_POINT('Ctrl Pts',(16.9309521642709,0.527977687913284,3.72548128085037));
#55040=CARTESIAN_POINT('Ctrl Pts',(16.9150468855833,0.437100625152047,3.55069880470573));
#55041=CARTESIAN_POINT('Ctrl Pts',(16.8991416068957,0.25081228213362,3.42552483105699));
#55042=CARTESIAN_POINT('Ctrl Pts',(16.8832363282081,0.054648384762208,3.40743395292956));
#55043=CARTESIAN_POINT('Ctrl Pts',(16.8673310495205,-0.141515512609204,
3.38934307480212));
#55044=CARTESIAN_POINT('Ctrl Pts',(16.8514257708328,-0.347554964333599,
3.47833529219599));
#55045=CARTESIAN_POINT('Ctrl Pts',(16.8355204921452,-0.468865370989487,
3.63354914383413));
#55046=CARTESIAN_POINT('Ctrl Pts',(16.8196152134576,-0.590175777645383,
3.78876299547228));
#55047=CARTESIAN_POINT('Ctrl Pts',(16.80370993477,-0.62675713923276,4.01019848135471));
#55048=CARTESIAN_POINT('Ctrl Pts',(16.7878046560824,-0.561812842140477,
4.19618179452704));
#55049=CARTESIAN_POINT('Ctrl Pts',(16.7718993773948,-0.496868545048197,
4.38216510769936));
#55050=CARTESIAN_POINT('Ctrl Pts',(16.7559940987072,-0.330398589276266,
4.53269624816158));
#55051=CARTESIAN_POINT('Ctrl Pts',(16.7400888200196,-0.138838935752124,
4.57865768466082));
#55052=CARTESIAN_POINT('Ctrl Pts',(16.7363410170989,-0.0937012275068688,
4.58948769960953));
#55053=CARTESIAN_POINT('Ctrl Pts',(16.7325932141782,-0.0471704703862807,
4.59451171761327));
#55054=CARTESIAN_POINT('Ctrl Pts',(16.7288454112575,-0.000548108868865471,
4.59408180714414));
#55055=CARTESIAN_POINT('Ctrl Pts',(16.6211545887425,-2.1752937549985E-5,
4.5931168278739));
#55056=CARTESIAN_POINT('Ctrl Pts',(16.629001911379,-0.0980428491191961,
4.59314873014073));
#55057=CARTESIAN_POINT('Ctrl Pts',(16.6368492340155,-0.196049888122182,
4.57020350190738));
#55058=CARTESIAN_POINT('Ctrl Pts',(16.6446965566521,-0.281666676968544,
4.52419924569128));
#55059=CARTESIAN_POINT('Ctrl Pts',(16.6606018353397,-0.455198332287519,
4.43095591292362));
#55060=CARTESIAN_POINT('Ctrl Pts',(16.6765071140273,-0.577829771800838,
4.24298410528626));
#55061=CARTESIAN_POINT('Ctrl Pts',(16.6924123927149,-0.593253826592341,
4.0465925244149));
#55062=CARTESIAN_POINT('Ctrl Pts',(16.7083176714025,-0.608677881383846,
3.85020094354353));
#55063=CARTESIAN_POINT('Ctrl Pts',(16.7242229500901,-0.516894551453523,
3.64538958943816));
#55064=CARTESIAN_POINT('Ctrl Pts',(16.7401282287778,-0.360046858872914,
3.52619917105016));
#55065=CARTESIAN_POINT('Ctrl Pts',(16.7560335074654,-0.203199166292313,
3.40700875266216));
#55066=CARTESIAN_POINT('Ctrl Pts',(16.771938786153,0.0187128889385656,3.37343926999153));
#55067=CARTESIAN_POINT('Ctrl Pts',(16.7878440648406,0.203796679382533,3.44090440927292));
#55068=CARTESIAN_POINT('Ctrl Pts',(16.8037493435282,0.388880469826499,3.50836954855431));
#55069=CARTESIAN_POINT('Ctrl Pts',(16.8196546222158,0.537135995483554,3.67686930978772));
#55070=CARTESIAN_POINT('Ctrl Pts',(16.8355599009034,0.58049059114602,3.86903573125179));
#55071=CARTESIAN_POINT('Ctrl Pts',(16.851465179591,0.623845186808487,4.06120215271587));
#55072=CARTESIAN_POINT('Ctrl Pts',(16.8673704582787,0.562298852476364,4.2770352344106));
#55073=CARTESIAN_POINT('Ctrl Pts',(16.8832757369663,0.424111061064287,4.41743355636644));
#55074=CARTESIAN_POINT('Ctrl Pts',(16.8959020208917,0.314411738992559,4.5288876912157));
#55075=CARTESIAN_POINT('Ctrl Pts',(16.9085283048171,0.156414067554279,4.59280392009262));
#55076=CARTESIAN_POINT('Ctrl Pts',(16.9211545887425,-0.000535257393875686,
4.59425998651214));
#55077=CARTESIAN_POINT('Origin',(4.,0.,4.));
#55078=CARTESIAN_POINT('',(17.3288454112575,0.000452601584348983,4.59351524744837));
#55079=CARTESIAN_POINT('',(17.2211545887425,0.000283723793354941,4.5949151055343));
#55080=CARTESIAN_POINT('',(4.,-7.27562663373442E-17,4.5941));
#55081=CARTESIAN_POINT('Ctrl Pts',(17.3288454112575,0.000452601584348983,
4.59351524744837));
#55082=CARTESIAN_POINT('Ctrl Pts',(17.3234565584296,0.0676518012035294,
4.59398979695312));
#55083=CARTESIAN_POINT('Ctrl Pts',(17.3180677056016,0.134706745978521,4.58346365752876));
#55084=CARTESIAN_POINT('Ctrl Pts',(17.3126788527736,0.197661386620268,4.56129398922237));
#55085=CARTESIAN_POINT('Ctrl Pts',(17.296773574086,0.383472937993069,4.49585988588324));
#55086=CARTESIAN_POINT('Ctrl Pts',(17.2808682953984,0.533564938357213,4.32899388620009));
#55087=CARTESIAN_POINT('Ctrl Pts',(17.2649630167108,0.579021491014364,4.13731379770915));
#55088=CARTESIAN_POINT('Ctrl Pts',(17.2490577380232,0.624478043671518,3.94563370921821));
#55089=CARTESIAN_POINT('Ctrl Pts',(17.2331524593355,0.565299148621668,3.72913953191949));
#55090=CARTESIAN_POINT('Ctrl Pts',(17.2172471806479,0.428657250819126,3.58723623291525));
#55091=CARTESIAN_POINT('Ctrl Pts',(17.2013419019603,0.292015353016592,3.44533293391101));
#55092=CARTESIAN_POINT('Ctrl Pts',(17.1854366232727,0.0779104524613767,
3.37802051320125));
#55093=CARTESIAN_POINT('Ctrl Pts',(17.1695313445851,-0.115349538542919,
3.41620598662221));
#55094=CARTESIAN_POINT('Ctrl Pts',(17.1536260658975,-0.308609529547215,
3.45439146004317));
#55095=CARTESIAN_POINT('Ctrl Pts',(17.1377207872099,-0.48102461100059,3.59807482759486));
#55096=CARTESIAN_POINT('Ctrl Pts',(17.1218155085223,-0.553429071780215,
3.78128276563952));
#55097=CARTESIAN_POINT('Ctrl Pts',(17.1059102298347,-0.625833532559839,
3.96449070368418));
#55098=CARTESIAN_POINT('Ctrl Pts',(17.090004951147,-0.598227372665711,4.18722321222181));
#55099=CARTESIAN_POINT('Ctrl Pts',(17.0740996724594,-0.483286172800906,
4.34721094636728));
#55100=CARTESIAN_POINT('Ctrl Pts',(17.0590149187255,-0.374274584390508,
4.4989451987145));
#55101=CARTESIAN_POINT('Ctrl Pts',(17.0439301649915,-0.186706445247169,
4.59424147319602));
#55102=CARTESIAN_POINT('Ctrl Pts',(17.0288454112575,0.000186802344652959,
4.59500977980842));
#55103=CARTESIAN_POINT('Ctrl Pts',(16.9211545887425,-0.000535257393875686,
4.59425998651214));
#55104=CARTESIAN_POINT('Ctrl Pts',(16.9244335835047,-0.0412943609811605,
4.59463812105998));
#55105=CARTESIAN_POINT('Ctrl Pts',(16.9277125782669,-0.0819827620002526,
4.59080381827239));
#55106=CARTESIAN_POINT('Ctrl Pts',(16.9309915730291,-0.121736182180322,
4.58249572362891));
#55107=CARTESIAN_POINT('Ctrl Pts',(16.9468968517167,-0.31456638552074,4.54219600671859));
#55108=CARTESIAN_POINT('Ctrl Pts',(16.9628021304043,-0.485397543709551,
4.39663301068103));
#55109=CARTESIAN_POINT('Ctrl Pts',(16.978707409092,-0.555791216176751,4.21264310503418));
#55110=CARTESIAN_POINT('Ctrl Pts',(16.9946126877796,-0.626184888643955,
4.02865319938731));
#55111=CARTESIAN_POINT('Ctrl Pts',(17.0105179664672,-0.596141075389537,
3.80623638413113));
#55112=CARTESIAN_POINT('Ctrl Pts',(17.0264232451548,-0.479454624411006,
3.64751705115182));
#55113=CARTESIAN_POINT('Ctrl Pts',(17.0423285238424,-0.362768173432475,
3.48879771817251));
#55114=CARTESIAN_POINT('Ctrl Pts',(17.05823380253,-0.159439084729831,3.39377586747005));
#55115=CARTESIAN_POINT('Ctrl Pts',(17.0741390812176,0.0371725263090214,
3.40608151284405));
#55116=CARTESIAN_POINT('Ctrl Pts',(17.0900443599052,0.233784137347885,3.41838715821804));
#55117=CARTESIAN_POINT('Ctrl Pts',(17.1059496385929,0.423678270722955,3.5380202996685));
#55118=CARTESIAN_POINT('Ctrl Pts',(17.1218549172805,0.519663574146654,3.71005045990219));
#55119=CARTESIAN_POINT('Ctrl Pts',(17.1377601959681,0.615648877570348,3.88208062013586));
#55120=CARTESIAN_POINT('Ctrl Pts',(17.1536654746557,0.617725351042682,4.10650779915277));
#55121=CARTESIAN_POINT('Ctrl Pts',(17.1695707533433,0.524939565793509,4.28028453107927));
#55122=CARTESIAN_POINT('Ctrl Pts',(17.1854760320309,0.432153780544336,4.45406126300578));
#55123=CARTESIAN_POINT('Ctrl Pts',(17.2013813107185,0.244505736573655,4.5771875478419));
#55124=CARTESIAN_POINT('Ctrl Pts',(17.2172865894061,0.0481554769387473,
4.59312900463441));
#55125=CARTESIAN_POINT('Ctrl Pts',(17.2185759225182,0.0322386925622284,
4.59442127046022));
#55126=CARTESIAN_POINT('Ctrl Pts',(17.2198652556304,0.0162647237884017,
4.5950091984451));
#55127=CARTESIAN_POINT('Ctrl Pts',(17.2211545887425,0.000283723793354941,
4.5949151055343));
#55128=CARTESIAN_POINT('Origin',(4.,0.,4.));
#55129=CARTESIAN_POINT('',(17.6288454112575,-0.000376811216598938,4.5933658344624));
#55130=CARTESIAN_POINT('',(17.5211545887425,0.000390292690419375,4.59338796628294));
#55131=CARTESIAN_POINT('',(4.,-7.27562663373442E-17,4.5941));
#55132=CARTESIAN_POINT('Ctrl Pts',(17.6288454112575,-0.000376811216598938,
4.5933658344624));
#55133=CARTESIAN_POINT('Ctrl Pts',(17.6188882305552,0.123868145157646,4.5926473455414));
#55134=CARTESIAN_POINT('Ctrl Pts',(17.608931049853,0.248515939035854,4.55458993700248));
#55135=CARTESIAN_POINT('Ctrl Pts',(17.5989738691507,0.348483110949462,4.48236965854082));
#55136=CARTESIAN_POINT('Ctrl Pts',(17.5830685904631,0.508167440925656,4.36700731952407));
#55137=CARTESIAN_POINT('Ctrl Pts',(17.5671633117754,0.604877102606476,4.16447556457896));
#55138=CARTESIAN_POINT('Ctrl Pts',(17.5512580330878,0.594207110796467,3.96776840716434));
#55139=CARTESIAN_POINT('Ctrl Pts',(17.5353527544002,0.583537118986457,3.77106124974973));
#55140=CARTESIAN_POINT('Ctrl Pts',(17.5194474757126,0.465487473685617,3.58017868986561));
#55141=CARTESIAN_POINT('Ctrl Pts',(17.503542197025,0.294261577747463,3.48276592343564));
#55142=CARTESIAN_POINT('Ctrl Pts',(17.4876369183374,0.123035681809298,3.38535315700567));
#55143=CARTESIAN_POINT('Ctrl Pts',(17.4717316396498,-0.101366464766187,
3.38141018402985));
#55144=CARTESIAN_POINT('Ctrl Pts',(17.4558263609621,-0.275908889943427,
3.47274745088526));
#55145=CARTESIAN_POINT('Ctrl Pts',(17.4399210822745,-0.450451315120656,
3.56408471774066));
#55146=CARTESIAN_POINT('Ctrl Pts',(17.4240158035869,-0.575134018899647,
3.75070222442727));
#55147=CARTESIAN_POINT('Ctrl Pts',(17.4081105248993,-0.592707978595278,
3.94691310701022));
#55148=CARTESIAN_POINT('Ctrl Pts',(17.3922052462117,-0.610281938290908,
4.14312398959316));
#55149=CARTESIAN_POINT('Ctrl Pts',(17.3762999675241,-0.520747153903178,
4.34892824807245));
#55150=CARTESIAN_POINT('Ctrl Pts',(17.3603946888365,-0.365214210518585,
4.46982927381454));
#55151=CARTESIAN_POINT('Ctrl Pts',(17.3498782629768,-0.262377240481122,
4.54976793433994));
#55152=CARTESIAN_POINT('Ctrl Pts',(17.3393618371172,-0.130687628661636,
4.59258915708319));
#55153=CARTESIAN_POINT('Ctrl Pts',(17.3288454112575,0.000452601584348983,
4.59351524744837));
#55154=CARTESIAN_POINT('Ctrl Pts',(17.2211545887425,0.000283723793354941,
4.5949151055343));
#55155=CARTESIAN_POINT('Ctrl Pts',(17.235770534318,-0.18087770297476,4.59384846352355));
#55156=CARTESIAN_POINT('Ctrl Pts',(17.2503864798935,-0.362942684182573,
4.50513801271133));
#55157=CARTESIAN_POINT('Ctrl Pts',(17.265002425469,-0.47285052735612,4.36129398677095));
#55158=CARTESIAN_POINT('Ctrl Pts',(17.2809077041566,-0.592453796716944,
4.20476088336606));
#55159=CARTESIAN_POINT('Ctrl Pts',(17.2968129828442,-0.626607860139456,
3.98293804780737));
#55160=CARTESIAN_POINT('Ctrl Pts',(17.3127182615318,-0.559630616639302,
3.79767714163318));
#55161=CARTESIAN_POINT('Ctrl Pts',(17.3286235402194,-0.492653373139145,
3.61241623545897));
#55162=CARTESIAN_POINT('Ctrl Pts',(17.3445288189071,-0.324544822716309,
3.46371725866926));
#55163=CARTESIAN_POINT('Ctrl Pts',(17.3604340975947,-0.132493299638714,
3.41985649047097));
#55164=CARTESIAN_POINT('Ctrl Pts',(17.3763393762823,0.0595582234388708,
3.37599572227269));
#55165=CARTESIAN_POINT('Ctrl Pts',(17.3922446549699,0.275552719171213,3.43697316266583));
#55166=CARTESIAN_POINT('Ctrl Pts',(17.4081499336575,0.416314653091553,3.5747905507646));
#55167=CARTESIAN_POINT('Ctrl Pts',(17.4240552123451,0.557076587011893,3.71260793886338));
#55168=CARTESIAN_POINT('Ctrl Pts',(17.4399604910327,0.622605959120231,3.92726527466781));
#55169=CARTESIAN_POINT('Ctrl Pts',(17.4558657697203,0.582814454063527,4.12020099097945));
#55170=CARTESIAN_POINT('Ctrl Pts',(17.4717710484079,0.543022949006823,4.31313670729109));
#55171=CARTESIAN_POINT('Ctrl Pts',(17.4876763270955,0.397910566785078,4.48435080410994));
#55172=CARTESIAN_POINT('Ctrl Pts',(17.5035816057832,0.214106774115907,4.55522901164789));
#55173=CARTESIAN_POINT('Ctrl Pts',(17.5094392667696,0.146414762764002,4.58133232736073));
#55174=CARTESIAN_POINT('Ctrl Pts',(17.515296927756,0.073474912906076,4.59382676872096));
#55175=CARTESIAN_POINT('Ctrl Pts',(17.5211545887425,0.000390292690419375,
4.59338796628294));
#55176=CARTESIAN_POINT('Origin',(4.,0.,4.));
#55177=CARTESIAN_POINT('',(17.9288454112575,-0.000301159635511528,4.59489313984584));
#55178=CARTESIAN_POINT('',(17.8211545887425,-0.000441626631060947,4.59348913571676));
#55179=CARTESIAN_POINT('',(4.,-7.27562663373442E-17,4.5941));
#55180=CARTESIAN_POINT('Ctrl Pts',(17.9288454112575,-0.000301159635511528,
4.59489313984584));
#55181=CARTESIAN_POINT('Ctrl Pts',(17.9143199026809,0.179756887528332,4.59377956832623));
#55182=CARTESIAN_POINT('Ctrl Pts',(17.8997943941043,0.360751589755073,4.50630604003092));
#55183=CARTESIAN_POINT('Ctrl Pts',(17.8852688855277,0.470789914960854,4.36397502945801));
#55184=CARTESIAN_POINT('Ctrl Pts',(17.8693636068401,0.591280720462369,4.20812407407766));
#55185=CARTESIAN_POINT('Ctrl Pts',(17.8534583281524,0.626694694978596,3.98649889312445));
#55186=CARTESIAN_POINT('Ctrl Pts',(17.8375530494648,0.560771239653389,3.80086039350393));
#55187=CARTESIAN_POINT('Ctrl Pts',(17.8216477707772,0.494847784328189,3.61522189388343));
#55188=CARTESIAN_POINT('Ctrl Pts',(17.8057424920896,0.327586899161578,3.46557007559562));
#55189=CARTESIAN_POINT('Ctrl Pts',(17.789837213402,0.135787706397568,3.42061872235194));
#55190=CARTESIAN_POINT('Ctrl Pts',(17.7739319347144,-0.0560114863664412,
3.37566736910827));
#55191=CARTESIAN_POINT('Ctrl Pts',(17.7580266560268,-0.272348986727849,
3.43541648090873));
#55192=CARTESIAN_POINT('Ctrl Pts',(17.7421213773392,-0.41389176700556,3.57243179339102));
#55193=CARTESIAN_POINT('Ctrl Pts',(17.7262160986515,-0.555434547283271,
3.7094471058733));
#55194=CARTESIAN_POINT('Ctrl Pts',(17.710310819964,-0.622182607477285,3.92372861903742));
#55195=CARTESIAN_POINT('Ctrl Pts',(17.6944055412763,-0.583488062224059,
4.11688732754162));
#55196=CARTESIAN_POINT('Ctrl Pts',(17.6785002625887,-0.544793516970831,
4.31004603604583));
#55197=CARTESIAN_POINT('Ctrl Pts',(17.6625949839011,-0.400656366270352,
4.48208193989012));
#55198=CARTESIAN_POINT('Ctrl Pts',(17.6466897052135,-0.217258291784321,
4.55400343026805));
#55199=CARTESIAN_POINT('Ctrl Pts',(17.6407416072282,-0.148672903323923,
4.58089991415997));
#55200=CARTESIAN_POINT('Ctrl Pts',(17.6347935092429,-0.0745967331795002,
4.59379503652584));
#55201=CARTESIAN_POINT('Ctrl Pts',(17.6288454112575,-0.000376811216598938,
4.5933658344624));
#55202=CARTESIAN_POINT('Ctrl Pts',(17.5211545887425,0.000390292690419375,
4.59338796628294));
#55203=CARTESIAN_POINT('Ctrl Pts',(17.5312022064437,-0.12497140465997,4.59263529057266));
#55204=CARTESIAN_POINT('Ctrl Pts',(17.5412498241448,-0.250759050797478,
4.55382993891589));
#55205=CARTESIAN_POINT('Ctrl Pts',(17.551297441846,-0.351218450958555,4.48038168762358));
#55206=CARTESIAN_POINT('Ctrl Pts',(17.5672027205336,-0.510244680247213,
4.36411383780432));
#55207=CARTESIAN_POINT('Ctrl Pts',(17.5831079992212,-0.605801935707933,
4.16103581990878));
#55208=CARTESIAN_POINT('Ctrl Pts',(17.5990132779088,-0.594014368327242,
3.96439246823218));
#55209=CARTESIAN_POINT('Ctrl Pts',(17.6149185565964,-0.58222680094655,3.76774911655557));
#55210=CARTESIAN_POINT('Ctrl Pts',(17.6308238352841,-0.463094410724447,
3.5775404310979));
#55211=CARTESIAN_POINT('Ctrl Pts',(17.6467291139717,-0.291317751175132,
3.48110219315546));
#55212=CARTESIAN_POINT('Ctrl Pts',(17.6626343926593,-0.119541091625818,
3.38466395521302));
#55213=CARTESIAN_POINT('Ctrl Pts',(17.6785396713469,0.104879837250709,3.38199616478582));
#55214=CARTESIAN_POINT('Ctrl Pts',(17.6944449500345,0.278900439380867,3.47432375837312));
#55215=CARTESIAN_POINT('Ctrl Pts',(17.7103502287221,0.452921041511034,3.56665135196042));
#55216=CARTESIAN_POINT('Ctrl Pts',(17.7262555074097,0.576541316894826,3.75397432956222));
#55217=CARTESIAN_POINT('Ctrl Pts',(17.7421607860974,0.593000065018554,3.95028190484542));
#55218=CARTESIAN_POINT('Ctrl Pts',(17.758066064785,0.60945881314228,4.1465894801286));
#55219=CARTESIAN_POINT('Ctrl Pts',(17.7739713434726,0.518756034005955,4.35188165309317));
#55220=CARTESIAN_POINT('Ctrl Pts',(17.7898766221602,0.362538606470845,4.47189694310939));
#55221=CARTESIAN_POINT('Ctrl Pts',(17.8003026110209,0.260137309937395,4.55056755941266));
#55222=CARTESIAN_POINT('Ctrl Pts',(17.8107285998817,0.129585238016204,4.59259583028147));
#55223=CARTESIAN_POINT('Ctrl Pts',(17.8211545887425,-0.000441626631060947,
4.59348913571676));
#55224=CARTESIAN_POINT('Origin',(4.,0.,4.));
#55225=CARTESIAN_POINT('',(18.2288454112575,0.000530626821107938,4.59429426521737));
#55226=CARTESIAN_POINT('',(18.1211545887425,-0.000206261771334874,4.59499421029555));
#55227=CARTESIAN_POINT('',(4.,-7.27562663373442E-17,4.5941));
#55228=CARTESIAN_POINT('Ctrl Pts',(18.2288454112575,0.000530626821107938,
4.59429426521737));
#55229=CARTESIAN_POINT('Ctrl Pts',(18.2256568534942,0.0401596894680921,
4.59466101186164));
#55230=CARTESIAN_POINT('Ctrl Pts',(18.2224682957309,0.0797220295111884,
4.5910372210354));
#55231=CARTESIAN_POINT('Ctrl Pts',(18.2192797379675,0.118424305077702,4.58317806034235));
#55232=CARTESIAN_POINT('Ctrl Pts',(18.2033744592799,0.311480390123117,4.54397471188459));
#55233=CARTESIAN_POINT('Ctrl Pts',(18.1874691805923,0.483135922039688,4.39938477867344));
#55234=CARTESIAN_POINT('Ctrl Pts',(18.1715639019047,0.554573942717995,4.21579784094385));
#55235=CARTESIAN_POINT('Ctrl Pts',(18.1556586232171,0.626011963396302,4.03221090321426));
#55236=CARTESIAN_POINT('Ctrl Pts',(18.1397533445295,0.597232472836345,3.80962696096622));
#55237=CARTESIAN_POINT('Ctrl Pts',(18.1238480658419,0.481449795543417,3.65024714373002));
#55238=CARTESIAN_POINT('Ctrl Pts',(18.1079427871543,0.365667118250483,3.49086732649381));
#55239=CARTESIAN_POINT('Ctrl Pts',(18.0920375084667,0.16288125422457,3.39469163426944));
#55240=CARTESIAN_POINT('Ctrl Pts',(18.076132229779,-0.0337971069360236,
3.40587987606835));
#55241=CARTESIAN_POINT('Ctrl Pts',(18.0602269510914,-0.230475468096606,
3.41706811786726));
#55242=CARTESIAN_POINT('Ctrl Pts',(18.0443216724038,-0.421046326391869,
3.53562029368944));
#55243=CARTESIAN_POINT('Ctrl Pts',(18.0284163937162,-0.518007606080761,
3.70710225992629));
#55244=CARTESIAN_POINT('Ctrl Pts',(18.0125111150286,-0.614968885769652,
3.87858422616314));
#55245=CARTESIAN_POINT('Ctrl Pts',(17.996605836341,-0.618320586852172,4.10299598281466));
#55246=CARTESIAN_POINT('Ctrl Pts',(17.9807005576534,-0.526523749990007,
4.27729714530494));
#55247=CARTESIAN_POINT('Ctrl Pts',(17.9647952789658,-0.434726913127837,
4.45159830779523));
#55248=CARTESIAN_POINT('Ctrl Pts',(17.9488900002781,-0.247781538320971,
4.57578887612429));
#55249=CARTESIAN_POINT('Ctrl Pts',(17.9329847215905,-0.0515250326741526,
4.59284579538505));
#55250=CARTESIAN_POINT('Ctrl Pts',(17.9316049514795,-0.0344999389365885,
4.59432546938787));
#55251=CARTESIAN_POINT('Ctrl Pts',(17.9302251813685,-0.0174047750035579,
4.59499891739512));
#55252=CARTESIAN_POINT('Ctrl Pts',(17.9288454112575,-0.000301159635511528,
4.59489313984584));
#55253=CARTESIAN_POINT('Ctrl Pts',(17.8211545887425,-0.000441626631060947,
4.59348913571676));
#55254=CARTESIAN_POINT('Ctrl Pts',(17.8266338785693,-0.0687761401428734,
4.59395860479535));
#55255=CARTESIAN_POINT('Ctrl Pts',(17.8321131683962,-0.136965594625977,
4.58306684864343));
#55256=CARTESIAN_POINT('Ctrl Pts',(17.837592458223,-0.200847632772524,4.56016175744822));
#55257=CARTESIAN_POINT('Ctrl Pts',(17.8534977369106,-0.386284368546891,
4.49367287470298));
#55258=CARTESIAN_POINT('Ctrl Pts',(17.8694030155983,-0.535425764161732,
4.32595670214462));
#55259=CARTESIAN_POINT('Ctrl Pts',(17.8853082942859,-0.579792400402821,
4.13402141072584));
#55260=CARTESIAN_POINT('Ctrl Pts',(17.9012135729735,-0.624159036643913,
3.94208611930704));
#55261=CARTESIAN_POINT('Ctrl Pts',(17.9171188516611,-0.563750913511241,
3.72593170902781));
#55262=CARTESIAN_POINT('Ctrl Pts',(17.9330241303487,-0.426304885490399,
3.58480714034942));
#55263=CARTESIAN_POINT('Ctrl Pts',(17.9489294090363,-0.288858857469565,
3.44368257167104));
#55264=CARTESIAN_POINT('Ctrl Pts',(17.9648346877239,-0.0743749245605683,
3.37758784459349));
#55265=CARTESIAN_POINT('Ctrl Pts',(17.9807399664116,0.118664965311668,3.41687086155347));
#55266=CARTESIAN_POINT('Ctrl Pts',(17.9966452450992,0.311704855183904,3.45615387851346));
#55267=CARTESIAN_POINT('Ctrl Pts',(18.0125505237868,0.483300702019379,3.60081463951098));
#55268=CARTESIAN_POINT('Ctrl Pts',(18.0284558024744,0.554662952572844,3.78443104318807));
#55269=CARTESIAN_POINT('Ctrl Pts',(18.044361081162,0.62602520312631,3.96804744686516));
#55270=CARTESIAN_POINT('Ctrl Pts',(18.0602663598496,0.597153857397765,4.19061949322182));
#55271=CARTESIAN_POINT('Ctrl Pts',(18.0761716385372,0.481305415899848,4.34995151481781));
#55272=CARTESIAN_POINT('Ctrl Pts',(18.0911659552723,0.372092100044007,4.50015792394613));
#55273=CARTESIAN_POINT('Ctrl Pts',(18.1061602720074,0.185579460002099,4.59416090236354));
#55274=CARTESIAN_POINT('Ctrl Pts',(18.1211545887425,-0.000206261771334874,
4.59499421029555));
#55275=CARTESIAN_POINT('Origin',(4.,0.,4.));
#55276=CARTESIAN_POINT('',(18.5288454112575,4.04073003155148E-5,4.59311858068669));
#55277=CARTESIAN_POINT('',(18.4211545887425,0.000547083855738422,4.59411609730493));
#55278=CARTESIAN_POINT('',(4.,-7.27562663373442E-17,4.5941));
#55279=CARTESIAN_POINT('Ctrl Pts',(18.5288454112575,4.04073003155148E-5,
4.59311858068669));
#55280=CARTESIAN_POINT('Ctrl Pts',(18.5210885256199,0.0969311390001333,
4.59317716754242));
#55281=CARTESIAN_POINT('Ctrl Pts',(18.5133316399822,0.193796352446061,4.57078374547556));
#55282=CARTESIAN_POINT('Ctrl Pts',(18.5055747543446,0.27868347559656,4.52579129559858));
#55283=CARTESIAN_POINT('Ctrl Pts',(18.489669475657,0.452742165355285,4.43353552600749));
#55284=CARTESIAN_POINT('Ctrl Pts',(18.4737641969693,0.576439736070726,4.24626358090446));
#55285=CARTESIAN_POINT('Ctrl Pts',(18.4578589182817,0.592979496483005,4.04996281465819));
#55286=CARTESIAN_POINT('Ctrl Pts',(18.4419536395941,0.609519256895283,3.85366204841193));
#55287=CARTESIAN_POINT('Ctrl Pts',(18.4260483609065,0.518901207004412,3.64833246102244));
#55288=CARTESIAN_POINT('Ctrl Pts',(18.4101430822189,0.362733321586741,3.52825271224048));
#55289=CARTESIAN_POINT('Ctrl Pts',(18.3942378035313,0.206565436169079,3.40817296345854));
#55290=CARTESIAN_POINT('Ctrl Pts',(18.3783325248437,-0.015152284775374,
3.37334305328413));
#55291=CARTESIAN_POINT('Ctrl Pts',(18.3624272461561,-0.200616443892158,
3.43975540293737));
#55292=CARTESIAN_POINT('Ctrl Pts',(18.3465219674685,-0.386080603008964,
3.50616775259061));
#55293=CARTESIAN_POINT('Ctrl Pts',(18.3306166887808,-0.535291200298091,
3.67382236207151));
#55294=CARTESIAN_POINT('Ctrl Pts',(18.3147114100932,-0.579737042064157,
3.86573932758804));
#55295=CARTESIAN_POINT('Ctrl Pts',(18.2988061314056,-0.624182883830224,
4.05765629310458));
#55296=CARTESIAN_POINT('Ctrl Pts',(18.282900852718,-0.563863970073232,4.27383561465674));
#55297=CARTESIAN_POINT('Ctrl Pts',(18.2669955740304,-0.426476194107598,
4.41501689358062));
#55298=CARTESIAN_POINT('Ctrl Pts',(18.2542788531061,-0.316630774880643,
4.52789532589669));
#55299=CARTESIAN_POINT('Ctrl Pts',(18.2415621321818,-0.157519428275204,
4.5928315930404));
#55300=CARTESIAN_POINT('Ctrl Pts',(18.2288454112575,0.000530626821107938,
4.59429426521737));
#55301=CARTESIAN_POINT('Ctrl Pts',(18.1211545887425,-0.000206261771334874,
4.59499421029555));
#55302=CARTESIAN_POINT('Ctrl Pts',(18.122065550695,-0.0114934532352288,
4.59504483693191));
#55303=CARTESIAN_POINT('Ctrl Pts',(18.1229765126475,-0.0227779616248223,
4.59475157188293));
#55304=CARTESIAN_POINT('Ctrl Pts',(18.1238874746001,-0.0340422900297544,
4.59410612569417));
#55305=CARTESIAN_POINT('Ctrl Pts',(18.1397927532877,-0.230716017194119,
4.58283671813918));
#55306=CARTESIAN_POINT('Ctrl Pts',(18.1556980319753,-0.421237934255556,
4.46420590619388));
#55307=CARTESIAN_POINT('Ctrl Pts',(18.1716033106629,-0.518128437217054,
4.29268393984778));
#55308=CARTESIAN_POINT('Ctrl Pts',(18.1875085893505,-0.615018940178556,
4.12116197350168));
#55309=CARTESIAN_POINT('Ctrl Pts',(18.2034138680381,-0.618278029040109,
3.89674885275477));
#55310=CARTESIAN_POINT('Ctrl Pts',(18.2193191467258,-0.526409268077163,
3.72248558851787));
#55311=CARTESIAN_POINT('Ctrl Pts',(18.2352244254134,-0.434540507114227,
3.54822232428098));
#55312=CARTESIAN_POINT('Ctrl Pts',(18.251129704101,-0.24754389632682,3.42410891655409));
#55313=CARTESIAN_POINT('Ctrl Pts',(18.2670349827886,-0.0512803682143169,
3.40713299136011));
#55314=CARTESIAN_POINT('Ctrl Pts',(18.2829402614762,0.144983159898198,3.39015706616613));
#55315=CARTESIAN_POINT('Ctrl Pts',(18.2988455401638,0.35051360533581,3.48031862350507));
#55316=CARTESIAN_POINT('Ctrl Pts',(18.3147508188514,0.470940082829639,3.63621929066782));
#55317=CARTESIAN_POINT('Ctrl Pts',(18.330656097539,0.591366560323475,3.79211995783059));
#55318=CARTESIAN_POINT('Ctrl Pts',(18.3465613762266,0.62668906987352,4.01375973481717));
#55319=CARTESIAN_POINT('Ctrl Pts',(18.3624666549143,0.560689009466533,4.199371012841));
#55320=CARTESIAN_POINT('Ctrl Pts',(18.3783719336019,0.49468894905955,4.38498229086483));
#55321=CARTESIAN_POINT('Ctrl Pts',(18.3942772122895,0.327366318695548,4.53456506992591));
#55322=CARTESIAN_POINT('Ctrl Pts',(18.4101824909771,0.135548591400956,4.57943726620491));
#55323=CARTESIAN_POINT('Ctrl Pts',(18.4138398568989,0.0914407431336166,
4.58975547846199));
#55324=CARTESIAN_POINT('Ctrl Pts',(18.4174972228207,0.0460377050408626,
4.59453706917327));
#55325=CARTESIAN_POINT('Ctrl Pts',(18.4211545887425,0.000547083855738422,
4.59411609730493));
#55326=CARTESIAN_POINT('Origin',(4.,0.,4.));
#55327=CARTESIAN_POINT('',(18.8288454112575,-0.000545657836941327,4.59414547262434));
#55328=CARTESIAN_POINT('',(18.7211545887425,-5.63168744233308E-5,4.59312091231189));
#55329=CARTESIAN_POINT('',(4.,-7.27562663373442E-17,4.5941));
#55330=CARTESIAN_POINT('Ctrl Pts',(18.8288454112575,-0.000545657836941327,
4.59414547262434));
#55331=CARTESIAN_POINT('Ctrl Pts',(18.8165201977456,0.15273698101805,4.59272393327212));
#55332=CARTESIAN_POINT('Ctrl Pts',(18.8041949842336,0.307016766534516,4.53213273669464));
#55333=CARTESIAN_POINT('Ctrl Pts',(18.7918697707216,0.416139138999065,4.42538122089617));
#55334=CARTESIAN_POINT('Ctrl Pts',(18.775964492034,0.556957936451544,4.28762193522949));
#55335=CARTESIAN_POINT('Ctrl Pts',(18.7600592133464,0.622575889387102,4.0729916608594));
#55336=CARTESIAN_POINT('Ctrl Pts',(18.7441539346588,0.582864009884755,3.88003953951897));
#55337=CARTESIAN_POINT('Ctrl Pts',(18.7282486559712,0.543152130382401,3.6870874181785));
#55338=CARTESIAN_POINT('Ctrl Pts',(18.7123433772835,0.3981104184421,3.51581344986768));
#55339=CARTESIAN_POINT('Ctrl Pts',(18.6964380985959,0.214335891977863,3.44485939483061));
#55340=CARTESIAN_POINT('Ctrl Pts',(18.6805328199083,0.0305613655136472,
3.37390533979354));
#55341=CARTESIAN_POINT('Ctrl Pts',(18.6646275412207,-0.191945975474496,
3.40327119803019));
#55342=CARTESIAN_POINT('Ctrl Pts',(18.6487222625331,-0.351020173514001,
3.51947340980541));
#55343=CARTESIAN_POINT('Ctrl Pts',(18.6328169838455,-0.510094371553506,
3.63567562158063));
#55344=CARTESIAN_POINT('Ctrl Pts',(18.6169117051579,-0.605735426644373,
3.83871418689441));
#55345=CARTESIAN_POINT('Ctrl Pts',(18.6010064264702,-0.594029012528289,
4.03536238640794));
#55346=CARTESIAN_POINT('Ctrl Pts',(18.5851011477826,-0.582322598412206,
4.23201058592146));
#55347=CARTESIAN_POINT('Ctrl Pts',(18.569195869095,-0.463268715089173,4.42226841963472));
#55348=CARTESIAN_POINT('Ctrl Pts',(18.5532905904074,-0.29153186902666,4.51877753945177));
#55349=CARTESIAN_POINT('Ctrl Pts',(18.5451421973574,-0.203549800283198,
4.56821988225003));
#55350=CARTESIAN_POINT('Ctrl Pts',(18.5369938043075,-0.101740616897797,
4.59305703682098));
#55351=CARTESIAN_POINT('Ctrl Pts',(18.5288454112575,4.04073003155148E-5,
4.59311858068669));
#55352=CARTESIAN_POINT('Ctrl Pts',(18.4211545887425,0.000547083855738422,
4.59411609730493));
#55353=CARTESIAN_POINT('Ctrl Pts',(18.4334025015083,-0.151793472668411,
4.59270633223614));
#55354=CARTESIAN_POINT('Ctrl Pts',(18.4456504142741,-0.305116246576315,
4.53295143150856));
#55355=CARTESIAN_POINT('Ctrl Pts',(18.4578983270399,-0.414068183831284,
4.42739736222451));
#55356=CARTESIAN_POINT('Ctrl Pts',(18.4738036057275,-0.555554407543751,
4.29032364846819));
#55357=CARTESIAN_POINT('Ctrl Pts',(18.4897088844152,-0.622214030743504,
4.07601460745865));
#55358=CARTESIAN_POINT('Ctrl Pts',(18.5056141631028,-0.583439774593308,
3.88287188415962));
#55359=CARTESIAN_POINT('Ctrl Pts',(18.5215194417904,-0.54466551844311,3.68972916086059));
#55360=CARTESIAN_POINT('Ctrl Pts',(18.537424720478,-0.400457382942952,3.51775275527208));
#55361=CARTESIAN_POINT('Ctrl Pts',(18.5533299991656,-0.217029642971419,
3.44590695711865));
#55362=CARTESIAN_POINT('Ctrl Pts',(18.5692352778532,-0.0336019029998957,
3.37406115896522));
#55363=CARTESIAN_POINT('Ctrl Pts',(18.5851405565408,0.189045441442997,3.40234596824686));
#55364=CARTESIAN_POINT('Ctrl Pts',(18.6010458352284,0.348682149221421,3.51777419717301));
#55365=CARTESIAN_POINT('Ctrl Pts',(18.6169511139161,0.508318856999844,3.63320242609916));
#55366=CARTESIAN_POINT('Ctrl Pts',(18.6328563926037,0.604944928113798,3.83577407466982));
#55367=CARTESIAN_POINT('Ctrl Pts',(18.6487616712913,0.594193758619731,4.03247681196108));
#55368=CARTESIAN_POINT('Ctrl Pts',(18.6646669499789,0.583442589125664,4.22917954925235));
#55369=CARTESIAN_POINT('Ctrl Pts',(18.6805722286665,0.465314179023576,4.42001337526422));
#55370=CARTESIAN_POINT('Ctrl Pts',(18.6964775073541,0.294048096631404,4.51735547060535));
#55371=CARTESIAN_POINT('Ctrl Pts',(18.7047032011502,0.205474838715737,4.56769764225005));
#55372=CARTESIAN_POINT('Ctrl Pts',(18.7129288949463,0.102689258835563,4.59303430424318));
#55373=CARTESIAN_POINT('Ctrl Pts',(18.7211545887425,-5.63168744233308E-5,
4.59312091231189));
#55374=CARTESIAN_POINT('Origin',(4.,0.,4.));
#55375=CARTESIAN_POINT('',(19.1288454112575,0.000222628893785728,4.59497983522242));
#55376=CARTESIAN_POINT('',(19.0211545887425,-0.000526118841417405,4.59432346427954));
#55377=CARTESIAN_POINT('',(4.,-7.27562663373442E-17,4.5941));
#55378=CARTESIAN_POINT('Ctrl Pts',(19.1288454112575,0.000222628893785728,
4.59497983522242));
#55379=CARTESIAN_POINT('Ctrl Pts',(19.1278571485589,0.012468395078646,4.59503853204781));
#55380=CARTESIAN_POINT('Ctrl Pts',(19.1268688858602,0.0247107891953784,
4.59469333777414));
#55381=CARTESIAN_POINT('Ctrl Pts',(19.1258806231615,0.0369274203756033,
4.59393377720877));
#55382=CARTESIAN_POINT('Ctrl Pts',(19.1099753444739,0.233544093050454,4.58170927203582));
#55383=CARTESIAN_POINT('Ctrl Pts',(19.0940700657862,0.423487581379576,4.46215450773496));
#55384=CARTESIAN_POINT('Ctrl Pts',(19.0781647870986,0.519543871337238,4.29016397409385));
#55385=CARTESIAN_POINT('Ctrl Pts',(19.062259508411,0.615600161294901,4.11817344045274));
#55386=CARTESIAN_POINT('Ctrl Pts',(19.0463542297234,0.617769252881104,3.89374713747137));
#55387=CARTESIAN_POINT('Ctrl Pts',(19.0304489510358,0.525055191022736,3.71993212880311));
#55388=CARTESIAN_POINT('Ctrl Pts',(19.0145436723482,0.432341129164367,3.54611712013485));
#55389=CARTESIAN_POINT('Ctrl Pts',(18.9986383936606,0.244743913861428,3.42291340577968));
#55390=CARTESIAN_POINT('Ctrl Pts',(18.982733114973,0.0484002497885746,3.40689091904056));
#55391=CARTESIAN_POINT('Ctrl Pts',(18.9668278362853,-0.147943414284278,
3.39086843230144));
#55392=CARTESIAN_POINT('Ctrl Pts',(18.9509225575977,-0.353033527127044,
3.48202717317836));
#55393=CARTESIAN_POINT('Ctrl Pts',(18.9350172789101,-0.472701385564812,
3.63851090447403));
#55394=CARTESIAN_POINT('Ctrl Pts',(18.9191120002225,-0.592369244002587,
3.79499463576972));
#55395=CARTESIAN_POINT('Ctrl Pts',(18.9032067215349,-0.626614848035354,
4.01680335748416));
#55396=CARTESIAN_POINT('Ctrl Pts',(18.8873014428473,-0.559714065105754,
4.20209188855652));
#55397=CARTESIAN_POINT('Ctrl Pts',(18.8713961641597,-0.492813282176159,
4.38738041962887));
#55398=CARTESIAN_POINT('Ctrl Pts',(18.8554908854721,-0.324766112284209,
4.53614876005914));
#55399=CARTESIAN_POINT('Ctrl Pts',(18.8395856067844,-0.132732706353525,
4.58008878179264));
#55400=CARTESIAN_POINT('Ctrl Pts',(18.8360055416088,-0.0895085590353085,
4.5899790920924));
#55401=CARTESIAN_POINT('Ctrl Pts',(18.8324254764332,-0.0450691735440342,
4.59455838259347));
#55402=CARTESIAN_POINT('Ctrl Pts',(18.8288454112575,-0.000545657836941327,
4.59414547262434));
#55403=CARTESIAN_POINT('Ctrl Pts',(18.7211545887425,-5.63168744233308E-5,
4.59312091231189));
#55404=CARTESIAN_POINT('Ctrl Pts',(18.728834173634,-0.0959805501911411,
4.59320177041728));
#55405=CARTESIAN_POINT('Ctrl Pts',(18.7365137585255,-0.191869914813978,
4.57127401300463));
#55406=CARTESIAN_POINT('Ctrl Pts',(18.744193343417,-0.276126457005151,4.5271386400555));
#55407=CARTESIAN_POINT('Ctrl Pts',(18.7600986221046,-0.450631173567243,
4.43572934949413));
#55408=CARTESIAN_POINT('Ctrl Pts',(18.7760039007922,-0.575236852009173,
4.249060403701));
#55409=CARTESIAN_POINT('Ctrl Pts',(18.7919091794798,-0.592729836422094,
4.05284228527226));
#55410=CARTESIAN_POINT('Ctrl Pts',(18.8078144581674,-0.610222820835014,
3.85662416684351));
#55411=CARTESIAN_POINT('Ctrl Pts',(18.823719736855,-0.520603111218926,3.65085687577915));
#55412=CARTESIAN_POINT('Ctrl Pts',(18.8396250155426,-0.365020286731977,
3.53002004684018));
#55413=CARTESIAN_POINT('Ctrl Pts',(18.8555302942302,-0.209437462245028,
3.40918321790122));
#55414=CARTESIAN_POINT('Ctrl Pts',(18.8714355729179,0.0121084771127808,
3.37327685108765));
#55415=CARTESIAN_POINT('Ctrl Pts',(18.8873408516055,0.197893008823487,3.43878763096633));
#55416=CARTESIAN_POINT('Ctrl Pts',(18.9032461302931,0.383677540534204,3.50429841084501));
#55417=CARTESIAN_POINT('Ctrl Pts',(18.9191514089807,0.533700664597814,3.67122633741595));
#55418=CARTESIAN_POINT('Ctrl Pts',(18.9350566876683,0.579078109400399,3.86292516893752));
#55419=CARTESIAN_POINT('Ctrl Pts',(18.9509619663559,0.624455554202981,4.05462400045908));
#55420=CARTESIAN_POINT('Ctrl Pts',(18.9668672450435,0.56518731974455,4.27109373693126));
#55421=CARTESIAN_POINT('Ctrl Pts',(18.9827725237311,0.428486871854059,4.41294063344238));
#55422=CARTESIAN_POINT('Ctrl Pts',(18.9955665454016,0.318526617336051,4.52704063153052));
#55423=CARTESIAN_POINT('Ctrl Pts',(19.008360567072,0.158464569423419,4.5928566151945));
#55424=CARTESIAN_POINT('Ctrl Pts',(19.0211545887425,-0.000526118841417405,
4.59432346427954));
#55425=CARTESIAN_POINT('Origin',(4.,0.,4.));
#55426=CARTESIAN_POINT('',(19.4288454112575,0.000431836873498515,4.59346738712276));
#55427=CARTESIAN_POINT('',(19.3211545887425,0.000315695961457875,4.59487351203822));
#55428=CARTESIAN_POINT('',(4.,-7.27562663373442E-17,4.5941));
#55429=CARTESIAN_POINT('Ctrl Pts',(19.4288454112575,0.000431836873498515,
4.59346738712276));
#55430=CARTESIAN_POINT('Ctrl Pts',(19.4232888206845,0.0697367837969298,
4.59393182999066));
#55431=CARTESIAN_POINT('Ctrl Pts',(19.4177322301115,0.13889623855249,4.58272225272434));
#55432=CARTESIAN_POINT('Ctrl Pts',(19.4121756395385,0.203565929825556,4.55917964700716));
#55433=CARTESIAN_POINT('Ctrl Pts',(19.3962703608509,0.38867754617092,4.49179089484985));
#55434=CARTESIAN_POINT('Ctrl Pts',(19.3803650821633,0.537002597765565,4.32335233206236));
#55435=CARTESIAN_POINT('Ctrl Pts',(19.3644598034757,0.580436494614329,4.13120381907284));
#55436=CARTESIAN_POINT('Ctrl Pts',(19.3485545247881,0.623870391463095,3.93905530608331));
#55437=CARTESIAN_POINT('Ctrl Pts',(19.3326492461004,0.562413133565966,3.72319684289176));
#55438=CARTESIAN_POINT('Ctrl Pts',(19.3167439674128,0.424283294458304,3.58274150440131));
#55439=CARTESIAN_POINT('Ctrl Pts',(19.3008386887252,0.286153455350651,3.44228616591086));
#55440=CARTESIAN_POINT('Ctrl Pts',(19.2849334100376,0.071351035032473,3.37723395212151));
#55441=CARTESIAN_POINT('Ctrl Pts',(19.26902813135,-0.12149578302492,3.4174540870367));
#55442=CARTESIAN_POINT('Ctrl Pts',(19.2531228526624,-0.314342601082313,
3.45767422195189));
#55443=CARTESIAN_POINT('Ctrl Pts',(19.2372175739748,-0.485233816878921,
3.60316670557164));
#55444=CARTESIAN_POINT('Ctrl Pts',(19.2213122952871,-0.555703413721375,
3.78712754492824));
#55445=CARTESIAN_POINT('Ctrl Pts',(19.2054070165995,-0.626173010563829,
3.97108838428485));
#55446=CARTESIAN_POINT('Ctrl Pts',(19.1895017379119,-0.59622098845213,4.19351757937831));
#55447=CARTESIAN_POINT('Ctrl Pts',(19.1735964592243,-0.479600048885993,
4.35228505390253));
#55448=CARTESIAN_POINT('Ctrl Pts',(19.1586794432354,-0.370225264934164,
4.50118762911129));
#55449=CARTESIAN_POINT('Ctrl Pts',(19.1437624272465,-0.184617181632464,
4.59409385471947));
#55450=CARTESIAN_POINT('Ctrl Pts',(19.1288454112575,0.000222628893785728,
4.59497983522242));
#55451=CARTESIAN_POINT('Ctrl Pts',(19.0211545887425,-0.000526118841417405,
4.59432346427954));
#55452=CARTESIAN_POINT('Ctrl Pts',(19.0242658457596,-0.0391895592568775,
4.59468017342281));
#55453=CARTESIAN_POINT('Ctrl Pts',(19.0273771027768,-0.0777896429211806,
4.59123148246997));
#55454=CARTESIAN_POINT('Ctrl Pts',(19.030488359794,-0.115590453236054,4.58374636034569));
#55455=CARTESIAN_POINT('Ctrl Pts',(19.0463936384816,-0.308834669113126,
4.5454811341878));
#55456=CARTESIAN_POINT('Ctrl Pts',(19.0622989171692,-0.481190439544719,
4.40172662532195));
#55457=CARTESIAN_POINT('Ctrl Pts',(19.0782041958568,-0.553519286527586,
4.21848882245705));
#55458=CARTESIAN_POINT('Ctrl Pts',(19.0941094745444,-0.625848133510457,
4.03525101959215));
#55459=CARTESIAN_POINT('Ctrl Pts',(19.1100147532321,-0.598150057044591,
3.81252992272818));
#55460=CARTESIAN_POINT('Ctrl Pts',(19.1259200319197,-0.483142842019737,
3.65258963701249));
#55461=CARTESIAN_POINT('Ctrl Pts',(19.1418253106073,-0.36813562699489,3.49264935129682));
#55462=CARTESIAN_POINT('Ctrl Pts',(19.1577305892949,-0.165819273411065,
3.39548987672941));
#55463=CARTESIAN_POINT('Ctrl Pts',(19.1736358679825,0.0309111084379188,
3.40572273351557));
#55464=CARTESIAN_POINT('Ctrl Pts',(19.1895411466701,0.227641490286902,3.41595559030173));
#55465=CARTESIAN_POINT('Ctrl Pts',(19.2054464253577,0.418785900401045,3.53358077844144));
#55466=CARTESIAN_POINT('Ctrl Pts',(19.2213517040453,0.516578912360374,3.70458978792342));
#55467=CARTESIAN_POINT('Ctrl Pts',(19.237256982733,0.614371924319703,3.87559879740541));
#55468=CARTESIAN_POINT('Ctrl Pts',(19.2531622614206,0.618813538124218,4.09999162822965));
#55469=CARTESIAN_POINT('Ctrl Pts',(19.2690675401082,0.527864352527146,4.27473658562515));
#55470=CARTESIAN_POINT('Ctrl Pts',(19.2849728187958,0.436915166930073,4.44948154302064));
#55471=CARTESIAN_POINT('Ctrl Pts',(19.3008780974834,0.250575181931413,4.5745786269874));
#55472=CARTESIAN_POINT('Ctrl Pts',(19.316783376171,0.0544038354309166,4.59258854924263));
#55473=CARTESIAN_POINT('Ctrl Pts',(19.3182404470282,0.0364327229714708,
4.59423842494573));
#55474=CARTESIAN_POINT('Ctrl Pts',(19.3196975178853,0.0183791031991185,
4.59498959766064));
#55475=CARTESIAN_POINT('Ctrl Pts',(19.3211545887425,0.000315695961457875,
4.59487351203822));
#55476=CARTESIAN_POINT('Origin',(4.,0.,4.));
#55477=CARTESIAN_POINT('',(19.7288454112575,-0.000401422265437046,4.59340756962635));
#55478=CARTESIAN_POINT('',(19.6211545887425,0.000364945106097663,4.59334757974602));
#55479=CARTESIAN_POINT('',(4.,-7.27562663373442E-17,4.5941));
#55480=CARTESIAN_POINT('Ctrl Pts',(19.7288454112575,-0.000401422265437046,
4.59340756962635));
#55481=CARTESIAN_POINT('Ctrl Pts',(19.7187204928102,0.125914276337785,4.59262579220321));
#55482=CARTESIAN_POINT('Ctrl Pts',(19.7085955743629,0.252675872983383,4.55317429478549));
#55483=CARTESIAN_POINT('Ctrl Pts',(19.6984706559155,0.353547469597214,4.47867015725961));
#55484=CARTESIAN_POINT('Ctrl Pts',(19.6825653772279,0.512007102052776,4.36163128164859));
#55485=CARTESIAN_POINT('Ctrl Pts',(19.6666600985403,0.606576931433326,4.15809158444534));
#55486=CARTESIAN_POINT('Ctrl Pts',(19.6507548198527,0.593834428727047,3.9615078130365));
#55487=CARTESIAN_POINT('Ctrl Pts',(19.6348495411651,0.581091926020768,3.76492404162769));
#55488=CARTESIAN_POINT('Ctrl Pts',(19.6189442624775,0.46103709122769,3.57529619601327));
#55489=CARTESIAN_POINT('Ctrl Pts',(19.6030389837899,0.288794059426421,3.47969339775167));
#55490=CARTESIAN_POINT('Ctrl Pts',(19.5871337051022,0.116551027625133,3.38409059949006));
#55491=CARTESIAN_POINT('Ctrl Pts',(19.5712284264146,-0.107880201184358,
3.38251284858128));
#55492=CARTESIAN_POINT('Ctrl Pts',(19.555323147727,-0.281450319664219,3.47568456171554));
#55493=CARTESIAN_POINT('Ctrl Pts',(19.5394178690394,-0.45502043814407,3.5688562748498));
#55494=CARTESIAN_POINT('Ctrl Pts',(19.5235125903518,-0.577729446294298,
3.75677745202708));
#55495=CARTESIAN_POINT('Ctrl Pts',(19.5076073116642,-0.593234549413986,
3.95316264945144));
#55496=CARTESIAN_POINT('Ctrl Pts',(19.4917020329766,-0.608739652533674,
4.1495478468758));
#55497=CARTESIAN_POINT('Ctrl Pts',(19.475796754289,-0.517040850622822,4.35439706454724));
#55498=CARTESIAN_POINT('Ctrl Pts',(19.4598914756013,-0.360242359119356,
4.47365220261941));
#55499=CARTESIAN_POINT('Ctrl Pts',(19.4495427874867,-0.258222223711561,
4.55124494740629));
#55500=CARTESIAN_POINT('Ctrl Pts',(19.4391940993721,-0.128642866595325,
4.59260240088276));
#55501=CARTESIAN_POINT('Ctrl Pts',(19.4288454112575,0.000431836873498515,
4.59346738712276));
#55502=CARTESIAN_POINT('Ctrl Pts',(19.3211545887425,0.000315695961457875,
4.59487351203822));
#55503=CARTESIAN_POINT('Ctrl Pts',(19.3356027965729,-0.178799726336078,
4.59372241551416));
#55504=CARTESIAN_POINT('Ctrl Pts',(19.3500510044034,-0.35887750705714,4.50729762043595));
#55505=CARTESIAN_POINT('Ctrl Pts',(19.3644992122339,-0.469016560662847,
4.36625733020606));
#55506=CARTESIAN_POINT('Ctrl Pts',(19.3804044909215,-0.590262902253753,
4.21099342837053));
#55507=CARTESIAN_POINT('Ctrl Pts',(19.3963097696091,-0.626752877433238,
3.98954286415574));
#55508=CARTESIAN_POINT('Ctrl Pts',(19.4122150482967,-0.561731832709929,
3.80358636875254));
#55509=CARTESIAN_POINT('Ctrl Pts',(19.4281203269843,-0.49671078798662,3.61762987334934));
#55510=CARTESIAN_POINT('Ctrl Pts',(19.4440256056719,-0.330178723360516,
3.46716744675772));
#55511=CARTESIAN_POINT('Ctrl Pts',(19.4599308843595,-0.138600118749324,
3.42128506802099));
#55512=CARTESIAN_POINT('Ctrl Pts',(19.4758361630471,0.0529784858618673,
3.37540268928427));
#55513=CARTESIAN_POINT('Ctrl Pts',(19.4917414417347,0.269603630458146,3.43410035840244));
#55514=CARTESIAN_POINT('Ctrl Pts',(19.5076467204224,0.411810215621333,3.57042659223364));
#55515=CARTESIAN_POINT('Ctrl Pts',(19.52355199911,0.554016800784528,3.70675282606484));
#55516=CARTESIAN_POINT('Ctrl Pts',(19.5394572777976,0.621804826514621,3.92070762460909));
#55517=CARTESIAN_POINT('Ctrl Pts',(19.5553625564852,0.584048894878601,4.11405198996909));
#55518=CARTESIAN_POINT('Ctrl Pts',(19.5712678351728,0.546292963242583,4.30739635532907));
#55519=CARTESIAN_POINT('Ctrl Pts',(19.5871731138604,0.402993074240464,4.4801302875048));
#55520=CARTESIAN_POINT('Ctrl Pts',(19.6030783925481,0.219946482677819,4.55294168410437));
#55521=CARTESIAN_POINT('Ctrl Pts',(19.6091037912795,0.150602919307179,4.5805248346624));
#55522=CARTESIAN_POINT('Ctrl Pts',(19.615129190011,0.0755552166468998,4.59376787586841));
#55523=CARTESIAN_POINT('Ctrl Pts',(19.6211545887425,0.000364945106097663,
4.59334757974602));
#55524=CARTESIAN_POINT('Origin',(4.,0.,4.));
#55525=CARTESIAN_POINT('',(20.0288454112575,-0.000266600559035268,4.5949350414008));
#55526=CARTESIAN_POINT('',(19.9211545887425,-0.000461335262921832,4.59353843444423));
#55527=CARTESIAN_POINT('',(4.,-7.27562663373442E-17,4.5941));
#55528=CARTESIAN_POINT('Ctrl Pts',(20.0288454112575,-0.000266600559035268,
4.5949350414008));
#55529=CARTESIAN_POINT('Ctrl Pts',(20.0141521649359,0.181839152323842,4.59391190659116));
#55530=CARTESIAN_POINT('Ctrl Pts',(19.9994589186142,0.364814066967773,4.50413264800542));
#55531=CARTESIAN_POINT('Ctrl Pts',(19.9847656722925,0.474598868642052,4.35899217880197));
#55532=CARTESIAN_POINT('Ctrl Pts',(19.9688603936049,0.593439717564554,4.20187920587587));
#55533=CARTESIAN_POINT('Ctrl Pts',(19.9529551149173,0.626517665065843,3.97989492921597));
#55534=CARTESIAN_POINT('Ctrl Pts',(19.9370498362297,0.558641803885684,3.79496194153783));
#55535=CARTESIAN_POINT('Ctrl Pts',(19.9211445575421,0.490765942705524,3.61002895385969));
#55536=CARTESIAN_POINT('Ctrl Pts',(19.9052392788545,0.321936272843916,3.46214725516331));
#55537=CARTESIAN_POINT('Ctrl Pts',(19.8893340001669,0.129673778938228,3.41921955761011));
#55538=CARTESIAN_POINT('Ctrl Pts',(19.8734287214793,-0.0625887149674591,
3.37629186005692));
#55539=CARTESIAN_POINT('Ctrl Pts',(19.8575234427916,-0.278284032917226,
3.43831816364691));
#55540=CARTESIAN_POINT('Ctrl Pts',(19.841618164104,-0.418374827314372,3.57681771754473));
#55541=CARTESIAN_POINT('Ctrl Pts',(19.8257128854164,-0.558465621711518,
3.71531727144255));
#55542=CARTESIAN_POINT('Ctrl Pts',(19.8098076067288,-0.622951892556044,
3.9302900756482));
#55543=CARTESIAN_POINT('Ctrl Pts',(19.7939023280412,-0.58222383973146,4.12303018792675));
#55544=CARTESIAN_POINT('Ctrl Pts',(19.7779970493536,-0.541495786906873,
4.3157703002053));
#55545=CARTESIAN_POINT('Ctrl Pts',(19.762091770666,-0.395553410413165,4.48627772055676));
#55546=CARTESIAN_POINT('Ctrl Pts',(19.7461864919784,-0.211407504401025,
4.55626240372308));
#55547=CARTESIAN_POINT('Ctrl Pts',(19.7404061317381,-0.144484459893097,
4.58169651826758));
#55548=CARTESIAN_POINT('Ctrl Pts',(19.7346257714978,-0.0725156072563085,
4.59385388977766));
#55549=CARTESIAN_POINT('Ctrl Pts',(19.7288454112575,-0.000401422265437046,
4.59340756962635));
#55550=CARTESIAN_POINT('Ctrl Pts',(19.6211545887425,0.000364945106097663,
4.59334757974602));
#55551=CARTESIAN_POINT('Ctrl Pts',(19.6310344686986,-0.122924963130536,
4.59265841784648));
#55552=CARTESIAN_POINT('Ctrl Pts',(19.6409143486547,-0.246598186964828,
4.55523353708024));
#55553=CARTESIAN_POINT('Ctrl Pts',(19.6507942286109,-0.346136160298313,
4.48405653351353));
#55554=CARTESIAN_POINT('Ctrl Pts',(19.6666995072985,-0.506378917588675,
4.36947112529969));
#55555=CARTESIAN_POINT('Ctrl Pts',(19.6826047859861,-0.60407113804621,4.16741144784858));
#55556=CARTESIAN_POINT('Ctrl Pts',(19.6985100646737,-0.5943566574826,3.97065479758251));
#55557=CARTESIAN_POINT('Ctrl Pts',(19.7144153433613,-0.584642176918989,
3.77389814731645));
#55558=CARTESIAN_POINT('Ctrl Pts',(19.7303206220489,-0.467520995334232,
3.58244452423543));
#55559=CARTESIAN_POINT('Ctrl Pts',(19.7462259007365,-0.296770260159971,
3.48420125495101));
#55560=CARTESIAN_POINT('Ctrl Pts',(19.7621311794242,-0.12601952498572,3.38595798566659));
#55561=CARTESIAN_POINT('Ctrl Pts',(19.7780364581118,0.098360763778029,3.38092507017875));
#55562=CARTESIAN_POINT('Ctrl Pts',(19.7939417367994,0.27334477570878,3.47141355644931));
#55563=CARTESIAN_POINT('Ctrl Pts',(19.809847015487,0.448328787639532,3.56190204271987));
#55564=CARTESIAN_POINT('Ctrl Pts',(19.8257522941746,0.573916522737285,3.74791193074883));
#55565=CARTESIAN_POINT('Ctrl Pts',(19.8416575728622,0.592443207149574,3.9440350735258));
#55566=CARTESIAN_POINT('Ctrl Pts',(19.8575628515498,0.610969891561863,4.14015821630277));
#55567=CARTESIAN_POINT('Ctrl Pts',(19.8734681302375,0.522435525288687,4.34639461382776));
#55568=CARTESIAN_POINT('Ctrl Pts',(19.8893734089251,0.367491719635661,4.46804975837363));
#55569=CARTESIAN_POINT('Ctrl Pts',(19.8999671355309,0.264291244586565,4.54907828775811));
#55570=CARTESIAN_POINT('Ctrl Pts',(19.9105608621367,0.131629953687138,4.59258455010229));
#55571=CARTESIAN_POINT('Ctrl Pts',(19.9211545887425,-0.000461335262921832,
4.59353843444423));
#55572=CARTESIAN_POINT('Origin',(4.,0.,4.));
#55573=CARTESIAN_POINT('',(20.3288454112575,0.000547175593784699,4.59423670486774));
#55574=CARTESIAN_POINT('',(20.2211545887425,-0.000159442692484791,4.59503650419094));
#55575=CARTESIAN_POINT('',(4.,-7.27562663373442E-17,4.5941));
#55576=CARTESIAN_POINT('Ctrl Pts',(20.3288454112575,0.000547175593784699,
4.59423670486774));
#55577=CARTESIAN_POINT('Ctrl Pts',(20.3254891157492,0.0422991098545892,
4.59465405164581));
#55578=CARTESIAN_POINT('Ctrl Pts',(20.3221328202408,0.0839734681026259,
4.59066114403672));
#55579=CARTESIAN_POINT('Ctrl Pts',(20.3187765247324,0.124636177719752,4.58197547152207));
#55580=CARTESIAN_POINT('Ctrl Pts',(20.3028712460448,0.317334266145104,4.54081460186972));
#55581=CARTESIAN_POINT('Ctrl Pts',(20.2869659673572,0.48731321493246,4.39426577643889));
#55582=CARTESIAN_POINT('Ctrl Pts',(20.2710606886696,0.556778600406793,4.20989870881916));
#55583=CARTESIAN_POINT('Ctrl Pts',(20.255155409982,0.626243985881127,4.02553164119943));
#55584=CARTESIAN_POINT('Ctrl Pts',(20.2392501312944,0.595195808042437,3.80334633139079));
#55585=CARTESIAN_POINT('Ctrl Pts',(20.2233448526068,0.477757630702126,3.64521515909767));
#55586=CARTESIAN_POINT('Ctrl Pts',(20.2074395739191,0.360319453361808,3.48708398680455));
#55587=CARTESIAN_POINT('Ctrl Pts',(20.1915342952315,0.156491276519859,3.39300695202695));
#55588=CARTESIAN_POINT('Ctrl Pts',(20.1756290165439,-0.04006765138094,3.40625706061923));
#55589=CARTESIAN_POINT('Ctrl Pts',(20.1597237378563,-0.236626579281727,
3.4195071692115));
#55590=CARTESIAN_POINT('Ctrl Pts',(20.1438184591687,-0.425916258241364,
3.54008442117362));
#55591=CARTESIAN_POINT('Ctrl Pts',(20.1279131804811,-0.521059912873915,
3.71258420787224));
#55592=CARTESIAN_POINT('Ctrl Pts',(20.1120079017935,-0.616203567506467,
3.88508399457085));
#55593=CARTESIAN_POINT('Ctrl Pts',(20.0961026231058,-0.617201197811932,
4.10950631600596));
#55594=CARTESIAN_POINT('Ctrl Pts',(20.0801973444182,-0.523575121773085,
4.28282745216878));
#55595=CARTESIAN_POINT('Ctrl Pts',(20.0642920657306,-0.429949045734243,
4.45614858833159));
#55596=CARTESIAN_POINT('Ctrl Pts',(20.048386787043,-0.241699263351099,4.57836853922213));
#55597=CARTESIAN_POINT('Ctrl Pts',(20.0324815083554,-0.0452724969876719,
4.59335768007126));
#55598=CARTESIAN_POINT('Ctrl Pts',(20.0312694759895,-0.030304158296608,
4.59449989984645));
#55599=CARTESIAN_POINT('Ctrl Pts',(20.0300574436235,-0.0152883365109376,
4.5950194388496));
#55600=CARTESIAN_POINT('Ctrl Pts',(20.0288454112575,-0.000266600559035268,
4.5949350414008));
#55601=CARTESIAN_POINT('Ctrl Pts',(19.9211545887425,-0.000461335262921832,
4.59353843444423));
#55602=CARTESIAN_POINT('Ctrl Pts',(19.9264661408243,-0.0666901315043342,
4.5940166992278));
#55603=CARTESIAN_POINT('Ctrl Pts',(19.9317776929061,-0.132775635823809,
4.58379778651276));
#55604=CARTESIAN_POINT('Ctrl Pts',(19.9370892449879,-0.194932679790098,
4.56224768701753));
#55605=CARTESIAN_POINT('Ctrl Pts',(19.9529945236755,-0.381060028529917,
4.49771657954882));
#55606=CARTESIAN_POINT('Ctrl Pts',(19.9688998023631,-0.531961480976676,
4.33158047304464));
#55607=CARTESIAN_POINT('Ctrl Pts',(19.9848050810507,-0.578348134104426,
4.14012389605102));
#55608=CARTESIAN_POINT('Ctrl Pts',(20.0007103597384,-0.624734787232175,
3.94866731905739));
#55609=CARTESIAN_POINT('Ctrl Pts',(20.016615638426,-0.566606641040915,3.73189027157431));
#55610=CARTESIAN_POINT('Ctrl Pts',(20.0325209171136,-0.430656211588969,
3.58932409618151));
#55611=CARTESIAN_POINT('Ctrl Pts',(20.0484261958012,-0.294705782137024,
3.44675792078871));
#55612=CARTESIAN_POINT('Ctrl Pts',(20.0643314744888,-0.080933069424392,
3.37840261748619));
#55613=CARTESIAN_POINT('Ctrl Pts',(20.0802367531764,0.112511319004002,3.41565067076361));
#55614=CARTESIAN_POINT('Ctrl Pts',(20.096142031864,0.305955707432406,3.45289872404102));
#55615=CARTESIAN_POINT('Ctrl Pts',(20.1120473105516,0.479071771576571,3.59575013389837));
#55616=CARTESIAN_POINT('Ctrl Pts',(20.1279525892393,0.552362916535151,3.77860107435498));
#55617=CARTESIAN_POINT('Ctrl Pts',(20.1438578679269,0.625654061493722,3.96145201481158));
#55618=CARTESIAN_POINT('Ctrl Pts',(20.1597631466145,0.599120287266732,4.18430248586742));
#55619=CARTESIAN_POINT('Ctrl Pts',(20.1756684253021,0.484961816589866,4.3448525870839));
#55620=CARTESIAN_POINT('Ctrl Pts',(20.1908304797822,0.376137759761604,4.49790047950022));
#55621=CARTESIAN_POINT('Ctrl Pts',(20.2059925342623,0.187686755696174,4.59433432972249));
#55622=CARTESIAN_POINT('Ctrl Pts',(20.2211545887425,-0.000159442692484791,
4.59503650419094));
#55623=CARTESIAN_POINT('Origin',(4.,0.,4.));
#55624=CARTESIAN_POINT('',(20.6288454112575,1.84392275237588E-6,4.59415158619139));
#55625=CARTESIAN_POINT('',(20.5211545887425,0.00014515264107467,4.59408556636595));
#55626=CARTESIAN_POINT('',(4.,-7.27562663373442E-17,4.5941));
#55627=CARTESIAN_POINT('Ctrl Pts',(20.6288454112575,1.84392275237588E-6,
4.59415158619139));
#55628=CARTESIAN_POINT('Ctrl Pts',(20.6209207878748,0.0985777406598016,
4.59414764832452));
#55629=CARTESIAN_POINT('Ctrl Pts',(20.6129961644921,0.197149291092008,4.56908802213256));
#55630=CARTESIAN_POINT('Ctrl Pts',(20.6050715411094,0.283761277174982,4.52200793915563));
#55631=CARTESIAN_POINT('Ctrl Pts',(20.5971189017656,0.370679463050262,4.47476141372331));
#55632=CARTESIAN_POINT('Ctrl Pts',(20.5891662624218,0.445553373684486,4.40533845822152));
#55633=CARTESIAN_POINT('Ctrl Pts',(20.581213623078,0.499196468040806,4.3222224876916));
#55634=CARTESIAN_POINT('Ctrl Pts',(20.5732609837342,0.552839562397126,4.23910651716169));
#55635=CARTESIAN_POINT('Ctrl Pts',(20.5653083443904,0.585251840475543,4.14229753160364));
#55636=CARTESIAN_POINT('Ctrl Pts',(20.5573557050466,0.592531230276538,4.04364021904617));
#55637=CARTESIAN_POINT('Ctrl Pts',(20.5494030657028,0.599810620077534,3.9449829064887));
#55638=CARTESIAN_POINT('Ctrl Pts',(20.541450426359,0.581957121601108,3.84447726693182));
#55639=CARTESIAN_POINT('Ctrl Pts',(20.5334977870152,0.541038843355354,3.75439549632807));
#55640=CARTESIAN_POINT('Ctrl Pts',(20.5255451476714,0.5001205651096,3.66431372572433));
#55641=CARTESIAN_POINT('Ctrl Pts',(20.5175925083276,0.436137507094518,3.58465582407373));
#55642=CARTESIAN_POINT('Ctrl Pts',(20.5096398689838,0.357128912623608,3.5251911792601));
#55643=CARTESIAN_POINT('Ctrl Pts',(20.50168722964,0.278120318152698,3.46572653444646));
#55644=CARTESIAN_POINT('Ctrl Pts',(20.4937345902962,0.184086187225959,3.42645514646979));
#55645=CARTESIAN_POINT('Ctrl Pts',(20.4857819509524,0.0861162623359374,
3.4121221101222));
#55646=CARTESIAN_POINT('Ctrl Pts',(20.4778293116085,-0.0118536625540841,
3.39778907377461));
#55647=CARTESIAN_POINT('Ctrl Pts',(20.4698766722647,-0.113759381407388,
3.4083943890561));
#55648=CARTESIAN_POINT('Ctrl Pts',(20.4619240329209,-0.206384677702653,
3.44274365129583));
#55649=CARTESIAN_POINT('Ctrl Pts',(20.4539713935771,-0.299009973997917,
3.47709291353557));
#55650=CARTESIAN_POINT('Ctrl Pts',(20.4460187542333,-0.382354847735142,
3.53518612273354));
#55651=CARTESIAN_POINT('Ctrl Pts',(20.4380661148895,-0.447563842371028,
3.60976099223211));
#55652=CARTESIAN_POINT('Ctrl Pts',(20.4301134755457,-0.512772837006921,
3.68433586173069));
#55653=CARTESIAN_POINT('Ctrl Pts',(20.4221608362019,-0.559845952541473,
3.77539239152987));
#55654=CARTESIAN_POINT('Ctrl Pts',(20.4142081968581,-0.580888308445953,
3.87190852591559));
#55655=CARTESIAN_POINT('Ctrl Pts',(20.3983029181705,-0.622973020254908,
4.06494079468701));
#55656=CARTESIAN_POINT('Ctrl Pts',(20.3823976394829,-0.5609346935436,4.27981148180459));
#55657=CARTESIAN_POINT('Ctrl Pts',(20.3664923607953,-0.422206916156273,
4.41936036842645));
#55658=CARTESIAN_POINT('Ctrl Pts',(20.353943377616,-0.312753156865475,4.52946196836027));
#55659=CARTESIAN_POINT('Ctrl Pts',(20.3413943944368,-0.155560747392339,
4.59267627084609));
#55660=CARTESIAN_POINT('Ctrl Pts',(20.3288454112575,0.000547175593784699,
4.59423670486774));
#55661=CARTESIAN_POINT('Ctrl Pts',(20.2211545887425,-0.000159442692484791,
4.59503650419094));
#55662=CARTESIAN_POINT('Ctrl Pts',(20.22189781295,-0.00936741923094289,
4.59507092387091));
#55663=CARTESIAN_POINT('Ctrl Pts',(20.2226410371574,-0.0185739425223631,
4.59487531632137));
#55664=CARTESIAN_POINT('Ctrl Pts',(20.2233842613649,-0.0277695625699301,
4.59444507412072));
#55665=CARTESIAN_POINT('Ctrl Pts',(20.2392895400526,-0.224559303926058,
4.58523772856393));
#55666=CARTESIAN_POINT('Ctrl Pts',(20.2551948187402,-0.416355619511548,
4.46857330607325));
#55667=CARTESIAN_POINT('Ctrl Pts',(20.2711000974278,-0.51503297954037,4.29810345018796));
#55668=CARTESIAN_POINT('Ctrl Pts',(20.2870053761154,-0.613710339569191,
4.12763359430267));
#55669=CARTESIAN_POINT('Ctrl Pts',(20.302910654803,-0.619268744041345,3.90335830502277));
#55670=CARTESIAN_POINT('Ctrl Pts',(20.3188159334906,-0.529271009537506,
3.72809546473432));
#55671=CARTESIAN_POINT('Ctrl Pts',(20.3347212121782,-0.439273275033663,
3.55283262444587));
#55672=CARTESIAN_POINT('Ctrl Pts',(20.3506264908658,-0.253719401553817,
3.42658223314887));
#55673=CARTESIAN_POINT('Ctrl Pts',(20.3665317695535,-0.0575887485100287,
3.40762076142476));
#55674=CARTESIAN_POINT('Ctrl Pts',(20.3824370482411,0.138541904533748,3.38865928970065));
#55675=CARTESIAN_POINT('Ctrl Pts',(20.3983423269287,0.345249337141466,3.47698673754941));
#55676=CARTESIAN_POINT('Ctrl Pts',(20.4142476056163,0.467192899405167,3.63141813202173));
#55677=CARTESIAN_POINT('Ctrl Pts',(20.4301528843039,0.589136461668875,3.78584952649406));
#55678=CARTESIAN_POINT('Ctrl Pts',(20.4460581629915,0.626316153588557,4.00638486758996));
#55679=CARTESIAN_POINT('Ctrl Pts',(20.4619634416791,0.562534942182983,4.19337293359078));
#55680=CARTESIAN_POINT('Ctrl Pts',(20.4699160810229,0.530644336480201,4.28686696659118));
#55681=CARTESIAN_POINT('Ctrl Pts',(20.4778687203667,0.473513504946115,4.3719741808178));
#55682=CARTESIAN_POINT('Ctrl Pts',(20.4858213597105,0.400240502138227,4.43864269813793));
#55683=CARTESIAN_POINT('Ctrl Pts',(20.4937739990544,0.326967499330329,4.50531121545807));
#55684=CARTESIAN_POINT('Ctrl Pts',(20.5017266383982,0.237552325248626,4.55354103587171));
#55685=CARTESIAN_POINT('Ctrl Pts',(20.509679277742,0.141619450488441,4.57712494713439));
#55686=CARTESIAN_POINT('Ctrl Pts',(20.5135043814088,0.0954771353210092,
4.58846846487098));
#55687=CARTESIAN_POINT('Ctrl Pts',(20.5173294850756,0.0478269697500401,
4.59411022582368));
#55688=CARTESIAN_POINT('Ctrl Pts',(20.5211545887425,0.00014515264107467,
4.59408556636595));
#55689=CARTESIAN_POINT('Origin',(4.,0.,4.));
#55690=CARTESIAN_POINT('',(20.9288454112575,-6.4040329070536E-6,4.59405282094147));
#55691=CARTESIAN_POINT('',(20.8211545887425,5.65245430726296E-6,4.59414685459231));
#55692=CARTESIAN_POINT('',(4.,-7.27562663373442E-17,4.5941));
#55693=CARTESIAN_POINT('Ctrl Pts',(20.9288454112575,-6.4040329070536E-6,
4.59405282094147));
#55694=CARTESIAN_POINT('Ctrl Pts',(20.9243050993443,0.0564994875152707,
4.59403151438501));
#55695=CARTESIAN_POINT('Ctrl Pts',(20.9197647874311,0.113011285737041,4.58603249222448));
#55696=CARTESIAN_POINT('Ctrl Pts',(20.9152244755179,0.167207550221224,4.57013805289591));
#55697=CARTESIAN_POINT('Ctrl Pts',(20.9072718361741,0.262135685878584,4.5422979516059));
#55698=CARTESIAN_POINT('Ctrl Pts',(20.8993191968303,0.349959832061366,4.49023494241839));
#55699=CARTESIAN_POINT('Ctrl Pts',(20.8913665574865,0.419942299057043,4.42031443844746));
#55700=CARTESIAN_POINT('Ctrl Pts',(20.8834139181427,0.489924766052721,4.35039393447653));
#55701=CARTESIAN_POINT('Ctrl Pts',(20.8754612787989,0.542065553861293,4.26261593572219));
#55702=CARTESIAN_POINT('Ctrl Pts',(20.8675086394551,0.569989725359365,4.16771249585991));
#55703=CARTESIAN_POINT('Ctrl Pts',(20.8595560001113,0.597913896857441,4.07280905599763));
#55704=CARTESIAN_POINT('Ctrl Pts',(20.8516033607674,0.601621452045013,3.97078017502742));
#55705=CARTESIAN_POINT('Ctrl Pts',(20.8436507214236,0.580659121393648,3.87410027737825));
#55706=CARTESIAN_POINT('Ctrl Pts',(20.8356980820798,0.559696790742287,3.77742037972911));
#55707=CARTESIAN_POINT('Ctrl Pts',(20.827745442736,0.514064574252002,3.686089465401));
#55708=CARTESIAN_POINT('Ctrl Pts',(20.8197928033922,0.44934157601673,3.61127397478397));
#55709=CARTESIAN_POINT('Ctrl Pts',(20.8118401640484,0.384618577781443,3.53645848416692));
#55710=CARTESIAN_POINT('Ctrl Pts',(20.8038875247046,0.300804797801161,3.47815841726095));
#55711=CARTESIAN_POINT('Ctrl Pts',(20.7959348853608,0.208147717693743,3.44350176598286));
#55712=CARTESIAN_POINT('Ctrl Pts',(20.787982246017,0.115490637586335,3.40884511470477));
#55713=CARTESIAN_POINT('Ctrl Pts',(20.7800296066732,0.0139902573517945,
3.39783187905454));
#55714=CARTESIAN_POINT('Ctrl Pts',(20.7720769673294,-0.0839438183138644,
3.41180854931868));
#55715=CARTESIAN_POINT('Ctrl Pts',(20.7641243279856,-0.181877893979523,
3.42578521958283));
#55716=CARTESIAN_POINT('Ctrl Pts',(20.7561716886418,-0.2762456650763,3.46475179576135));
#55717=CARTESIAN_POINT('Ctrl Pts',(20.748219049298,-0.355509010203556,3.52394413563581));
#55718=CARTESIAN_POINT('Ctrl Pts',(20.7402664099542,-0.434772355330821,
3.58313647551028));
#55719=CARTESIAN_POINT('Ctrl Pts',(20.7323137706103,-0.498931274488562,
3.66255457908069));
#55720=CARTESIAN_POINT('Ctrl Pts',(20.7243611312665,-0.54014217617541,3.75248840252759));
#55721=CARTESIAN_POINT('Ctrl Pts',(20.7164084919227,-0.581353077862249,
3.84242222597448));
#55722=CARTESIAN_POINT('Ctrl Pts',(20.7084558525789,-0.599615962078206,
3.94287176929784));
#55723=CARTESIAN_POINT('Ctrl Pts',(20.7005032132351,-0.592696601504336,
4.0415558946729));
#55724=CARTESIAN_POINT('Ctrl Pts',(20.6925505738913,-0.585777240930466,
4.14024002004797));
#55725=CARTESIAN_POINT('Ctrl Pts',(20.6845979345475,-0.553675635566762,
4.23715872747472));
#55726=CARTESIAN_POINT('Ctrl Pts',(20.6766452952037,-0.50031917594212,4.32046203197985));
#55727=CARTESIAN_POINT('Ctrl Pts',(20.6686926558599,-0.446962716317479,
4.40376533648498));
#55728=CARTESIAN_POINT('Ctrl Pts',(20.6607400165161,-0.3723514024319,4.47345323806848));
#55729=CARTESIAN_POINT('Ctrl Pts',(20.6527873771723,-0.285602702553558,
4.52100610813718));
#55730=CARTESIAN_POINT('Ctrl Pts',(20.6448347378285,-0.198854002675205,
4.56855897820588));
#55731=CARTESIAN_POINT('Ctrl Pts',(20.6368820984847,-0.099967916804087,
4.59397681675976));
#55732=CARTESIAN_POINT('Ctrl Pts',(20.6289294591409,-0.00104364331035449,
4.59415068835528));
#55733=CARTESIAN_POINT('Ctrl Pts',(20.6289014431798,-0.000695147863829354,
4.59415130087895));
#55734=CARTESIAN_POINT('Ctrl Pts',(20.6288734272186,-0.000346651943377611,
4.59415160011295));
#55735=CARTESIAN_POINT('Ctrl Pts',(20.6288454112575,1.84392275237588E-6,
4.59415158619139));
#55736=CARTESIAN_POINT('Ctrl Pts',(20.5211545887425,0.00014515264107467,
4.59408556636595));
#55737=CARTESIAN_POINT('Ctrl Pts',(20.5252821244194,-0.0513066296901884,
4.59405895720698));
#55738=CARTESIAN_POINT('Ctrl Pts',(20.5294096600964,-0.102795266482965,
4.58743447362686));
#55739=CARTESIAN_POINT('Ctrl Pts',(20.5335371957734,-0.152465997634008,
4.57425651377355));
#55740=CARTESIAN_POINT('Ctrl Pts',(20.5414898351172,-0.248167995557571,
4.5488661670383));
#55741=CARTESIAN_POINT('Ctrl Pts',(20.549442474461,-0.33712141596603,4.49914747145609));
#55742=CARTESIAN_POINT('Ctrl Pts',(20.5573951138048,-0.408848640915227,
4.43107686705031));
#55743=CARTESIAN_POINT('Ctrl Pts',(20.5653477531486,-0.480575865864423,
4.36300626264453));
#55744=CARTESIAN_POINT('Ctrl Pts',(20.5733003924924,-0.535076895354358,
4.27658374941519));
#55745=CARTESIAN_POINT('Ctrl Pts',(20.5812530318362,-0.565476628275392,
4.18243021985824));
#55746=CARTESIAN_POINT('Ctrl Pts',(20.58920567118,-0.595876361196427,4.08827669030129));
#55747=CARTESIAN_POINT('Ctrl Pts',(20.5971583105238,-0.602174797548561,
3.98639214441672));
#55748=CARTESIAN_POINT('Ctrl Pts',(20.6051109498677,-0.58371402745925,3.88920441471463));
#55749=CARTESIAN_POINT('Ctrl Pts',(20.6130635892115,-0.565253257369939,
3.79201668501254));
#55750=CARTESIAN_POINT('Ctrl Pts',(20.6210162285553,-0.522033280839182,
3.69952577149293));
#55751=CARTESIAN_POINT('Ctrl Pts',(20.6289688678991,-0.459278917219465,
3.62305528060961));
#55752=CARTESIAN_POINT('Ctrl Pts',(20.6369215072429,-0.396524553599749,
3.54658478972629));
#55753=CARTESIAN_POINT('Ctrl Pts',(20.6448741465867,-0.314235802891072,
3.48613472147926));
#55754=CARTESIAN_POINT('Ctrl Pts',(20.6528267859305,-0.222505051509483,
3.44908779917463));
#55755=CARTESIAN_POINT('Ctrl Pts',(20.6607794252743,-0.130774300127894,
3.41204087687));
#55756=CARTESIAN_POINT('Ctrl Pts',(20.6687320646181,-0.029601548073392,
3.39839710050778));
#55757=CARTESIAN_POINT('Ctrl Pts',(20.6766847039619,0.0686601223983595,
3.40982890848785));
#55758=CARTESIAN_POINT('Ctrl Pts',(20.6846373433057,0.1669217928701,3.42126071646792));
#55759=CARTESIAN_POINT('Ctrl Pts',(20.6925899826495,0.262272381759091,3.45776810879028));
#55760=CARTESIAN_POINT('Ctrl Pts',(20.7005426219933,0.343045155251024,3.51488528173127));
#55761=CARTESIAN_POINT('Ctrl Pts',(20.7084952613371,0.423817928742975,3.57200245467228));
#55762=CARTESIAN_POINT('Ctrl Pts',(20.7164479006809,0.490012886837861,3.64972940823193));
#55763=CARTESIAN_POINT('Ctrl Pts',(20.7244005400247,0.533541468465666,3.73856417004634));
#55764=CARTESIAN_POINT('Ctrl Pts',(20.7323531793686,0.577070050093471,3.82739893186076));
#55765=CARTESIAN_POINT('Ctrl Pts',(20.7403058187123,0.597932255254196,3.92734150192994));
#55766=CARTESIAN_POINT('Ctrl Pts',(20.7482584580562,0.593574919799613,4.02617190099588));
#55767=CARTESIAN_POINT('Ctrl Pts',(20.7562110974,0.589217584345031,4.1250023000618));
#55768=CARTESIAN_POINT('Ctrl Pts',(20.7641637367438,0.559640708275147,4.22272052812447));
#55769=CARTESIAN_POINT('Ctrl Pts',(20.7721163760876,0.508461778515953,4.30737953925928));
#55770=CARTESIAN_POINT('Ctrl Pts',(20.7800690154314,0.457282848756759,4.39203855039408));
#55771=CARTESIAN_POINT('Ctrl Pts',(20.7880216547752,0.384501865308254,4.46363834460102));
#55772=CARTESIAN_POINT('Ctrl Pts',(20.795974294119,0.299016600344635,4.51342469267633));
#55773=CARTESIAN_POINT('Ctrl Pts',(20.8039269334628,0.213531335381016,4.56321104075164));
#55774=CARTESIAN_POINT('Ctrl Pts',(20.8118795728066,0.115341788902283,4.59118394269532));
#55775=CARTESIAN_POINT('Ctrl Pts',(20.8198322121504,0.0164533379892873,
4.59392342516246));
#55776=CARTESIAN_POINT('Ctrl Pts',(20.8202730043478,0.0109722321971217,
4.59407526688998));
#55777=CARTESIAN_POINT('Ctrl Pts',(20.8207137965451,0.00548897925183007,
4.59414958726715));
#55778=CARTESIAN_POINT('Ctrl Pts',(20.8211545887425,5.65245430726296E-6,
4.59414685459231));
#55779=CARTESIAN_POINT('Origin',(4.,0.,4.));
#55780=CARTESIAN_POINT('',(21.2288454112575,1.28243205298473E-5,4.59412621697841));
#55781=CARTESIAN_POINT('',(21.1211545887425,-1.09306879613159E-5,4.5940621922514));
#55782=CARTESIAN_POINT('',(4.,-7.27562663373442E-17,4.5941));
#55783=CARTESIAN_POINT('Ctrl Pts',(21.2288454112575,1.28243205298473E-5,
4.59412621697841));
#55784=CARTESIAN_POINT('Ctrl Pts',(21.2276894108138,0.0143945780386088,
4.59413985249388));
#55785=CARTESIAN_POINT('Ctrl Pts',(21.2265334103701,0.028775363636007,4.59362827285675));
#55786=CARTESIAN_POINT('Ctrl Pts',(21.2253774099263,0.043117441953227,4.59258471957415));
#55787=CARTESIAN_POINT('Ctrl Pts',(21.2174247705826,0.141782954511012,4.58540565408365));
#55788=CARTESIAN_POINT('Ctrl Pts',(21.2094721312387,0.238616577754522,4.55305001116024));
#55789=CARTESIAN_POINT('Ctrl Pts',(21.2015194918949,0.321779082392626,4.49947370882601));
#55790=CARTESIAN_POINT('Ctrl Pts',(21.1935668525511,0.404941587030731,4.44589740649178));
#55791=CARTESIAN_POINT('Ctrl Pts',(21.1856142132073,0.474432973063433,4.37110044474674));
#55792=CARTESIAN_POINT('Ctrl Pts',(21.1776615738635,0.521756972098598,4.28422777087894));
#55793=CARTESIAN_POINT('Ctrl Pts',(21.1697089345197,0.569080971133768,4.19735509701114));
#55794=CARTESIAN_POINT('Ctrl Pts',(21.1617562951759,0.594237583171398,4.09840671102057));
#55795=CARTESIAN_POINT('Ctrl Pts',(21.1538036558321,0.594151069756079,3.9994804007435));
#55796=CARTESIAN_POINT('Ctrl Pts',(21.1458510164883,0.59406455634076,3.90055409046644));
#55797=CARTESIAN_POINT('Ctrl Pts',(21.1378983771445,0.568734917472505,3.80164985590287));
#55798=CARTESIAN_POINT('Ctrl Pts',(21.1299457378007,0.521259046500119,3.71486008677882));
#55799=CARTESIAN_POINT('Ctrl Pts',(21.1219930984569,0.473783175527722,3.62807031765475));
#55800=CARTESIAN_POINT('Ctrl Pts',(21.114040459113,0.40416107245118,3.5533950139702));
#55801=CARTESIAN_POINT('Ctrl Pts',(21.1060878197692,0.320904987578411,3.49996424865404));
#55802=CARTESIAN_POINT('Ctrl Pts',(21.0981351804254,0.237648902705652,3.44653348333788));
#55803=CARTESIAN_POINT('Ctrl Pts',(21.0901825410817,0.140758836036697,3.41434725639011));
#55804=CARTESIAN_POINT('Ctrl Pts',(21.0822299017378,0.042080917889342,3.40734077242984));
#55805=CARTESIAN_POINT('Ctrl Pts',(21.074277262394,-0.056597000258024,3.40033428846957));
#55806=CARTESIAN_POINT('Ctrl Pts',(21.0663246230502,-0.157062769883762,
3.41850754749682));
#55807=CARTESIAN_POINT('Ctrl Pts',(21.0583719837064,-0.247033082431791,
3.45963862106718));
#55808=CARTESIAN_POINT('Ctrl Pts',(21.0504193443626,-0.337003394979799,
3.50076969463752));
#55809=CARTESIAN_POINT('Ctrl Pts',(21.0424667050188,-0.416478250450111,
3.56485858275095));
#55810=CARTESIAN_POINT('Ctrl Pts',(21.034514065675,-0.475740765152555,3.644069545988));
#55811=CARTESIAN_POINT('Ctrl Pts',(21.0265614263312,-0.535003279855012,
3.72328050922507));
#55812=CARTESIAN_POINT('Ctrl Pts',(21.0186087869874,-0.574053453789596,
3.81761354758578));
#55813=CARTESIAN_POINT('Ctrl Pts',(21.0106561476436,-0.588116871685884,
3.91553516229212));
#55814=CARTESIAN_POINT('Ctrl Pts',(21.0027035082998,-0.60218028958217,4.01345677699845));
#55815=CARTESIAN_POINT('Ctrl Pts',(20.994750868956,-0.591256951440166,4.11496696805043));
#55816=CARTESIAN_POINT('Ctrl Pts',(20.9867982296121,-0.556682383467722,
4.20765473214191));
#55817=CARTESIAN_POINT('Ctrl Pts',(20.9788455902683,-0.522107815495282,
4.30034249623339));
#55818=CARTESIAN_POINT('Ctrl Pts',(20.9708929509246,-0.463882017692404,
4.38420783336438));
#55819=CARTESIAN_POINT('Ctrl Pts',(20.9629403115808,-0.389123888092725,
4.4489970636758));
#55820=CARTESIAN_POINT('Ctrl Pts',(20.9549876722369,-0.314365758493028,
4.51378629398723));
#55821=CARTESIAN_POINT('Ctrl Pts',(20.9470350328931,-0.223075297096518,
4.5594994174791));
#55822=CARTESIAN_POINT('Ctrl Pts',(20.9390823935493,-0.12641400383229,4.58054738252877));
#55823=CARTESIAN_POINT('Ctrl Pts',(20.9356700661187,-0.0849384674446181,
4.58957866703598));
#55824=CARTESIAN_POINT('Ctrl Pts',(20.9322577386881,-0.0424741039190781,
4.59406883414683));
#55825=CARTESIAN_POINT('Ctrl Pts',(20.9288454112575,-6.4040329070536E-6,
4.59405282094147));
#55826=CARTESIAN_POINT('Ctrl Pts',(20.8211545887425,5.65245430726296E-6,
4.59414685459231));
#55827=CARTESIAN_POINT('Ctrl Pts',(20.8286664358889,-0.0934395423672534,
4.59410028517524));
#55828=CARTESIAN_POINT('Ctrl Pts',(20.8361782830354,-0.18690618531264,4.57167601133058));
#55829=CARTESIAN_POINT('Ctrl Pts',(20.8436901301818,-0.270133012248912,
4.529191754035));
#55830=CARTESIAN_POINT('Ctrl Pts',(20.8516427695256,-0.358243556226857,
4.4842145374498));
#55831=CARTESIAN_POINT('Ctrl Pts',(20.8595954088694,-0.434877288835492,
4.41675404128879));
#55832=CARTESIAN_POINT('Ctrl Pts',(20.8675480482133,-0.490664589397756,
4.33505825661903));
#55833=CARTESIAN_POINT('Ctrl Pts',(20.8755006875571,-0.546451889960021,
4.25336247194927));
#55834=CARTESIAN_POINT('Ctrl Pts',(20.8834533269009,-0.581392758475918,
4.15743139877076));
#55835=CARTESIAN_POINT('Ctrl Pts',(20.8914059662447,-0.591215252505097,
4.05899390323763));
#55836=CARTESIAN_POINT('Ctrl Pts',(20.8993586055885,-0.601037746534278,
3.96055640770449));
#55837=CARTESIAN_POINT('Ctrl Pts',(20.9073112449323,-0.585741866076735,
3.85961248981672));
#55838=CARTESIAN_POINT('Ctrl Pts',(20.9152638842761,-0.547197711916726,
3.76850392583047));
#55839=CARTESIAN_POINT('Ctrl Pts',(20.9232165236199,-0.508653557756717,
3.67739536184422));
#55840=CARTESIAN_POINT('Ctrl Pts',(20.9311691629637,-0.446861129894262,
3.59612215175949));
#55841=CARTESIAN_POINT('Ctrl Pts',(20.9391218023075,-0.369375409551539,
3.53462104847409));
#55842=CARTESIAN_POINT('Ctrl Pts',(20.9470744416513,-0.291889689208826,
3.4731199451887));
#55843=CARTESIAN_POINT('Ctrl Pts',(20.9550270809951,-0.198710676385865,
3.43139094870266));
#55844=CARTESIAN_POINT('Ctrl Pts',(20.9629797203389,-0.101230766359376,
3.41453599926792));
#55845=CARTESIAN_POINT('Ctrl Pts',(20.9709323596827,-0.00375085633288601,
3.39768104983318));
#55846=CARTESIAN_POINT('Ctrl Pts',(20.9788849990265,0.0980299508971346,
3.40570014744973));
#55847=CARTESIAN_POINT('Ctrl Pts',(20.9868376383704,0.191667561123074,3.43761284710704));
#55848=CARTESIAN_POINT('Ctrl Pts',(20.9947902777142,0.285305171349014,3.46952554676435));
#55849=CARTESIAN_POINT('Ctrl Pts',(21.002742917058,0.37079958457088,3.52533184846243));
#55850=CARTESIAN_POINT('Ctrl Pts',(21.0106955564018,0.437697946637459,3.59820867233944));
#55851=CARTESIAN_POINT('Ctrl Pts',(21.0186481957456,0.504596308704037,3.67108549621644));
#55852=CARTESIAN_POINT('Ctrl Pts',(21.0266008350894,0.552898619615334,3.76103284227238));
#55853=CARTESIAN_POINT('Ctrl Pts',(21.0345534744332,0.576699262792956,3.8570534220826));
#55854=CARTESIAN_POINT('Ctrl Pts',(21.042506113777,0.600499905970578,3.95307400189282));
#55855=CARTESIAN_POINT('Ctrl Pts',(21.0504587531208,0.599798881414527,4.05516781545734));
#55856=CARTESIAN_POINT('Ctrl Pts',(21.0584113924646,0.574681899562831,4.15085250374278));
#55857=CARTESIAN_POINT('Ctrl Pts',(21.0663640318084,0.549564917711138,4.24653719202821));
#55858=CARTESIAN_POINT('Ctrl Pts',(21.0743166711522,0.500031978563804,4.33581275503458));
#55859=CARTESIAN_POINT('Ctrl Pts',(21.082269310496,0.432139158218639,4.40776403918836));
#55860=CARTESIAN_POINT('Ctrl Pts',(21.0902219498398,0.364246337873458,4.47971532334216));
#55861=CARTESIAN_POINT('Ctrl Pts',(21.0981745891836,0.277993636330433,4.53434232864337));
#55862=CARTESIAN_POINT('Ctrl Pts',(21.1061272285274,0.183926621270441,4.56496615973523));
#55863=CARTESIAN_POINT('Ctrl Pts',(21.1111363485991,0.124676735433976,4.5842551580617));
#55864=CARTESIAN_POINT('Ctrl Pts',(21.1161454686708,0.0623266393968894,
4.59402126159141));
#55865=CARTESIAN_POINT('Ctrl Pts',(21.1211545887425,-1.09306879613159E-5,
4.5940621922514));
#55866=CARTESIAN_POINT('Origin',(4.,0.,4.));
#55867=CARTESIAN_POINT('',(21.5288454112575,-1.51073027558624E-5,4.59408477831653));
#55868=CARTESIAN_POINT('',(21.4211545887425,1.51733402061755E-5,4.59410821609125));
#55869=CARTESIAN_POINT('',(4.,-7.27562663373442E-17,4.5941));
#55870=CARTESIAN_POINT('Ctrl Pts',(21.5288454112575,-1.51073027558624E-5,
4.59408477831653));
#55871=CARTESIAN_POINT('Ctrl Pts',(21.5231210829395,0.0712153309254728,
4.59401644885886));
#55872=CARTESIAN_POINT('Ctrl Pts',(21.5173967546214,0.142469702059594,4.58119587380047));
#55873=CARTESIAN_POINT('Ctrl Pts',(21.5116724263034,0.209120766622247,4.55613331912479));
#55874=CARTESIAN_POINT('Ctrl Pts',(21.5037197869596,0.301717111362981,4.52131465616629));
#55875=CARTESIAN_POINT('Ctrl Pts',(21.4957671476158,0.385428743083265,4.46286809139133));
#55876=CARTESIAN_POINT('Ctrl Pts',(21.4878145082719,0.450020774675764,4.38793951336988));
#55877=CARTESIAN_POINT('Ctrl Pts',(21.4798618689281,0.514612806268249,4.31301093534845));
#55878=CARTESIAN_POINT('Ctrl Pts',(21.4719092295843,0.560085237732952,4.22160034408054));
#55879=CARTESIAN_POINT('Ctrl Pts',(21.4639565902405,0.58087844500124,4.1248839293359));
#55880=CARTESIAN_POINT('Ctrl Pts',(21.4560039508967,0.601671652269532,4.02816751459124));
#55881=CARTESIAN_POINT('Ctrl Pts',(21.4480513115529,0.597785635341394,3.92614527636987));
#55882=CARTESIAN_POINT('Ctrl Pts',(21.4400986722091,0.569695512712777,3.83129082280931));
#55883=CARTESIAN_POINT('Ctrl Pts',(21.4321460328653,0.541605390084162,3.73643636924876));
#55884=CARTESIAN_POINT('Ctrl Pts',(21.4241933935215,0.489311161755075,3.64874970034904));
#55885=CARTESIAN_POINT('Ctrl Pts',(21.4162407541777,0.419206509371839,3.57895170565158));
#55886=CARTESIAN_POINT('Ctrl Pts',(21.4082881148339,0.349101856988603,3.50915371095413));
#55887=CARTESIAN_POINT('Ctrl Pts',(21.4003354754901,0.261186780551223,3.45724439045894));
#55888=CARTESIAN_POINT('Ctrl Pts',(21.3923828361463,0.16621009553345,3.42957036558731));
#55889=CARTESIAN_POINT('Ctrl Pts',(21.3844301968025,0.0712334105156764,
3.40189634071567));
#55890=CARTESIAN_POINT('Ctrl Pts',(21.3764775574587,-0.0308048830825163,
3.3984576114676));
#55891=CARTESIAN_POINT('Ctrl Pts',(21.3685249181149,-0.127429214135013,
3.41967460932821));
#55892=CARTESIAN_POINT('Ctrl Pts',(21.360572278771,-0.22405354518751,3.44089160718882));
#55893=CARTESIAN_POINT('Ctrl Pts',(21.3526196394272,-0.315263913694308,
3.4867643321581));
#55894=CARTESIAN_POINT('Ctrl Pts',(21.3446670000834,-0.389908609845283,
3.5516842188346));
#55895=CARTESIAN_POINT('Ctrl Pts',(21.3367143607396,-0.464553305996249,
3.6166041055111));
#55896=CARTESIAN_POINT('Ctrl Pts',(21.3287617213958,-0.522632329791381,
3.70057115389483));
#55897=CARTESIAN_POINT('Ctrl Pts',(21.320809082052,-0.557044729551177,3.79331924871262));
#55898=CARTESIAN_POINT('Ctrl Pts',(21.3128564427082,-0.591457129310977,
3.88606734353042));
#55899=CARTESIAN_POINT('Ctrl Pts',(21.3049038033644,-0.602202905035458,
3.9875964847823));
#55900=CARTESIAN_POINT('Ctrl Pts',(21.2969511640206,-0.587968239287942,
4.08549335215105));
#55901=CARTESIAN_POINT('Ctrl Pts',(21.2889985246768,-0.573733573540424,
4.18339021951981));
#55902=CARTESIAN_POINT('Ctrl Pts',(21.281045885333,-0.534518466320906,4.27765481300544));
#55903=CARTESIAN_POINT('Ctrl Pts',(21.2730932459892,-0.47511749858569,4.35676200219639));
#55904=CARTESIAN_POINT('Ctrl Pts',(21.2651406066454,-0.415716530850488,
4.43586919138732));
#55905=CARTESIAN_POINT('Ctrl Pts',(21.2571879673016,-0.336129702599601,
4.49981897628356));
#55906=CARTESIAN_POINT('Ctrl Pts',(21.2492353279577,-0.246087587538132,
4.54079262470289));
#55907=CARTESIAN_POINT('Ctrl Pts',(21.2424386890577,-0.169134048541188,
4.57581031891556));
#55908=CARTESIAN_POINT('Ctrl Pts',(21.2356420501576,-0.0845438791841879,
4.59404604774026));
#55909=CARTESIAN_POINT('Ctrl Pts',(21.2288454112575,1.28243205298473E-5,
4.59412621697841));
#55910=CARTESIAN_POINT('Ctrl Pts',(21.1211545887425,-1.09306879613159E-5,
4.5940621922514));
#55911=CARTESIAN_POINT('Ctrl Pts',(21.1240981080146,-0.0366424819978743,
4.5940862444172));
#55912=CARTESIAN_POINT('Ctrl Pts',(21.1270416272867,-0.0732697079540161,
4.59075208378119));
#55913=CARTESIAN_POINT('Ctrl Pts',(21.1299851465589,-0.109260984540888,
4.58401866488291));
#55914=CARTESIAN_POINT('Ctrl Pts',(21.1379377859027,-0.20650024671525,4.56582668205621));
#55915=CARTESIAN_POINT('Ctrl Pts',(21.1458904252465,-0.299097442487026,
4.52282205952027));
#55916=CARTESIAN_POINT('Ctrl Pts',(21.1538430645903,-0.375731303474415,
4.46026269810429));
#55917=CARTESIAN_POINT('Ctrl Pts',(21.1617957039341,-0.452365164461805,
4.3977033366883));
#55918=CARTESIAN_POINT('Ctrl Pts',(21.1697483432779,-0.513035690664809,
4.31558923639226));
#55919=CARTESIAN_POINT('Ctrl Pts',(21.1777009826217,-0.550325083965727,
4.22395996434209));
#55920=CARTESIAN_POINT('Ctrl Pts',(21.1856536219655,-0.587614477266646,
4.13233069229192));
#55921=CARTESIAN_POINT('Ctrl Pts',(21.1936062613093,-0.601522737665479,
4.03118624848761));
#55922=CARTESIAN_POINT('Ctrl Pts',(21.2015589006531,-0.590349390887683,
3.93289291874755));
#55923=CARTESIAN_POINT('Ctrl Pts',(21.2095115399969,-0.579176044109886,
3.83459958900749));
#55924=CARTESIAN_POINT('Ctrl Pts',(21.2174641793407,-0.542921090155459,
3.73915737333167));
#55925=CARTESIAN_POINT('Ctrl Pts',(21.2254168186845,-0.486017190935348,
3.65823538248142));
#55926=CARTESIAN_POINT('Ctrl Pts',(21.2333694580283,-0.429113291715238,
3.57731339163117));
#55927=CARTESIAN_POINT('Ctrl Pts',(21.2413220973721,-0.351560447229444,
3.51091162560648));
#55928=CARTESIAN_POINT('Ctrl Pts',(21.249274736716,-0.262840548960938,3.46714860467879));
#55929=CARTESIAN_POINT('Ctrl Pts',(21.2572273760598,-0.174120650692433,
3.4233855837511));
#55930=CARTESIAN_POINT('Ctrl Pts',(21.2651800154036,-0.0742336986412151,
3.40226130792041));
#55931=CARTESIAN_POINT('Ctrl Pts',(21.2731326547474,0.0246077668693877,
3.40635850761334));
#55932=CARTESIAN_POINT('Ctrl Pts',(21.2810852940912,0.123449232380002,3.41045570730627));
#55933=CARTESIAN_POINT('Ctrl Pts',(21.289037933435,0.221245211350001,3.43977438252282));
#55934=CARTESIAN_POINT('Ctrl Pts',(21.2969905727788,0.306038813396919,3.49072992590572));
#55935=CARTESIAN_POINT('Ctrl Pts',(21.3049432121226,0.390832415443818,3.54168546928862));
#55936=CARTESIAN_POINT('Ctrl Pts',(21.3128958514664,0.462623640567642,3.61427788083785));
#55937=CARTESIAN_POINT('Ctrl Pts',(21.3208484908102,0.512635033719562,3.69963174955258));
#55938=CARTESIAN_POINT('Ctrl Pts',(21.328801130154,0.562646426871494,3.78498561826733));
#55939=CARTESIAN_POINT('Ctrl Pts',(21.3367537694978,0.590877988051513,3.88310094414759));
#55940=CARTESIAN_POINT('Ctrl Pts',(21.3447064088416,0.59387802439953,3.98198179230066));
#55941=CARTESIAN_POINT('Ctrl Pts',(21.3526590481854,0.596878060747546,4.08086264045372));
#55942=CARTESIAN_POINT('Ctrl Pts',(21.3606116875293,0.574646572263566,4.1805090108796));
#55943=CARTESIAN_POINT('Ctrl Pts',(21.3685643268731,0.529901661201384,4.26873777763737));
#55944=CARTESIAN_POINT('Ctrl Pts',(21.3765169662169,0.485156750139203,4.35696654439514));
#55945=CARTESIAN_POINT('Ctrl Pts',(21.3844696055607,0.417898416498819,4.4337777074848));
#55946=CARTESIAN_POINT('Ctrl Pts',(21.3924222449045,0.336349907607971,4.48978005607163));
#55947=CARTESIAN_POINT('Ctrl Pts',(21.4003748842483,0.254801398717122,4.54578240465847));
#55948=CARTESIAN_POINT('Ctrl Pts',(21.4083275235921,0.158962714575808,4.58097593874246));
#55949=CARTESIAN_POINT('Ctrl Pts',(21.4162801629359,0.0605514396169286,
4.59105776945554));
#55950=CARTESIAN_POINT('Ctrl Pts',(21.4179049715381,0.0404449719157324,
4.59311759444699));
#55951=CARTESIAN_POINT('Ctrl Pts',(21.4195297801403,0.0202311170044278,
4.59412918598148));
#55952=CARTESIAN_POINT('Ctrl Pts',(21.4211545887425,1.51733402061755E-5,
4.59410821609125));
#55953=CARTESIAN_POINT('Origin',(4.,0.,4.));
#55954=CARTESIAN_POINT('',(21.8288454112575,1.47252919898561E-5,4.59408074293421));
#55955=CARTESIAN_POINT('',(21.7211545887425,-1.54601956517634E-5,4.59410286710644));
#55956=CARTESIAN_POINT('',(4.,-7.27562663373442E-17,4.5941));
#55957=CARTESIAN_POINT('Ctrl Pts',(21.8288454112575,1.47252919898561E-5,
4.59408074293421));
#55958=CARTESIAN_POINT('Ctrl Pts',(21.826505394409,0.0291331941223908,4.59410767674242));
#55959=CARTESIAN_POINT('Ctrl Pts',(21.8241653775604,0.0582478076928112,
4.59200528777341));
#55960=CARTESIAN_POINT('Ctrl Pts',(21.8218253607118,0.0870422430987805,
4.58774093918134));
#55961=CARTESIAN_POINT('Ctrl Pts',(21.813872721368,0.184901264939656,4.57324838268129));
#55962=CARTESIAN_POINT('Ctrl Pts',(21.8059200820242,0.279062206656402,4.53378504179028));
#55963=CARTESIAN_POINT('Ctrl Pts',(21.7979674426804,0.358012610677869,4.47417584741217));
#55964=CARTESIAN_POINT('Ctrl Pts',(21.7900148033366,0.436963014699336,4.41456665303406));
#55965=CARTESIAN_POINT('Ctrl Pts',(21.7820621639928,0.500702881025523,4.33481160516884));
#55966=CARTESIAN_POINT('Ctrl Pts',(21.774109524649,0.541439142878506,4.24466184465998));
#55967=CARTESIAN_POINT('Ctrl Pts',(21.7661568853052,0.58217540473149,4.15451208415111));
#55968=CARTESIAN_POINT('Ctrl Pts',(21.7582042459614,0.599908062111268,4.0539676109986));
#55969=CARTESIAN_POINT('Ctrl Pts',(21.7502516066176,0.59246905613922,3.95532135643358));
#55970=CARTESIAN_POINT('Ctrl Pts',(21.7422989672738,0.585030050167171,3.85667510186855));
#55971=CARTESIAN_POINT('Ctrl Pts',(21.73434632793,0.552419380843296,3.759927065891));
#55972=CARTESIAN_POINT('Ctrl Pts',(21.7263936885861,0.498624146640836,3.67690601358098));
#55973=CARTESIAN_POINT('Ctrl Pts',(21.7184410492423,0.444828912438376,3.59388496127097));
#55974=CARTESIAN_POINT('Ctrl Pts',(21.7104884098985,0.369849113357332,3.52459089262848));
#55975=CARTESIAN_POINT('Ctrl Pts',(21.7025357705547,0.28285205103972,3.47749595131133));
#55976=CARTESIAN_POINT('Ctrl Pts',(21.6945831312109,0.195854988722108,3.43040100999418));
#55977=CARTESIAN_POINT('Ctrl Pts',(21.6866304918671,0.0968406631679286,
3.40550519600236));
#55978=CARTESIAN_POINT('Ctrl Pts',(21.6786778525233,-0.00208507577578169,
3.40585236167057));
#55979=CARTESIAN_POINT('Ctrl Pts',(21.6707252131795,-0.101010814719503,
3.40619952733877));
#55980=CARTESIAN_POINT('Ctrl Pts',(21.6627725738357,-0.199847967052756,
3.431789672667));
#55981=CARTESIAN_POINT('Ctrl Pts',(21.6548199344919,-0.28651234476781,3.47949405385809));
#55982=CARTESIAN_POINT('Ctrl Pts',(21.6468672951481,-0.373176722482865,
3.52719843504918));
#55983=CARTESIAN_POINT('Ctrl Pts',(21.6389146558043,-0.44766832557972,3.59701705210314));
#55984=CARTESIAN_POINT('Ctrl Pts',(21.6309620164605,-0.500879541024521,
3.68041362817464));
#55985=CARTESIAN_POINT('Ctrl Pts',(21.6230093771167,-0.55409075646931,3.76381020424612));
#55986=CARTESIAN_POINT('Ctrl Pts',(21.6150567377728,-0.586021584262053,
3.86078473933514));
#55987=CARTESIAN_POINT('Ctrl Pts',(21.607104098429,-0.592768045815946,3.95948077576042));
#55988=CARTESIAN_POINT('Ctrl Pts',(21.5991514590852,-0.599514507369841,
4.05817681218572));
#55989=CARTESIAN_POINT('Ctrl Pts',(21.5911988197414,-0.581076602684875,
4.15859434994728));
#55990=CARTESIAN_POINT('Ctrl Pts',(21.5832461803976,-0.539708616728004,
4.24845597739434));
#55991=CARTESIAN_POINT('Ctrl Pts',(21.5752935410538,-0.498340630771147,
4.33831760484137));
#55992=CARTESIAN_POINT('Ctrl Pts',(21.56734090171,-0.434042563542403,4.41762332197391));
#55993=CARTESIAN_POINT('Ctrl Pts',(21.5593882623662,-0.354675729482573,
4.47667692475034));
#55994=CARTESIAN_POINT('Ctrl Pts',(21.5514356230224,-0.275308895422716,
4.53573052752678));
#55995=CARTESIAN_POINT('Ctrl Pts',(21.5434829836786,-0.180873294531764,
4.57453201594709));
#55996=CARTESIAN_POINT('Ctrl Pts',(21.5355303443348,-0.0829149652056982,
4.58833737958621));
#55997=CARTESIAN_POINT('Ctrl Pts',(21.533302033309,-0.055467269432644,4.59220561033096));
#55998=CARTESIAN_POINT('Ctrl Pts',(21.5310737222833,-0.0277430016607059,
4.5941113769453));
#55999=CARTESIAN_POINT('Ctrl Pts',(21.5288454112575,-1.51073027558624E-5,
4.59408477831653));
#56000=CARTESIAN_POINT('Ctrl Pts',(21.4211545887425,1.51733402061755E-5,
4.59410821609125));
#56001=CARTESIAN_POINT('Ctrl Pts',(21.4274824194841,-0.0787159889745399,
4.59402654867773));
#56002=CARTESIAN_POINT('Ctrl Pts',(21.4338102502257,-0.15747883181342,4.57828382012605));
#56003=CARTESIAN_POINT('Ctrl Pts',(21.4401380809673,-0.230053504748576,
4.54780575811717));
#56004=CARTESIAN_POINT('Ctrl Pts',(21.4480907203111,-0.321263308378747,
4.50950178872359));
#56005=CARTESIAN_POINT('Ctrl Pts',(21.4560433596549,-0.402699049862651,
4.44792372259427));
#56006=CARTESIAN_POINT('Ctrl Pts',(21.4639959989987,-0.464404100671371,
4.37060031698995));
#56007=CARTESIAN_POINT('Ctrl Pts',(21.4719486383425,-0.526109151480106,
4.2932769113856));
#56008=CARTESIAN_POINT('Ctrl Pts',(21.4799012776864,-0.568083511613643,
4.20020816630624));
#56009=CARTESIAN_POINT('Ctrl Pts',(21.4878539170302,-0.585195243866348,
4.10277300340868));
#56010=CARTESIAN_POINT('Ctrl Pts',(21.495806556374,-0.602306976119048,4.00533784051114));
#56011=CARTESIAN_POINT('Ctrl Pts',(21.5037591957178,-0.594556080490919,
3.90353625979537));
#56012=CARTESIAN_POINT('Ctrl Pts',(21.5117118350616,-0.562890209537588,
3.80981489101362));
#56013=CARTESIAN_POINT('Ctrl Pts',(21.5196644744054,-0.53122433858425,3.71609352223184));
#56014=CARTESIAN_POINT('Ctrl Pts',(21.5276171137492,-0.47564349230572,3.63045236538409));
#56015=CARTESIAN_POINT('Ctrl Pts',(21.535569753093,-0.402943186155437,3.56336221830407));
#56016=CARTESIAN_POINT('Ctrl Pts',(21.5435223924368,-0.330242880005154,
3.49627207122406));
#56017=CARTESIAN_POINT('Ctrl Pts',(21.5514750317806,-0.24042311398314,3.44773293391182));
#56018=CARTESIAN_POINT('Ctrl Pts',(21.5594276711244,-0.144465577806233,
3.42367937699355));
#56019=CARTESIAN_POINT('Ctrl Pts',(21.5673803104682,-0.0485080416293372,
3.39962582007528));
#56020=CARTESIAN_POINT('Ctrl Pts',(21.575332949812,0.0535872647024426,3.40005784355098));
#56021=CARTESIAN_POINT('Ctrl Pts',(21.5832855891558,0.149337799479898,3.42492262666669));
#56022=CARTESIAN_POINT('Ctrl Pts',(21.5912382284996,0.245088334257342,3.44978740978241));
#56023=CARTESIAN_POINT('Ctrl Pts',(21.5991908678434,0.33449409748049,3.49908495253815));
#56024=CARTESIAN_POINT('Ctrl Pts',(21.6071435071872,0.406624016913212,3.56678795891296));
#56025=CARTESIAN_POINT('Ctrl Pts',(21.6150961465311,0.478753936345942,3.63449096528778));
#56026=CARTESIAN_POINT('Ctrl Pts',(21.6230487858749,0.533608011988269,3.72059943528167));
#56027=CARTESIAN_POINT('Ctrl Pts',(21.6310014252187,0.564479585995414,3.81458543566408));
#56028=CARTESIAN_POINT('Ctrl Pts',(21.6389540645625,0.595351160002559,3.90857143604649));
#56029=CARTESIAN_POINT('Ctrl Pts',(21.6469067039063,0.602240232374519,4.0104349668174));
#56030=CARTESIAN_POINT('Ctrl Pts',(21.6548593432501,0.584304520186539,4.10772182398666));
#56031=CARTESIAN_POINT('Ctrl Pts',(21.6628119825939,0.566368807998562,4.2050086811559));
#56032=CARTESIAN_POINT('Ctrl Pts',(21.6707646219377,0.523608311250652,4.29771886472347));
#56033=CARTESIAN_POINT('Ctrl Pts',(21.6787172612815,0.461251083056512,4.37451729206089));
#56034=CARTESIAN_POINT('Ctrl Pts',(21.6866699006253,0.398893854862358,4.45131571939834));
#56035=CARTESIAN_POINT('Ctrl Pts',(21.6946225399691,0.316939895221968,4.51220239050563));
#56036=CARTESIAN_POINT('Ctrl Pts',(21.7025751793129,0.225409191891896,4.54973308058009));
#56037=CARTESIAN_POINT('Ctrl Pts',(21.7087683157894,0.15412944274098,4.5789601931952));
#56038=CARTESIAN_POINT('Ctrl Pts',(21.7149614522659,0.0770418275534371,
4.59402294959611));
#56039=CARTESIAN_POINT('Ctrl Pts',(21.7211545887425,-1.54601956517634E-5,
4.59410286710644));
#56040=CARTESIAN_POINT('Origin',(4.,0.,4.));
#56041=CARTESIAN_POINT('',(22.1288454112575,-1.19684274697274E-5,4.59413016891312));
#56042=CARTESIAN_POINT('',(22.0211545887425,1.20066176157995E-5,4.59406577061205));
#56043=CARTESIAN_POINT('',(4.,-7.27562663373442E-17,4.5941));
#56044=CARTESIAN_POINT('Ctrl Pts',(22.1288454112575,-1.19684274697274E-5,
4.59413016891312));
#56045=CARTESIAN_POINT('Ctrl Pts',(22.1219370665346,0.0859328098890183,
4.59405244111828));
#56046=CARTESIAN_POINT('Ctrl Pts',(22.1150287218117,0.171910584533005,4.57519344187135));
#56047=CARTESIAN_POINT('Ctrl Pts',(22.1081203770888,0.24987714748571,4.53905210772026));
#56048=CARTESIAN_POINT('Ctrl Pts',(22.100167737745,0.339629466009183,4.49744749656716));
#56049=CARTESIAN_POINT('Ctrl Pts',(22.0922150984012,0.418765494330909,4.4329406966096));
#56050=CARTESIAN_POINT('Ctrl Pts',(22.0842624590574,0.477609775176754,4.35341854270704));
#56051=CARTESIAN_POINT('Ctrl Pts',(22.0763098197136,0.536454056022584,4.2738963888045));
#56052=CARTESIAN_POINT('Ctrl Pts',(22.0683571803698,0.575006589392542,4.17935888095698));
#56053=CARTESIAN_POINT('Ctrl Pts',(22.060404541026,0.588553803007579,4.081364517074));
#56054=CARTESIAN_POINT('Ctrl Pts',(22.0524519016822,0.60210101662262,3.983370153191));
#56055=CARTESIAN_POINT('Ctrl Pts',(22.0444992623384,0.590642910482727,3.88191893327255));
#56056=CARTESIAN_POINT('Ctrl Pts',(22.0365466229946,0.55558039411957,3.78941465069146));
#56057=CARTESIAN_POINT('Ctrl Pts',(22.0285939836508,0.520517877756421,3.69691036811039));
#56058=CARTESIAN_POINT('Ctrl Pts',(22.020641344307,0.461850951170019,3.61335302286667));
#56059=CARTESIAN_POINT('Ctrl Pts',(22.0126887049632,0.386752445163155,3.5489586384446));
#56060=CARTESIAN_POINT('Ctrl Pts',(22.0047360656194,0.311653939156274,3.48456425402251));
#56061=CARTESIAN_POINT('Ctrl Pts',(21.9967834262756,0.220123853728924,3.43933283042207));
#56062=CARTESIAN_POINT('Ctrl Pts',(21.9888307869318,0.123352988439278,3.41879452521803));
#56063=CARTESIAN_POINT('Ctrl Pts',(21.980878147588,0.0265821231496428,3.398256220014));
#56064=CARTESIAN_POINT('Ctrl Pts',(21.9729255082441,-0.075429522002288,
3.40241103320635));
#56065=CARTESIAN_POINT('Ctrl Pts',(21.9649728689003,-0.170209634025949,
3.43075098229493));
#56066=CARTESIAN_POINT('Ctrl Pts',(21.9570202295565,-0.26498974604961,3.4590909313835));
#56067=CARTESIAN_POINT('Ctrl Pts',(21.9490675902127,-0.352538324945002,
3.5116160163683));
#56068=CARTESIAN_POINT('Ctrl Pts',(21.9411149508689,-0.422151364554475,
3.58190433023263));
#56069=CARTESIAN_POINT('Ctrl Pts',(21.9331623115251,-0.491764404163956,
3.65219264409696));
#56070=CARTESIAN_POINT('Ctrl Pts',(21.9252096721813,-0.543441904487514,
3.74024418684083));
#56071=CARTESIAN_POINT('Ctrl Pts',(21.9172570328375,-0.570865587277161,
3.83529345812586));
#56072=CARTESIAN_POINT('Ctrl Pts',(21.9093043934937,-0.598289270066803,
3.93034272941087));
#56073=CARTESIAN_POINT('Ctrl Pts',(21.9013517541499,-0.601459135322544,
4.03238972923704));
#56074=CARTESIAN_POINT('Ctrl Pts',(21.8933991148061,-0.579987623844179,
4.12895782202339));
#56075=CARTESIAN_POINT('Ctrl Pts',(21.8854464754623,-0.558516112365809,
4.22552591480976));
#56076=CARTESIAN_POINT('Ctrl Pts',(21.8774938361185,-0.512403224153321,
4.31661510055631));
#56077=CARTESIAN_POINT('Ctrl Pts',(21.8695411967747,-0.447286887835617,
4.39108848569571));
#56078=CARTESIAN_POINT('Ctrl Pts',(21.8615885574308,-0.38217055151792,4.46556187083511));
#56079=CARTESIAN_POINT('Ctrl Pts',(21.853635918087,-0.298050767095013,4.52341945536736));
#56080=CARTESIAN_POINT('Ctrl Pts',(21.8456832787432,-0.205212323901057,
4.55758736157894));
#56081=CARTESIAN_POINT('Ctrl Pts',(21.840070656248,-0.139691040693493,4.58170156451555));
#56082=CARTESIAN_POINT('Ctrl Pts',(21.8344580337528,-0.0698270680627233,
4.59401614113532));
#56083=CARTESIAN_POINT('Ctrl Pts',(21.8288454112575,1.47252919898561E-5,
4.59408074293421));
#56084=CARTESIAN_POINT('Ctrl Pts',(21.7211545887425,-1.54601956517634E-5,
4.59410286710644));
#56085=CARTESIAN_POINT('Ctrl Pts',(21.7229140916097,-0.0219078436841643,
4.59412557209431));
#56086=CARTESIAN_POINT('Ctrl Pts',(21.724673594477,-0.0437977792686499,
4.59293892497318));
#56087=CARTESIAN_POINT('Ctrl Pts',(21.7264330973443,-0.0655513867134097,
4.59052415646896));
#56088=CARTESIAN_POINT('Ctrl Pts',(21.7343857366881,-0.163873814968881,
4.57960983324176));
#56089=CARTESIAN_POINT('Ctrl Pts',(21.742338376032,-0.259411224460086,4.54360647774573));
#56090=CARTESIAN_POINT('Ctrl Pts',(21.7502910153758,-0.340482865683332,
4.48691599054611));
#56091=CARTESIAN_POINT('Ctrl Pts',(21.7582436547196,-0.421554506906578,
4.4302255033465));
#56092=CARTESIAN_POINT('Ctrl Pts',(21.7661962940634,-0.488160379861865,
4.3528478844433));
#56093=CARTESIAN_POINT('Ctrl Pts',(21.7741489334072,-0.532157009426634,
4.26424360160945));
#56094=CARTESIAN_POINT('Ctrl Pts',(21.782101572751,-0.576153638991403,4.1756393187756));
#56095=CARTESIAN_POINT('Ctrl Pts',(21.7900542120948,-0.597541025165654,
4.0758083720111));
#56096=CARTESIAN_POINT('Ctrl Pts',(21.7980068514386,-0.593704268699233,
3.9769564542281));
#56097=CARTESIAN_POINT('Ctrl Pts',(21.8059594907824,-0.589867512232813,
3.87810453644509));
#56098=CARTESIAN_POINT('Ctrl Pts',(21.8139121301262,-0.560806613125721,
3.78023164764359));
#56099=CARTESIAN_POINT('Ctrl Pts',(21.82186476947,-0.510074662095298,3.69530408148155));
#56100=CARTESIAN_POINT('Ctrl Pts',(21.8298174088138,-0.459342711064876,
3.61037651531951));
#56101=CARTESIAN_POINT('Ctrl Pts',(21.8377700481576,-0.386939708111122,
3.53839427179695));
#56102=CARTESIAN_POINT('Ctrl Pts',(21.8457226875014,-0.301717906454235,
3.48815816056295));
#56103=CARTESIAN_POINT('Ctrl Pts',(21.8536753268452,-0.216496104797349,
3.43792204932895));
#56104=CARTESIAN_POINT('Ctrl Pts',(21.8616279661891,-0.118455504437329,
3.40943207038352));
#56105=CARTESIAN_POINT('Ctrl Pts',(21.8695806055329,-0.0195829040543552,
3.40617151167847));
#56106=CARTESIAN_POINT('Ctrl Pts',(21.8775332448767,0.0792896963286298,
3.40291095297342));
#56107=CARTESIAN_POINT('Ctrl Pts',(21.8854858842205,0.178994296734569,3.42487981450875));
#56108=CARTESIAN_POINT('Ctrl Pts',(21.8934385235643,0.267340651814441,3.46939210375187));
#56109=CARTESIAN_POINT('Ctrl Pts',(21.9013911629081,0.355687006894294,3.51390439299499));
#56110=CARTESIAN_POINT('Ctrl Pts',(21.9093438022519,0.432675116648084,3.58096010994589));
#56111=CARTESIAN_POINT('Ctrl Pts',(21.9172964415957,0.488892136101412,3.66236077992681));
#56112=CARTESIAN_POINT('Ctrl Pts',(21.9252490809395,0.545109155554752,3.74376144990775));
#56113=CARTESIAN_POINT('Ctrl Pts',(21.9332017202833,0.580555084707621,3.8395070729187));
#56114=CARTESIAN_POINT('Ctrl Pts',(21.9411543596271,0.590896175957217,3.93789144251738));
#56115=CARTESIAN_POINT('Ctrl Pts',(21.9491069989709,0.601237267206812,4.03627581211605));
#56116=CARTESIAN_POINT('Ctrl Pts',(21.9570596383147,0.58647352055314,4.13729892830245));
#56117=CARTESIAN_POINT('Ctrl Pts',(21.9650122776585,0.548410005102802,4.22860933921557));
#56118=CARTESIAN_POINT('Ctrl Pts',(21.9729649170023,0.510346489652465,4.31991975012869));
#56119=CARTESIAN_POINT('Ctrl Pts',(21.9809175563462,0.448983205405461,4.40151745576853));
#56120=CARTESIAN_POINT('Ctrl Pts',(21.98887019569,0.371822649612145,4.46342602528218));
#56121=CARTESIAN_POINT('Ctrl Pts',(21.9968228350338,0.29466209381883,4.52533459479583));
#56122=CARTESIAN_POINT('Ctrl Pts',(22.0047754743776,0.201704266479203,4.5675540281833));
#56123=CARTESIAN_POINT('Ctrl Pts',(22.0127281137214,0.104314528045707,4.58492242469582));
#56124=CARTESIAN_POINT('Ctrl Pts',(22.0155369387284,0.069917050565085,4.59105683924014));
#56125=CARTESIAN_POINT('Ctrl Pts',(22.0183457637354,0.0349667096964542,
4.59409118517947));
#56126=CARTESIAN_POINT('Ctrl Pts',(22.0211545887425,1.20066176157995E-5,
4.59406577061205));
#56127=CARTESIAN_POINT('Origin',(4.,0.,4.));
#56128=CARTESIAN_POINT('',(22.4288454112575,5.18920962550018E-6,4.59405135764298));
#56129=CARTESIAN_POINT('',(22.3211545887424,-7.30827440488969E-6,4.59414400810326));
#56130=CARTESIAN_POINT('',(4.,-7.27562663373442E-17,4.5941));
#56131=CARTESIAN_POINT('Ctrl Pts',(22.4288454112575,5.18920962550018E-6,
4.59405135764298));
#56132=CARTESIAN_POINT('Ctrl Pts',(22.4253213780041,0.0438634191921666,
4.5940647188338));
#56133=CARTESIAN_POINT('Ctrl Pts',(22.4217973447507,0.0877187745911938,
4.589273164082));
#56134=CARTESIAN_POINT('Ctrl Pts',(22.4182733114973,0.130485535360993,4.57964583089408));
#56135=CARTESIAN_POINT('Ctrl Pts',(22.4103206721535,0.226996720088313,4.55791995512033));
#56136=CARTESIAN_POINT('Ctrl Pts',(22.4023680328097,0.317964089339764,4.51156722320365));
#56137=CARTESIAN_POINT('Ctrl Pts',(22.3944153934659,0.392265646131591,4.44625488916104));
#56138=CARTESIAN_POINT('Ctrl Pts',(22.3864627541221,0.4665672029234,4.38094255511845));
#56139=CARTESIAN_POINT('Ctrl Pts',(22.3785101147783,0.524202947255594,4.29667061894994));
#56140=CARTESIAN_POINT('Ctrl Pts',(22.3705574754345,0.558126122886914,4.20374247196213));
#56141=CARTESIAN_POINT('Ctrl Pts',(22.3626048360906,0.592049298518242,4.11081432497429));
#56142=CARTESIAN_POINT('Ctrl Pts',(22.3546521967468,0.602259905448686,4.00922996716717));
#56143=CARTESIAN_POINT('Ctrl Pts',(22.346699557403,0.587509558716917,3.91140947017845));
#56144=CARTESIAN_POINT('Ctrl Pts',(22.3387469180592,0.572759211985149,3.81358897318973));
#56145=CARTESIAN_POINT('Ctrl Pts',(22.3307942787154,0.533047911591167,3.71953233701942));
#56146=CARTESIAN_POINT('Ctrl Pts',(22.3228416393716,0.473230904440663,3.6407392662825));
#56147=CARTESIAN_POINT('Ctrl Pts',(22.3148890000278,0.413413897290173,3.5619461955456));
#56148=CARTESIAN_POINT('Ctrl Pts',(22.306936360684,0.333491183383171,3.49841669024209));
#56149=CARTESIAN_POINT('Ctrl Pts',(22.2989837213402,0.243234403245124,3.45791809774646));
#56150=CARTESIAN_POINT('Ctrl Pts',(22.2910310819964,0.152977623107077,3.41741950525082));
#56151=CARTESIAN_POINT('Ctrl Pts',(22.2830784426526,0.0523867767379842,
3.39995182556307));
#56152=CARTESIAN_POINT('Ctrl Pts',(22.2751258033088,-0.0462395349927855,
3.40765072037886));
#56153=CARTESIAN_POINT('Ctrl Pts',(22.267173163965,-0.144865846723578,3.41534961519466));
#56154=CARTESIAN_POINT('Ctrl Pts',(22.2592205246212,-0.241527623816046,
3.448215084514));
#56155=CARTESIAN_POINT('Ctrl Pts',(22.2512678852774,-0.324406647450603,
3.50222887712101));
#56156=CARTESIAN_POINT('Ctrl Pts',(22.2433152459336,-0.40728567108515,3.55624266972802));
#56157=CARTESIAN_POINT('Ctrl Pts',(22.2353626065897,-0.476381941261788,
3.63140478562268));
#56158=CARTESIAN_POINT('Ctrl Pts',(22.2274099672459,-0.523247497912515,
3.71852563243507));
#56159=CARTESIAN_POINT('Ctrl Pts',(22.2194573279021,-0.570113054563243,
3.80564647924745));
#56160=CARTESIAN_POINT('Ctrl Pts',(22.2115046885583,-0.59474789768806,3.90472605697756));
#56161=CARTESIAN_POINT('Ctrl Pts',(22.2035520492145,-0.594140082177443,
4.00365053781872));
#56162=CARTESIAN_POINT('Ctrl Pts',(22.1955994098707,-0.593532266666827,
4.10257501865988));
#56163=CARTESIAN_POINT('Ctrl Pts',(22.1876467705269,-0.567681792520777,
4.2013444026121));
#56164=CARTESIAN_POINT('Ctrl Pts',(22.1796941311831,-0.519749232289404,
4.2878827872712));
#56165=CARTESIAN_POINT('Ctrl Pts',(22.1717414918393,-0.471816672058032,
4.37442117193029));
#56166=CARTESIAN_POINT('Ctrl Pts',(22.1637888524955,-0.401802025741336,
4.44872855729627));
#56167=CARTESIAN_POINT('Ctrl Pts',(22.1558362131517,-0.318265537426909,
4.50171985346399));
#56168=CARTESIAN_POINT('Ctrl Pts',(22.1478835738079,-0.234729049112483,
4.55471114963171));
#56169=CARTESIAN_POINT('Ctrl Pts',(22.1399309344641,-0.137670718800326,
4.58638635660118));
#56170=CARTESIAN_POINT('Ctrl Pts',(22.1319782951203,-0.0389572492816432,
4.5928727489116));
#56171=CARTESIAN_POINT('Ctrl Pts',(22.1309340004994,-0.0259947671705595,
4.5937245044491));
#56172=CARTESIAN_POINT('Ctrl Pts',(22.1298897058784,-0.0130037447923657,
4.5941419185755));
#56173=CARTESIAN_POINT('Ctrl Pts',(22.1288454112575,-1.19684274697274E-5,
4.59413016891312));
#56174=CARTESIAN_POINT('Ctrl Pts',(22.0211545887425,1.20066176157995E-5,
4.59406577061205));
#56175=CARTESIAN_POINT('Ctrl Pts',(22.0262984030792,-0.064000704172389,
4.59401922879619));
#56176=CARTESIAN_POINT('Ctrl Pts',(22.031442217416,-0.128028044405449,4.5837112392356));
#56177=CARTESIAN_POINT('Ctrl Pts',(22.0365860317528,-0.188701337098646,
4.56338935830438));
#56178=CARTESIAN_POINT('Ctrl Pts',(22.0445386710966,-0.282505814282095,
4.53197053576284));
#56179=CARTESIAN_POINT('Ctrl Pts',(22.0524913104404,-0.368293119121642,
4.4766155310422));
#56180=CARTESIAN_POINT('Ctrl Pts',(22.0604439497842,-0.435574585201076,
4.40409224738955));
#56181=CARTESIAN_POINT('Ctrl Pts',(22.068396589128,-0.502856051280518,4.33156896373689));
#56182=CARTESIAN_POINT('Ctrl Pts',(22.0763492284718,-0.551631678599843,
4.24187740115222));
#56183=CARTESIAN_POINT('Ctrl Pts',(22.0843018678156,-0.575937982408454,
4.14598357473613));
#56184=CARTESIAN_POINT('Ctrl Pts',(22.0922545071594,-0.600244286217068,
4.05008974832002));
#56185=CARTESIAN_POINT('Ctrl Pts',(22.1002071465032,-0.600081266514962,
3.94799365807249));
#56186=CARTESIAN_POINT('Ctrl Pts',(22.1081597858471,-0.575468854681199,
3.85217794154701));
#56187=CARTESIAN_POINT('Ctrl Pts',(22.1161124251909,-0.550856442847438,
3.75636222502155));
#56188=CARTESIAN_POINT('Ctrl Pts',(22.1240650645347,-0.501794638882025,
3.66682688221814));
#56189=CARTESIAN_POINT('Ctrl Pts',(22.1320177038785,-0.434281916527717,
3.5945188282416));
#56190=CARTESIAN_POINT('Ctrl Pts',(22.1399703432223,-0.366769194173409,
3.52221077426505));
#56191=CARTESIAN_POINT('Ctrl Pts',(22.1479229825661,-0.280805553430205,
3.46713000911538));
#56192=CARTESIAN_POINT('Ctrl Pts',(22.1558756219099,-0.186901220180937,
3.43601090651668));
#56193=CARTESIAN_POINT('Ctrl Pts',(22.1638282612537,-0.0929968869316588,
3.40489180391798));
#56194=CARTESIAN_POINT('Ctrl Pts',(22.1717809005975,0.00884813882368474,
3.39773436387026));
#56195=CARTESIAN_POINT('Ctrl Pts',(22.1797335399413,0.106181915586414,3.41541368090248));
#56196=CARTESIAN_POINT('Ctrl Pts',(22.1876861792851,0.203515692349121,3.4330929979347));
#56197=CARTESIAN_POINT('Ctrl Pts',(22.1956388186289,0.296338220119215,3.47560907204686));
#56198=CARTESIAN_POINT('Ctrl Pts',(22.2035914579727,0.373300680656879,3.53776373412001));
#56199=CARTESIAN_POINT('Ctrl Pts',(22.2115440973165,0.450263141194552,3.59991839619317));
#56200=CARTESIAN_POINT('Ctrl Pts',(22.2194967366603,0.511365534499791,3.68171164622733));
#56201=CARTESIAN_POINT('Ctrl Pts',(22.2274493760041,0.549137260797828,3.7731431454068));
#56202=CARTESIAN_POINT('Ctrl Pts',(22.2354020153479,0.586908987095865,3.86457464458628));
#56203=CARTESIAN_POINT('Ctrl Pts',(22.2433546546918,0.6013500463867,3.96564439291107));
#56204=CARTESIAN_POINT('Ctrl Pts',(22.2513072940356,0.590694822479903,4.06399523710107));
#56205=CARTESIAN_POINT('Ctrl Pts',(22.2592599333794,0.580039598573106,4.16234608129106));
#56206=CARTESIAN_POINT('Ctrl Pts',(22.2672125727232,0.544288091468676,4.25797802134625));
#56207=CARTESIAN_POINT('Ctrl Pts',(22.275165212067,0.487811409852587,4.33919875012361));
#56208=CARTESIAN_POINT('Ctrl Pts',(22.2831178514108,0.431334728236497,4.42041947890096));
#56209=CARTESIAN_POINT('Ctrl Pts',(22.2910704907546,0.354132872108749,4.48722899640046));
#56210=CARTESIAN_POINT('Ctrl Pts',(22.2990231300984,0.265644819817582,4.53145892916239));
#56211=CARTESIAN_POINT('Ctrl Pts',(22.3064002829798,0.183560135512932,4.57248819778762));
#56212=CARTESIAN_POINT('Ctrl Pts',(22.3137774358611,0.0917635873240076,
4.59408754951618));
#56213=CARTESIAN_POINT('Ctrl Pts',(22.3211545887424,-7.30827440488969E-6,
4.59414400810326));
#56214=CARTESIAN_POINT('Origin',(4.,0.,4.));
#56215=CARTESIAN_POINT('',(22.7288454112575,-7.11440487624268E-7,4.59414971000239));
#56216=CARTESIAN_POINT('',(22.6211545887425,-1.51245797256638E-7,4.59404869726453));
#56217=CARTESIAN_POINT('',(4.,-7.27562663373442E-17,4.5941));
#56218=CARTESIAN_POINT('Ctrl Pts',(22.7288454112575,-7.11440487624268E-7,
4.59414971000239));
#56219=CARTESIAN_POINT('Ctrl Pts',(22.7287056894736,0.0017373052546791,
4.59414999869406));
#56220=CARTESIAN_POINT('Ctrl Pts',(22.7285659676897,0.0034753215591825,
4.59414251282321));
#56221=CARTESIAN_POINT('Ctrl Pts',(22.7284262459057,0.00521327185949689,
4.59412723628209));
#56222=CARTESIAN_POINT('Ctrl Pts',(22.7204736065619,0.104133365400505,4.59325773105135));
#56223=CARTESIAN_POINT('Ctrl Pts',(22.7125209672181,0.202839630323109,4.56714939948764));
#56224=CARTESIAN_POINT('Ctrl Pts',(22.7045683278743,0.289252680684759,4.51898953373575));
#56225=CARTESIAN_POINT('Ctrl Pts',(22.6966156885305,0.375665731046408,4.47082966798385));
#56226=CARTESIAN_POINT('Ctrl Pts',(22.6886630491867,0.449785566847107,4.40061826804377));
#56227=CARTESIAN_POINT('Ctrl Pts',(22.6807104098429,0.502555912967013,4.31694216252228));
#56228=CARTESIAN_POINT('Ctrl Pts',(22.6727577704991,0.555326259086918,4.23326605700079));
#56229=CARTESIAN_POINT('Ctrl Pts',(22.6648051311553,0.586747115526033,4.13612524589788));
#56230=CARTESIAN_POINT('Ctrl Pts',(22.6568524918115,0.592973744123511,4.03739517928057));
#56231=CARTESIAN_POINT('Ctrl Pts',(22.6488998524677,0.59920037272099,3.93866511266326));
#56232=CARTESIAN_POINT('Ctrl Pts',(22.6409472131239,0.580232773476834,3.83834579053153));
#56233=CARTESIAN_POINT('Ctrl Pts',(22.6329945737801,0.538391640361539,3.74870332422701));
#56234=CARTESIAN_POINT('Ctrl Pts',(22.6250419344363,0.496550507246239,3.65906085792248));
#56235=CARTESIAN_POINT('Ctrl Pts',(22.6170892950925,0.431835840259791,3.58009524744515));
#56236=CARTESIAN_POINT('Ctrl Pts',(22.6091366557487,0.35215901686313,3.52146073929621));
#56237=CARTESIAN_POINT('Ctrl Pts',(22.6011840164048,0.272482193466486,3.46282623114728));
#56238=CARTESIAN_POINT('Ctrl Pts',(22.593231377061,0.17784321365963,3.42452282532672));
#56239=CARTESIAN_POINT('Ctrl Pts',(22.5852787377172,0.0798134434713266,
3.41123383340666));
#56240=CARTESIAN_POINT('Ctrl Pts',(22.5773260983734,-0.0182163267169884,
3.3979448414866));
#56241=CARTESIAN_POINT('Ctrl Pts',(22.5693734590296,-0.119636887286728,
3.40967026346704));
#56242=CARTESIAN_POINT('Ctrl Pts',(22.5614208196858,-0.212048437952692,
3.44497640167274));
#56243=CARTESIAN_POINT('Ctrl Pts',(22.553468180342,-0.304459988618666,3.48028253987845));
#56244=CARTESIAN_POINT('Ctrl Pts',(22.5455155409982,-0.387862529380837,
3.53916939430943));
#56245=CARTESIAN_POINT('Ctrl Pts',(22.5375629016544,-0.452058834188948,
3.61443730067171));
#56246=CARTESIAN_POINT('Ctrl Pts',(22.5296102623106,-0.516255138997059,
3.689705207034));
#56247=CARTESIAN_POINT('Ctrl Pts',(22.5216576229668,-0.561245207851117,
3.7813541653276));
#56248=CARTESIAN_POINT('Ctrl Pts',(22.513704983623,-0.581528460676763,3.87817881267738));
#56249=CARTESIAN_POINT('Ctrl Pts',(22.5057523442792,-0.601811713502406,
3.97500346002715));
#56250=CARTESIAN_POINT('Ctrl Pts',(22.4977997049354,-0.597388150299644,
4.07700379643311));
#56251=CARTESIAN_POINT('Ctrl Pts',(22.4898470655916,-0.568798575589296,
4.17170890717095));
#56252=CARTESIAN_POINT('Ctrl Pts',(22.4818944262477,-0.540209000878948,
4.26641401790879));
#56253=CARTESIAN_POINT('Ctrl Pts',(22.4739417869039,-0.487453414661012,
4.35382390297851));
#56254=CARTESIAN_POINT('Ctrl Pts',(22.4659891475601,-0.416981925106977,
4.42325150516024));
#56255=CARTESIAN_POINT('Ctrl Pts',(22.4580365082163,-0.346510435552941,
4.49267910734197));
#56256=CARTESIAN_POINT('Ctrl Pts',(22.4500838688725,-0.258323042662803,
4.54412442663572));
#56257=CARTESIAN_POINT('Ctrl Pts',(22.4421312295287,-0.163201846116148,
4.57129757646718));
#56258=CARTESIAN_POINT('Ctrl Pts',(22.4377026234383,-0.11023146834083,4.58642955613285));
#56259=CARTESIAN_POINT('Ctrl Pts',(22.4332740173479,-0.0551108697057404,
4.59403456681078));
#56260=CARTESIAN_POINT('Ctrl Pts',(22.4288454112575,5.18920962550018E-6,
4.59405135764298));
#56261=CARTESIAN_POINT('Ctrl Pts',(22.3211545887424,-7.30827440488969E-6,
4.59414400810326));
#56262=CARTESIAN_POINT('Ctrl Pts',(22.3217300752049,-0.00716629073194701,
4.59414841239758));
#56263=CARTESIAN_POINT('Ctrl Pts',(22.3223055616673,-0.0143251170819474,
4.59402171850555));
#56264=CARTESIAN_POINT('Ctrl Pts',(22.3228810481298,-0.0214791647150919,
4.59376292335171));
#56265=CARTESIAN_POINT('Ctrl Pts',(22.3308336874736,-0.120340848501978,
4.59018663675477));
#56266=CARTESIAN_POINT('Ctrl Pts',(22.3387863268174,-0.218289967621164,
4.56138371553656));
#56267=CARTESIAN_POINT('Ctrl Pts',(22.3467389661612,-0.303350908332583,
4.51087570903952));
#56268=CARTESIAN_POINT('Ctrl Pts',(22.3546916055051,-0.388411849044011,
4.46036770254246));
#56269=CARTESIAN_POINT('Ctrl Pts',(22.3626442448489,-0.460584611347669,
4.38815461076656));
#56270=CARTESIAN_POINT('Ctrl Pts',(22.3705968841927,-0.511045091866278,
4.3030654678256));
#56271=CARTESIAN_POINT('Ctrl Pts',(22.3785495235365,-0.561505572384874,
4.21797632488466));
#56272=CARTESIAN_POINT('Ctrl Pts',(22.3865021628803,-0.590253771118432,
4.12001113077866));
#56273=CARTESIAN_POINT('Ctrl Pts',(22.3944548022241,-0.593774829630164,
4.02114746451658));
#56274=CARTESIAN_POINT('Ctrl Pts',(22.4024074415679,-0.597295888141896,
3.92228379825449));
#56275=CARTESIAN_POINT('Ctrl Pts',(22.4103600809117,-0.575589806431797,
3.82252165983632));
#56276=CARTESIAN_POINT('Ctrl Pts',(22.4183127202555,-0.531310447862662,
3.73405832985033));
#56277=CARTESIAN_POINT('Ctrl Pts',(22.4262653595993,-0.487031089293526,
3.64559499986435));
#56278=CARTESIAN_POINT('Ctrl Pts',(22.4342179989431,-0.420178453865353,
3.56843047831055));
#56279=CARTESIAN_POINT('Ctrl Pts',(22.4421706382869,-0.338926188203527,
3.51199917808983));
#56280=CARTESIAN_POINT('Ctrl Pts',(22.4501232776307,-0.257673922541701,
3.45556787786912));
#56281=CARTESIAN_POINT('Ctrl Pts',(22.4580759169745,-0.162022026646223,
3.41986979898149));
#56282=CARTESIAN_POINT('Ctrl Pts',(22.4660285563183,-0.0636652448434586,
3.40926951931498));
#56283=CARTESIAN_POINT('Ctrl Pts',(22.4739811956621,0.0346915369593057,
3.39866923964846));
#56284=CARTESIAN_POINT('Ctrl Pts',(22.4819338350059,0.135753204669356,3.41316675920307));
#56285=CARTESIAN_POINT('Ctrl Pts',(22.4898864743497,0.227163587879617,3.45098955584192));
#56286=CARTESIAN_POINT('Ctrl Pts',(22.4978391136936,0.318573971089878,3.48881235248077));
#56287=CARTESIAN_POINT('Ctrl Pts',(22.5057917530374,0.40033306980035,3.54996042620388));
#56288=CARTESIAN_POINT('Ctrl Pts',(22.5137443923812,0.462444730281743,3.62695759769032));
#56289=CARTESIAN_POINT('Ctrl Pts',(22.521697031725,0.524556390763143,3.70395476917678));
#56290=CARTESIAN_POINT('Ctrl Pts',(22.5296496710688,0.567020613015458,3.79680103842659));
#56291=CARTESIAN_POINT('Ctrl Pts',(22.5376023104126,0.584645549343987,3.89414467407578));
#56292=CARTESIAN_POINT('Ctrl Pts',(22.5455549497564,0.602270485672515,3.99148830972497));
#56293=CARTESIAN_POINT('Ctrl Pts',(22.5535075891002,0.595056136077256,4.09332931177355));
#56294=CARTESIAN_POINT('Ctrl Pts',(22.561460228444,0.563884587368514,4.18721625032571));
#56295=CARTESIAN_POINT('Ctrl Pts',(22.5694128677878,0.532713038659782,4.28110318887784));
#56296=CARTESIAN_POINT('Ctrl Pts',(22.5773655071316,0.477584290837583,4.36703606393356));
#56297=CARTESIAN_POINT('Ctrl Pts',(22.5853181464754,0.405238519368296,4.43450837402952));
#56298=CARTESIAN_POINT('Ctrl Pts',(22.5932707858192,0.332892747898984,4.5019806841255));
#56299=CARTESIAN_POINT('Ctrl Pts',(22.601223425163,0.24332995278257,4.55099242926169));
#56300=CARTESIAN_POINT('Ctrl Pts',(22.6091760645068,0.14750052788588,4.57555132613148));
#56301=CARTESIAN_POINT('Ctrl Pts',(22.6131689059187,0.0993867282199646,
4.58788179608141));
#56302=CARTESIAN_POINT('Ctrl Pts',(22.6171617473306,0.0496932250345643,
4.5940481472271));
#56303=CARTESIAN_POINT('Ctrl Pts',(22.6211545887425,-1.51173456864708E-7,
4.59404872180247));
#56304=CARTESIAN_POINT('Origin',(3.42660065607856,0.,4.));
#56305=CARTESIAN_POINT('',(22.7766006560786,-4.98014040841517E-7,4.41590979742004));
#56306=CARTESIAN_POINT('',(22.8,4.87367679877478E-13,4.415875));
#56307=CARTESIAN_POINT('',(3.42660065607856,4.87367679877478E-13,4.415875));
#56308=CARTESIAN_POINT('',(22.8,-0.195748955928421,4.36692555359082));
#56309=CARTESIAN_POINT('Ctrl Pts',(22.7766006560786,-4.98014040834069E-7,
4.41590979742004));
#56310=CARTESIAN_POINT('Ctrl Pts',(22.7844004373857,-0.0679170312443507,
4.41589851620688));
#56311=CARTESIAN_POINT('Ctrl Pts',(22.7922002186928,-0.135834416676695,
4.39892762624317));
#56312=CARTESIAN_POINT('Ctrl Pts',(22.8,-0.195762566582618,4.36695865185838));
#56313=CARTESIAN_POINT('Origin',(22.8,0.,4.));
#56314=CARTESIAN_POINT('Origin',(3.42660065607856,0.,4.));
#56315=CARTESIAN_POINT('',(22.4766006560785,3.63249072247605E-6,4.41584094994071));
#56316=CARTESIAN_POINT('',(22.5733993439214,-1.05822049303872E-7,4.41583910483016));
#56317=CARTESIAN_POINT('',(3.42660065607856,4.87367679877478E-13,4.415875));
#56318=CARTESIAN_POINT('Ctrl Pts',(22.4766006560785,3.63249072248342E-6,
4.41584094994071));
#56319=CARTESIAN_POINT('Ctrl Pts',(22.4810292621689,-0.0385780726118879,
4.41582919621688));
#56320=CARTESIAN_POINT('Ctrl Pts',(22.4934105076031,-0.146451497349971,
4.40094585736882));
#56321=CARTESIAN_POINT('Ctrl Pts',(22.5137443923812,-0.304292138366774,
4.30886736509782));
#56322=CARTESIAN_POINT('Ctrl Pts',(22.5376023104126,-0.415080201412036,
4.12530439950267));
#56323=CARTESIAN_POINT('Ctrl Pts',(22.561460228444,-0.424369795825249,3.91110111771763));
#56324=CARTESIAN_POINT('Ctrl Pts',(22.5853181464754,-0.329889515310188,
3.71863599132299));
#56325=CARTESIAN_POINT('Ctrl Pts',(22.6091760645068,-0.154742073939436,
3.59497211022641));
#56326=CARTESIAN_POINT('Ctrl Pts',(22.6330339825383,0.0582436639512456,
3.57034842802071));
#56327=CARTESIAN_POINT('Ctrl Pts',(22.6568919005697,0.256987911016647,3.65078654733876));
#56328=CARTESIAN_POINT('Ctrl Pts',(22.6807498186011,0.39289034562191,3.81661632308649));
#56329=CARTESIAN_POINT('Ctrl Pts',(22.7046077366325,0.432722782933869,4.02728943245291));
#56330=CARTESIAN_POINT('Ctrl Pts',(22.7284656546639,0.366738191089385,4.2312875884069));
#56331=CARTESIAN_POINT('Ctrl Pts',(22.7523235726953,0.211084664509997,4.37873330099785));
#56332=CARTESIAN_POINT('Ctrl Pts',(22.7683685731669,0.0716802821347026,
4.41560650088387));
#56333=CARTESIAN_POINT('Ctrl Pts',(22.7764609342946,0.00121612829983627,
4.41590999950663));
#56334=CARTESIAN_POINT('Ctrl Pts',(22.7766006560786,-4.98014040834069E-7,
4.41590979742004));
#56335=CARTESIAN_POINT('',(22.8,0.415641328671541,4.01393920819689));
#56336=CARTESIAN_POINT('Origin',(22.8,0.,4.));
#56337=CARTESIAN_POINT('Ctrl Pts',(22.5733993439214,-1.0582204931428E-7,
4.41583910483016));
#56338=CARTESIAN_POINT('Ctrl Pts',(22.5773591418533,-0.034498011376554,
4.41583950370926));
#56339=CARTESIAN_POINT('Ctrl Pts',(22.5892715791291,-0.138279341065089,
4.40307041914735));
#56340=CARTESIAN_POINT('Ctrl Pts',(22.6091366557487,-0.295063722636797,
4.31769517074077));
#56341=CARTESIAN_POINT('Ctrl Pts',(22.6329945737801,-0.411209141905604,
4.13747522778479));
#56342=CARTESIAN_POINT('Ctrl Pts',(22.6568524918115,-0.426804986482714,
3.92363755172126));
#56343=CARTESIAN_POINT('Ctrl Pts',(22.6807104098429,-0.33803111495158,3.72847502015617));
#56344=CARTESIAN_POINT('Ctrl Pts',(22.7045683278743,-0.16660749730952,3.59970312177549));
#56345=CARTESIAN_POINT('Ctrl Pts',(22.7284262459057,0.0455714674079685,
3.56882345794434));
#56346=CARTESIAN_POINT('Ctrl Pts',(22.7522841639372,0.246577802732478,3.64336153500176));
#56347=CARTESIAN_POINT('Ctrl Pts',(22.7761420819686,0.387346815298129,3.80514019809748));
#56348=CARTESIAN_POINT('Ctrl Pts',(22.7920473606562,0.417963038852713,3.94471011778788));
#56349=CARTESIAN_POINT('Ctrl Pts',(22.8,0.415641328671541,4.01393920819689));
#56350=CARTESIAN_POINT('Origin',(3.42660065607856,0.,4.));
#56351=CARTESIAN_POINT('',(22.1766006560786,-8.37799962078257E-6,4.41589611849309));
#56352=CARTESIAN_POINT('',(22.2733993439214,-5.11585294796223E-6,4.41590580604266));
#56353=CARTESIAN_POINT('',(3.42660065607856,4.87367679877478E-13,4.415875));
#56354=CARTESIAN_POINT('Ctrl Pts',(22.1766006560786,-8.37799962077716E-6,
4.41589611849309));
#56355=CARTESIAN_POINT('Ctrl Pts',(22.1776449506995,-0.0091027307950905,
4.41590434335565));
#56356=CARTESIAN_POINT('Ctrl Pts',(22.1866418846642,-0.0874489573854402,
4.4133870032437));
#56357=CARTESIAN_POINT('Ctrl Pts',(22.2035914579727,-0.232253957950086,
4.36612956178204));
#56358=CARTESIAN_POINT('Ctrl Pts',(22.2274493760041,-0.379286482964224,
4.21008217638027));
#56359=CARTESIAN_POINT('Ctrl Pts',(22.2513072940356,-0.433573131350875,
4.00266397632408));
#56360=CARTESIAN_POINT('Ctrl Pts',(22.275165212067,-0.381839338801546,3.79459436150246));
#56361=CARTESIAN_POINT('Ctrl Pts',(22.2990231300984,-0.236735426869051,
3.63675202040985));
#56362=CARTESIAN_POINT('Ctrl Pts',(22.3228810481298,-0.0337432544318164,
3.56773370504276));
#56363=CARTESIAN_POINT('Ctrl Pts',(22.3467389661613,0.177500062688638,3.60441627341574));
#56364=CARTESIAN_POINT('Ctrl Pts',(22.3705968841926,0.345339779804043,3.73782983856348));
#56365=CARTESIAN_POINT('Ctrl Pts',(22.3944548022241,0.428734513273282,3.93535114928888));
#56366=CARTESIAN_POINT('Ctrl Pts',(22.4183127202555,0.407291980919218,4.1486808655136));
#56367=CARTESIAN_POINT('Ctrl Pts',(22.4421706382869,0.286255462618544,4.32565405918856));
#56368=CARTESIAN_POINT('Ctrl Pts',(22.4615999502279,0.130682174689606,4.40492695636159));
#56369=CARTESIAN_POINT('Ctrl Pts',(22.4730766228251,0.0307047625933256,
4.41585030288671));
#56370=CARTESIAN_POINT('Ctrl Pts',(22.4766006560785,3.63249072248342E-6,
4.41584094994071));
#56371=CARTESIAN_POINT('Ctrl Pts',(22.2733993439214,-5.11585294797612E-6,
4.41590580604266));
#56372=CARTESIAN_POINT('Ctrl Pts',(22.2739748303838,-0.0050164638240448,
4.41590888908576));
#56373=CARTESIAN_POINT('Ctrl Pts',(22.2825029561901,-0.0792779396689182,
4.41459464077989));
#56374=CARTESIAN_POINT('Ctrl Pts',(22.2989837213402,-0.221370022215225,
4.37281103827166));
#56375=CARTESIAN_POINT('Ctrl Pts',(22.3228416393716,-0.372934645290675,
4.22116172228637));
#56376=CARTESIAN_POINT('Ctrl Pts',(22.346699557403,-0.43330658847365,4.01543234121164));
#56377=CARTESIAN_POINT('Ctrl Pts',(22.3705574754345,-0.387723268841402,
3.80592933171158));
#56378=CARTESIAN_POINT('Ctrl Pts',(22.3944153934659,-0.247331046528593,
3.64388188817752));
#56379=CARTESIAN_POINT('Ctrl Pts',(22.4182733114973,-0.0464596501027702,
3.56891502119853));
#56380=CARTESIAN_POINT('Ctrl Pts',(22.4421312295287,0.165772403721094,3.59936017830047));
#56381=CARTESIAN_POINT('Ctrl Pts',(22.4659891475602,0.337468575289321,3.7277726770023));
#56382=CARTESIAN_POINT('Ctrl Pts',(22.4898470655915,0.426644514167594,3.92275218663495));
#56383=CARTESIAN_POINT('Ctrl Pts',(22.513704983623,0.411494197867752,4.13662086224655));
#56384=CARTESIAN_POINT('Ctrl Pts',(22.5375629016544,0.295722435535401,4.31708206952049));
#56385=CARTESIAN_POINT('Ctrl Pts',(22.5574610217539,0.138855410360913,4.40292493148274));
#56386=CARTESIAN_POINT('Ctrl Pts',(22.5694065025095,0.0347856757474044,
4.41583870262252));
#56387=CARTESIAN_POINT('Ctrl Pts',(22.5733993439214,-1.0582204931428E-7,
4.41583910483016));
#56388=CARTESIAN_POINT('Origin',(3.42660065607856,0.,4.));
#56389=CARTESIAN_POINT('',(21.8766006560786,1.03078286340212E-5,4.41586151989188));
#56390=CARTESIAN_POINT('',(21.9733993439214,8.40473402259622E-6,4.41585103914036));
#56391=CARTESIAN_POINT('',(3.42660065607856,4.87367679877478E-13,4.415875));
#56392=CARTESIAN_POINT('Ctrl Pts',(21.8766006560786,1.03078286340201E-5,
4.41586151989188));
#56393=CARTESIAN_POINT('Ctrl Pts',(21.8822132785738,-0.0488795353146484,
4.415816298089));
#56394=CARTESIAN_POINT('Ctrl Pts',(21.8957785404128,-0.167079919178725,
4.39498170153279));
#56395=CARTESIAN_POINT('Ctrl Pts',(21.9172964415957,-0.326407159500644,
4.28539643168872));
#56396=CARTESIAN_POINT('Ctrl Pts',(21.9411543596271,-0.423245389017799,
4.09410684177624));
#56397=CARTESIAN_POINT('Ctrl Pts',(21.9650122776585,-0.416588591947193,
3.87980556563057));
#56398=CARTESIAN_POINT('Ctrl Pts',(21.98887019569,-0.30806453650007,3.69489510271888));
#56399=CARTESIAN_POINT('Ctrl Pts',(22.0127281137213,-0.12421031036921,3.58459109808296));
#56400=CARTESIAN_POINT('Ctrl Pts',(22.0365860317528,0.0900167200678817,
3.57586588547707));
#56401=CARTESIAN_POINT('Ctrl Pts',(22.0604439497842,0.282232210442068,3.67085301705332));
#56402=CARTESIAN_POINT('Ctrl Pts',(22.0843018678157,0.405434237512275,3.8463255517439));
#56403=CARTESIAN_POINT('Ctrl Pts',(22.108159785847,0.429496549703537,4.05937567504088));
#56404=CARTESIAN_POINT('Ctrl Pts',(22.1320177038785,0.348535256241736,4.25790682842971));
#56405=CARTESIAN_POINT('Ctrl Pts',(22.1548313272889,0.18962186617866,4.38744320371645));
#56406=CARTESIAN_POINT('Ctrl Pts',(22.1696923113557,0.0601536901409818,
4.41584170838249));
#56407=CARTESIAN_POINT('Ctrl Pts',(22.1766006560786,-8.37799962077716E-6,
4.41589611849309));
#56408=CARTESIAN_POINT('Ctrl Pts',(21.9733993439214,8.40473402260317E-6,
4.41585103914036));
#56409=CARTESIAN_POINT('Ctrl Pts',(21.9785431582582,-0.044801031555974,
4.41581845947763));
#56410=CARTESIAN_POINT('Ctrl Pts',(21.9916396119388,-0.158914563981884,
4.39744691543598));
#56411=CARTESIAN_POINT('Ctrl Pts',(22.0126887049632,-0.317860118355158,
4.29488591379237));
#56412=CARTESIAN_POINT('Ctrl Pts',(22.0365466229946,-0.420290167226249,
4.10653136780738));
#56413=CARTESIAN_POINT('Ctrl Pts',(22.060404541026,-0.419947821735935,3.89212700053744));
#56414=CARTESIAN_POINT('Ctrl Pts',(22.0842624590574,-0.316916794682727,
3.70410052003731));
#56415=CARTESIAN_POINT('Ctrl Pts',(22.1081203770888,-0.136390978688423,
3.58842952252864));
#56416=CARTESIAN_POINT('Ctrl Pts',(22.1319782951203,0.0774861468089536,
3.57339871771534));
#56417=CARTESIAN_POINT('Ctrl Pts',(22.1558362131517,0.27241579873489,3.66268354680831));
#56418=CARTESIAN_POINT('Ctrl Pts',(22.1796941311831,0.400732367405962,3.83445143701846));
#56419=CARTESIAN_POINT('Ctrl Pts',(22.2035520492145,0.431058956528623,4.04670046033727));
#56420=CARTESIAN_POINT('Ctrl Pts',(22.227409967246,0.355979888945518,4.24752994899471));
#56421=CARTESIAN_POINT('Ctrl Pts',(22.2506923988149,0.197764744804664,4.38444734931837));
#56422=CARTESIAN_POINT('Ctrl Pts',(22.26602219104,0.064235283418036,4.41586628455644));
#56423=CARTESIAN_POINT('Ctrl Pts',(22.2733993439214,-5.11585294797612E-6,
4.41590580604266));
#56424=CARTESIAN_POINT('Origin',(3.42660065607856,0.,4.));
#56425=CARTESIAN_POINT('',(21.5766006560785,-1.05752387382048E-5,4.41586434469346));
#56426=CARTESIAN_POINT('',(21.6733993439214,-1.08222664516599E-5,4.41587700699864));
#56427=CARTESIAN_POINT('',(3.42660065607856,4.87367679877478E-13,4.415875));
#56428=CARTESIAN_POINT('Ctrl Pts',(21.5766006560785,-1.05752387381843E-5,
4.41586434469346));
#56429=CARTESIAN_POINT('Ctrl Pts',(21.5788289671043,-0.0194203346498642,
4.41588296395747));
#56430=CARTESIAN_POINT('Ctrl Pts',(21.5890099174739,-0.10809016089515,4.40978779866957));
#56431=CARTESIAN_POINT('Ctrl Pts',(21.6071435071872,-0.258824259222961,
4.34785450957493));
#56432=CARTESIAN_POINT('Ctrl Pts',(21.6310014252187,-0.39385182381868,4.18131050126406));
#56433=CARTESIAN_POINT('Ctrl Pts',(21.6548593432501,-0.432571889182456,
3.97043113659525));
#56434=CARTESIAN_POINT('Ctrl Pts',(21.6787172612815,-0.365516344619441,
3.76678216446856));
#56435=CARTESIAN_POINT('Ctrl Pts',(21.702575179313,-0.209082097331647,3.62016130585559));
#56436=CARTESIAN_POINT('Ctrl Pts',(21.7264330973443,-0.00152158196427748,
3.56642135455923));
#56437=CARTESIAN_POINT('Ctrl Pts',(21.7502910153758,0.206411001640417,3.61870319251831));
#56438=CARTESIAN_POINT('Ctrl Pts',(21.7741489334072,0.363870472821225,3.76422248622317));
#56439=CARTESIAN_POINT('Ctrl Pts',(21.7980068514386,0.432353701764573,3.96739580449697));
#56440=CARTESIAN_POINT('Ctrl Pts',(21.82186476947,0.395114673548107,4.17854173669174));
#56441=CARTESIAN_POINT('Ctrl Pts',(21.8457226875014,0.261259344941517,4.3460293508861));
#56442=CARTESIAN_POINT('Ctrl Pts',(21.8639679830376,0.110037800305057,4.4094070875278));
#56443=CARTESIAN_POINT('Ctrl Pts',(21.87426063923,0.0203934810735595,4.41588037378429));
#56444=CARTESIAN_POINT('Ctrl Pts',(21.8766006560786,1.03078286340201E-5,
4.41586151989188));
#56445=CARTESIAN_POINT('Ctrl Pts',(21.6733993439214,-1.0822266451653E-5,
4.41587700699864));
#56446=CARTESIAN_POINT('Ctrl Pts',(21.6751588467887,-0.0153356749568721,
4.41589290068126));
#56447=CARTESIAN_POINT('Ctrl Pts',(21.6848709889998,-0.0999166717736498,
4.41130778913604));
#56448=CARTESIAN_POINT('Ctrl Pts',(21.7025357705547,-0.248467031045983,
4.35532645760922));
#56449=CARTESIAN_POINT('Ctrl Pts',(21.7263936885861,-0.388341045935521,
4.1928315042612));
#56450=CARTESIAN_POINT('Ctrl Pts',(21.7502516066176,-0.433255096896122,
3.98318399549658));
#56451=CARTESIAN_POINT('Ctrl Pts',(21.774109524649,-0.372226475033738,3.77764845789182));
#56452=CARTESIAN_POINT('Ctrl Pts',(21.7979674426804,-0.220178340780001,
3.62648392906691));
#56453=CARTESIAN_POINT('Ctrl Pts',(21.8218253607118,-0.0142906046679706,
3.56665425395863));
#56454=CARTESIAN_POINT('Ctrl Pts',(21.8456832787432,0.195091573553633,3.61278941785858));
#56455=CARTESIAN_POINT('Ctrl Pts',(21.8695411967747,0.356768547853618,3.75360811649661));
#56456=CARTESIAN_POINT('Ctrl Pts',(21.8933991148061,0.431205894023261,3.95467634223136));
#56457=CARTESIAN_POINT('Ctrl Pts',(21.9172570328375,0.400201653291494,4.16682743688221));
#56458=CARTESIAN_POINT('Ctrl Pts',(21.941114950869,0.271337207055788,4.33818467892719));
#56459=CARTESIAN_POINT('Ctrl Pts',(21.9598290545635,0.118211900824938,4.40773087908456));
#56460=CARTESIAN_POINT('Ctrl Pts',(21.9705905189143,0.0244769910710258,
4.41586882955141));
#56461=CARTESIAN_POINT('Ctrl Pts',(21.9733993439214,8.40473402260317E-6,
4.41585103914036));
#56462=CARTESIAN_POINT('Origin',(3.42660065607856,0.,4.));
#56463=CARTESIAN_POINT('',(21.2766006560785,8.9771325895615E-6,4.41589335210553));
#56464=CARTESIAN_POINT('',(21.3733993439214,1.06214664634743E-5,4.41588075133303));
#56465=CARTESIAN_POINT('',(3.42660065607856,4.87367679877478E-13,4.415875));
#56466=CARTESIAN_POINT('Ctrl Pts',(21.2766006560785,8.97713258955941E-6,
4.41589335210553));
#56467=CARTESIAN_POINT('Ctrl Pts',(21.2833972949786,-0.0591814269577189,
4.41583723296416));
#56468=CARTESIAN_POINT('Ctrl Pts',(21.2981465732225,-0.187680420990878,
4.38813575385326));
#56469=CARTESIAN_POINT('Ctrl Pts',(21.3208484908102,-0.346716519889314,
4.26034671465164));
#56470=CARTESIAN_POINT('Ctrl Pts',(21.3447064088417,-0.429069235164158,
4.0623886883135));
#56471=CARTESIAN_POINT('Ctrl Pts',(21.368564326873,-0.406502834830527,3.8491749282489));
#56472=CARTESIAN_POINT('Ctrl Pts',(21.3924222449045,-0.284535418465691,
3.67284200661995));
#56473=CARTESIAN_POINT('Ctrl Pts',(21.4162801629359,-0.0929913416969399,
3.5765081259772));
#56474=CARTESIAN_POINT('Ctrl Pts',(21.4401380809674,0.121291651150069,3.58372954422009));
#56475=CARTESIAN_POINT('Ctrl Pts',(21.4639959989987,0.305915531372611,3.69274042788069));
#56476=CARTESIAN_POINT('Ctrl Pts',(21.4878539170302,0.415734731202803,3.87688464650718));
#56477=CARTESIAN_POINT('Ctrl Pts',(21.5117118350615,0.423895464867194,4.09113392265755));
#56478=CARTESIAN_POINT('Ctrl Pts',(21.535569753093,0.328402210690932,4.28309847227994));
#56479=CARTESIAN_POINT('Ctrl Pts',(21.5571993600986,0.169024930905334,4.39437398220882));
#56480=CARTESIAN_POINT('Ctrl Pts',(21.5708763277605,0.0498513310028489,
4.41581651349798));
#56481=CARTESIAN_POINT('Ctrl Pts',(21.5766006560785,-1.05752387381843E-5,
4.41586434469346));
#56482=CARTESIAN_POINT('Ctrl Pts',(21.3733993439214,1.06214664634605E-5,
4.41588075133303));
#56483=CARTESIAN_POINT('Ctrl Pts',(21.379727174663,-0.0551018547626871,
4.41582358345633));
#56484=CARTESIAN_POINT('Ctrl Pts',(21.3940076447484,-0.1795281855266,4.39095386216025));
#56485=CARTESIAN_POINT('Ctrl Pts',(21.4162407541777,-0.338898428465248,
4.27044521104599));
#56486=CARTESIAN_POINT('Ctrl Pts',(21.4400986722091,-0.427045644525908,
4.07499849655415));
#56487=CARTESIAN_POINT('Ctrl Pts',(21.4639565902406,-0.410768568010174,
3.86121260673678));
#56488=CARTESIAN_POINT('Ctrl Pts',(21.4878145082719,-0.294047387504818,
3.68136401506497));
#56489=CARTESIAN_POINT('Ctrl Pts',(21.5116724263034,-0.105423611064507,
3.57943060117972));
#56490=CARTESIAN_POINT('Ctrl Pts',(21.5355303443348,0.108979109962582,3.58033786138646));
#56491=CARTESIAN_POINT('Ctrl Pts',(21.5593882623662,0.296733470072461,3.68386394585134));
#56492=CARTESIAN_POINT('Ctrl Pts',(21.5832461803976,0.411928413892185,3.86469390692879));
#56493=CARTESIAN_POINT('Ctrl Pts',(21.6071040984291,0.426395639810567,4.07860989342611));
#56494=CARTESIAN_POINT('Ctrl Pts',(21.6309620164605,0.33659751701124,4.27330361969026));
#56495=CARTESIAN_POINT('Ctrl Pts',(21.6530604316246,0.177184770587036,4.39173732935402));
#56496=CARTESIAN_POINT('Ctrl Pts',(21.6672062074449,0.0539299276789421,
4.41582106406873));
#56497=CARTESIAN_POINT('Ctrl Pts',(21.6733993439214,-1.0822266451653E-5,
4.41587700699864));
#56498=CARTESIAN_POINT('Origin',(3.42660065607856,0.,4.));
#56499=CARTESIAN_POINT('',(20.9766006560786,-4.48287659654576E-6,4.41584197426197));
#56500=CARTESIAN_POINT('',(21.0733993439214,-7.65157297119567E-6,4.41584853425778));
#56501=CARTESIAN_POINT('',(3.42660065607856,4.87367679877478E-13,4.415875));
#56502=CARTESIAN_POINT('Ctrl Pts',(20.9766006560786,-4.48287659652116E-6,
4.41584197426197));
#56503=CARTESIAN_POINT('Ctrl Pts',(20.9800129835092,-0.0297322302090305,
4.41585318364051));
#56504=CARTESIAN_POINT('Ctrl Pts',(20.9913779502836,-0.128734546054536,
4.40538471300776));
#56505=CARTESIAN_POINT('Ctrl Pts',(21.0106955564018,-0.28396276796243,4.32765515869354));
#56506=CARTESIAN_POINT('Ctrl Pts',(21.0345534744332,-0.40623841344949,4.15153583326342));
#56507=CARTESIAN_POINT('Ctrl Pts',(21.0584113924646,-0.429177699343215,
3.93836186909709));
#56508=CARTESIAN_POINT('Ctrl Pts',(21.082269310496,-0.347171348131155,3.74026010679315));
#56509=CARTESIAN_POINT('Ctrl Pts',(21.1061272285274,-0.180272145040548,
3.605671823621));
#56510=CARTESIAN_POINT('Ctrl Pts',(21.1299851465589,0.0307085077608185,
3.56750752082027));
#56511=CARTESIAN_POINT('Ctrl Pts',(21.1538430645903,0.234180094072738,3.63509941005724));
#56512=CARTESIAN_POINT('Ctrl Pts',(21.1777009826217,0.380388268371489,3.79191943321731));
#56513=CARTESIAN_POINT('Ctrl Pts',(21.2015589006531,0.433581149524578,3.99962082296209));
#56514=CARTESIAN_POINT('Ctrl Pts',(21.2254168186846,0.380751629084578,4.2074149318183));
#56515=CARTESIAN_POINT('Ctrl Pts',(21.2492747367159,0.234817963878357,4.36449043997717));
#56516=CARTESIAN_POINT('Ctrl Pts',(21.2663360158473,0.0893960873046664,
4.41308118928586));
#56517=CARTESIAN_POINT('Ctrl Pts',(21.2754446556348,0.0100763257733538,
4.41590289708112));
#56518=CARTESIAN_POINT('Ctrl Pts',(21.2766006560785,8.97713258955941E-6,
4.41589335210553));
#56519=CARTESIAN_POINT('Ctrl Pts',(21.0733993439214,-7.65157297121996E-6,
4.41584853425778));
#56520=CARTESIAN_POINT('Ctrl Pts',(21.0763428631935,-0.0256500457845501,
4.41586537097631));
#56521=CARTESIAN_POINT('Ctrl Pts',(21.0872390218095,-0.120560449820324,
4.40722571769055));
#56522=CARTESIAN_POINT('Ctrl Pts',(21.1060878197692,-0.274189543318984,
4.33587624407661));
#56523=CARTESIAN_POINT('Ctrl Pts',(21.1299457378007,-0.401599180171465,
4.16343456021562));
#56524=CARTESIAN_POINT('Ctrl Pts',(21.1538036558321,-0.430806878168669,
3.95102867450389));
#56525=CARTESIAN_POINT('Ctrl Pts',(21.1776615738635,-0.354670559489406,
3.75059761183336));
#56526=CARTESIAN_POINT('Ctrl Pts',(21.2015194918949,-0.191807627993766,
3.61115222665144));
#56527=CARTESIAN_POINT('Ctrl Pts',(21.2253774099264,0.0179574932869785,
3.56679071405539));
#56528=CARTESIAN_POINT('Ctrl Pts',(21.2492353279577,0.223331518303719,3.62836067225603));
#56529=CARTESIAN_POINT('Ctrl Pts',(21.2730932459892,0.374094903668402,3.78080656934254));
#56530=CARTESIAN_POINT('Ctrl Pts',(21.2969511640206,0.433381894944723,3.98685123093373));
#56531=CARTESIAN_POINT('Ctrl Pts',(21.320809082052,0.386695207821707,4.19611112472705));
#56532=CARTESIAN_POINT('Ctrl Pts',(21.3446670000834,0.245451009020076,4.35741650656472));
#56533=CARTESIAN_POINT('Ctrl Pts',(21.3621970873732,0.0975684711839555,
4.41172139589413));
#56534=CARTESIAN_POINT('Ctrl Pts',(21.3717745353192,0.014161952170494,4.41589543043265));
#56535=CARTESIAN_POINT('Ctrl Pts',(21.3733993439214,1.06214664634605E-5,
4.41588075133303));
#56536=CARTESIAN_POINT('Origin',(3.42660065607856,0.,4.));
#56537=CARTESIAN_POINT('',(20.6766006560786,1.29204965968245E-6,4.41591114679826));
#56538=CARTESIAN_POINT('',(20.7733993439214,3.9567662055099E-6,4.41590779860895));
#56539=CARTESIAN_POINT('',(3.42660065607856,4.87367679877478E-13,4.415875));
#56540=CARTESIAN_POINT('Ctrl Pts',(20.6766006560786,1.29076178055295E-6,
4.41591111076812));
#56541=CARTESIAN_POINT('Ctrl Pts',(20.6766286720397,-0.000242659277546582,
4.41591112051333));
#56542=CARTESIAN_POINT('Ctrl Pts',(20.6846093273446,-0.0697345275278937,
4.41585145172406));
#56543=CARTESIAN_POINT('Ctrl Pts',(20.7005426219933,-0.208420567790133,
4.38020336888205));
#56544=CARTESIAN_POINT('Ctrl Pts',(20.7244005400248,-0.365106210756856,
4.23385701605743));
#56545=CARTESIAN_POINT('Ctrl Pts',(20.7482584580562,-0.432520392530856,
4.03032528343114));
#56546=CARTESIAN_POINT('Ctrl Pts',(20.7721163760876,-0.394167874571092,
3.81937870627435));
#56547=CARTESIAN_POINT('Ctrl Pts',(20.795974294119,-0.259432524437891,3.65259868360638));
#56548=CARTESIAN_POINT('Ctrl Pts',(20.8198322121504,-0.0612578225112809,
3.57076788979259));
#56549=CARTESIAN_POINT('Ctrl Pts',(20.8436901301819,0.151895538690754,3.5938959627232));
#56550=CARTESIAN_POINT('Ctrl Pts',(20.8675480482132,0.327906592802717,3.71632757520176));
#56551=CARTESIAN_POINT('Ctrl Pts',(20.8914059662447,0.423735399567132,3.90812480123879));
#56552=CARTESIAN_POINT('Ctrl Pts',(20.9152638842761,0.415949440063929,4.12238802732943));
#56553=CARTESIAN_POINT('Ctrl Pts',(20.9391218023075,0.30645246920106,4.30672404095661));
#56554=CARTESIAN_POINT('Ctrl Pts',(20.9595673929083,0.148398440326279,4.40042000858165));
#56555=CARTESIAN_POINT('Ctrl Pts',(20.9720603441653,0.0395501167658222,
4.4158270594931));
#56556=CARTESIAN_POINT('Ctrl Pts',(20.9766006560786,-4.48287659652116E-6,
4.41584197426197));
#56557=CARTESIAN_POINT('Ctrl Pts',(20.7733993439214,3.95676620551077E-6,
4.41590779860895));
#56558=CARTESIAN_POINT('Ctrl Pts',(20.7809111910678,-0.0654084660523611,
4.41587519962517));
#56559=CARTESIAN_POINT('Ctrl Pts',(20.7963756775582,-0.200102595337945,
4.3835597345012));
#56560=CARTESIAN_POINT('Ctrl Pts',(20.8197928033922,-0.358062019934396,
4.24450842127602));
#56561=CARTESIAN_POINT('Ctrl Pts',(20.8436507214237,-0.431438726014498,
4.04305074550709));
#56562=CARTESIAN_POINT('Ctrl Pts',(20.867508639455,-0.399316990859146,3.83106596928302));
#56563=CARTESIAN_POINT('Ctrl Pts',(20.8913665574865,-0.269551332195825,
3.66039017609669));
#56564=CARTESIAN_POINT('Ctrl Pts',(20.9152244755179,-0.0738730526583281,
3.57275822989076));
#56565=CARTESIAN_POINT('Ctrl Pts',(20.9390823935493,0.139869212314499,3.58959853735383));
#56566=CARTESIAN_POINT('Ctrl Pts',(20.9629403115807,0.319409638666883,3.70679317993256));
#56567=CARTESIAN_POINT('Ctrl Pts',(20.9867982296122,0.420845711130686,3.8956848776653));
#56568=CARTESIAN_POINT('Ctrl Pts',(21.0106561476436,0.419373541863394,4.11008446384341));
#56569=CARTESIAN_POINT('Ctrl Pts',(21.034514065675,0.315353119032788,4.29756540021079));
#56570=CARTESIAN_POINT('Ctrl Pts',(21.0554284644342,0.156567902793621,4.39812991232556));
#56571=CARTESIAN_POINT('Ctrl Pts',(21.0683902238497,0.0436291721249729,
4.41581988245125));
#56572=CARTESIAN_POINT('Ctrl Pts',(21.0733993439214,-7.65157297121996E-6,
4.41584853425778));
#56573=CARTESIAN_POINT('Origin',(3.42660065607856,0.,4.));
#56574=CARTESIAN_POINT('',(20.3766006560786,0.000383027521040961,4.41597069455794));
#56575=CARTESIAN_POINT('',(20.4733993439214,0.000101608071013781,4.41586489633469));
#56576=CARTESIAN_POINT('',(3.42660065607856,4.87367679877478E-13,4.415875));
#56577=CARTESIAN_POINT('Ctrl Pts',(20.3766006560786,0.000383027521040954,
4.41597069455794));
#56578=CARTESIAN_POINT('Ctrl Pts',(20.3891496392578,-0.108893832387875,
4.41487837761012));
#56579=CARTESIAN_POINT('Ctrl Pts',(20.4176039011246,-0.35839559572325,4.31454223548297));
#56580=CARTESIAN_POINT('Ctrl Pts',(20.4540108023354,-0.457800032585507,
3.97025345815189));
#56581=CARTESIAN_POINT('Ctrl Pts',(20.4858213597105,-0.325993724402262,
3.71529210935379));
#56582=CARTESIAN_POINT('Ctrl Pts',(20.509679277742,-0.15096738523986,3.59329490328468));
#56583=CARTESIAN_POINT('Ctrl Pts',(20.5335371957734,0.0630371972956549,
3.57102347342756));
#56584=CARTESIAN_POINT('Ctrl Pts',(20.5573951138048,0.260511246441404,3.65349437971329));
#56585=CARTESIAN_POINT('Ctrl Pts',(20.5812530318362,0.394877283734959,3.82077798440408));
#56586=CARTESIAN_POINT('Ctrl Pts',(20.6051109498677,0.432370081305563,4.03184236506754));
#56587=CARTESIAN_POINT('Ctrl Pts',(20.6289688678991,0.364303478986858,4.23514367899931));
#56588=CARTESIAN_POINT('Ctrl Pts',(20.6527987699694,0.207251017164088,4.38076243960928));
#56589=CARTESIAN_POINT('Ctrl Pts',(20.6686760326959,0.0690052481014253,
4.41590835422812));
#56590=CARTESIAN_POINT('Ctrl Pts',(20.6766006560786,1.29076178055295E-6,
4.41591111076812));
#56591=CARTESIAN_POINT('Ctrl Pts',(20.4733993439214,0.000101608071013788,
4.4158648963347));
#56592=CARTESIAN_POINT('Ctrl Pts',(20.4775268795984,-0.0359150725839473,
4.41584626969953));
#56593=CARTESIAN_POINT('Ctrl Pts',(20.4896070546192,-0.141401612166324,
4.40227446254147));
#56594=CARTESIAN_POINT('Ctrl Pts',(20.5096398689838,-0.298255971346869,
4.31460392554555));
#56595=CARTESIAN_POINT('Ctrl Pts',(20.5334977870152,-0.412709509332759,
4.13311446574462));
#56596=CARTESIAN_POINT('Ctrl Pts',(20.5573557050466,-0.425936384696969,
3.91915434697803));
#56597=CARTESIAN_POINT('Ctrl Pts',(20.581213623078,-0.335173342752607,3.72492109335083));
#56598=CARTESIAN_POINT('Ctrl Pts',(20.6050715411095,-0.162364888615448,
3.59797442377207));
#56599=CARTESIAN_POINT('Ctrl Pts',(20.6289294591408,0.0501004451364318,
3.56932214892951));
#56600=CARTESIAN_POINT('Ctrl Pts',(20.6527873771723,0.250339089241223,3.64598859455508));
#56601=CARTESIAN_POINT('Ctrl Pts',(20.6766452952037,0.389350172549011,3.80921715950176));
#56602=CARTESIAN_POINT('Ctrl Pts',(20.7005032132352,0.433161330121289,4.01909908002448));
#56603=CARTESIAN_POINT('Ctrl Pts',(20.7243611312665,0.371049143609512,4.22430982617278));
#56604=CARTESIAN_POINT('Ctrl Pts',(20.748219049298,0.218207240773441,4.37467120177868));
#56605=CARTESIAN_POINT('Ctrl Pts',(20.7645651201829,0.0769305199015265,
4.41491906931248));
#56606=CARTESIAN_POINT('Ctrl Pts',(20.772958551724,0.00384233167249433,
4.41590971150433));
#56607=CARTESIAN_POINT('Ctrl Pts',(20.7733993439214,3.95676620551077E-6,
4.41590779860895));
#56608=CARTESIAN_POINT('Origin',(3.42660065607856,0.,4.));
#56609=CARTESIAN_POINT('',(20.0766006560786,-0.000186622634748148,4.41645953600834));
#56610=CARTESIAN_POINT('',(20.1733993439214,-0.000111611226006447,4.41653056081536));
#56611=CARTESIAN_POINT('',(3.42660065607856,4.87367679877478E-13,4.415875));
#56612=CARTESIAN_POINT('Ctrl Pts',(20.0766006560786,-0.000186622634748109,
4.41645953600834));
#56613=CARTESIAN_POINT('Ctrl Pts',(20.0778126884445,-0.0107019642254321,
4.4165186149328));
#56614=CARTESIAN_POINT('Ctrl Pts',(20.0949299994981,-0.159149739060163,
4.41138240526969));
#56615=CARTESIAN_POINT('Ctrl Pts',(20.1279525892393,-0.432744382500041,
4.23375285658289));
#56616=CARTESIAN_POINT('Ctrl Pts',(20.1756684253021,-0.430649333670284,
3.76246031529274));
#56617=CARTESIAN_POINT('Ctrl Pts',(20.223384261365,-0.033136228617316,3.50924504180455));
#56618=CARTESIAN_POINT('Ctrl Pts',(20.2711000974278,0.394908089060633,3.70680919012016));
#56619=CARTESIAN_POINT('Ctrl Pts',(20.3188159334906,0.460110046434968,4.17340395051402));
#56620=CARTESIAN_POINT('Ctrl Pts',(20.3539827863742,0.197028357007358,4.40022211154544));
#56621=CARTESIAN_POINT('Ctrl Pts',(20.3732443605702,0.0296097328916507,
4.416262840815));
#56622=CARTESIAN_POINT('Ctrl Pts',(20.3766006560786,0.000383027521040954,
4.41597069455794));
#56623=CARTESIAN_POINT('Ctrl Pts',(20.1733993439214,-0.000111611226006447,
4.41653056081536));
#56624=CARTESIAN_POINT('Ctrl Pts',(20.1741425681289,-0.00655727229825777,
4.41655465488103));
#56625=CARTESIAN_POINT('Ctrl Pts',(20.190791071024,-0.150919726673813,4.41348743992374));
#56626=CARTESIAN_POINT('Ctrl Pts',(20.2233448526067,-0.425711472830213,
4.24633918020534));
#56627=CARTESIAN_POINT('Ctrl Pts',(20.2710606886696,-0.437384262562023,
3.77535541015343));
#56628=CARTESIAN_POINT('Ctrl Pts',(20.3187765247324,-0.0477164433392854,
3.51022640082505));
#56629=CARTESIAN_POINT('Ctrl Pts',(20.3664923607953,0.386374384143037,3.69571627142296));
#56630=CARTESIAN_POINT('Ctrl Pts',(20.4062555575143,0.45143962727185,4.08165775845481));
#56631=CARTESIAN_POINT('Ctrl Pts',(20.4380661148895,0.291471375703242,4.31996082336987));
#56632=CARTESIAN_POINT('Ctrl Pts',(20.4577964972439,0.136183087716603,4.40372206768731));
#56633=CARTESIAN_POINT('Ctrl Pts',(20.4695742402546,0.0334792813416625,
4.41588215816259));
#56634=CARTESIAN_POINT('Ctrl Pts',(20.4733993439214,0.000101608071013788,
4.4158648963347));
#56635=CARTESIAN_POINT('Origin',(3.42660065607856,0.,4.));
#56636=CARTESIAN_POINT('',(19.7766006560786,-0.000280998963924209,4.41539029291088));
#56637=CARTESIAN_POINT('',(19.8733993439214,-0.000322938566065189,4.41548189938477));
#56638=CARTESIAN_POINT('',(3.42660065607856,4.87367679877478E-13,4.415875));
#56639=CARTESIAN_POINT('Ctrl Pts',(19.7766006560786,-0.000280998963924181,
4.41539029291088));
#56640=CARTESIAN_POINT('Ctrl Pts',(19.7823810163188,-0.0507615353771658,
4.41570272077311));
#56641=CARTESIAN_POINT('Ctrl Pts',(19.8040666552467,-0.23976299482565,4.3837755623668));
#56642=CARTESIAN_POINT('Ctrl Pts',(19.8416575728622,-0.481212499922896,
4.10168523844358));
#56643=CARTESIAN_POINT('Ctrl Pts',(19.8893734089251,-0.345789702982467,
3.65023692191923));
#56644=CARTESIAN_POINT('Ctrl Pts',(19.9370892449879,0.107175910646637,3.51998011832295));
#56645=CARTESIAN_POINT('Ctrl Pts',(19.9848050810508,0.461722480014006,3.83053541934297));
#56646=CARTESIAN_POINT('Ctrl Pts',(20.0313088847476,0.394022427012164,4.28486673161383));
#56647=CARTESIAN_POINT('Ctrl Pts',(20.0619074097569,0.127288937001902,4.4157433330307));
#56648=CARTESIAN_POINT('Ctrl Pts',(20.0766006560786,-0.000186622634748109,
4.41645953600834));
#56649=CARTESIAN_POINT('Ctrl Pts',(19.8733993439214,-0.000322938566065196,
4.41548189938477));
#56650=CARTESIAN_POINT('Ctrl Pts',(19.8787108960032,-0.0466836533228258,
4.41581668875846));
#56651=CARTESIAN_POINT('Ctrl Pts',(19.8999277267727,-0.231469429366377,
4.38724295332581));
#56652=CARTESIAN_POINT('Ctrl Pts',(19.9370498362297,-0.47800980043334,4.11581244897344));
#56653=CARTESIAN_POINT('Ctrl Pts',(19.9847656722926,-0.355939225796451,
3.66057517601247));
#56654=CARTESIAN_POINT('Ctrl Pts',(20.0324815083554,0.0929888682922082,
3.51702731322357));
#56655=CARTESIAN_POINT('Ctrl Pts',(20.0801973444182,0.456536973876988,3.81701888067549));
#56656=CARTESIAN_POINT('Ctrl Pts',(20.1271699562736,0.401683300383188,4.27772103607547));
#56657=CARTESIAN_POINT('Ctrl Pts',(20.1582372894413,0.131382308576697,4.41603903277767));
#56658=CARTESIAN_POINT('Ctrl Pts',(20.1733993439214,-0.000111611226006447,
4.41653056081536));
#56659=CARTESIAN_POINT('Origin',(3.42660065607856,0.,4.));
#56660=CARTESIAN_POINT('',(19.4766006560786,0.000302289446139524,4.41543216566181));
#56661=CARTESIAN_POINT('',(19.5733993439214,0.000255464646300079,4.41534829948978));
#56662=CARTESIAN_POINT('',(3.42660065607856,4.87367679877478E-13,4.415875));
#56663=CARTESIAN_POINT('Ctrl Pts',(19.4766006560786,0.000302289446139546,
4.41543216566181));
#56664=CARTESIAN_POINT('Ctrl Pts',(19.4869493441932,-0.0900510892866153,
4.41482666801407));
#56665=CARTESIAN_POINT('Ctrl Pts',(19.5132033109954,-0.320168095705801,
4.3413809155508));
#56666=CARTESIAN_POINT('Ctrl Pts',(19.5553625564852,-0.490312813065352,
3.96128857502183));
#56667=CARTESIAN_POINT('Ctrl Pts',(19.603078392548,-0.232620797759261,3.56664935826393));
#56668=CARTESIAN_POINT('Ctrl Pts',(19.6507942286109,0.238690449241969,3.56996267500769));
#56669=CARTESIAN_POINT('Ctrl Pts',(19.6985100646737,0.490808633485035,3.96818593857384));
#56670=CARTESIAN_POINT('Ctrl Pts',(19.7404455404963,0.316268156276861,4.34384396940031));
#56671=CARTESIAN_POINT('Ctrl Pts',(19.7664757376312,0.0881410531427697,
4.41484304213512));
#56672=CARTESIAN_POINT('Ctrl Pts',(19.7766006560786,-0.000280998963924181,
4.41539029291088));
#56673=CARTESIAN_POINT('Ctrl Pts',(19.5733993439214,0.000255464646300094,
4.41534829948978));
#56674=CARTESIAN_POINT('Ctrl Pts',(19.5832792238775,-0.0860485087386658,
4.41486588036018));
#56675=CARTESIAN_POINT('Ctrl Pts',(19.6090643825213,-0.311990568344336,
4.34649332259355));
#56676=CARTESIAN_POINT('Ctrl Pts',(19.6507548198527,-0.491240257057309,
3.97574594767572));
#56677=CARTESIAN_POINT('Ctrl Pts',(19.6984706559155,-0.245282818621706,
3.57368850533185));
#56678=CARTESIAN_POINT('Ctrl Pts',(19.7461864919783,0.225921452997342,3.56311925573479));
#56679=CARTESIAN_POINT('Ctrl Pts',(19.7939023280412,0.489658867576397,3.95374471702426));
#56680=CARTESIAN_POINT('Ctrl Pts',(19.8363066120222,0.324430886710512,4.33863507066385));
#56681=CARTESIAN_POINT('Ctrl Pts',(19.8628056173156,0.0921420753912029,
4.4148141723173));
#56682=CARTESIAN_POINT('Ctrl Pts',(19.8733993439214,-0.000322938566065196,
4.41548189938477));
#56683=CARTESIAN_POINT('Origin',(3.42660065607856,0.,4.));
#56684=CARTESIAN_POINT('',(19.1766006560786,0.000155842099650094,4.41649089206047));
#56685=CARTESIAN_POINT('',(19.2733993439214,0.000220989830587742,4.4164164649367));
#56686=CARTESIAN_POINT('',(3.42660065607856,4.87367679877478E-13,4.415875));
#56687=CARTESIAN_POINT('Ctrl Pts',(19.1766006560786,0.000155842099650088,
4.41649089206047));
#56688=CARTESIAN_POINT('Ctrl Pts',(19.1915176720675,-0.129233580897558,
4.41587069825202));
#56689=CARTESIAN_POINT('Ctrl Pts',(19.2223399667441,-0.397695790553126,
4.28149179527637));
#56690=CARTESIAN_POINT('Ctrl Pts',(19.2690675401082,-0.459293044881286,
3.82405931712685));
#56691=CARTESIAN_POINT('Ctrl Pts',(19.316783376171,-0.100417177000157,3.51852142809106));
#56692=CARTESIAN_POINT('Ctrl Pts',(19.3644992122339,0.350673329058588,3.65513271950473));
#56693=CARTESIAN_POINT('Ctrl Pts',(19.4122150482967,0.479735122332443,4.10844094226069));
#56694=CARTESIAN_POINT('Ctrl Pts',(19.4495821962449,0.235804435834584,4.38544967282755));
#56695=CARTESIAN_POINT('Ctrl Pts',(19.4710440655056,0.0488163355692654,
4.4157572795781));
#56696=CARTESIAN_POINT('Ctrl Pts',(19.4766006560786,0.000302289446139546,
4.41543216566181));
#56697=CARTESIAN_POINT('Ctrl Pts',(19.2733993439214,0.000220989830587761,
4.4164164649367));
#56698=CARTESIAN_POINT('Ctrl Pts',(19.2878475517519,-0.125161313229646,
4.41561068768233));
#56699=CARTESIAN_POINT('Ctrl Pts',(19.31820103827,-0.389985711500173,4.28851341748863));
#56700=CARTESIAN_POINT('Ctrl Pts',(19.3644598034757,-0.464275578741542,
3.8376626582024));
#56701=CARTESIAN_POINT('Ctrl Pts',(19.4121756395385,-0.114554038379521,
3.52168776344319));
#56702=CARTESIAN_POINT('Ctrl Pts',(19.4598914756013,0.340364234683876,3.64495435060606));
#56703=CARTESIAN_POINT('Ctrl Pts',(19.5076073116642,0.482720800247919,4.09426482953845));
#56704=CARTESIAN_POINT('Ctrl Pts',(19.5454432677708,0.244097666198316,4.38190156491584));
#56705=CARTESIAN_POINT('Ctrl Pts',(19.5673739451899,0.0528892875329133,
4.41564251031262));
#56706=CARTESIAN_POINT('Ctrl Pts',(19.5733993439214,0.000255464646300094,
4.41534829948978));
#56707=CARTESIAN_POINT('Origin',(3.42660065607856,0.,4.));
#56708=CARTESIAN_POINT('',(18.8766006560785,-0.00038196507782994,4.41590683121974));
#56709=CARTESIAN_POINT('',(18.9733993439214,-0.000368287616214491,4.41603142687637));
#56710=CARTESIAN_POINT('',(3.42660065607856,4.87367679877478E-13,4.415875));
#56711=CARTESIAN_POINT('Ctrl Pts',(18.8766006560785,-0.000381965077829925,
4.41590683121974));
#56712=CARTESIAN_POINT('Ctrl Pts',(18.8801807212542,-0.0315488007868432,
4.41619587167324));
#56713=CARTESIAN_POINT('Ctrl Pts',(18.8996660651174,-0.200861076696893,
4.39874895857547));
#56714=CARTESIAN_POINT('Ctrl Pts',(18.9350566876684,-0.462607878309702,
4.16703046362027));
#56715=CARTESIAN_POINT('Ctrl Pts',(18.9827725237311,-0.39069124519864,3.70122654773242));
#56716=CARTESIAN_POINT('Ctrl Pts',(19.030488359794,0.0400031699426168,3.50979089028978));
#56717=CARTESIAN_POINT('Ctrl Pts',(19.0782041958568,0.433962058584907,3.76852180111673));
#56718=CARTESIAN_POINT('Ctrl Pts',(19.1259200319197,0.429406911488226,4.23982270375453));
#56719=CARTESIAN_POINT('Ctrl Pts',(19.1587188519936,0.155221332864305,4.41240136130926));
#56720=CARTESIAN_POINT('Ctrl Pts',(19.1756123933799,0.00872798149047904,
4.41653198033223));
#56721=CARTESIAN_POINT('Ctrl Pts',(19.1766006560786,0.000155842099650088,
4.41649089206047));
#56722=CARTESIAN_POINT('Ctrl Pts',(18.9733993439214,-0.000368287616214533,
4.41603142687637));
#56723=CARTESIAN_POINT('Ctrl Pts',(18.9765106009386,-0.0274330213022572,
4.4162811262788));
#56724=CARTESIAN_POINT('Ctrl Pts',(18.9955271366434,-0.192586232161443,
4.40152565608163));
#56725=CARTESIAN_POINT('Ctrl Pts',(19.0304489510358,-0.457487847288108,
4.18058265263639));
#56726=CARTESIAN_POINT('Ctrl Pts',(19.0781647870987,-0.399321187381313,
3.71286272589862));
#56727=CARTESIAN_POINT('Ctrl Pts',(19.1258806231614,0.0255482632835279,
3.50882537619781));
#56728=CARTESIAN_POINT('Ctrl Pts',(19.1735964592243,0.426956350589889,3.75584124112414));
#56729=CARTESIAN_POINT('Ctrl Pts',(19.2213122952871,0.436283851722622,4.22707185138688));
#56730=CARTESIAN_POINT('Ctrl Pts',(19.2545799235195,0.163455264474221,4.41023200720537));
#56731=CARTESIAN_POINT('Ctrl Pts',(19.2719422730642,0.0128655269200745,
4.41649772584937));
#56732=CARTESIAN_POINT('Ctrl Pts',(19.2733993439214,0.000220989830587761,
4.4164164649367));
#56733=CARTESIAN_POINT('Origin',(3.42660065607856,0.,4.));
#56734=CARTESIAN_POINT('',(18.5766006560786,2.82854505807383E-5,4.41518799822097));
#56735=CARTESIAN_POINT('',(18.6733993439214,-3.94222854199766E-5,4.41518963037823));
#56736=CARTESIAN_POINT('',(3.42660065607856,4.87367679877478E-13,4.415875));
#56737=CARTESIAN_POINT('Ctrl Pts',(18.5766006560786,2.82854505807215E-5,
4.41518799822097));
#56738=CARTESIAN_POINT('Ctrl Pts',(18.5847490491285,-0.0712192880865648,
4.41514491699706));
#56739=CARTESIAN_POINT('Ctrl Pts',(18.6088027208661,-0.281596950705947,
4.36382162423513));
#56740=CARTESIAN_POINT('Ctrl Pts',(18.6487616712913,-0.49096944006335,4.0292272779409));
#56741=CARTESIAN_POINT('Ctrl Pts',(18.6964775073541,-0.290120809601049,
3.60284116440841));
#56742=CARTESIAN_POINT('Ctrl Pts',(18.744193343417,0.177150224400508,3.54117212067402));
#56743=CARTESIAN_POINT('Ctrl Pts',(18.7919091794797,0.481741481528227,3.90085177849878));
#56744=CARTESIAN_POINT('Ctrl Pts',(18.836044950367,0.354281053487698,4.31776308733785));
#56745=CARTESIAN_POINT('Ctrl Pts',(18.8642754425666,0.106917172161326,4.4149117417093));
#56746=CARTESIAN_POINT('Ctrl Pts',(18.8766006560785,-0.000381965077829925,
4.41590683121974));
#56747=CARTESIAN_POINT('Ctrl Pts',(18.6733993439214,-3.94222854199489E-5,
4.41518963037823));
#56748=CARTESIAN_POINT('Ctrl Pts',(18.6810789288129,-0.0671871929144198,
4.41524623173262));
#56749=CARTESIAN_POINT('Ctrl Pts',(18.704663792392,-0.273330541024821,4.36810584919535));
#56750=CARTESIAN_POINT('Ctrl Pts',(18.7441539346588,-0.489895661254576,
4.0436745456279));
#56751=CARTESIAN_POINT('Ctrl Pts',(18.7918697707216,-0.301692008317894,
3.6115580391236));
#56752=CARTESIAN_POINT('Ctrl Pts',(18.8395856067845,0.163560057986223,3.53615376224111));
#56753=CARTESIAN_POINT('Ctrl Pts',(18.8873014428472,0.478612406344963,3.88670662268212));
#56754=CARTESIAN_POINT('Ctrl Pts',(18.9319060218929,0.362263203066427,4.31165738429376));
#56755=CARTESIAN_POINT('Ctrl Pts',(18.960605322251,0.110926532249199,4.41500462017153));
#56756=CARTESIAN_POINT('Ctrl Pts',(18.9733993439214,-0.000368287616214533,
4.41603142687637));
#56757=CARTESIAN_POINT('Origin',(3.42660065607856,0.,4.));
#56758=CARTESIAN_POINT('',(18.2766006560786,0.000371443240938316,4.41601098728712));
#56759=CARTESIAN_POINT('',(18.3733993439214,0.000382963303967143,4.41588626824893));
#56760=CARTESIAN_POINT('',(3.42660065607856,4.87367679877478E-13,4.415875));
#56761=CARTESIAN_POINT('Ctrl Pts',(18.2766006560785,0.000371443240938293,
4.41601098728712));
#56762=CARTESIAN_POINT('Ctrl Pts',(18.2893173770028,-0.110264925490287,
4.41498710445335));
#56763=CARTESIAN_POINT('Ctrl Pts',(18.3179393766147,-0.360950442388199,
4.31267773405576));
#56764=CARTESIAN_POINT('Ctrl Pts',(18.3624666549143,-0.479157019140895,
3.88903254594255));
#56765=CARTESIAN_POINT('Ctrl Pts',(18.4101824909771,-0.165810997523729,
3.5369536330429));
#56766=CARTESIAN_POINT('Ctrl Pts',(18.4578983270399,0.299801814449608,3.61009732380414));
#56767=CARTESIAN_POINT('Ctrl Pts',(18.5056141631028,0.49010200717001,4.04129464153984));
#56768=CARTESIAN_POINT('Ctrl Pts',(18.5451816061157,0.274694351318236,4.36741107590602));
#56769=CARTESIAN_POINT('Ctrl Pts',(18.5688437704409,0.0678526130816757,
4.41522900951301));
#56770=CARTESIAN_POINT('Ctrl Pts',(18.5766006560786,2.82854505807215E-5,
4.41518799822097));
#56771=CARTESIAN_POINT('Ctrl Pts',(18.3733993439214,0.000382963303967157,
4.41588626824893));
#56772=CARTESIAN_POINT('Ctrl Pts',(18.3856472566872,-0.106256708375174,
4.41489942083623));
#56773=CARTESIAN_POINT('Ctrl Pts',(18.4138004481407,-0.352960303644862,
4.31875095920395));
#56774=CARTESIAN_POINT('Ctrl Pts',(18.4578589182817,-0.482217355384067,
3.90319273261591));
#56775=CARTESIAN_POINT('Ctrl Pts',(18.5055747543446,-0.179376629827252,
3.54203793877243));
#56776=CARTESIAN_POINT('Ctrl Pts',(18.5532905904074,0.288188414964166,3.60143675240633));
#56777=CARTESIAN_POINT('Ctrl Pts',(18.6010064264702,0.491105603945206,4.02684232898929));
#56778=CARTESIAN_POINT('Ctrl Pts',(18.6410426776416,0.282958802096416,4.36309886994028));
#56779=CARTESIAN_POINT('Ctrl Pts',(18.6651736501253,0.0718833454275778,
4.41512900400112));
#56780=CARTESIAN_POINT('Ctrl Pts',(18.6733993439214,-3.94222854199489E-5,
4.41518963037823));
#56781=CARTESIAN_POINT('Origin',(3.42660065607856,0.,4.));
#56782=CARTESIAN_POINT('',(17.9766006560786,-0.000210814279110197,4.41643020456723));
#56783=CARTESIAN_POINT('',(18.0733993439214,-0.000144384975211464,4.41650095473263));
#56784=CARTESIAN_POINT('',(3.42660065607856,4.87367679877478E-13,4.415875));
#56785=CARTESIAN_POINT('Ctrl Pts',(17.9766006560786,-0.000210814279110157,
4.41643020456723));
#56786=CARTESIAN_POINT('Ctrl Pts',(17.9779804261896,-0.0121834889824064,
4.41650424974197));
#56787=CARTESIAN_POINT('Ctrl Pts',(17.9952654749882,-0.162096873242269,
4.41059855206721));
#56788=CARTESIAN_POINT('Ctrl Pts',(18.0284558024744,-0.435175833605105,
4.22918817311999));
#56789=CARTESIAN_POINT('Ctrl Pts',(18.0761716385373,-0.428137176707308,
3.75791781814212));
#56790=CARTESIAN_POINT('Ctrl Pts',(18.1238874746,-0.0279335627019553,3.5089552556775));
#56791=CARTESIAN_POINT('Ctrl Pts',(18.1716033106629,0.397921871745719,3.71092663761881));
#56792=CARTESIAN_POINT('Ctrl Pts',(18.2193191467257,0.458359528554279,4.17835853620019));
#56793=CARTESIAN_POINT('Ctrl Pts',(18.2543182618643,0.193950155243433,4.40107745006558));
#56794=CARTESIAN_POINT('Ctrl Pts',(18.2734120983152,0.0281121206155762,
4.41626771302466));
#56795=CARTESIAN_POINT('Ctrl Pts',(18.2766006560785,0.000371443240938293,
4.41601098728712));
#56796=CARTESIAN_POINT('Ctrl Pts',(18.0733993439214,-0.000144384975211439,
4.41650095473263));
#56797=CARTESIAN_POINT('Ctrl Pts',(18.0743103058739,-0.00804551399413891,
4.41653639380418));
#56798=CARTESIAN_POINT('Ctrl Pts',(18.0911265465141,-0.153864670001157,
4.41274680364665));
#56799=CARTESIAN_POINT('Ctrl Pts',(18.1238480658419,-0.428237044548737,
4.24190547436581));
#56800=CARTESIAN_POINT('Ctrl Pts',(18.1715639019047,-0.435081213444543,
3.7706322547532));
#56801=CARTESIAN_POINT('Ctrl Pts',(18.2192797379675,-0.0423836094492617,
3.50999096487715));
#56802=CARTESIAN_POINT('Ctrl Pts',(18.2669955740304,0.389235515258945,3.69933251171255));
#56803=CARTESIAN_POINT('Ctrl Pts',(18.3147114100932,0.463413677146622,4.16478163940629));
#56804=CARTESIAN_POINT('Ctrl Pts',(18.3501793333902,0.202226156869028,4.39827758107438));
#56805=CARTESIAN_POINT('Ctrl Pts',(18.3697419779996,0.0322267809866215,
4.41618095209965));
#56806=CARTESIAN_POINT('Ctrl Pts',(18.3733993439214,0.000382963303967157,
4.41588626824893));
#56807=CARTESIAN_POINT('Origin',(3.42660065607856,0.,4.));
#56808=CARTESIAN_POINT('',(17.6766006560786,-0.000263771022561219,4.41536107794487));
#56809=CARTESIAN_POINT('',(17.7733993439214,-0.000309142357869163,4.41544738986064));
#56810=CARTESIAN_POINT('',(3.42660065607856,4.87367679877478E-13,4.415875));
#56811=CARTESIAN_POINT('Ctrl Pts',(17.6766006560786,-0.000263771022561289,
4.41536107794487));
#56812=CARTESIAN_POINT('Ctrl Pts',(17.6825487540639,-0.0522183410383149,
4.41566152300153));
#56813=CARTESIAN_POINT('Ctrl Pts',(17.7044021307368,-0.24273028972288,4.38249735042552));
#56814=CARTESIAN_POINT('Ctrl Pts',(17.7421607860973,-0.48225726547346,4.09660825404716));
#56815=CARTESIAN_POINT('Ctrl Pts',(17.7898766221602,-0.342084653792828,
3.64661166616396));
#56816=CARTESIAN_POINT('Ctrl Pts',(17.837592458223,0.112229559114723,3.52113702282083));
#56817=CARTESIAN_POINT('Ctrl Pts',(17.8853082942859,0.463481641013499,3.83540961967535));
#56818=CARTESIAN_POINT('Ctrl Pts',(17.9316443602377,0.391261919872151,4.28736986940801));
#56819=CARTESIAN_POINT('Ctrl Pts',(17.962075147502,0.125831334120538,4.41565069513148));
#56820=CARTESIAN_POINT('Ctrl Pts',(17.9766006560786,-0.000210814279110157,
4.41643020456723));
#56821=CARTESIAN_POINT('Ctrl Pts',(17.7733993439214,-0.000309142357869142,
4.41544738986064));
#56822=CARTESIAN_POINT('Ctrl Pts',(17.7788786337482,-0.0481438769258273,
4.41577602216682));
#56823=CARTESIAN_POINT('Ctrl Pts',(17.8002632022627,-0.23443694547481,4.38601982759396));
#56824=CARTESIAN_POINT('Ctrl Pts',(17.8375530494648,-0.479202773223469,
4.11076970247734));
#56825=CARTESIAN_POINT('Ctrl Pts',(17.8852688855277,-0.352344189444135,
3.65683998336499));
#56826=CARTESIAN_POINT('Ctrl Pts',(17.9329847215905,0.0980774850139738,
3.51803938772416));
#56827=CARTESIAN_POINT('Ctrl Pts',(17.9807005576534,0.458433095867658,3.82183063825345));
#56828=CARTESIAN_POINT('Ctrl Pts',(18.0275054317636,0.3989600628602,4.28031410431705));
#56829=CARTESIAN_POINT('Ctrl Pts',(18.0584050271863,0.129907183855675,4.41591763216682));
#56830=CARTESIAN_POINT('Ctrl Pts',(18.0733993439214,-0.000144384975211439,
4.41650095473263));
#56831=CARTESIAN_POINT('Origin',(3.42660065607856,0.,4.));
#56832=CARTESIAN_POINT('',(17.3766006560786,0.000316824918469052,4.41546566829253));
#56833=CARTESIAN_POINT('',(17.4733993439214,0.000273208168652644,4.41537657040552));
#56834=CARTESIAN_POINT('',(3.42660065607856,4.87367679877478E-13,4.415875));
#56835=CARTESIAN_POINT('Ctrl Pts',(17.3766006560786,0.000316824918469058,
4.41546566829253));
#56836=CARTESIAN_POINT('Ctrl Pts',(17.3871170819382,-0.0914824399419538,
4.4148173972429));
#56837=CARTESIAN_POINT('Ctrl Pts',(17.4135387864855,-0.323087181591141,
4.33950699049548));
#56838=CARTESIAN_POINT('Ctrl Pts',(17.4558657697204,-0.489877595596684,
3.956123284257));
#56839=CARTESIAN_POINT('Ctrl Pts',(17.5035816057832,-0.228040769637767,
3.56422180844494));
#56840=CARTESIAN_POINT('Ctrl Pts',(17.551297441846,0.243209403937772,3.57250215124727));
#56841=CARTESIAN_POINT('Ctrl Pts',(17.5990132779089,0.491116639619549,3.97336034645914));
#56842=CARTESIAN_POINT('Ctrl Pts',(17.6407810159864,0.313340775136121,4.34566293955037));
#56843=CARTESIAN_POINT('Ctrl Pts',(17.6666434753763,0.0867087440962768,
4.41485812965324));
#56844=CARTESIAN_POINT('Ctrl Pts',(17.6766006560786,-0.000263771022561289,
4.41536107794487));
#56845=CARTESIAN_POINT('Ctrl Pts',(17.4733993439214,0.000273208168652693,
4.41537657040552));
#56846=CARTESIAN_POINT('Ctrl Pts',(17.4834469616226,-0.0874810350323011,
4.41484969107387));
#56847=CARTESIAN_POINT('Ctrl Pts',(17.5093998580114,-0.314919534962053,
4.34468516187688));
#56848=CARTESIAN_POINT('Ctrl Pts',(17.5512580330878,-0.490957336521241,
3.97057010757845));
#56849=CARTESIAN_POINT('Ctrl Pts',(17.5989738691507,-0.240776309167652,
3.57112706567612));
#56850=CARTESIAN_POINT('Ctrl Pts',(17.6466897052135,0.230513307714322,3.56552463842171));
#56851=CARTESIAN_POINT('Ctrl Pts',(17.6944055412763,0.490119007219086,3.95890762096741));
#56852=CARTESIAN_POINT('Ctrl Pts',(17.7366420875123,0.321513805022658,4.34052027563639));
#56853=CARTESIAN_POINT('Ctrl Pts',(17.7629733550606,0.090710757213051,4.41482206853766));
#56854=CARTESIAN_POINT('Ctrl Pts',(17.7733993439214,-0.000309142357869142,
4.41544738986064));
#56855=CARTESIAN_POINT('Origin',(3.42660065607856,0.,4.));
#56856=CARTESIAN_POINT('',(17.0766006560786,0.000130763213737631,4.41651185352269));
#56857=CARTESIAN_POINT('',(17.1733993439214,0.000198609043858391,4.41644558073401));
#56858=CARTESIAN_POINT('',(3.42660065607856,4.87367679877478E-13,4.415875));
#56859=CARTESIAN_POINT('Ctrl Pts',(17.0766006560786,0.000130763213737628,
4.41651185352269));
#56860=CARTESIAN_POINT('Ctrl Pts',(17.0916854098125,-0.130696083011285,
4.41597403242798));
#56861=CARTESIAN_POINT('Ctrl Pts',(17.1226754422341,-0.400436570105288,
4.2789290971087));
#56862=CARTESIAN_POINT('Ctrl Pts',(17.1695707533433,-0.457413284126125,
3.81922856321607));
#56863=CARTESIAN_POINT('Ctrl Pts',(17.2172865894061,-0.0953372598908034,
3.51748986360026));
#56864=CARTESIAN_POINT('Ctrl Pts',(17.265002425469,0.354288437054553,3.6588476466131));
#56865=CARTESIAN_POINT('Ctrl Pts',(17.3127182615318,0.478565610824392,4.11349088504481));
#56866=CARTESIAN_POINT('Ctrl Pts',(17.349917671735,0.232837083242772,4.38668157013213));
#56867=CARTESIAN_POINT('Ctrl Pts',(17.3712118032506,0.0473568302064652,
4.41579785693967));
#56868=CARTESIAN_POINT('Ctrl Pts',(17.3766006560786,0.000316824918469058,
4.41546566829253));
#56869=CARTESIAN_POINT('Ctrl Pts',(17.1733993439214,0.000198609043858397,
4.41644558073401));
#56870=CARTESIAN_POINT('Ctrl Pts',(17.1880152894969,-0.126615914365149,
4.41569892234974));
#56871=CARTESIAN_POINT('Ctrl Pts',(17.2185365137601,-0.392752582168809,
4.28602487069057));
#56872=CARTESIAN_POINT('Ctrl Pts',(17.2649630167107,-0.462538907526291,
3.83277863809798));
#56873=CARTESIAN_POINT('Ctrl Pts',(17.3126788527736,-0.109506707187599,
3.52050703244687));
#56874=CARTESIAN_POINT('Ctrl Pts',(17.3603946888365,0.344087187338735,3.64856119684745));
#56875=CARTESIAN_POINT('Ctrl Pts',(17.4081105248993,0.481700523269991,4.09934702176407));
#56876=CARTESIAN_POINT('Ctrl Pts',(17.4457787432609,0.241130489326423,4.3831889686244));
#56877=CARTESIAN_POINT('Ctrl Pts',(17.467541682935,0.0514330574063097,4.41568373580506));
#56878=CARTESIAN_POINT('Ctrl Pts',(17.4733993439214,0.000273208168652693,
4.41537657040552));
#56879=CARTESIAN_POINT('Origin',(3.42660065607856,0.,4.));
#56880=CARTESIAN_POINT('',(16.7766006560786,-0.000383680820852129,4.41586226484778));
#56881=CARTESIAN_POINT('',(16.8733993439214,-0.000374684679869397,4.41598699190495));
#56882=CARTESIAN_POINT('',(3.42660065607856,4.87367679877478E-13,4.415875));
#56883=CARTESIAN_POINT('Ctrl Pts',(16.7766006560786,-0.000383680820852189,
4.41586226484779));
#56884=CARTESIAN_POINT('Ctrl Pts',(16.7803484589992,-0.0330197262611539,
4.41616320579436));
#56885=CARTESIAN_POINT('Ctrl Pts',(16.8000015406075,-0.203823433586872,
4.39772119122577));
#56886=CARTESIAN_POINT('Ctrl Pts',(16.8355599009034,-0.464342533291602,
4.16214572651883));
#56887=CARTESIAN_POINT('Ctrl Pts',(16.8832757369663,-0.387520750342007,
3.69712561530174));
#56888=CARTESIAN_POINT('Ctrl Pts',(16.9309915730291,0.0451673004198413,
3.51023971187451));
#56889=CARTESIAN_POINT('Ctrl Pts',(16.978707409092,0.436377524217892,3.7731082169636));
#56890=CARTESIAN_POINT('Ctrl Pts',(17.0264232451548,0.426855552995382,4.24433493759383));
#56891=CARTESIAN_POINT('Ctrl Pts',(17.0590543274837,0.152277829190936,4.41314658311127));
#56892=CARTESIAN_POINT('Ctrl Pts',(17.0757801311249,0.00724700082869906,
4.41654110793655));
#56893=CARTESIAN_POINT('Ctrl Pts',(17.0766006560786,0.000130763213737628,
4.41651185352269));
#56894=CARTESIAN_POINT('Ctrl Pts',(16.8733993439214,-0.000374684679869387,
4.41598699190495));
#56895=CARTESIAN_POINT('Ctrl Pts',(16.8766783386836,-0.0289064002234668,
4.4162516892709));
#56896=CARTESIAN_POINT('Ctrl Pts',(16.8958626121335,-0.195546116663039,
4.40054826733105));
#56897=CARTESIAN_POINT('Ctrl Pts',(16.9309521642709,-0.459365614209645,
4.17575112327883));
#56898=CARTESIAN_POINT('Ctrl Pts',(16.9786680003337,-0.396272847821079,
3.70867019559999));
#56899=CARTESIAN_POINT('Ctrl Pts',(17.0263838363966,0.0307233721630972,
3.5091219099869));
#56900=CARTESIAN_POINT('Ctrl Pts',(17.0740996724594,0.429505846750062,3.76035452756312));
#56901=CARTESIAN_POINT('Ctrl Pts',(17.1218155085223,0.433866493469502,4.23165726989771));
#56902=CARTESIAN_POINT('Ctrl Pts',(17.1549153990096,0.160507997039396,4.41102293437065));
#56903=CARTESIAN_POINT('Ctrl Pts',(17.1721100108093,0.0113854435377776,
4.41651144656345));
#56904=CARTESIAN_POINT('Ctrl Pts',(17.1733993439214,0.000198609043858397,
4.41644558073401));
#56905=CARTESIAN_POINT('Origin',(3.42660065607856,0.,4.));
#56906=CARTESIAN_POINT('',(16.4766006560786,5.2409936866527E-5,4.41519222098806));
#56907=CARTESIAN_POINT('',(16.5733993439214,-1.52272386678698E-5,4.41518677123726));
#56908=CARTESIAN_POINT('',(3.42660065607856,4.87367679877478E-13,4.415875));
#56909=CARTESIAN_POINT('Ctrl Pts',(16.4766006560786,5.2409936866539E-5,
4.41519222098806));
#56910=CARTESIAN_POINT('Ctrl Pts',(16.4849167868736,-0.0726599781719204,
4.41511070701236));
#56911=CARTESIAN_POINT('Ctrl Pts',(16.5091381963562,-0.284551613766983,
4.36224737480062));
#56912=CARTESIAN_POINT('Ctrl Pts',(16.5492648845264,-0.4912502013546,4.02405128938415));
#56913=CARTESIAN_POINT('Ctrl Pts',(16.5969807205893,-0.285919008936969,
3.59980561575594));
#56914=CARTESIAN_POINT('Ctrl Pts',(16.6446965566521,0.181976008816936,3.54306460296116));
#56915=CARTESIAN_POINT('Ctrl Pts',(16.6924123927149,0.482759657613431,3.90593439612197));
#56916=CARTESIAN_POINT('Ctrl Pts',(16.7363804258571,0.351413532087107,4.31989995948535));
#56917=CARTESIAN_POINT('Ctrl Pts',(16.7644431803116,0.105484194296011,4.41488604428797));
#56918=CARTESIAN_POINT('Ctrl Pts',(16.7766006560786,-0.000383680820852189,
4.41586226484779));
#56919=CARTESIAN_POINT('Ctrl Pts',(16.5733993439214,-1.52272386678906E-5,
4.41518677123726));
#56920=CARTESIAN_POINT('Ctrl Pts',(16.5812466665579,-0.0686308195205231,
4.41520910309265));
#56921=CARTESIAN_POINT('Ctrl Pts',(16.6049992678821,-0.276289552895371,
4.36659242126669));
#56922=CARTESIAN_POINT('Ctrl Pts',(16.6446571478939,-0.490328743065594,
4.03850907134293));
#56923=CARTESIAN_POINT('Ctrl Pts',(16.6923729839567,-0.297581432841348,
3.60840005658827));
#56924=CARTESIAN_POINT('Ctrl Pts',(16.7400888200196,0.168439486040012,3.53790329540825));
#56925=CARTESIAN_POINT('Ctrl Pts',(16.7878046560824,0.479779833116189,3.89175704832657));
#56926=CARTESIAN_POINT('Ctrl Pts',(16.832241497383,0.359412856911567,4.31386464726761));
#56927=CARTESIAN_POINT('Ctrl Pts',(16.860773059996,0.109491163683573,4.41496773315674));
#56928=CARTESIAN_POINT('Ctrl Pts',(16.8733993439214,-0.000374684679869387,
4.41598699190495));
#56929=CARTESIAN_POINT('Origin',(3.42660065607856,0.,4.));
#56930=CARTESIAN_POINT('',(16.1766006560786,0.000364146841390381,4.41605523138122));
#56931=CARTESIAN_POINT('',(16.2733993439214,0.000380345806842055,4.41593091837313));
#56932=CARTESIAN_POINT('',(3.42660065607856,4.87367679877478E-13,4.415875));
#56933=CARTESIAN_POINT('Ctrl Pts',(16.1766006560786,0.000364146841390366,
4.41605523138122));
#56934=CARTESIAN_POINT('Ctrl Pts',(16.1894851147479,-0.111700864104492,
4.41502624848758));
#56935=CARTESIAN_POINT('Ctrl Pts',(16.2182748521048,-0.363797281821349,
4.31045679267864));
#56936=CARTESIAN_POINT('Ctrl Pts',(16.2629698681494,-0.477960913216358,
3.88398883549692));
#56937=CARTESIAN_POINT('Ctrl Pts',(16.3106857042122,-0.160921706883503,
3.53523185446324));
#56938=CARTESIAN_POINT('Ctrl Pts',(16.358401540275,0.303894378979202,3.6132786128531));
#56939=CARTESIAN_POINT('Ctrl Pts',(16.4061173763379,0.489639580609251,4.04645757153336));
#56940=CARTESIAN_POINT('Ctrl Pts',(16.4455170816057,0.271734615807756,4.36891289568356));
#56941=CARTESIAN_POINT('Ctrl Pts',(16.4690115081859,0.0664083969439258,
4.41526660914191));
#56942=CARTESIAN_POINT('Ctrl Pts',(16.4766006560786,5.2409936866539E-5,
4.41519222098806));
#56943=CARTESIAN_POINT('Ctrl Pts',(16.2733993439214,0.000380345806842052,
4.41593091837313));
#56944=CARTESIAN_POINT('Ctrl Pts',(16.2858149944323,-0.107690075887363,
4.41492720978183));
#56945=CARTESIAN_POINT('Ctrl Pts',(16.3141359236307,-0.35582464097624,4.31660057631701));
#56946=CARTESIAN_POINT('Ctrl Pts',(16.3583621315169,-0.481170314810987,
3.89811598262401));
#56947=CARTESIAN_POINT('Ctrl Pts',(16.4060779675797,-0.174540169679895,
3.54017290856226));
#56948=CARTESIAN_POINT('Ctrl Pts',(16.4537938036425,0.292372898913969,3.60449612791703));
#56949=CARTESIAN_POINT('Ctrl Pts',(16.5015096397054,0.490795435699827,4.0320166386149));
#56950=CARTESIAN_POINT('Ctrl Pts',(16.5413781531317,0.280003220364278,4.36466130212541));
#56951=CARTESIAN_POINT('Ctrl Pts',(16.5653413878703,0.0704421061260754,
4.4151638399628));
#56952=CARTESIAN_POINT('Ctrl Pts',(16.5733993439214,-1.52272386678906E-5,
4.41518677123726));
#56953=CARTESIAN_POINT('Origin',(3.42660065607856,0.,4.));
#56954=CARTESIAN_POINT('',(15.8766006560786,-0.00023258108979477,4.41639972388928));
#56955=CARTESIAN_POINT('',(15.9733993439214,-0.000169011902647176,4.4164782780785));
#56956=CARTESIAN_POINT('',(3.42660065607856,4.87367679877478E-13,4.415875));
#56957=CARTESIAN_POINT('Ctrl Pts',(15.8766006560786,-0.000232581089794846,
4.41639972388928));
#56958=CARTESIAN_POINT('Ctrl Pts',(15.8781481639346,-0.0136633580705269,
4.41648966084242));
#56959=CARTESIAN_POINT('Ctrl Pts',(15.8956009504782,-0.165044849757219,
4.40979870506104));
#56960=CARTESIAN_POINT('Ctrl Pts',(15.9289590157095,-0.437567097060412,
4.22458909239344));
#56961=CARTESIAN_POINT('Ctrl Pts',(15.9766748517724,-0.425562075928853,
3.75341909160864));
#56962=CARTESIAN_POINT('Ctrl Pts',(16.0243906878352,-0.0227568523576073,
3.50868813313462));
#56963=CARTESIAN_POINT('Ctrl Pts',(16.072106523898,0.400946338892803,3.71513642180785));
#56964=CARTESIAN_POINT('Ctrl Pts',(16.1198223599609,0.456454337785543,4.1831793175245));
#56965=CARTESIAN_POINT('Ctrl Pts',(16.1546537373544,0.190990792023167,4.40204523666471));
#56966=CARTESIAN_POINT('Ctrl Pts',(16.1735798360603,0.0266382990664043,
4.41629648110721));
#56967=CARTESIAN_POINT('Ctrl Pts',(16.1766006560786,0.000364146841390366,
4.41605523138122));
#56968=CARTESIAN_POINT('Ctrl Pts',(15.9733993439214,-0.000169011902647174,
4.4164782780785));
#56969=CARTESIAN_POINT('Ctrl Pts',(15.974478043619,-0.00952634975615679,
4.4165263696097));
#56970=CARTESIAN_POINT('Ctrl Pts',(15.9914620220042,-0.156808910032117,
4.4119928338179));
#56971=CARTESIAN_POINT('Ctrl Pts',(16.024351279077,-0.430762722000766,4.23737881579128));
#56972=CARTESIAN_POINT('Ctrl Pts',(16.0720671151398,-0.432639725453012,
3.76605963834362));
#56973=CARTESIAN_POINT('Ctrl Pts',(16.1197829512026,-0.0372170120039125,
3.50957149464017));
#56974=CARTESIAN_POINT('Ctrl Pts',(16.1674987872655,0.392382656225717,3.70345139362117));
#56975=CARTESIAN_POINT('Ctrl Pts',(16.2152146233283,0.461651293660056,4.16965644082667));
#56976=CARTESIAN_POINT('Ctrl Pts',(16.2505148088803,0.199264245432362,4.39929555075695));
#56977=CARTESIAN_POINT('Ctrl Pts',(16.2699097157447,0.0307553622657438,
4.41621302761729));
#56978=CARTESIAN_POINT('Ctrl Pts',(16.2733993439214,0.000380345806842052,
4.41593091837313));
#56979=CARTESIAN_POINT('Origin',(3.42660065607856,0.,4.));
#56980=CARTESIAN_POINT('',(15.5766006560786,-0.000245472137683418,4.41533389801214));
#56981=CARTESIAN_POINT('',(15.6733993439214,-0.00029394562308721,4.41541483535501));
#56982=CARTESIAN_POINT('',(3.42660065607856,4.87367679877478E-13,4.415875));
#56983=CARTESIAN_POINT('Ctrl Pts',(15.5766006560786,-0.000245472137683396,
4.41533389801214));
#56984=CARTESIAN_POINT('Ctrl Pts',(15.5827164918089,-0.0536739331835165,
4.41562024719655));
#56985=CARTESIAN_POINT('Ctrl Pts',(15.6047376062269,-0.245697356182912,
4.38119912149661));
#56986=CARTESIAN_POINT('Ctrl Pts',(15.6426639993325,-0.483248643997369,
4.09152034160055));
#56987=CARTESIAN_POINT('Ctrl Pts',(15.6903798353953,-0.338341267922855,
3.64302603558196));
#56988=CARTESIAN_POINT('Ctrl Pts',(15.7380956714582,0.117270100534806,3.52234641383892));
#56989=CARTESIAN_POINT('Ctrl Pts',(15.785811507521,0.465190531238913,3.84030342991275));
#56990=CARTESIAN_POINT('Ctrl Pts',(15.8319798357278,0.388490242362186,4.28984418805176));
#56991=CARTESIAN_POINT('Ctrl Pts',(15.862242885247,0.124378106492246,4.41556528924811));
#56992=CARTESIAN_POINT('Ctrl Pts',(15.8766006560786,-0.000232581089794846,
4.41639972388928));
#56993=CARTESIAN_POINT('Ctrl Pts',(15.6733993439214,-0.000293945623087231,
4.41541483535501));
#56994=CARTESIAN_POINT('Ctrl Pts',(15.6790463714933,-0.0496027558454661,
4.41573527017753));
#56995=CARTESIAN_POINT('Ctrl Pts',(15.7005986777528,-0.23740431922453,4.38477730872224));
#56996=CARTESIAN_POINT('Ctrl Pts',(15.7380562626999,-0.480343569999647,
4.1057131950703));
#56997=CARTESIAN_POINT('Ctrl Pts',(15.7857720987628,-0.348708030819167,
3.6531456586776));
#56998=CARTESIAN_POINT('Ctrl Pts',(15.8334879348256,0.103151458625294,3.5190998009613));
#56999=CARTESIAN_POINT('Ctrl Pts',(15.8812037708885,0.460285376424935,3.82667199562295));
#57000=CARTESIAN_POINT('Ctrl Pts',(15.9278409072537,0.396214095655672,4.28286244744368));
#57001=CARTESIAN_POINT('Ctrl Pts',(15.9585727649314,0.128446309981357,4.41581726659612));
#57002=CARTESIAN_POINT('Ctrl Pts',(15.9733993439214,-0.000169011902647174,
4.4164782780785));
#57003=CARTESIAN_POINT('Origin',(3.42660065607856,0.,4.));
#57004=CARTESIAN_POINT('',(15.2766006560786,0.000330084823988869,4.41550084660604));
#57005=CARTESIAN_POINT('',(15.3733993439214,0.000289868078815952,4.41540680128743));
#57006=CARTESIAN_POINT('',(3.42660065607856,4.87367679877478E-13,4.415875));
#57007=CARTESIAN_POINT('Ctrl Pts',(15.2766006560786,0.000330084823988861,
4.41550084660604));
#57008=CARTESIAN_POINT('Ctrl Pts',(15.2872848196833,-0.0929135079625664,
4.41481081573461));
#57009=CARTESIAN_POINT('Ctrl Pts',(15.3138742619755,-0.32600240339937,4.33760928826424));
#57010=CARTESIAN_POINT('Ctrl Pts',(15.3563689829555,-0.489387968817152,
3.95096286275689));
#57011=CARTESIAN_POINT('Ctrl Pts',(15.4040848190183,-0.223435404337718,
3.56184267101825));
#57012=CARTESIAN_POINT('Ctrl Pts',(15.4518006550811,0.24770132994065,3.57508909640066));
#57013=CARTESIAN_POINT('Ctrl Pts',(15.499516491144,0.491370121559653,3.97853774265298));
#57014=CARTESIAN_POINT('Ctrl Pts',(15.5411164914764,0.310410063586636,4.3474585185963));
#57015=CARTESIAN_POINT('Ctrl Pts',(15.5668112131213,0.0852759340546689,
4.41487554708019));
#57016=CARTESIAN_POINT('Ctrl Pts',(15.5766006560786,-0.000245472137683396,
4.41533389801214));
#57017=CARTESIAN_POINT('Ctrl Pts',(15.3733993439214,0.000289868078815973,
4.41540680128743));
#57018=CARTESIAN_POINT('Ctrl Pts',(15.3836146993676,-0.0889130762729256,
4.41483587894927));
#57019=CARTESIAN_POINT('Ctrl Pts',(15.4097353335015,-0.317845114095608,
4.34285359523591));
#57020=CARTESIAN_POINT('Ctrl Pts',(15.4517612463229,-0.490619905976795,
3.96539750426199));
#57021=CARTESIAN_POINT('Ctrl Pts',(15.4994770823858,-0.236243011612202,
3.56861332390027));
#57022=CARTESIAN_POINT('Ctrl Pts',(15.5471929184486,0.235079475381852,3.56797816593814));
#57023=CARTESIAN_POINT('Ctrl Pts',(15.5949087545115,0.490524862970081,3.9640753057054));
#57024=CARTESIAN_POINT('Ctrl Pts',(15.6369775630024,0.318592711010818,4.34238143198936));
#57025=CARTESIAN_POINT('Ctrl Pts',(15.6631410928057,0.0892792238074376,
4.41483274135358));
#57026=CARTESIAN_POINT('Ctrl Pts',(15.6733993439214,-0.000293945623087231,
4.41541483535501));
#57027=CARTESIAN_POINT('Origin',(3.42660065607856,0.,4.));
#57028=CARTESIAN_POINT('',(14.9766006560786,0.000104941934236194,4.41652945172571));
#57029=CARTESIAN_POINT('',(15.0733993439214,0.000175165248676303,4.41647198785975));
#57030=CARTESIAN_POINT('',(3.42660065607856,4.87367679877478E-13,4.415875));
#57031=CARTESIAN_POINT('Ctrl Pts',(14.9766006560786,0.000104941934236227,
4.41652945172572));
#57032=CARTESIAN_POINT('Ctrl Pts',(14.9918531475576,-0.132161740438444,
4.41608294134065));
#57033=CARTESIAN_POINT('Ctrl Pts',(15.0230109177242,-0.40316752945992,4.27633971254324));
#57034=CARTESIAN_POINT('Ctrl Pts',(15.0700739665785,-0.455482716161518,
3.8144178884426));
#57035=CARTESIAN_POINT('Ctrl Pts',(15.1177898026413,-0.0902467530057116,
3.51651189422706));
#57036=CARTESIAN_POINT('Ctrl Pts',(15.1655056387041,0.357864192060027,3.66260046696357));
#57037=CARTESIAN_POINT('Ctrl Pts',(15.2132214747669,0.47734294310866,4.11852822244656));
#57038=CARTESIAN_POINT('Ctrl Pts',(15.2502531472251,0.229869832763757,4.3878938710325));
#57039=CARTESIAN_POINT('Ctrl Pts',(15.2713795409956,0.0458961718568525,
4.41583804947224));
#57040=CARTESIAN_POINT('Ctrl Pts',(15.2766006560786,0.000330084823988861,
4.41550084660604));
#57041=CARTESIAN_POINT('Ctrl Pts',(15.0733993439214,0.000175165248676341,
4.41647198785975));
#57042=CARTESIAN_POINT('Ctrl Pts',(15.0881830272419,-0.128073190246274,
4.41579247653651));
#57043=CARTESIAN_POINT('Ctrl Pts',(15.1188719892501,-0.395510344386944,
4.28350986851547));
#57044=CARTESIAN_POINT('Ctrl Pts',(15.1654662299459,-0.46075086019608,3.82791319143947));
#57045=CARTESIAN_POINT('Ctrl Pts',(15.2131820660087,-0.104447211543591,
3.51937956259357));
#57046=CARTESIAN_POINT('Ctrl Pts',(15.2608979020716,0.347771918596306,3.652207076714));
#57047=CARTESIAN_POINT('Ctrl Pts',(15.3086137381344,0.480626744730421,4.10441818376995));
#57048=CARTESIAN_POINT('Ctrl Pts',(15.346114218751,0.238163166260598,4.38445638366753));
#57049=CARTESIAN_POINT('Ctrl Pts',(15.36770942068,0.0499756483669043,4.41572480336754));
#57050=CARTESIAN_POINT('Ctrl Pts',(15.3733993439214,0.000289868078815973,
4.41540680128743));
#57051=CARTESIAN_POINT('Origin',(3.42660065607856,0.,4.));
#57052=CARTESIAN_POINT('',(14.6766006560786,-0.000383732061438463,4.41581798673635));
#57053=CARTESIAN_POINT('',(14.7733993439214,-0.000379407362125217,4.41594234696178));
#57054=CARTESIAN_POINT('',(3.42660065607856,4.87367679877478E-13,4.415875));
#57055=CARTESIAN_POINT('Ctrl Pts',(14.6766006560786,-0.000383732061438387,
4.41581798673635));
#57056=CARTESIAN_POINT('Ctrl Pts',(14.6805161967443,-0.0344897130604965,
4.41612948839573));
#57057=CARTESIAN_POINT('Ctrl Pts',(14.7003370160976,-0.206786574235377,
4.39667515056147));
#57058=CARTESIAN_POINT('Ctrl Pts',(14.7360631141386,-0.466025611307368,
4.15724297904063));
#57059=CARTESIAN_POINT('Ctrl Pts',(14.7837789502014,-0.38430721152129,3.69305832471834));
#57060=CARTESIAN_POINT('Ctrl Pts',(14.8314947862642,0.0503264139313189,
3.51074293371195));
#57061=CARTESIAN_POINT('Ctrl Pts',(14.8792106223271,0.438744519099385,3.77771983486548));
#57062=CARTESIAN_POINT('Ctrl Pts',(14.9269264583899,0.42425678142631,4.24882003188202));
#57063=CARTESIAN_POINT('Ctrl Pts',(14.9593898029737,0.149335702075518,4.41387566524124));
#57064=CARTESIAN_POINT('Ctrl Pts',(14.97594786887,0.00576578747519492,4.41654856180149));
#57065=CARTESIAN_POINT('Ctrl Pts',(14.9766006560786,0.000104941934236227,
4.41652945172572));
#57066=CARTESIAN_POINT('Ctrl Pts',(14.7733993439214,-0.000379407362125234,
4.41594234696178));
#57067=CARTESIAN_POINT('Ctrl Pts',(14.7768460764287,-0.0303789312965351,
4.41622104989506));
#57068=CARTESIAN_POINT('Ctrl Pts',(14.7961980876235,-0.198506931257387,
4.39955296987463));
#57069=CARTESIAN_POINT('Ctrl Pts',(14.831455377506,-0.461192356972643,4.17090007232882));
#57070=CARTESIAN_POINT('Ctrl Pts',(14.8791712135689,-0.393180492164677,
3.7045100248179));
#57071=CARTESIAN_POINT('Ctrl Pts',(14.9268870496317,0.0358950684576197,
3.50947296821438));
#57072=CARTESIAN_POINT('Ctrl Pts',(14.9746028856945,0.432007635398663,3.76489443262817));
#57073=CARTESIAN_POINT('Ctrl Pts',(15.0223187217574,0.431400943461215,4.23621695712364));
#57074=CARTESIAN_POINT('Ctrl Pts',(15.0552508744997,0.157562060208247,4.41179740605063));
#57075=CARTESIAN_POINT('Ctrl Pts',(15.0722777485543,0.00990499767517082,
4.41652354042182));
#57076=CARTESIAN_POINT('Ctrl Pts',(15.0733993439214,0.000175165248676341,
4.41647198785975));
#57077=CARTESIAN_POINT('Origin',(3.42660065607856,0.,4.));
#57078=CARTESIAN_POINT('',(14.3766006560786,7.63317591858645E-5,4.41519896243726));
#57079=CARTESIAN_POINT('',(14.4733993439214,9.02664646690309E-6,4.41518644689786));
#57080=CARTESIAN_POINT('',(3.42660065607856,4.87367679877478E-13,4.415875));
#57081=CARTESIAN_POINT('Ctrl Pts',(14.3766006560786,7.63317591858798E-5,
4.41519896243726));
#57082=CARTESIAN_POINT('Ctrl Pts',(14.3850845246186,-0.0740996743586071,
4.41507773880187));
#57083=CARTESIAN_POINT('Ctrl Pts',(14.4094736718463,-0.287504468978829,
4.360651101065));
#57084=CARTESIAN_POINT('Ctrl Pts',(14.4497680977616,-0.491476396904638,
4.01887262932433));
#57085=CARTESIAN_POINT('Ctrl Pts',(14.4974839338244,-0.281685449746218,
3.59681451879656));
#57086=CARTESIAN_POINT('Ctrl Pts',(14.5451997698872,0.186781580201919,3.54500783946397));
#57087=CARTESIAN_POINT('Ctrl Pts',(14.59291560595,0.483724211046603,3.91102746210588));
#57088=CARTESIAN_POINT('Ctrl Pts',(14.6367159013472,0.348540265561382,4.32201186060262));
#57089=CARTESIAN_POINT('Ctrl Pts',(14.6646109180567,0.104051852208848,4.41486414061182));
#57090=CARTESIAN_POINT('Ctrl Pts',(14.6766006560786,-0.000383732061438387,
4.41581798673635));
#57091=CARTESIAN_POINT('Ctrl Pts',(14.4733993439214,9.0266464668684E-6,
4.41518644689786));
#57092=CARTESIAN_POINT('Ctrl Pts',(14.481414404303,-0.0700733710850898,
4.41517292627706));
#57093=CARTESIAN_POINT('Ctrl Pts',(14.5053347433722,-0.279247125311621,
4.3650573561381));
#57094=CARTESIAN_POINT('Ctrl Pts',(14.545160361129,-0.490707361486496,4.03333931965322));
#57095=CARTESIAN_POINT('Ctrl Pts',(14.5928761971918,-0.293437803431633,
3.60528557111603));
#57096=CARTESIAN_POINT('Ctrl Pts',(14.6405920332547,0.173300204635467,3.53970415608515));
#57097=CARTESIAN_POINT('Ctrl Pts',(14.6883078693175,0.480893968219416,3.89681949708321));
#57098=CARTESIAN_POINT('Ctrl Pts',(14.7325769728731,0.356556173733762,4.31604662460621));
#57099=CARTESIAN_POINT('Ctrl Pts',(14.760940797741,0.10805675748006,4.41493494840171));
#57100=CARTESIAN_POINT('Ctrl Pts',(14.7733993439214,-0.000379407362125234,
4.41594234696178));
#57101=CARTESIAN_POINT('Origin',(3.42660065607856,0.,4.));
#57102=CARTESIAN_POINT('',(14.0766006560786,0.000355193352615291,4.41609897421413));
#57103=CARTESIAN_POINT('',(14.1733993439214,0.000376051973931104,4.41597558743442));
#57104=CARTESIAN_POINT('',(3.42660065607856,4.87367679877478E-13,4.415875));
#57105=CARTESIAN_POINT('Ctrl Pts',(14.0766006560786,0.000355193352615277,
4.41609897421413));
#57106=CARTESIAN_POINT('Ctrl Pts',(14.0896528524929,-0.113137957382804,
4.41506966208575));
#57107=CARTESIAN_POINT('Ctrl Pts',(14.1186103275949,-0.366637448157006,
4.30821039815648));
#57108=CARTESIAN_POINT('Ctrl Pts',(14.1634730813845,-0.476711717661702,
3.87895801102093));
#57109=CARTESIAN_POINT('Ctrl Pts',(14.2111889174473,-0.156014541823709,
3.53356170012368));
#57110=CARTESIAN_POINT('Ctrl Pts',(14.2589047535102,0.307953188363286,3.61650285707861));
#57111=CARTESIAN_POINT('Ctrl Pts',(14.306620589573,0.4891227672074,4.05161534124029));
#57112=CARTESIAN_POINT('Ctrl Pts',(14.3458525570958,0.268773633406098,4.37039329245586));
#57113=CARTESIAN_POINT('Ctrl Pts',(14.369179245931,0.0649630708582953,4.4153050049005));
#57114=CARTESIAN_POINT('Ctrl Pts',(14.3766006560786,7.63317591858798E-5,
4.41519896243726));
#57115=CARTESIAN_POINT('Ctrl Pts',(14.1733993439214,0.000376051973931098,
4.41597558743442));
#57116=CARTESIAN_POINT('Ctrl Pts',(14.1859827321773,-0.109124255432428,
4.41495896305428));
#57117=CARTESIAN_POINT('Ctrl Pts',(14.2144713991208,-0.358682910161539,
4.31442504752535));
#57118=CARTESIAN_POINT('Ctrl Pts',(14.258865344752,-0.480069828122688,3.8930505494253));
#57119=CARTESIAN_POINT('Ctrl Pts',(14.3065811808148,-0.169684322438749,
3.53835895376334));
#57120=CARTESIAN_POINT('Ctrl Pts',(14.3542970168777,0.296524907469595,3.60759943412104));
#57121=CARTESIAN_POINT('Ctrl Pts',(14.4020128529405,0.49043075222644,4.0371873919842));
#57122=CARTESIAN_POINT('Ctrl Pts',(14.4417136286217,0.277046036654804,4.36620192284859));
#57123=CARTESIAN_POINT('Ctrl Pts',(14.4655091256154,0.0689998253659925,
4.41519975692232));
#57124=CARTESIAN_POINT('Ctrl Pts',(14.4733993439214,9.0266464668684E-6,
4.41518644689786));
#57125=CARTESIAN_POINT('Origin',(3.42660065607856,0.,4.));
#57126=CARTESIAN_POINT('',(13.7766006560786,-0.000253139125078747,4.41636688691614));
#57127=CARTESIAN_POINT('',(13.8733993439214,-0.000192710833643805,4.4164526008213));
#57128=CARTESIAN_POINT('',(3.42660065607856,4.87367679877478E-13,4.415875));
#57129=CARTESIAN_POINT('Ctrl Pts',(13.7766006560786,-0.000253139125078718,
4.41636688691614));
#57130=CARTESIAN_POINT('Ctrl Pts',(13.7783159016796,-0.0151427949580853,
4.41647347977994));
#57131=CARTESIAN_POINT('Ctrl Pts',(13.7959364259683,-0.167994124135391,
4.40898222403799));
#57132=CARTESIAN_POINT('Ctrl Pts',(13.8294622289446,-0.439909757638992,
4.21996506537626));
#57133=CARTESIAN_POINT('Ctrl Pts',(13.8771780650075,-0.422939705734467,
3.74894775411238));
#57134=CARTESIAN_POINT('Ctrl Pts',(13.9248939010703,-0.0175776142901187,
3.50847558318244));
#57135=CARTESIAN_POINT('Ctrl Pts',(13.9726097371332,0.403926270823208,3.71937784729135));
#57136=CARTESIAN_POINT('Ctrl Pts',(14.020325573196,0.454498446235019,4.18797975215946));
#57137=CARTESIAN_POINT('Ctrl Pts',(14.0549892128445,0.188032430710383,4.40299531219535));
#57138=CARTESIAN_POINT('Ctrl Pts',(14.0737475738053,0.0251636842930195,
4.41632397176197));
#57139=CARTESIAN_POINT('Ctrl Pts',(14.0766006560786,0.000355193352615277,
4.41609897421413));
#57140=CARTESIAN_POINT('Ctrl Pts',(13.8733993439214,-0.000192710833643682,
4.4164526008213));
#57141=CARTESIAN_POINT('Ctrl Pts',(13.874645781364,-0.0110068809386406,
4.41651469495978));
#57142=CARTESIAN_POINT('Ctrl Pts',(13.8917974974943,-0.15975450351916,4.41122255187585));
#57143=CARTESIAN_POINT('Ctrl Pts',(13.9248544923121,-0.433240552373761,
4.23282579030437));
#57144=CARTESIAN_POINT('Ctrl Pts',(13.9725703283749,-0.430150181893835,
3.76151300691929));
#57145=CARTESIAN_POINT('Ctrl Pts',(14.0202861644378,-0.032046280669499,
3.50920649887429));
#57146=CARTESIAN_POINT('Ctrl Pts',(14.0680020005006,0.39548621318905,3.70760321474174));
#57147=CARTESIAN_POINT('Ctrl Pts',(14.1157178365634,0.459837632138507,4.1745123976147));
#57148=CARTESIAN_POINT('Ctrl Pts',(14.1508502843704,0.196303200904851,4.40029544879449));
#57149=CARTESIAN_POINT('Ctrl Pts',(14.1700774534897,0.0292830534939708,
4.41624396624722));
#57150=CARTESIAN_POINT('Ctrl Pts',(14.1733993439214,0.000376051973931098,
4.41597558743442));
#57151=CARTESIAN_POINT('Origin',(3.42660065607856,0.,4.));
#57152=CARTESIAN_POINT('',(13.4766006560786,-0.000226204729293368,4.4153088088013));
#57153=CARTESIAN_POINT('',(13.5733993439214,-0.000277574767750837,4.41538411867388));
#57154=CARTESIAN_POINT('',(3.42660065607856,4.87367679877478E-13,4.415875));
#57155=CARTESIAN_POINT('Ctrl Pts',(13.4766006560786,-0.000226204729293314,
4.4153088088013));
#57156=CARTESIAN_POINT('Ctrl Pts',(13.482884229554,-0.0551283395969922,
4.41557894444213));
#57157=CARTESIAN_POINT('Ctrl Pts',(13.505073081717,-0.248664136397309,4.37988069596112));
#57158=CARTESIAN_POINT('Ctrl Pts',(13.5431672125676,-0.484186345555107,
4.08642226350871));
#57159=CARTESIAN_POINT('Ctrl Pts',(13.5908830486304,-0.334560300710407,
3.63948005597396));
#57160=CARTESIAN_POINT('Ctrl Pts',(13.6385988846933,0.122297616148583,3.52360886035071));
#57161=CARTESIAN_POINT('Ctrl Pts',(13.6863147207561,0.466847750307624,3.8452149784873));
#57162=CARTESIAN_POINT('Ctrl Pts',(13.7323153112179,0.38570983934117,4.29229218593957));
#57163=CARTESIAN_POINT('Ctrl Pts',(13.762410622992,0.122927301498021,4.41548505619568));
#57164=CARTESIAN_POINT('Ctrl Pts',(13.7766006560786,-0.000253139125078718,
4.41636688691614));
#57165=CARTESIAN_POINT('Ctrl Pts',(13.5733993439214,-0.000277574767750817,
4.41538411867388));
#57166=CARTESIAN_POINT('Ctrl Pts',(13.5792141092383,-0.0510604653080308,
4.41569425641003));
#57167=CARTESIAN_POINT('Ctrl Pts',(13.6009341532429,-0.240371663949131,
4.38351498152559));
#57168=CARTESIAN_POINT('Ctrl Pts',(13.6385594759351,-0.481431012491488,
4.10064494554323));
#57169=CARTESIAN_POINT('Ctrl Pts',(13.6862753119979,-0.345033139360895,
3.64948986092447));
#57170=CARTESIAN_POINT('Ctrl Pts',(13.7339911480608,0.108213974662067,3.52021363031051));
#57171=CARTESIAN_POINT('Ctrl Pts',(13.7817069841236,0.462086530666827,3.83153260544464));
#57172=CARTESIAN_POINT('Ctrl Pts',(13.8281763827438,0.393458703070077,4.28538422885222));
#57173=CARTESIAN_POINT('Ctrl Pts',(13.8587405026764,0.126988323162951,4.4157223370415));
#57174=CARTESIAN_POINT('Ctrl Pts',(13.8733993439214,-0.000192710833643682,
4.4164526008213));
#57175=CARTESIAN_POINT('Origin',(3.42660065607856,0.,4.));
#57176=CARTESIAN_POINT('',(13.1766006560786,0.000342007958933446,4.41553758638116));
#57177=CARTESIAN_POINT('',(13.2733993439214,0.000305371599794934,4.41543889539504));
#57178=CARTESIAN_POINT('',(3.42660065607856,4.87367679877478E-13,4.415875));
#57179=CARTESIAN_POINT('Ctrl Pts',(13.1766006560786,0.000342007958933428,
4.41553758638117));
#57180=CARTESIAN_POINT('Ctrl Pts',(13.1874525574283,-0.0943443719380771,
4.41480703635833));
#57181=CARTESIAN_POINT('Ctrl Pts',(13.2142097374657,-0.328913583769224,
4.33568767983454));
#57182=CARTESIAN_POINT('Ctrl Pts',(13.2568721961906,-0.488843983144383,
3.94580788806928));
#57183=CARTESIAN_POINT('Ctrl Pts',(13.3045880322534,-0.218805220893238,
3.55951220202843));
#57184=CARTESIAN_POINT('Ctrl Pts',(13.3523038683163,0.252165742455243,3.57772323864086));
#57185=CARTESIAN_POINT('Ctrl Pts',(13.4000197043791,0.491569024438394,3.98371752277252));
#57186=CARTESIAN_POINT('Ctrl Pts',(13.4414519669665,0.307476227900318,4.34923088347422));
#57187=CARTESIAN_POINT('Ctrl Pts',(13.4669789508664,0.0838425436168888,
4.41489516431802));
#57188=CARTESIAN_POINT('Ctrl Pts',(13.4766006560786,-0.000226204729293314,
4.4153088088013));
#57189=CARTESIAN_POINT('Ctrl Pts',(13.2733993439214,0.000305371599794949,
4.41543889539504));
#57190=CARTESIAN_POINT('Ctrl Pts',(13.2837824371127,-0.0903447040275099,
4.41482455235666));
#57191=CARTESIAN_POINT('Ctrl Pts',(13.3100708089916,-0.320767143545349,
4.3409984814332));
#57192=CARTESIAN_POINT('Ctrl Pts',(13.352264459558,-0.490227979701372,3.96022874442655));
#57193=CARTESIAN_POINT('Ctrl Pts',(13.3999802956209,-0.23168347330409,3.56614749850931));
#57194=CARTESIAN_POINT('Ctrl Pts',(13.4476961316837,0.239619531536799,3.57047968038978));
#57195=CARTESIAN_POINT('Ctrl Pts',(13.4954119677466,0.490876233547033,3.96924698078795));
#57196=CARTESIAN_POINT('Ctrl Pts',(13.5373130384925,0.315668023336251,4.34421900798688));
#57197=CARTESIAN_POINT('Ctrl Pts',(13.5633088305507,0.0878472949503496,
4.41484592860038));
#57198=CARTESIAN_POINT('Ctrl Pts',(13.5733993439214,-0.000277574767750817,
4.41538411867388));
#57199=CARTESIAN_POINT('Origin',(3.42660065607856,0.,4.));
#57200=CARTESIAN_POINT('',(12.8766006560786,7.85109994957766E-5,4.41654344863055));
#57201=CARTESIAN_POINT('',(12.9733993439214,0.000150764780949702,4.41649545414489));
#57202=CARTESIAN_POINT('',(3.42660065607856,4.87367679877478E-13,4.415875));
#57203=CARTESIAN_POINT('Ctrl Pts',(12.8766006560786,7.85109994958138E-5,
4.41654344863055));
#57204=CARTESIAN_POINT('Ctrl Pts',(12.8920208853026,-0.133630732206743,
4.41619751255639));
#57205=CARTESIAN_POINT('Ctrl Pts',(12.9233463932143,-0.405888408666218,
4.27372356364211));
#57206=CARTESIAN_POINT('Ctrl Pts',(12.9705771798136,-0.453501555338242,
3.80962782724943));
#57207=CARTESIAN_POINT('Ctrl Pts',(13.0182930158764,-0.0851462219395619,
3.51558762841831));
#57208=CARTESIAN_POINT('Ctrl Pts',(13.0660088519392,0.361400197209248,3.66639076405307));
#57209=CARTESIAN_POINT('Ctrl Pts',(13.1137246880021,0.476067254403989,4.1235523942958));
#57210=CARTESIAN_POINT('Ctrl Pts',(13.1505886227152,0.226902767145371,4.38908671404106));
#57211=CARTESIAN_POINT('Ctrl Pts',(13.1715472787407,0.0444343739838573,
4.41587777975472));
#57212=CARTESIAN_POINT('Ctrl Pts',(13.1766006560786,0.000342007958933428,
4.41553758638117));
#57213=CARTESIAN_POINT('Ctrl Pts',(12.9733993439214,0.000150764780949724,
4.4164954541449));
#57214=CARTESIAN_POINT('Ctrl Pts',(12.988350764987,-0.12953330947047,4.41589144324702));
#57215=CARTESIAN_POINT('Ctrl Pts',(13.0192074647402,-0.39825874617628,4.28096832590395));
#57216=CARTESIAN_POINT('Ctrl Pts',(13.065969443181,-0.458911634846768,3.82306685936703));
#57217=CARTESIAN_POINT('Ctrl Pts',(13.1136852792439,-0.0993761143989603,
3.51830547777773));
#57218=CARTESIAN_POINT('Ctrl Pts',(13.1614011153067,0.351418020999476,3.65589158776806));
#57219=CARTESIAN_POINT('Ctrl Pts',(13.2091169513695,0.479499580452807,4.10947774749948));
#57220=CARTESIAN_POINT('Ctrl Pts',(13.2464496942411,0.235195791588524,4.38570395495548));
#57221=CARTESIAN_POINT('Ctrl Pts',(13.2678771584251,0.0485170676377186,
4.41576563003508));
#57222=CARTESIAN_POINT('Ctrl Pts',(13.2733993439214,0.000305371599794949,
4.41543889539504));
#57223=CARTESIAN_POINT('Origin',(3.42660065607856,0.,4.));
#57224=CARTESIAN_POINT('',(12.5766006560786,-0.000382134531266273,4.41577416496379));
#57225=CARTESIAN_POINT('',(12.6733993439214,-0.000382453243898073,4.41589767499446));
#57226=CARTESIAN_POINT('',(3.42660065607856,4.87367679877478E-13,4.415875));
#57227=CARTESIAN_POINT('Ctrl Pts',(12.5766006560786,-0.000382134531266193,
4.41577416496379));
#57228=CARTESIAN_POINT('Ctrl Pts',(12.5806839344893,-0.0359587315295452,
4.41609477791077));
#57229=CARTESIAN_POINT('Ctrl Pts',(12.6006724915877,-0.209750441210566,
4.39561070447123));
#57230=CARTESIAN_POINT('Ctrl Pts',(12.6365663273737,-0.4676569254097,4.15232276575852));
#57231=CARTESIAN_POINT('Ctrl Pts',(12.6842821634365,-0.381050985679211,
3.68902512775968));
#57232=CARTESIAN_POINT('Ctrl Pts',(12.7319979994994,0.0554799374235607,
3.5113004999026));
#57233=CARTESIAN_POINT('Ctrl Pts',(12.7797138355622,0.441062780321708,3.78235614259331));
#57234=CARTESIAN_POINT('Ctrl Pts',(12.8274296716251,0.421610885427219,4.2532774884218));
#57235=CARTESIAN_POINT('Ctrl Pts',(12.8597252784638,0.146394963767536,4.4145887178469));
#57236=CARTESIAN_POINT('Ctrl Pts',(12.876115606615,0.00428438860018927,
4.4165543301878));
#57237=CARTESIAN_POINT('Ctrl Pts',(12.8766006560786,7.85109994958138E-5,
4.41654344863055));
#57238=CARTESIAN_POINT('Ctrl Pts',(12.6733993439214,-0.000382453243898042,
4.41589767499447));
#57239=CARTESIAN_POINT('Ctrl Pts',(12.6770138141737,-0.0318505807336982,
4.4161892599907));
#57240=CARTESIAN_POINT('Ctrl Pts',(12.6965335631136,-0.201468625965512,
4.39853963407534));
#57241=CARTESIAN_POINT('Ctrl Pts',(12.7319585907412,-0.462967872677167,
4.16603003860975));
#57242=CARTESIAN_POINT('Ctrl Pts',(12.779674426804,-0.390044463885,3.70038267566003));
#57243=CARTESIAN_POINT('Ctrl Pts',(12.8273902628668,0.0410627776982723,
3.50987851185683));
#57244=CARTESIAN_POINT('Ctrl Pts',(12.8751060989297,0.434461438689172,3.76946045210395));
#57245=CARTESIAN_POINT('Ctrl Pts',(12.9228219349925,0.42888747548329,4.24075040649094));
#57246=CARTESIAN_POINT('Ctrl Pts',(12.9555863499897,0.154617472482897,4.41255553662561));
#57247=CARTESIAN_POINT('Ctrl Pts',(12.9724454862994,0.00842423538524961,
4.41653398830136));
#57248=CARTESIAN_POINT('Ctrl Pts',(12.9733993439214,0.000150764780949724,
4.4164954541449));
#57249=CARTESIAN_POINT('Origin',(3.42660065607856,0.,4.));
#57250=CARTESIAN_POINT('',(12.2766006560786,9.99581421417901E-5,4.41520820259509));
#57251=CARTESIAN_POINT('',(12.3733993439214,3.32456539758885E-5,4.41518865831861));
#57252=CARTESIAN_POINT('',(3.42660065607856,4.87367679877478E-13,4.415875));
#57253=CARTESIAN_POINT('Ctrl Pts',(12.2766006560786,9.99581421418094E-5,
4.41520820259509));
#57254=CARTESIAN_POINT('Ctrl Pts',(12.2852522623637,-0.0755384113923865,
4.41504611816934));
#57255=CARTESIAN_POINT('Ctrl Pts',(12.3098091473364,-0.290455378639464,
4.35903266527152));
#57256=CARTESIAN_POINT('Ctrl Pts',(12.3502713109967,-0.49164800158875,4.0136918729824));
#57257=CARTESIAN_POINT('Ctrl Pts',(12.3979871470595,-0.277420602272412,
3.59386820576715));
#57258=CARTESIAN_POINT('Ctrl Pts',(12.4457029831224,0.191566404775332,3.54700161433684));
#57259=CARTESIAN_POINT('Ctrl Pts',(12.4934188191852,0.484635034689867,3.91613041073711));
#57260=CARTESIAN_POINT('Ctrl Pts',(12.5370513768373,0.345661459897227,4.32409890635003));
#57261=CARTESIAN_POINT('Ctrl Pts',(12.5647786558017,0.102620036091023,4.41484591908716));
#57262=CARTESIAN_POINT('Ctrl Pts',(12.5766006560786,-0.000382134531266193,
4.41577416496379));
#57263=CARTESIAN_POINT('Ctrl Pts',(12.3733993439214,3.32456539758746E-5,
4.41518865831861));
#57264=CARTESIAN_POINT('Ctrl Pts',(12.381582142048,-0.071514873974996,4.41513780400291));
#57265=CARTESIAN_POINT('Ctrl Pts',(12.4056702188623,-0.282203129244181,
4.36350051499509));
#57266=CARTESIAN_POINT('Ctrl Pts',(12.4456635743641,-0.491031474462283,
4.0281658647901));
#57267=CARTESIAN_POINT('Ctrl Pts',(12.493379410427,-0.289261580343189,3.60221492864948));
#57268=CARTESIAN_POINT('Ctrl Pts',(12.5410952464898,0.178141673866572,3.54155614424011));
#57269=CARTESIAN_POINT('Ctrl Pts',(12.5888110825527,0.481954687902679,3.90189340664049));
#57270=CARTESIAN_POINT('Ctrl Pts',(12.6329124483632,0.353693368040787,4.31820342736526));
#57271=CARTESIAN_POINT('Ctrl Pts',(12.6611085354861,0.106623193447456,4.41490615616012));
#57272=CARTESIAN_POINT('Ctrl Pts',(12.6733993439214,-0.000382453243898042,
4.41589767499447));
#57273=CARTESIAN_POINT('Origin',(3.42660065607856,0.,4.));
#57274=CARTESIAN_POINT('',(11.9766006560786,0.000344603143201134,4.41614202049347));
#57275=CARTESIAN_POINT('',(12.0733993439214,0.00037008249145147,4.41602009379307));
#57276=CARTESIAN_POINT('',(3.42660065607856,4.87367679877478E-13,4.415875));
#57277=CARTESIAN_POINT('Ctrl Pts',(11.9766006560786,0.000344603143201134,
4.41614202049347));
#57278=CARTESIAN_POINT('Ctrl Pts',(11.989820590238,-0.114576335025177,4.41511745277426));
#57279=CARTESIAN_POINT('Ctrl Pts',(12.018945803085,-0.369470719226983,4.30593844396252));
#57280=CARTESIAN_POINT('Ctrl Pts',(12.0639762946196,-0.475409571231627,
3.87394063131468));
#57281=CARTESIAN_POINT('Ctrl Pts',(12.1116921306825,-0.151090047408964,
3.53194335553704));
#57282=CARTESIAN_POINT('Ctrl Pts',(12.1594079667453,0.311977791768556,3.61976969834691));
#57283=CARTESIAN_POINT('Ctrl Pts',(12.2071238028081,0.488551624369653,4.05676737776005));
#57284=CARTESIAN_POINT('Ctrl Pts',(12.2461880325859,0.265811525316043,4.37185240566124));
#57285=CARTESIAN_POINT('Ctrl Pts',(12.269346983676,0.0635166157645696,4.41534409728183));
#57286=CARTESIAN_POINT('Ctrl Pts',(12.2766006560786,9.99581421418094E-5,
4.41520820259509));
#57287=CARTESIAN_POINT('Ctrl Pts',(12.0733993439214,0.000370082491451453,
4.41602009379308));
#57288=CARTESIAN_POINT('Ctrl Pts',(12.0861504699224,-0.110559366248508,
4.41499479059613));
#57289=CARTESIAN_POINT('Ctrl Pts',(12.1148068746109,-0.361534897467509,
4.3122242613332));
#57290=CARTESIAN_POINT('Ctrl Pts',(12.1593685579871,-0.478916017555994,
3.88799699566402));
#57291=CARTESIAN_POINT('Ctrl Pts',(12.2070843940499,-0.164809627468288,
3.53659627586117));
#57292=CARTESIAN_POINT('Ctrl Pts',(12.2548002301128,0.300643979445627,3.61074632631782));
#57293=CARTESIAN_POINT('Ctrl Pts',(12.3025160661756,0.490011594032383,4.04235401475446));
#57294=CARTESIAN_POINT('Ctrl Pts',(12.3420491041118,0.274087380788525,4.36772087084377));
#57295=CARTESIAN_POINT('Ctrl Pts',(12.3656768633604,0.0675564760281007,
4.41523665186048));
#57296=CARTESIAN_POINT('Ctrl Pts',(12.3733993439214,3.32456539758746E-5,
4.41518865831861));
#57297=CARTESIAN_POINT('Origin',(3.42660065607856,0.,4.));
#57298=CARTESIAN_POINT('',(11.6766006560786,-0.000272404999166542,4.41633191892761));
#57299=CARTESIAN_POINT('',(11.7733993439214,-0.000215373091504267,4.41642415578018));
#57300=CARTESIAN_POINT('',(3.42660065607856,4.87367679877478E-13,4.415875));
#57301=CARTESIAN_POINT('Ctrl Pts',(11.6766006560786,-0.000272404999166455,
4.41633191892761));
#57302=CARTESIAN_POINT('Ctrl Pts',(11.6784836394247,-0.0166217551361539,
4.41645573239506));
#57303=CARTESIAN_POINT('Ctrl Pts',(11.6962719014584,-0.170944672110958,
4.40814899119985));
#57304=CARTESIAN_POINT('Ctrl Pts',(11.7299654421798,-0.44220355512924,4.21531660568344));
#57305=CARTESIAN_POINT('Ctrl Pts',(11.7776812782426,-0.420270357404582,
3.74450430230823));
#57306=CARTESIAN_POINT('Ctrl Pts',(11.8253971143054,-0.0123964237846327,
3.50831762943));
#57307=CARTESIAN_POINT('Ctrl Pts',(11.8731129503683,0.406861336540243,3.72365044295193));
#57308=CARTESIAN_POINT('Ctrl Pts',(11.9208287864311,0.452492071153857,4.1927593068956));
#57309=CARTESIAN_POINT('Ctrl Pts',(11.9553246883346,0.185075114683736,4.40392780377));
#57310=CARTESIAN_POINT('Ctrl Pts',(11.9739153115504,0.0236883133891,4.41635013933017));
#57311=CARTESIAN_POINT('Ctrl Pts',(11.9766006560786,0.000344603143201134,
4.41614202049347));
#57312=CARTESIAN_POINT('Ctrl Pts',(11.7733993439214,-0.000215373091504231,
4.41642415578018));
#57313=CARTESIAN_POINT('Ctrl Pts',(11.7748135191091,-0.0124870613922979,
4.41650138834433));
#57314=CARTESIAN_POINT('Ctrl Pts',(11.7921329729843,-0.162701432614141,
4.41043584391465));
#57315=CARTESIAN_POINT('Ctrl Pts',(11.8253577055472,-0.435670260442099,
4.22824690363353));
#57316=CARTESIAN_POINT('Ctrl Pts',(11.8730735416101,-0.427612859293677,
3.75699286549843));
#57317=CARTESIAN_POINT('Ctrl Pts',(11.9207893776729,-0.0268719897862959,
3.50889601812151));
#57318=CARTESIAN_POINT('Ctrl Pts',(11.9685052137357,0.398545841420554,3.71178751390968));
#57319=CARTESIAN_POINT('Ctrl Pts',(12.0162210497986,0.457972894034889,4.17934897039372));
#57320=CARTESIAN_POINT('Ctrl Pts',(12.0511857598605,0.193343073938706,4.40127740506484));
#57321=CARTESIAN_POINT('Ctrl Pts',(12.0702451912347,0.0278098881012828,
4.41627371553856));
#57322=CARTESIAN_POINT('Ctrl Pts',(12.0733993439214,0.000370082491451453,
4.41602009379308));
#57323=CARTESIAN_POINT('Origin',(3.42660065607856,0.,4.));
#57324=CARTESIAN_POINT('',(11.3766006560786,-0.000206048103233091,4.41528588740701));
#57325=CARTESIAN_POINT('',(11.4733993439214,-0.000260100423148973,4.41535533657191));
#57326=CARTESIAN_POINT('',(3.42660065607856,4.87367679877478E-13,4.415875));
#57327=CARTESIAN_POINT('Ctrl Pts',(11.3766006560786,-0.000206048103232999,
4.41528588740701));
#57328=CARTESIAN_POINT('Ctrl Pts',(11.383051967299,-0.0565815589273492,
4.41553770218085));
#57329=CARTESIAN_POINT('Ctrl Pts',(11.4054085572071,-0.251630532720247,
4.37854193442951));
#57330=CARTESIAN_POINT('Ctrl Pts',(11.4436704258028,-0.485070265991237,
4.08131458604192));
#57331=CARTESIAN_POINT('Ctrl Pts',(11.4913862618656,-0.330742172127369,
3.63597412121053));
#57332=CARTESIAN_POINT('Ctrl Pts',(11.5391020979284,0.127311547523522,3.52492422212962));
#57333=CARTESIAN_POINT('Ctrl Pts',(11.5868179339912,0.468453114143607,3.85014371984754));
#57334=CARTESIAN_POINT('Ctrl Pts',(11.632650786708,0.382920955827079,4.29471395365306));
#57335=CARTESIAN_POINT('Ctrl Pts',(11.6625783607371,0.121478760105588,4.41540989855421));
#57336=CARTESIAN_POINT('Ctrl Pts',(11.6766006560786,-0.000272404999166455,
4.41633191892761));
#57337=CARTESIAN_POINT('Ctrl Pts',(11.4733993439214,-0.000260100423148869,
4.41535533657191));
#57338=CARTESIAN_POINT('Ctrl Pts',(11.4793818469834,-0.0525169974224216,
4.41565306322741));
#57339=CARTESIAN_POINT('Ctrl Pts',(11.501269628733,-0.243338890257842,4.3822327073369));
#57340=CARTESIAN_POINT('Ctrl Pts',(11.5390626891702,-0.482464979911041,
4.09556551685319));
#57341=CARTESIAN_POINT('Ctrl Pts',(11.586778525233,-0.341319923258817,3.64587299617429));
#57342=CARTESIAN_POINT('Ctrl Pts',(11.6344943612959,0.113264470804062,3.5213807520529));
#57343=CARTESIAN_POINT('Ctrl Pts',(11.6822101973587,0.463836358529674,3.83641192782507));
#57344=CARTESIAN_POINT('Ctrl Pts',(11.7285118582339,0.390694138047139,4.28787953265104));
#57345=CARTESIAN_POINT('Ctrl Pts',(11.7589082404215,0.125533053862222,4.41563275094549));
#57346=CARTESIAN_POINT('Ctrl Pts',(11.7733993439214,-0.000215373091504231,
4.41642415578018));
#57347=CARTESIAN_POINT('Origin',(3.42660065607856,0.,4.));
#57348=CARTESIAN_POINT('',(11.0766006560786,0.000352537510456688,4.41557576695298));
#57349=CARTESIAN_POINT('',(11.1733993439214,0.000319650745578964,4.41547275084625));
#57350=CARTESIAN_POINT('',(3.42660065607856,4.87367679877478E-13,4.415875));
#57351=CARTESIAN_POINT('Ctrl Pts',(11.0766006560786,0.000352537510456667,
4.41557576695298));
#57352=CARTESIAN_POINT('Ctrl Pts',(11.0876202951733,-0.0957751134661499,
4.41480617263661));
#57353=CARTESIAN_POINT('Ctrl Pts',(11.1145452129557,-0.331820540820521,
4.33374203885914));
#57354=CARTESIAN_POINT('Ctrl Pts',(11.1573754094257,-0.488245699001722,
3.94065893278431));
#57355=CARTESIAN_POINT('Ctrl Pts',(11.2050912454886,-0.214150733603143,
3.55723066033293));
#57356=CARTESIAN_POINT('Ctrl Pts',(11.2528070815514,0.256602145595791,3.58040428537983));
#57357=CARTESIAN_POINT('Ctrl Pts',(11.3005229176142,0.491713326162588,3.98889911147238));
#57358=CARTESIAN_POINT('Ctrl Pts',(11.3417874424566,0.304539430122629,4.35098016691413));
#57359=CARTESIAN_POINT('Ctrl Pts',(11.3671466886114,0.0824085130402235,
4.41491686960609));
#57360=CARTESIAN_POINT('Ctrl Pts',(11.3766006560786,-0.000206048103232999,
4.41528588740701));
#57361=CARTESIAN_POINT('Ctrl Pts',(11.1733993439214,0.000319650745578978,
4.41547275084625));
#57362=CARTESIAN_POINT('Ctrl Pts',(11.1839501748577,-0.0917759901056567,
4.4148158243975));
#57363=CARTESIAN_POINT('Ctrl Pts',(11.2104062844816,-0.32368545017211,4.33911969104981));
#57364=CARTESIAN_POINT('Ctrl Pts',(11.2527676727932,-0.489781601228288,
3.95506440219344));
#57365=CARTESIAN_POINT('Ctrl Pts',(11.300483508856,-0.227098200695192,3.56372986339542));
#57366=CARTESIAN_POINT('Ctrl Pts',(11.3481993449188,0.244132971891272,3.57302890392028));
#57367=CARTESIAN_POINT('Ctrl Pts',(11.3959151809817,0.491173079921361,3.97442207176994));
#57368=CARTESIAN_POINT('Ctrl Pts',(11.4376485139825,0.312739912806573,4.34603313379779));
#57369=CARTESIAN_POINT('Ctrl Pts',(11.4634765682958,0.0864149014017155,
4.41486151738456));
#57370=CARTESIAN_POINT('Ctrl Pts',(11.4733993439214,-0.000260100423148869,
4.41535533657191));
#57371=CARTESIAN_POINT('Origin',(3.42660065607856,0.,4.));
#57372=CARTESIAN_POINT('',(10.7766006560786,5.16128798610187E-5,4.41655360457584));
#57373=CARTESIAN_POINT('',(10.8733993439214,0.000125523266313186,4.41651574507477));
#57374=CARTESIAN_POINT('',(3.42660065607856,4.87367679877478E-13,4.415875));
#57375=CARTESIAN_POINT('Ctrl Pts',(10.7766006560786,5.16128798610299E-5,
4.41655360457584));
#57376=CARTESIAN_POINT('Ctrl Pts',(10.7921886230477,-0.135103241057852,
4.41631783152902));
#57377=CARTESIAN_POINT('Ctrl Pts',(10.8236818687044,-0.408598944994929,
4.27108057505162));
#57378=CARTESIAN_POINT('Ctrl Pts',(10.8710803930487,-0.451470021714238,
3.80485891169382));
#57379=CARTESIAN_POINT('Ctrl Pts',(10.9187962291115,-0.080036233235122,
3.51471716883706));
#57380=CARTESIAN_POINT('Ctrl Pts',(10.9665120651743,0.364896059739551,3.6702181168734));
#57381=CARTESIAN_POINT('Ctrl Pts',(11.0142279012372,0.47473868640782,4.1285628425314));
#57382=CARTESIAN_POINT('Ctrl Pts',(11.0509240982053,0.223935965514619,4.3902602363912));
#57383=CARTESIAN_POINT('Ctrl Pts',(11.0717150164857,0.0429714521173939,
4.4159169723618));
#57384=CARTESIAN_POINT('Ctrl Pts',(11.0766006560786,0.000352537510456667,
4.41557576695298));
#57385=CARTESIAN_POINT('Ctrl Pts',(10.8733993439214,0.000125523266313226,
4.41651574507477));
#57386=CARTESIAN_POINT('Ctrl Pts',(10.888518502732,-0.130996444363694,4.41599591363288));
#57387=CARTESIAN_POINT('Ctrl Pts',(10.9195429402303,-0.400997532511054,
4.27840016053723));
#57388=CARTESIAN_POINT('Ctrl Pts',(10.9664726564161,-0.45702143577077,3.81824018018824));
#57389=CARTESIAN_POINT('Ctrl Pts',(11.014188492479,-0.0942939790271268,
3.51728489730359));
#57390=CARTESIAN_POINT('Ctrl Pts',(11.0619043285418,0.355025089556487,3.65961432075161));
#57391=CARTESIAN_POINT('Ctrl Pts',(11.1096201646047,0.478319155637209,4.11452515096033));
#57392=CARTESIAN_POINT('Ctrl Pts',(11.1467851697312,0.23222845252417,4.38693182090163));
#57393=CARTESIAN_POINT('Ctrl Pts',(11.1680448961701,0.0470573247768451,
4.41580613485813));
#57394=CARTESIAN_POINT('Ctrl Pts',(11.1733993439214,0.000319650745578978,
4.41547275084625));
#57395=CARTESIAN_POINT('Origin',(3.42660065607856,0.,4.));
#57396=CARTESIAN_POINT('',(10.4766006560786,-0.000378910032885682,4.4157309619862));
#57397=CARTESIAN_POINT('',(10.5733993439214,-0.000383826598418624,4.41585315377736));
#57398=CARTESIAN_POINT('',(3.42660065607856,4.87367679877478E-13,4.415875));
#57399=CARTESIAN_POINT('Ctrl Pts',(10.4766006560786,-0.000378910032885704,
4.4157309619862));
#57400=CARTESIAN_POINT('Ctrl Pts',(10.4808516722344,-0.0374267536145521,
4.41605913507464));
#57401=CARTESIAN_POINT('Ctrl Pts',(10.5010079670778,-0.212714974368116,
4.3945277200383));
#57402=CARTESIAN_POINT('Ctrl Pts',(10.5370695406088,-0.469236294399976,
4.14738563318641));
#57403=CARTESIAN_POINT('Ctrl Pts',(10.5847853766716,-0.377752434501872,
3.68502647241413));
#57404=CARTESIAN_POINT('Ctrl Pts',(10.6325012127345,0.0606272984676223,
3.51191234851464));
#57405=CARTESIAN_POINT('Ctrl Pts',(10.6802170487973,0.443332050383407,3.78701662516801));
#57406=CARTESIAN_POINT('Ctrl Pts',(10.7279328848602,0.418918158891686,4.25770681210006));
#57407=CARTESIAN_POINT('Ctrl Pts',(10.7600607539539,0.143455624352724,4.41528584951654));
#57408=CARTESIAN_POINT('Ctrl Pts',(10.7762833443601,0.00280285164340033,
4.41655840401831));
#57409=CARTESIAN_POINT('Ctrl Pts',(10.7766006560786,5.16128798610299E-5,
4.41655360457584));
#57410=CARTESIAN_POINT('Ctrl Pts',(10.5733993439214,-0.000383826598418617,
4.41585315377736));
#57411=CARTESIAN_POINT('Ctrl Pts',(10.5771815519187,-0.0333213161677604,
4.41615637378185));
#57412=CARTESIAN_POINT('Ctrl Pts',(10.5968690386037,-0.20443114816448,4.39750812937281));
#57413=CARTESIAN_POINT('Ctrl Pts',(10.6324618039763,-0.464691964107356,
4.16114156306187));
#57414=CARTESIAN_POINT('Ctrl Pts',(10.6801776400391,-0.386865111317189,
3.69628860657276));
#57415=CARTESIAN_POINT('Ctrl Pts',(10.7278934761019,0.0462259258804368,
3.51033849586834));
#57416=CARTESIAN_POINT('Ctrl Pts',(10.7756093121648,0.436866984064762,3.77405207881873));
#57417=CARTESIAN_POINT('Ctrl Pts',(10.8233251482276,0.426326368719826,4.24525711444552));
#57418=CARTESIAN_POINT('Ctrl Pts',(10.8559218254798,0.151674250044741,4.4132974389186));
#57419=CARTESIAN_POINT('Ctrl Pts',(10.8726132240444,0.00694320316194716,
4.41654277368359));
#57420=CARTESIAN_POINT('Ctrl Pts',(10.8733993439214,0.000125523266313226,
4.41651574507477));
#57421=CARTESIAN_POINT('Origin',(3.42660065607856,0.,4.));
#57422=CARTESIAN_POINT('',(10.1766006560786,0.000123197149224082,4.41521991402453));
#57423=CARTESIAN_POINT('',(10.2733993439214,5.7336166378985E-5,4.41519339896199));
#57424=CARTESIAN_POINT('',(3.42660065607856,4.87367679877478E-13,4.415875));
#57425=CARTESIAN_POINT('Ctrl Pts',(10.1766006560786,0.000123197149224097,
4.41521991402453));
#57426=CARTESIAN_POINT('Ctrl Pts',(10.1854200001087,-0.0769762270984491,
4.41501595190525));
#57427=CARTESIAN_POINT('Ctrl Pts',(10.2101446228264,-0.293404201931947,
4.35739193013711));
#57428=CARTESIAN_POINT('Ctrl Pts',(10.2507745242318,-0.491764996345908,
4.00850959581219));
#57429=CARTESIAN_POINT('Ctrl Pts',(10.2984903602946,-0.273124940234581,
3.59096700393021));
#57430=CARTESIAN_POINT('Ctrl Pts',(10.3462061963575,0.196329951061554,3.54904570612073));
#57431=CARTESIAN_POINT('Ctrl Pts',(10.3939220324203,0.485492027373267,3.92124267520431));
#57432=CARTESIAN_POINT('Ctrl Pts',(10.4373868523273,0.34277731801193,4.32616121393696));
#57433=CARTESIAN_POINT('Ctrl Pts',(10.4649463935468,0.101188639822117,4.41483126760997));
#57434=CARTESIAN_POINT('Ctrl Pts',(10.4766006560786,-0.000378910032885704,
4.4157309619862));
#57435=CARTESIAN_POINT('Ctrl Pts',(10.2733993439214,5.73361663789851E-5,
4.41519339896199));
#57436=CARTESIAN_POINT('Ctrl Pts',(10.2817498797931,-0.0729553575157724,
4.41510384014646));
#57437=CARTESIAN_POINT('Ctrl Pts',(10.3060056943524,-0.285157432566911,
4.36192175935665));
#57438=CARTESIAN_POINT('Ctrl Pts',(10.3461667875993,-0.491301045992024,
4.02298928139638));
#57439=CARTESIAN_POINT('Ctrl Pts',(10.3938826236621,-0.285053227451061,
3.599188470261));
#57440=CARTESIAN_POINT('Ctrl Pts',(10.4415984597249,0.182963355965895,3.54345905416307));
#57441=CARTESIAN_POINT('Ctrl Pts',(10.4893142957878,0.482961874346273,3.9069782134126));
#57442=CARTESIAN_POINT('Ctrl Pts',(10.5332479238533,0.35082465130295,4.32033516829581));
#57443=CARTESIAN_POINT('Ctrl Pts',(10.5612762732311,0.105190355120073,4.41488124595214));
#57444=CARTESIAN_POINT('Ctrl Pts',(10.5733993439214,-0.000383826598418617,
4.41585315377736));
#57445=CARTESIAN_POINT('Origin',(3.42660065607856,0.,4.));
#57446=CARTESIAN_POINT('',(9.87660065607859,0.000332404019580576,4.41618417038907));
#57447=CARTESIAN_POINT('',(9.9733993439214,0.000362444897862246,4.41606425076498));
#57448=CARTESIAN_POINT('',(3.42660065607856,4.87367679877478E-13,4.415875));
#57449=CARTESIAN_POINT('Ctrl Pts',(9.87660065607859,0.000332404019580564,
4.41618417038907));
#57450=CARTESIAN_POINT('Ctrl Pts',(9.88998832798303,-0.116016130490024,
4.41516972706101));
#57451=CARTESIAN_POINT('Ctrl Pts',(9.91928127857509,-0.372296869871387,
4.30364082544554));
#57452=CARTESIAN_POINT('Ctrl Pts',(9.96447950785476,-0.474054618562381,
3.8689372536849));
#57453=CARTESIAN_POINT('Ctrl Pts',(10.0121953439176,-0.146148770628728,
3.53037700046135));
#57454=CARTESIAN_POINT('Ctrl Pts',(10.0599111799804,0.315967742161179,3.62307877379278));
#57455=CARTESIAN_POINT('Ctrl Pts',(10.1076270160433,0.487926215535836,4.06191310882887));
#57456=CARTESIAN_POINT('Ctrl Pts',(10.146523508076,0.262848409674369,4.37329037489646));
#57457=CARTESIAN_POINT('Ctrl Pts',(10.1695147214211,0.062069015396409,4.41538378814543));
#57458=CARTESIAN_POINT('Ctrl Pts',(10.1766006560786,0.000123197149224097,
4.41521991402453));
#57459=CARTESIAN_POINT('Ctrl Pts',(9.9733993439214,0.000362444897862267,
4.41606425076498));
#57460=CARTESIAN_POINT('Ctrl Pts',(9.9863182076674,-0.111995531308361,4.41503480155798));
#57461=CARTESIAN_POINT('Ctrl Pts',(10.015142350101,-0.364380386131072,4.30999810797653));
#57462=CARTESIAN_POINT('Ctrl Pts',(10.0598717712222,-0.477709011270712,
3.88295588266498));
#57463=CARTESIAN_POINT('Ctrl Pts',(10.1075876072851,-0.159916626226494,
3.53488507064564));
#57464=CARTESIAN_POINT('Ctrl Pts',(10.1553034433479,0.304729657315094,3.61393645496551));
#57465=CARTESIAN_POINT('Ctrl Pts',(10.2030192794107,0.489538007675758,4.04751593304174));
#57466=CARTESIAN_POINT('Ctrl Pts',(10.2423845796019,0.271127379494919,4.3692182851415));
#57467=CARTESIAN_POINT('Ctrl Pts',(10.2658446011055,0.0661120339180705,
4.41527442296197));
#57468=CARTESIAN_POINT('Ctrl Pts',(10.2733993439214,5.73361663789851E-5,
4.41519339896199));
#57469=CARTESIAN_POINT('Origin',(3.42660065607856,0.,4.));
#57470=CARTESIAN_POINT('',(9.57660065607859,-0.000290304052950346,4.41629504206998));
#57471=CARTESIAN_POINT('',(9.6733993439214,-0.000236899196693507,4.41639317328699));
#57472=CARTESIAN_POINT('',(3.42660065607856,4.87367679877478E-13,4.415875));
#57473=CARTESIAN_POINT('Ctrl Pts',(9.57660065607859,-0.000290304052950335,
4.41629504206998));
#57474=CARTESIAN_POINT('Ctrl Pts',(9.57865137716975,-0.0181001948149981,
4.41643644713422));
#57475=CARTESIAN_POINT('Ctrl Pts',(9.59660737694851,-0.173896467062472,
4.40729888742394));
#57476=CARTESIAN_POINT('Ctrl Pts',(9.63046865541489,-0.444448234747017,
4.21064422964382));
#57477=CARTESIAN_POINT('Ctrl Pts',(9.67818449147773,-0.41755432743774,3.74008922975375));
#57478=CARTESIAN_POINT('Ctrl Pts',(9.72590032754057,-0.00721385634321597,
3.50821428942208));
#57479=CARTESIAN_POINT('Ctrl Pts',(9.77361616360341,0.40975121003073,3.72795373420991));
#57480=CARTESIAN_POINT('Ctrl Pts',(9.82133199966624,0.450435435400681,4.19751745084266));
#57481=CARTESIAN_POINT('Ctrl Pts',(9.85566016382464,0.182118884769847,4.40484283743537));
#57482=CARTESIAN_POINT('Ctrl Pts',(9.87408304929542,0.0222122246324328,
4.41637494063069));
#57483=CARTESIAN_POINT('Ctrl Pts',(9.87660065607859,0.000332404019580564,
4.41618417038907));
#57484=CARTESIAN_POINT('Ctrl Pts',(9.6733993439214,-0.00023689919669354,
4.41639317328699));
#57485=CARTESIAN_POINT('Ctrl Pts',(9.67498125685411,-0.0139668454918635,
4.4164864708936));
#57486=CARTESIAN_POINT('Ctrl Pts',(9.69246844847443,-0.165649677201134,
4.40963259460397));
#57487=CARTESIAN_POINT('Ctrl Pts',(9.72586091878235,-0.438051576325333,
4.22364266437974));
#57488=CARTESIAN_POINT('Ctrl Pts',(9.77357675484519,-0.425028039486299,
3.75249971615691));
#57489=CARTESIAN_POINT('Ctrl Pts',(9.82129259090803,-0.0216947140899849,
3.50864008686857));
#57490=CARTESIAN_POINT('Ctrl Pts',(9.86900842697087,0.401561201071248,3.7160038263529));
#57491=CARTESIAN_POINT('Ctrl Pts',(9.91672426303371,0.456057286475463,4.18416562194019));
#57492=CARTESIAN_POINT('Ctrl Pts',(9.95152123535055,0.190383912560376,4.40224154849284));
#57493=CARTESIAN_POINT('Ctrl Pts',(9.97041292897978,0.0263359008882403,
4.4163022254471));
#57494=CARTESIAN_POINT('Ctrl Pts',(9.9733993439214,0.000362444897862267,
4.41606425076498));
#57495=CARTESIAN_POINT('Origin',(3.42660065607856,0.,4.));
#57496=CARTESIAN_POINT('',(9.27660065607858,-0.000185084181660103,4.41526520375254));
#57497=CARTESIAN_POINT('',(9.37339934392141,-0.000241596553487405,4.41532857883968));
#57498=CARTESIAN_POINT('',(3.42660065607856,4.87367679877478E-13,4.415875));
#57499=CARTESIAN_POINT('Ctrl Pts',(9.27660065607858,-0.000185084181660189,
4.41526520375254));
#57500=CARTESIAN_POINT('Ctrl Pts',(9.28321970504406,-0.0580335922681754,
4.4154966095816));
#57501=CARTESIAN_POINT('Ctrl Pts',(9.30574403269715,-0.254596444523232,
4.37718269734299));
#57502=CARTESIAN_POINT('Ctrl Pts',(9.34417363903789,-0.485900307124067,
4.07619787653679));
#57503=CARTESIAN_POINT('Ctrl Pts',(9.39188947510068,-0.326887306273347,
3.63250862071426));
#57504=CARTESIAN_POINT('Ctrl Pts',(9.43960531116356,0.13231133773591,3.52629235307153));
#57505=CARTESIAN_POINT('Ctrl Pts',(9.48732114722637,0.470006444430667,3.85508910653225));
#57506=CARTESIAN_POINT('Ctrl Pts',(9.53298626219807,0.380123833963086,4.29710958399465));
#57507=CARTESIAN_POINT('Ctrl Pts',(9.56274609848214,0.120032327051623,4.41533971732329));
#57508=CARTESIAN_POINT('Ctrl Pts',(9.57660065607859,-0.000290304052950335,
4.41629504206998));
#57509=CARTESIAN_POINT('Ctrl Pts',(9.3733993439214,-0.000241596553487357,
4.41532857883968));
#57510=CARTESIAN_POINT('Ctrl Pts',(9.37954958472843,-0.0539723465869793,
4.41561177485228));
#57511=CARTESIAN_POINT('Ctrl Pts',(9.40160510422307,-0.246305905820531,
4.3809303471886));
#57512=CARTESIAN_POINT('Ctrl Pts',(9.43956590240532,-0.483445357410111,
4.09047547319903));
#57513=CARTESIAN_POINT('Ctrl Pts',(9.48728173846818,-0.337568794959357,
3.64229546617122));
#57514=CARTESIAN_POINT('Ctrl Pts',(9.53499757453099,0.118302386066128,3.5226010365501));
#57515=CARTESIAN_POINT('Ctrl Pts',(9.58271341059386,0.465534665650901,3.84130942079228));
#57516=CARTESIAN_POINT('Ctrl Pts',(9.62884733372396,0.387920650713885,4.29034844530944));
#57517=CARTESIAN_POINT('Ctrl Pts',(9.65907597816649,0.124080336294106,4.41554841393524));
#57518=CARTESIAN_POINT('Ctrl Pts',(9.6733993439214,-0.00023689919669354,
4.41639317328699));
#57519=CARTESIAN_POINT('Origin',(3.42660065607856,0.,4.));
#57520=CARTESIAN_POINT('',(8.97660065607858,0.000361621133123973,4.41561526113518));
#57521=CARTESIAN_POINT('',(9.0733993439214,0.00033264130393823,4.41550825894961));
#57522=CARTESIAN_POINT('',(3.42660065607856,4.87367679877478E-13,4.415875));
#57523=CARTESIAN_POINT('Ctrl Pts',(8.97660065607858,0.000361621133123963,
4.41561526113518));
#57524=CARTESIAN_POINT('Ctrl Pts',(8.98778803291839,-0.097205817696177,
4.41480833810253));
#57525=CARTESIAN_POINT('Ctrl Pts',(9.01488068844582,-0.334723089553266,
4.33177224018802));
#57526=CARTESIAN_POINT('Ctrl Pts',(9.05787862266083,-0.487593182843731,
3.93551656882348));
#57527=CARTESIAN_POINT('Ctrl Pts',(9.10559445872368,-0.209472459465777,
3.55499829935456));
#57528=CARTESIAN_POINT('Ctrl Pts',(9.15331029478651,0.261010046587687,3.58313193881964));
#57529=CARTESIAN_POINT('Ctrl Pts',(9.20102613084934,0.491803010703882,3.99408193320625));
#57530=CARTESIAN_POINT('Ctrl Pts',(9.24212291794672,0.301599829163518,4.35270650246492));
#57531=CARTESIAN_POINT('Ctrl Pts',(9.26731442635645,0.0809737859182142,
4.41494055172187));
#57532=CARTESIAN_POINT('Ctrl Pts',(9.27660065607858,-0.000185084181660189,
4.41526520375254));
#57533=CARTESIAN_POINT('Ctrl Pts',(9.0733993439214,0.000332641303938268,
4.41550825894961));
#57534=CARTESIAN_POINT('Ctrl Pts',(9.08411791260276,-0.093207009794584,
4.4148098083896));
#57535=CARTESIAN_POINT('Ctrl Pts',(9.11074175997173,-0.326599857706223,
4.33721709571948));
#57536=CARTESIAN_POINT('Ctrl Pts',(9.1532708860283,-0.489280820139143,3.94990505119329));
#57537=CARTESIAN_POINT('Ctrl Pts',(9.20098672209113,-0.222487703095825,
3.56136068709803));
#57538=CARTESIAN_POINT('Ctrl Pts',(9.24870255815399,0.248619295113741,3.57562555337399));
#57539=CARTESIAN_POINT('Ctrl Pts',(9.29641839421681,0.49141536912078,3.97960000382683));
#57540=CARTESIAN_POINT('Ctrl Pts',(9.33798398947263,0.309808547095179,4.34782394055348));
#57541=CARTESIAN_POINT('Ctrl Pts',(9.36364430604082,0.0849819773478622,
4.41487939515448));
#57542=CARTESIAN_POINT('Ctrl Pts',(9.3733993439214,-0.000241596553487357,
4.41532857883968));
#57543=CARTESIAN_POINT('Origin',(3.42660065607856,0.,4.));
#57544=CARTESIAN_POINT('',(8.67660065607859,2.43999233753954E-5,4.41655967853978));
#57545=CARTESIAN_POINT('',(8.77339934392141,9.9565801791445E-5,4.41653262406943));
#57546=CARTESIAN_POINT('',(3.42660065607856,4.87367679877478E-13,4.415875));
#57547=CARTESIAN_POINT('Ctrl Pts',(8.67660065607859,2.43999233753836E-5,
4.41655967853978));
#57548=CARTESIAN_POINT('Ctrl Pts',(8.69235636079272,-0.136579453435425,
4.41644398151286));
#57549=CARTESIAN_POINT('Ctrl Pts',(8.72401734419445,-0.411298873006737,
4.26841067400337));
#57550=CARTESIAN_POINT('Ctrl Pts',(8.7715836062838,-0.449388340942622,3.80011167148426));
#57551=CARTESIAN_POINT('Ctrl Pts',(8.81929944234665,-0.0749173544856965,
3.51390061216986));
#57552=CARTESIAN_POINT('Ctrl Pts',(8.86701527840948,0.368351391347115,3.67408210030036));
#57553=CARTESIAN_POINT('Ctrl Pts',(8.91473111447233,0.473357386691186,4.13355901061654));
#57554=CARTESIAN_POINT('Ctrl Pts',(8.95125957369535,0.220969504140389,4.39141457480799));
#57555=CARTESIAN_POINT('Ctrl Pts',(8.97188275423077,0.0415074238114615,
4.41595555392421));
#57556=CARTESIAN_POINT('Ctrl Pts',(8.97660065607858,0.000361621133123963,
4.41561526113518));
#57557=CARTESIAN_POINT('Ctrl Pts',(8.77339934392141,9.95658017914599E-5,
4.41653262406943));
#57558=CARTESIAN_POINT('Ctrl Pts',(8.78868624047708,-0.132462770989084,
4.416105976883));
#57559=CARTESIAN_POINT('Ctrl Pts',(8.81987841572037,-0.403726445587972,
4.27580529254432));
#57560=CARTESIAN_POINT('Ctrl Pts',(8.86697586965126,-0.455080472922433,
3.81343369002772));
#57561=CARTESIAN_POINT('Ctrl Pts',(8.91469170571412,-0.0892013699275644,
3.51631793453238));
#57562=CARTESIAN_POINT('Ctrl Pts',(8.96240754177693,0.358592723611288,3.66337486216116));
#57563=CARTESIAN_POINT('Ctrl Pts',(9.0101233778398,0.477085601399612,4.11955983351088));
#57564=CARTESIAN_POINT('Ctrl Pts',(9.04712064522126,0.229261233371815,4.38814011953822));
#57565=CARTESIAN_POINT('Ctrl Pts',(9.06821263391514,0.0455964315317218,
4.41584623882512));
#57566=CARTESIAN_POINT('Ctrl Pts',(9.0733993439214,0.000332641303938268,
4.41550825894961));
#57567=CARTESIAN_POINT('Origin',(3.42660065607856,0.,4.));
#57568=CARTESIAN_POINT('',(8.37660065607859,-0.000374086211409503,4.41568853448753));
#57569=CARTESIAN_POINT('',(8.47339934392141,-0.000383538171196851,4.41580895574666));
#57570=CARTESIAN_POINT('',(3.42660065607856,4.87367679877478E-13,4.415875));
#57571=CARTESIAN_POINT('Ctrl Pts',(8.37660065607859,-0.000374086211409545,
4.41568853448753));
#57572=CARTESIAN_POINT('Ctrl Pts',(8.38101940997943,-0.0388937529272332,
4.41602262289185));
#57573=CARTESIAN_POINT('Ctrl Pts',(8.40134344256788,-0.215680110827853,
4.3934260635833));
#57574=CARTESIAN_POINT('Ctrl Pts',(8.43757275384394,-0.470763542849379,
4.14243212971755));
#57575=CARTESIAN_POINT('Ctrl Pts',(8.48528858990678,-0.37441192437669,3.68106280283335));
#57576=CARTESIAN_POINT('Ctrl Pts',(8.53300442596962,0.0657679253190804,
3.51257841158684));
#57577=CARTESIAN_POINT('Ctrl Pts',(8.58072026203246,0.445552077224736,3.79170076492532));
#57578=CARTESIAN_POINT('Ctrl Pts',(8.62843609809529,0.41617890091499,4.26210751092856));
#57579=CARTESIAN_POINT('Ctrl Pts',(8.66039622944401,0.140517691799823,4.41596716726027));
#57580=CARTESIAN_POINT('Ctrl Pts',(8.6764510821051,0.00132122424898086,
4.41656077688887));
#57581=CARTESIAN_POINT('Ctrl Pts',(8.67660065607859,2.43999233753836E-5,
4.41655967853978));
#57582=CARTESIAN_POINT('Ctrl Pts',(8.47339934392141,-0.000383538171196768,
4.41580895574666));
#57583=CARTESIAN_POINT('Ctrl Pts',(8.47734928966379,-0.0347911067166248,
4.41612244784963));
#57584=CARTESIAN_POINT('Ctrl Pts',(8.4972045140938,-0.207394442561863,4.39645832432586));
#57585=CARTESIAN_POINT('Ctrl Pts',(8.5329650172114,-0.466364439759318,4.15623518867385));
#57586=CARTESIAN_POINT('Ctrl Pts',(8.58068085327425,-0.383642787608637,
3.69222827230584));
#57587=CARTESIAN_POINT('Ctrl Pts',(8.62839668933707,0.0513839395061145,
3.51085286915611));
#57588=CARTESIAN_POINT('Ctrl Pts',(8.67611252539993,0.439224004328866,3.77866880275638));
#57589=CARTESIAN_POINT('Ctrl Pts',(8.72382836146275,0.42371790764641,4.24973658040369));
#57590=CARTESIAN_POINT('Ctrl Pts',(8.75625730096992,0.148732406864234,4.41402322426773));
#57591=CARTESIAN_POINT('Ctrl Pts',(8.77278096178947,0.00546194790078228,
4.41654988270631));
#57592=CARTESIAN_POINT('Ctrl Pts',(8.77339934392141,9.95658017914599E-5,
4.41653262406943));
#57593=CARTESIAN_POINT('Origin',(3.42660065607856,0.,4.));
#57594=CARTESIAN_POINT('',(8.07660065607859,0.000145957947245773,4.41523406184916));
#57595=CARTESIAN_POINT('',(8.1733993439214,8.12049300508987E-5,4.41520065480005));
#57596=CARTESIAN_POINT('',(3.42660065607856,4.87367679877478E-13,4.415875));
#57597=CARTESIAN_POINT('Ctrl Pts',(8.07660065607858,0.00014595794724577,
4.41523406184916));
#57598=CARTESIAN_POINT('Ctrl Pts',(8.08558773785375,-0.0784131624224431,
4.41498734772332));
#57599=CARTESIAN_POINT('Ctrl Pts',(8.11048009831652,-0.296350794919178,
4.35572875890285));
#57600=CARTESIAN_POINT('Ctrl Pts',(8.15127773746691,-0.491827368180951,
4.00332637343646));
#57601=CARTESIAN_POINT('Ctrl Pts',(8.19899357352975,-0.268798940774433,
3.58811123553743));
#57602=CARTESIAN_POINT('Ctrl Pts',(8.24670940959259,0.201071689948468,3.55113988776764));
#57603=CARTESIAN_POINT('Ctrl Pts',(8.29442524565542,0.486295093906121,3.92636368766143));
#57604=CARTESIAN_POINT('Ctrl Pts',(8.33772232781743,0.339888039743562,4.32819890206972));
#57605=CARTESIAN_POINT('Ctrl Pts',(8.36511413129181,0.0997575609540166,
4.41482007364463));
#57606=CARTESIAN_POINT('Ctrl Pts',(8.37660065607859,-0.000374086211409545,
4.41568853448753));
#57607=CARTESIAN_POINT('Ctrl Pts',(8.1733993439214,8.12049300509751E-5,
4.41520065480005));
#57608=CARTESIAN_POINT('Ctrl Pts',(8.18191761753811,-0.0743948540356096,
4.41507113968239));
#57609=CARTESIAN_POINT('Ctrl Pts',(8.20634116984244,-0.288109900049694,
4.36032095112539));
#57610=CARTESIAN_POINT('Ctrl Pts',(8.24667000083438,-0.491516046133,4.01781014446235));
#57611=CARTESIAN_POINT('Ctrl Pts',(8.29438583689722,-0.280813212199106,
3.59620653211525));
#57612=CARTESIAN_POINT('Ctrl Pts',(8.34210167296004,0.187764715363875,3.54541267448783));
#57613=CARTESIAN_POINT('Ctrl Pts',(8.38981750902289,0.483915415676709,3.91207335260334));
#57614=CARTESIAN_POINT('Ctrl Pts',(8.43358339934334,0.347950231939931,4.32244196179047));
#57615=CARTESIAN_POINT('Ctrl Pts',(8.46144401097618,0.1037581297464,4.41486010664565));
#57616=CARTESIAN_POINT('Ctrl Pts',(8.47339934392141,-0.000383538171196768,
4.41580895574666));
#57617=CARTESIAN_POINT('Origin',(3.42660065607856,0.,4.));
#57618=CARTESIAN_POINT('',(7.77660065607858,0.000318631424802313,4.41622521972442));
#57619=CARTESIAN_POINT('',(7.8733993439214,0.000353153796088606,4.4161078667978));
#57620=CARTESIAN_POINT('',(3.42660065607856,4.87367679877478E-13,4.415875));
#57621=CARTESIAN_POINT('Ctrl Pts',(7.77660065607859,0.000318631424802297,
4.41622521972442));
#57622=CARTESIAN_POINT('Ctrl Pts',(7.79015606572807,-0.117457481003694,
4.41522659035305));
#57623=CARTESIAN_POINT('Ctrl Pts',(7.81961675406517,-0.375115671948731,
4.30131743988157));
#57624=CARTESIAN_POINT('Ctrl Pts',(7.86498272108989,-0.472647010158531,
3.86394843388276));
#57625=CARTESIAN_POINT('Ctrl Pts',(7.91269855715272,-0.141191260335066,
3.52886280888004));
#57626=CARTESIAN_POINT('Ctrl Pts',(7.96041439321556,0.31992259635559,3.62642971585976));
#57627=CARTESIAN_POINT('Ctrl Pts',(8.0081302292784,0.48724661017382,4.0670519628834));
#57628=CARTESIAN_POINT('Ctrl Pts',(8.04685898356608,0.259884401562094,4.37470733986759));
#57629=CARTESIAN_POINT('Ctrl Pts',(8.06968245916614,0.0606202562326388,
4.41542398077349));
#57630=CARTESIAN_POINT('Ctrl Pts',(8.07660065607858,0.00014595794724577,
4.41523406184916));
#57631=CARTESIAN_POINT('Ctrl Pts',(7.8733993439214,0.000353153796088627,
4.4161078667978));
#57632=CARTESIAN_POINT('Ctrl Pts',(7.88648594541244,-0.113432877329791,
4.41507910421771));
#57633=CARTESIAN_POINT('Ctrl Pts',(7.9154778255911,-0.367219156371593,4.30774647947464));
#57634=CARTESIAN_POINT('Ctrl Pts',(7.96037498445733,-0.476448943335793,
3.87792777037096));
#57635=CARTESIAN_POINT('Ctrl Pts',(8.0080908205202,-0.1550058622045,3.53322552818936));
#57636=CARTESIAN_POINT('Ctrl Pts',(8.05580665658301,0.308781487260178,3.61716946571973));
#57637=CARTESIAN_POINT('Ctrl Pts',(8.10352249264587,0.489010045760349,4.0526725734847));
#57638=CARTESIAN_POINT('Ctrl Pts',(8.14272005509199,0.26816615642074,4.37069430501912));
#57639=CARTESIAN_POINT('Ctrl Pts',(8.1660123388505,0.064666477720629,4.4153129696744));
#57640=CARTESIAN_POINT('Ctrl Pts',(8.1733993439214,8.12049300509751E-5,
4.41520065480005));
#57641=CARTESIAN_POINT('Origin',(3.42660065607856,0.,4.));
#57642=CARTESIAN_POINT('',(7.47660065607859,-0.000306770237538029,4.41625647512786));
#57643=CARTESIAN_POINT('',(7.5733993439214,-0.000257198714157858,4.41635988094829));
#57644=CARTESIAN_POINT('',(3.42660065607856,4.87367679877478E-13,4.415875));
#57645=CARTESIAN_POINT('Ctrl Pts',(7.47660065607859,-0.00030677023753798,
4.41625647512786));
#57646=CARTESIAN_POINT('Ctrl Pts',(7.47881911491479,-0.0195780710793754,
4.41641565502598));
#57647=CARTESIAN_POINT('Ctrl Pts',(7.4969428524386,-0.176849480241104,4.4064317922735));
#57648=CARTESIAN_POINT('Ctrl Pts',(7.53097186865002,-0.44664354691983,4.20594845626764));
#57649=CARTESIAN_POINT('Ctrl Pts',(7.57868770471286,-0.414791917646955,
3.73570302684109));
#57650=CARTESIAN_POINT('Ctrl Pts',(7.62640354077569,-0.00203048755240202,
3.50816557464413));
#57651=CARTESIAN_POINT('Ctrl Pts',(7.67411937683853,0.412595570264971,3.73228724307244));
#57652=CARTESIAN_POINT('Ctrl Pts',(7.72183521290137,0.448328767436039,4.20225365549051));
#57653=CARTESIAN_POINT('Ctrl Pts',(7.75599563931472,0.179163779268806,4.40574053813273));
#57654=CARTESIAN_POINT('Ctrl Pts',(7.77425078704046,0.0207354574140521,
4.41639833498254));
#57655=CARTESIAN_POINT('Ctrl Pts',(7.77660065607859,0.000318631424802297,
4.41622521972442));
#57656=CARTESIAN_POINT('Ctrl Pts',(7.5733993439214,-0.000257198714157839,
4.41635988094829));
#57657=CARTESIAN_POINT('Ctrl Pts',(7.57514899459915,-0.0154461882200338,
4.41646996636401));
#57658=CARTESIAN_POINT('Ctrl Pts',(7.59280392396451,-0.168599214901356,
4.40881268721627));
#57659=CARTESIAN_POINT('Ctrl Pts',(7.62636413201748,-0.440384235482588,
4.21901358396786));
#57660=CARTESIAN_POINT('Ctrl Pts',(7.67407996808031,-0.422396009600076,
3.7480340579683));
#57661=CARTESIAN_POINT('Ctrl Pts',(7.72179580414317,-0.0165150286377962,
3.50843873354525));
#57662=CARTESIAN_POINT('Ctrl Pts',(7.76951164020598,0.404531957204003,3.72025168374225));
#57663=CARTESIAN_POINT('Ctrl Pts',(7.81722747626884,0.454091022239626,4.18896181724392));
#57664=CARTESIAN_POINT('Ctrl Pts',(7.85185671084063,0.187425762196077,4.40318800700955));
#57665=CARTESIAN_POINT('Ctrl Pts',(7.87058066672482,0.02486112795907,4.41632944836175));
#57666=CARTESIAN_POINT('Ctrl Pts',(7.8733993439214,0.000353153796088627,
4.4161078667978));
#57667=CARTESIAN_POINT('Origin',(3.42660065607856,0.,4.));
#57668=CARTESIAN_POINT('',(7.17660065607858,-0.000163391746992416,4.4152468210878));
#57669=CARTESIAN_POINT('',(7.2733993439214,-0.000222139526412562,4.4153039283715));
#57670=CARTESIAN_POINT('',(3.42660065607856,4.87367679877478E-13,4.415875));
#57671=CARTESIAN_POINT('Ctrl Pts',(7.17660065607859,-0.000163391746992363,
4.4152468210878));
#57672=CARTESIAN_POINT('Ctrl Pts',(7.18338744278911,-0.0594844418834033,
4.41545575762517));
#57673=CARTESIAN_POINT('Ctrl Pts',(7.20607950818724,-0.257561782965025,
4.37580284351512));
#57674=CARTESIAN_POINT('Ctrl Pts',(7.24467685227299,-0.486676365692783,
4.07107270446015));
#57675=CARTESIAN_POINT('Ctrl Pts',(7.29239268833582,-0.322996137187983,
3.62908393881966));
#57676=CARTESIAN_POINT('Ctrl Pts',(7.34010852439867,0.137296434535941,3.52771310152703));
#57677=CARTESIAN_POINT('Ctrl Pts',(7.3878243604615,0.471507566988788,3.86005058906394));
#57678=CARTESIAN_POINT('Ctrl Pts',(7.43332173768814,0.377318713751663,4.29947917201381));
#57679=CARTESIAN_POINT('Ctrl Pts',(7.46291383622717,0.118587850938607,4.41527441201542));
#57680=CARTESIAN_POINT('Ctrl Pts',(7.47660065607859,-0.00030677023753798,
4.41625647512786));
#57681=CARTESIAN_POINT('Ctrl Pts',(7.2733993439214,-0.000222139526412493,
4.4153039283715));
#57682=CARTESIAN_POINT('Ctrl Pts',(7.27971732247348,-0.0554265094472961,
4.41557047734173));
#57683=CARTESIAN_POINT('Ctrl Pts',(7.30194057971316,-0.249272617462211,
4.37960776139715));
#57684=CARTESIAN_POINT('Ctrl Pts',(7.34006911564044,-0.484372034479295,
4.08537538031203));
#57685=CARTESIAN_POINT('Ctrl Pts',(7.3877849517033,-0.333780171974684,3.63875766810317));
#57686=CARTESIAN_POINT('Ctrl Pts',(7.43550078776612,0.123327161313159,3.52387434835784));
#57687=CARTESIAN_POINT('Ctrl Pts',(7.48321662382897,0.467181263150904,3.84622454030349));
#57688=CARTESIAN_POINT('Ctrl Pts',(7.52918280921405,0.385138488472668,4.29279105563264));
#57689=CARTESIAN_POINT('Ctrl Pts',(7.55924371591154,0.122630008444172,4.41546922990911));
#57690=CARTESIAN_POINT('Ctrl Pts',(7.5733993439214,-0.000257198714157839,
4.41635988094829));
#57691=CARTESIAN_POINT('Origin',(3.42660065607856,0.,4.));
#57692=CARTESIAN_POINT('',(6.87660065607859,0.000369753976522709,4.4156559906262));
#57693=CARTESIAN_POINT('',(6.9733993439214,0.000344359613660638,4.41554532105972));
#57694=CARTESIAN_POINT('',(3.42660065607856,4.87367679877478E-13,4.415875));
#57695=CARTESIAN_POINT('Ctrl Pts',(6.87660065607859,0.000369753976522759,
4.4156559906262));
#57696=CARTESIAN_POINT('Ctrl Pts',(6.88795577066343,-0.0986361616094132,
4.41481368816743));
#57697=CARTESIAN_POINT('Ctrl Pts',(6.91521616393589,-0.337621850525623,
4.32977807754403));
#57698=CARTESIAN_POINT('Ctrl Pts',(6.95838183589596,-0.486886005735063,
3.93038141845316));
#57699=CARTESIAN_POINT('Ctrl Pts',(7.0060976719588,-0.204771183672361,3.55281534000283));
#57700=CARTESIAN_POINT('Ctrl Pts',(7.05381350802163,0.265389096458903,3.58590591031157));
#57701=CARTESIAN_POINT('Ctrl Pts',(7.10152934408448,0.491837993618785,3.99926540470374));
#57702=CARTESIAN_POINT('Ctrl Pts',(7.14245839343679,0.298657604039877,4.35441002681052));
#57703=CARTESIAN_POINT('Ctrl Pts',(7.16748216410149,0.0795383202432945,
4.41496610118));
#57704=CARTESIAN_POINT('Ctrl Pts',(7.17660065607859,-0.000163391746992363,
4.4152468210878));
#57705=CARTESIAN_POINT('Ctrl Pts',(6.9733993439214,0.00034435961366068,
4.41554532105972));
#57706=CARTESIAN_POINT('Ctrl Pts',(6.9842856503478,-0.0946377878655052,
4.41480662962373));
#57707=CARTESIAN_POINT('Ctrl Pts',(7.0110772354618,-0.329510302625179,4.33529054280597));
#57708=CARTESIAN_POINT('Ctrl Pts',(7.05377409926342,-0.488725618924084,
3.94475128051735));
#57709=CARTESIAN_POINT('Ctrl Pts',(7.10148993532626,-0.21785253135038,3.55904022429238));
#57710=CARTESIAN_POINT('Ctrl Pts',(7.14920577138909,0.253078023397415,3.57826934481931));
#57711=CARTESIAN_POINT('Ctrl Pts',(7.19692160745195,0.491603063369337,3.98478019943955));
#57712=CARTESIAN_POINT('Ctrl Pts',(7.2383194649627,0.306874094293292,4.34959156107453));
#57713=CARTESIAN_POINT('Ctrl Pts',(7.26381204378586,0.0835484619188193,
4.41489945011039));
#57714=CARTESIAN_POINT('Ctrl Pts',(7.2733993439214,-0.000222139526412493,
4.4153039283715));
#57715=CARTESIAN_POINT('Origin',(3.42660065607856,0.,4.));
#57716=CARTESIAN_POINT('',(6.57660065607858,1.8302248101926E-5,4.41656360501758));
#57717=CARTESIAN_POINT('',(6.6733993439214,7.63499956435865E-5,4.4165465803965));
#57718=CARTESIAN_POINT('',(3.42660065607856,4.87367679877478E-13,4.415875));
#57719=CARTESIAN_POINT('Ctrl Pts',(6.57660065607858,1.83022481018748E-5,
4.41656360501758));
#57720=CARTESIAN_POINT('Ctrl Pts',(6.57661881985014,-0.000139156870309867,
4.41656362372179));
#57721=CARTESIAN_POINT('Ctrl Pts',(6.59254226230931,-0.138177237712184,
4.41649399470799));
#57722=CARTESIAN_POINT('Ctrl Pts',(6.62437098345609,-0.41404349770976,4.26553045144514));
#57723=CARTESIAN_POINT('Ctrl Pts',(6.67208681951894,-0.447234019333667,
3.79538894860702));
#57724=CARTESIAN_POINT('Ctrl Pts',(6.71980265558177,-0.0698021891909718,
3.51313682319347));
#57725=CARTESIAN_POINT('Ctrl Pts',(6.76751849164461,0.371772181936036,3.67798293440124));
#57726=CARTESIAN_POINT('Ctrl Pts',(6.81523432770745,0.471920133146607,4.13853999974893));
#57727=CARTESIAN_POINT('Ctrl Pts',(6.85159504918544,0.21800401543618,4.39254992240466));
#57728=CARTESIAN_POINT('Ctrl Pts',(6.87205049197582,0.0400429038769189,
4.41599351380864));
#57729=CARTESIAN_POINT('Ctrl Pts',(6.87660065607859,0.000369753976522759,
4.4156559906262));
#57730=CARTESIAN_POINT('Ctrl Pts',(6.6733993439214,7.63499956435956E-5,
4.4165465803965));
#57731=CARTESIAN_POINT('Ctrl Pts',(6.68885397822212,-0.133927014866661,
4.41622291450327));
#57732=CARTESIAN_POINT('Ctrl Pts',(6.72021389121046,-0.406451392834186,
4.27318229388465));
#57733=CARTESIAN_POINT('Ctrl Pts',(6.76747908288639,-0.453085647428837,
3.80864864857145));
#57734=CARTESIAN_POINT('Ctrl Pts',(6.81519491894923,-0.0841006081168706,
3.51540431248109));
#57735=CARTESIAN_POINT('Ctrl Pts',(6.86291075501207,0.362121456530253,3.66717299786736));
#57736=CARTESIAN_POINT('Ctrl Pts',(6.91062659107491,0.475798562415156,4.124581128109));
#57737=CARTESIAN_POINT('Ctrl Pts',(6.94745612071136,0.226294304474162,4.38932900794447));
#57738=CARTESIAN_POINT('Ctrl Pts',(6.96838037166019,0.0441344886838037,
4.41588588393584));
#57739=CARTESIAN_POINT('Ctrl Pts',(6.9733993439214,0.00034435961366068,
4.41554532105972));
#57740=CARTESIAN_POINT('Origin',(3.42660065607856,0.,4.));
#57741=CARTESIAN_POINT('',(6.27660065607859,-8.94903747701068E-6,4.41582842213685));
#57742=CARTESIAN_POINT('',(6.3733993439214,-0.000441664590319634,4.4157663968931));
#57743=CARTESIAN_POINT('',(3.42660065607856,4.87367679877478E-13,4.415875));
#57744=CARTESIAN_POINT('Ctrl Pts',(6.27660065607859,-8.94903747701223E-6,
4.41582842213685));
#57745=CARTESIAN_POINT('Ctrl Pts',(6.28118714772447,-0.0399801639742102,
4.41579747358059));
#57746=CARTESIAN_POINT('Ctrl Pts',(6.29372627871415,-0.149263049162913,
4.40013952362907));
#57747=CARTESIAN_POINT('Ctrl Pts',(6.31421804904765,-0.307151379675736,
4.3060270879454));
#57748=CARTESIAN_POINT('Ctrl Pts',(6.33807596707907,-0.416657206472865,
4.12081787696614));
#57749=CARTESIAN_POINT('Ctrl Pts',(6.36193388511048,-0.422829889105799,
3.9075587958503));
#57750=CARTESIAN_POINT('Ctrl Pts',(6.39374444248571,-0.296437506874183,
3.64987069373525));
#57751=CARTESIAN_POINT('Ctrl Pts',(6.43350763920474,0.0703302468340302,
3.51324810367198));
#57752=CARTESIAN_POINT('Ctrl Pts',(6.48122347526758,0.448014600657906,3.7964368525222));
#57753=CARTESIAN_POINT('Ctrl Pts',(6.52892114755886,0.413253290380966,4.26628466471864));
#57754=CARTESIAN_POINT('Ctrl Pts',(6.56071354116253,0.137741412285014,4.41654724519979));
#57755=CARTESIAN_POINT('Ctrl Pts',(6.57660065607858,1.83022481018748E-5,
4.41656360501758));
#57756=CARTESIAN_POINT('Ctrl Pts',(6.3733993439214,-0.000441664590319611,
4.4157663968931));
#57757=CARTESIAN_POINT('Ctrl Pts',(6.37751702740883,-0.0362476131304844,
4.41610293027605));
#57758=CARTESIAN_POINT('Ctrl Pts',(6.39753998958387,-0.210006484715375,
4.39546152579387));
#57759=CARTESIAN_POINT('Ctrl Pts',(6.43346823044653,-0.468271923807345,
4.15124960425567));
#57760=CARTESIAN_POINT('Ctrl Pts',(6.48118406650937,-0.380227249479543,
3.6882349865083));
#57761=CARTESIAN_POINT('Ctrl Pts',(6.52889990257221,0.0564566449812287,
3.51140415777354));
#57762=CARTESIAN_POINT('Ctrl Pts',(6.57661573863504,0.441574375138847,3.78331933667001));
#57763=CARTESIAN_POINT('Ctrl Pts',(6.62433157469789,0.421040068198854,4.25418342072721));
#57764=CARTESIAN_POINT('Ctrl Pts',(6.65659277646,0.145792717270209,4.41473316952435));
#57765=CARTESIAN_POINT('Ctrl Pts',(6.6729486995345,0.00398377756883227,
4.41655601822694));
#57766=CARTESIAN_POINT('Ctrl Pts',(6.6733993439214,7.63499956435956E-5,
4.4165465803965));
#57767=CARTESIAN_POINT('Origin',(3.42660065607856,0.,4.));
#57768=CARTESIAN_POINT('',(5.97660065607859,-9.19412645702589E-6,4.41589218083175));
#57769=CARTESIAN_POINT('',(6.0733993439214,-6.65563173402051E-6,4.41590255337155));
#57770=CARTESIAN_POINT('',(3.42660065607856,4.87367679877478E-13,4.415875));
#57771=CARTESIAN_POINT('Ctrl Pts',(5.97660065607858,-9.19412645705893E-6,
4.41589218083175));
#57772=CARTESIAN_POINT('Ctrl Pts',(5.97780283625498,-0.0104787976275591,
4.4159022685469));
#57773=CARTESIAN_POINT('Ctrl Pts',(5.98695765577519,-0.0902010538040918,
4.41295272969856));
#57774=CARTESIAN_POINT('Ctrl Pts',(6.0040651146392,-0.23587461323539,4.36380751861078));
#57775=CARTESIAN_POINT('Ctrl Pts',(6.02792303267061,-0.381351759249696,
4.20630938167977));
#57776=CARTESIAN_POINT('Ctrl Pts',(6.05178095070204,-0.433578399193506,
3.9983625870902));
#57777=CARTESIAN_POINT('Ctrl Pts',(6.07563886873346,-0.379782579589031,
3.79081692866841));
#57778=CARTESIAN_POINT('Ctrl Pts',(6.09949678676487,-0.233120953551068,
3.63442082419035));
#57779=CARTESIAN_POINT('Ctrl Pts',(6.12335470479629,-0.0294522997972467,
3.5674214393556));
#57780=CARTESIAN_POINT('Ctrl Pts',(6.14721262282771,0.181413325723775,3.60619428643423));
#57781=CARTESIAN_POINT('Ctrl Pts',(6.17107054085913,0.347927737305898,3.74127281623538));
#57782=CARTESIAN_POINT('Ctrl Pts',(6.19492845889055,0.429346806292137,3.93959933010928));
#57783=CARTESIAN_POINT('Ctrl Pts',(6.21878637692197,0.405811992579865,4.15272917617017));
#57784=CARTESIAN_POINT('Ctrl Pts',(6.24264429495339,0.282982581651336,4.32844890303245));
#57785=CARTESIAN_POINT('Ctrl Pts',(6.26191572133893,0.127967070080381,4.40561019629887));
#57786=CARTESIAN_POINT('Ctrl Pts',(6.27323450838066,0.029326984292613,4.415851136102));
#57787=CARTESIAN_POINT('Ctrl Pts',(6.27660065607859,-8.94903747701223E-6,
4.41582842213685));
#57788=CARTESIAN_POINT('Ctrl Pts',(6.0733993439214,-6.65563173397714E-6,
4.41590255337156));
#57789=CARTESIAN_POINT('Ctrl Pts',(6.07413271593935,-0.00639299139291402,
4.41590724351385));
#57790=CARTESIAN_POINT('Ctrl Pts',(6.0828187273011,-0.0820297780542147,
4.41420140028919));
#57791=CARTESIAN_POINT('Ctrl Pts',(6.09945737800665,-0.2250554921608,4.3705991908187));
#57792=CARTESIAN_POINT('Ctrl Pts',(6.12331529603809,-0.375113923638194,
4.21744656883549));
#57793=CARTESIAN_POINT('Ctrl Pts',(6.1471732140695,-0.433431396087355,4.01114207710762));
#57794=CARTESIAN_POINT('Ctrl Pts',(6.17103113210093,-0.385792139046387,
3.80207577201042));
#57795=CARTESIAN_POINT('Ctrl Pts',(6.19488905013233,-0.243761337718234,
3.64147770828707));
#57796=CARTESIAN_POINT('Ctrl Pts',(6.21874696816376,-0.042227823444436,
3.56841523311022));
#57797=CARTESIAN_POINT('Ctrl Pts',(6.24260488619517,0.16982704650124,3.60113783246665));
#57798=CARTESIAN_POINT('Ctrl Pts',(6.2664628042266,0.339985970990829,3.73091992247201));
#57799=CARTESIAN_POINT('Ctrl Pts',(6.29032072225801,0.427700638223926,3.92738904240251));
#57800=CARTESIAN_POINT('Ctrl Pts',(6.31417864028943,0.409561128158778,4.13996490148311));
#57801=CARTESIAN_POINT('Ctrl Pts',(6.34187151417723,0.27471212230801,4.35031587281991));
#57802=CARTESIAN_POINT('Ctrl Pts',(6.36161174872122,0.102059178040878,4.41480301073152));
#57803=CARTESIAN_POINT('Ctrl Pts',(6.3733993439214,-0.000441664590319611,
4.4157663968931));
#57804=CARTESIAN_POINT('Origin',(3.42660065607856,0.,4.));
#57805=CARTESIAN_POINT('',(5.67660065607858,1.06631253201556E-5,4.41586554077139));
#57806=CARTESIAN_POINT('',(5.7733993439214,9.17748676071416E-6,4.4158542849441));
#57807=CARTESIAN_POINT('',(3.42660065607856,4.87367679877478E-13,4.415875));
#57808=CARTESIAN_POINT('Ctrl Pts',(5.67660065607858,1.06631253201268E-5,
4.41586554077139));
#57809=CARTESIAN_POINT('Ctrl Pts',(5.68237116412931,-0.050253077703417,
4.41581669384736));
#57810=CARTESIAN_POINT('Ctrl Pts',(5.69609431152383,-0.169828933264711,
4.3941204493343));
#57811=CARTESIAN_POINT('Ctrl Pts',(5.71777009826218,-0.329222253834466,
4.28214440376531));
#57812=CARTESIAN_POINT('Ctrl Pts',(5.74162801629359,-0.424158110434281,
4.08990358344764));
#57813=CARTESIAN_POINT('Ctrl Pts',(5.76548593432501,-0.415375755386326,
3.8756788878607));
#57814=CARTESIAN_POINT('Ctrl Pts',(5.78934385235642,-0.305022713182347,
3.69185409099321));
#57815=CARTESIAN_POINT('Ctrl Pts',(5.81320177038785,-0.120083309624962,
3.58337936191985));
#57816=CARTESIAN_POINT('Ctrl Pts',(5.83705968841926,0.0942197354074567,
3.57677972866706));
#57817=CARTESIAN_POINT('Ctrl Pts',(5.86091760645069,0.285483486244351,3.673668977605));
#57818=CARTESIAN_POINT('Ctrl Pts',(5.8847755244821,0.406938752801468,3.85035505520226));
#57819=CARTESIAN_POINT('Ctrl Pts',(5.90863344251353,0.428886400972996,4.06363338935351));
#57820=CARTESIAN_POINT('Ctrl Pts',(5.93249136054494,0.345959657594393,4.261351642888));
#57821=CARTESIAN_POINT('Ctrl Pts',(5.95514709839996,0.186877681905787,4.38841966610496));
#57822=CARTESIAN_POINT('Ctrl Pts',(5.96985019691118,0.0587795235055939,
4.41583553648629));
#57823=CARTESIAN_POINT('Ctrl Pts',(5.97660065607858,-9.19412645705893E-6,
4.41589218083175));
#57824=CARTESIAN_POINT('Ctrl Pts',(5.7733993439214,9.17748676073846E-6,
4.4158542849441));
#57825=CARTESIAN_POINT('Ctrl Pts',(5.77870104381367,-0.0461746181927863,
4.41581721944429));
#57826=CARTESIAN_POINT('Ctrl Pts',(5.79195538304975,-0.161664917198308,
4.3966319946429));
#57827=CARTESIAN_POINT('Ctrl Pts',(5.81316236162963,-0.320769768688322,
4.29171820750724));
#57828=CARTESIAN_POINT('Ctrl Pts',(5.83702027966105,-0.421326288178809,
4.10235681181338));
#57829=CARTESIAN_POINT('Ctrl Pts',(5.86087819769247,-0.418857046020503,
3.88796639709818));
#57830=CARTESIAN_POINT('Ctrl Pts',(5.88473611572389,-0.313965860818636,
3.70097123187977));
#57831=CARTESIAN_POINT('Ctrl Pts',(5.90859403375531,-0.132301443679057,
3.58709678011166));
#57832=CARTESIAN_POINT('Ctrl Pts',(5.93245195178673,0.0817142298265842,
3.57418834816524));
#57833=CARTESIAN_POINT('Ctrl Pts',(5.95630986981814,0.275748643515392,3.66540258613358));
#57834=CARTESIAN_POINT('Ctrl Pts',(5.98016778784957,0.402354822815078,3.83843477537114));
#57835=CARTESIAN_POINT('Ctrl Pts',(6.00402570588098,0.430574627524036,4.05097449853386));
#57836=CARTESIAN_POINT('Ctrl Pts',(6.02788362391241,0.353506566116634,4.25104874587108));
#57837=CARTESIAN_POINT('Ctrl Pts',(6.05100816992587,0.195023852357142,4.38547315270063));
#57838=CARTESIAN_POINT('Ctrl Pts',(6.06618007659554,0.06286002589468,4.4158563839102));
#57839=CARTESIAN_POINT('Ctrl Pts',(6.0733993439214,-6.65563173397714E-6,
4.41590255337156));
#57840=CARTESIAN_POINT('Origin',(3.42660065607856,0.,4.));
#57841=CARTESIAN_POINT('',(5.37660065607858,-1.01751121954902E-5,4.41586038335289));
#57842=CARTESIAN_POINT('',(5.4733993439214,-1.09014992595302E-5,4.41587264340464));
#57843=CARTESIAN_POINT('',(3.42660065607856,4.87367679877478E-13,4.415875));
#57844=CARTESIAN_POINT('Ctrl Pts',(5.37660065607859,-1.01751121954468E-5,
4.41586038335289));
#57845=CARTESIAN_POINT('Ctrl Pts',(5.37898685265982,-0.0207957689391596,
4.41587928195339));
#57846=CARTESIAN_POINT('Ctrl Pts',(5.38932568858487,-0.110842971866809,
4.40924760552439));
#57847=CARTESIAN_POINT('Ctrl Pts',(5.40761716385372,-0.26226226804932,4.34526983614494));
#57848=CARTESIAN_POINT('Ctrl Pts',(5.43147508188515,-0.395631058815178,
4.17739453851434));
#57849=CARTESIAN_POINT('Ctrl Pts',(5.45533299991656,-0.432257278927009,
3.96614144408682));
#57850=CARTESIAN_POINT('Ctrl Pts',(5.47919091794798,-0.363184819889405,
3.76316768886851));
#57851=CARTESIAN_POINT('Ctrl Pts',(5.5030488359794,-0.205303779432806,3.61810588490468));
#57852=CARTESIAN_POINT('Ctrl Pts',(5.52690675401082,0.00277962745745752,
3.56642759466814));
#57853=CARTESIAN_POINT('Ctrl Pts',(5.55076467204224,0.210183339719457,3.62076956781107));
#57854=CARTESIAN_POINT('Ctrl Pts',(5.57462259007365,0.36619150013966,3.76784371165257));
#57855=CARTESIAN_POINT('Ctrl Pts',(5.59848050810508,0.432655863921731,3.97168639180759));
#57856=CARTESIAN_POINT('Ctrl Pts',(5.62233842613649,0.393324083661671,4.18245252040861));
#57857=CARTESIAN_POINT('Ctrl Pts',(5.64619634416792,0.257813851021257,4.34860403787086));
#57858=CARTESIAN_POINT('Ctrl Pts',(5.66428375414861,0.107285005985459,4.40994309575933));
#57859=CARTESIAN_POINT('Ctrl Pts',(5.6744185247855,0.0190180158238588,4.41588401235146));
#57860=CARTESIAN_POINT('Ctrl Pts',(5.67660065607858,1.06631253201268E-5,
4.41586554077139));
#57861=CARTESIAN_POINT('Ctrl Pts',(5.4733993439214,-1.0901499259525E-5,
4.41587264340464));
#57862=CARTESIAN_POINT('Ctrl Pts',(5.47531673234419,-0.0167114040746605,
4.41588973972128));
#57863=CARTESIAN_POINT('Ctrl Pts',(5.48518676011079,-0.102669266038577,
4.41080986982701));
#57864=CARTESIAN_POINT('Ctrl Pts',(5.50300942722118,-0.251979671819092,
4.35284416104532));
#57865=CARTESIAN_POINT('Ctrl Pts',(5.52686734525261,-0.390234841353927,
4.18896964197264));
#57866=CARTESIAN_POINT('Ctrl Pts',(5.55072526328402,-0.433066962396004,
3.97888689800548));
#57867=CARTESIAN_POINT('Ctrl Pts',(5.57458318131544,-0.370002414621403,
3.77396688259));
#57868=CARTESIAN_POINT('Ctrl Pts',(5.59844109934686,-0.21646219781534,3.62431812139094));
#57869=CARTESIAN_POINT('Ctrl Pts',(5.62229901737828,-0.00999107731853999,
3.56653381289738));
#57870=CARTESIAN_POINT('Ctrl Pts',(5.64615693540971,0.198923133709572,3.61474379450078));
#57871=CARTESIAN_POINT('Ctrl Pts',(5.67001485344111,0.359195220034686,3.75715941257656));
#57872=CARTESIAN_POINT('Ctrl Pts',(5.69387277147254,0.431634290692432,3.95895616900985));
#57873=CARTESIAN_POINT('Ctrl Pts',(5.71773068950395,0.398527019959163,4.1707892603438));
#57874=CARTESIAN_POINT('Ctrl Pts',(5.74158860753538,0.267969036875697,4.34085972491723));
#57875=CARTESIAN_POINT('Ctrl Pts',(5.76014482567452,0.115458993192439,4.40830959117706));
#57876=CARTESIAN_POINT('Ctrl Pts',(5.77074840446986,0.0231018550196917,
4.41587281831976));
#57877=CARTESIAN_POINT('Ctrl Pts',(5.7733993439214,9.17748676073846E-6,
4.4158542849441));
#57878=CARTESIAN_POINT('Origin',(3.42660065607856,0.,4.));
#57879=CARTESIAN_POINT('',(5.07660065607859,8.10857529294212E-6,4.41589722116852));
#57880=CARTESIAN_POINT('',(5.1733993439214,1.02299162792543E-5,4.4158851107878));
#57881=CARTESIAN_POINT('',(3.42660065607856,4.87367679877478E-13,4.415875));
#57882=CARTESIAN_POINT('Ctrl Pts',(5.07660065607858,8.10857529294148E-6,
4.41589722116852));
#57883=CARTESIAN_POINT('Ctrl Pts',(5.08355518053415,-0.060555656273516,
4.41584370653314));
#57884=CARTESIAN_POINT('Ctrl Pts',(5.09846234433351,-0.190424342306974,
4.38715451669839));
#57885=CARTESIAN_POINT('Ctrl Pts',(5.1213221474767,-0.349282119693095,4.256894448863));
#57886=CARTESIAN_POINT('Ctrl Pts',(5.1451800655081,-0.4296670234643,4.05812921762123));
#57887=CARTESIAN_POINT('Ctrl Pts',(5.16903798353954,-0.404986636103755,
3.84514980926298));
#57888=CARTESIAN_POINT('Ctrl Pts',(5.19289590157095,-0.281275984601366,
3.67003549057442));
#57889=CARTESIAN_POINT('Ctrl Pts',(5.21675381960238,-0.0887856930599551,
3.5756064824932));
#57890=CARTESIAN_POINT('Ctrl Pts',(5.24061173763379,0.125415118908336,3.58495324968971));
#57891=CARTESIAN_POINT('Ctrl Pts',(5.26446965566521,0.308948518064291,3.69579025298356));
#57892=CARTESIAN_POINT('Ctrl Pts',(5.28832757369662,0.416935588964862,3.88101482593007));
#57893=CARTESIAN_POINT('Ctrl Pts',(5.31218549172805,0.422970551266107,4.09533451502773));
#57894=CARTESIAN_POINT('Ctrl Pts',(5.33604340975946,0.325577692296299,4.28634231834109));
#57895=CARTESIAN_POINT('Ctrl Pts',(5.35751513120965,0.166275769440666,4.39523064161658));
#57896=CARTESIAN_POINT('Ctrl Pts',(5.37103421331602,0.0484777907299229,
4.41581629730449));
#57897=CARTESIAN_POINT('Ctrl Pts',(5.37660065607859,-1.01751121954468E-5,
4.41586038335289));
#57898=CARTESIAN_POINT('Ctrl Pts',(5.1733993439214,1.02299162792474E-5,
4.4158851107878));
#57899=CARTESIAN_POINT('Ctrl Pts',(5.17988506021851,-0.0564756498766958,
4.41582730150705));
#57900=CARTESIAN_POINT('Ctrl Pts',(5.19432341585943,-0.182274442988225,
4.39002065289559));
#57901=CARTESIAN_POINT('Ctrl Pts',(5.21671441084416,-0.341564590845109,
4.26707000444592));
#57902=CARTESIAN_POINT('Ctrl Pts',(5.24057232887557,-0.427768622694993,
4.07075847957352));
#57903=CARTESIAN_POINT('Ctrl Pts',(5.264430246907,-0.409371574112622,3.85714457902312));
#57904=CARTESIAN_POINT('Ctrl Pts',(5.2882881649384,-0.290872024601924,3.6784627202051));
#57905=CARTESIAN_POINT('Ctrl Pts',(5.31214608296984,-0.101246341881189,
3.57840548479658));
#57906=CARTESIAN_POINT('Ctrl Pts',(5.33600400100125,0.113136829324483,3.58143959235932));
#57907=CARTESIAN_POINT('Ctrl Pts',(5.35986191903268,0.299854963974951,3.68682312094679));
#57908=CARTESIAN_POINT('Ctrl Pts',(5.38371983706408,0.413250392048343,3.8687869272297));
#57909=CARTESIAN_POINT('Ctrl Pts',(5.40757775509551,0.425594842551202,4.08283590397723));
#57910=CARTESIAN_POINT('Ctrl Pts',(5.43143567312693,0.333869761079625,4.27662924579771));
#57911=CARTESIAN_POINT('Ctrl Pts',(5.45337620273556,0.174437273907163,4.39264091290779));
#57912=CARTESIAN_POINT('Ctrl Pts',(5.46736409300038,0.0525562895569378,
4.41581883033293));
#57913=CARTESIAN_POINT('Ctrl Pts',(5.4733993439214,-1.0901499259525E-5,
4.41587264340464));
#57914=CARTESIAN_POINT('Origin',(3.42660065607856,0.,4.));
#57915=CARTESIAN_POINT('',(4.77660065607858,-3.27394476109793E-6,4.41584059078716));
#57916=CARTESIAN_POINT('',(4.8733993439214,-6.67049670156904E-6,4.4158459349409));
#57917=CARTESIAN_POINT('',(3.42660065607856,4.87367679877478E-13,4.415875));
#57918=CARTESIAN_POINT('Ctrl Pts',(4.77660065607858,-3.27394476113199E-6,
4.41584059078717));
#57919=CARTESIAN_POINT('Ctrl Pts',(4.78017086906467,-0.0311067951354469,
4.4158491206715));
#57920=CARTESIAN_POINT('Ctrl Pts',(4.79169372139456,-0.131487321212171,
4.40473555835468));
#57921=CARTESIAN_POINT('Ctrl Pts',(4.81116921306824,-0.287199161490599,
4.32482210305491));
#57922=CARTESIAN_POINT('Ctrl Pts',(4.83502713109967,-0.407721671464292,
4.14749845969467));
#57923=CARTESIAN_POINT('Ctrl Pts',(4.85888504913109,-0.42854512664958,3.93410742516172));
#57924=CARTESIAN_POINT('Ctrl Pts',(4.8827429671625,-0.344577625034195,3.73682892005441));
#57925=CARTESIAN_POINT('Ctrl Pts',(4.90660088519393,-0.176351507991885,
3.60390291263011));
#57926=CARTESIAN_POINT('Ctrl Pts',(4.93045880322534,0.0349973564730633,
3.56783343253575));
#57927=CARTESIAN_POINT('Ctrl Pts',(4.95431672125677,0.237788413971502,3.63744045016736));
#57928=CARTESIAN_POINT('Ctrl Pts',(4.97817463928818,0.382433727027559,3.79570315365689));
#57929=CARTESIAN_POINT('Ctrl Pts',(5.0020325573196,0.433563576539811,4.00392200101168));
#57930=CARTESIAN_POINT('Ctrl Pts',(5.02589047535102,0.378675321553375,4.21118181228595));
#57931=CARTESIAN_POINT('Ctrl Pts',(5.04974839338244,0.231190635538481,4.36680191797922));
#57932=CARTESIAN_POINT('Ctrl Pts',(5.0666517869583,0.086644022961884,4.4135113916189));
#57933=CARTESIAN_POINT('Ctrl Pts',(5.07560254119034,0.00870023350343714,
4.41590490160082));
#57934=CARTESIAN_POINT('Ctrl Pts',(5.07660065607858,8.10857529294148E-6,
4.41589722116852));
#57935=CARTESIAN_POINT('Ctrl Pts',(4.8733993439214,-6.67049670157252E-6,
4.41584593494091));
#57936=CARTESIAN_POINT('Ctrl Pts',(4.87650074874903,-0.0270249643080214,
4.41586127519519));
#57937=CARTESIAN_POINT('Ctrl Pts',(4.88755479292047,-0.123313358466266,
4.40662010077424));
#57938=CARTESIAN_POINT('Ctrl Pts',(4.90656147643571,-0.277507970732168,
4.33313973520738));
#57939=CARTESIAN_POINT('Ctrl Pts',(4.93041939446713,-0.403200703213916,
4.15944262266324));
#57940=CARTESIAN_POINT('Ctrl Pts',(4.95427731249855,-0.430299880793222,
3.94675744574809));
#57941=CARTESIAN_POINT('Ctrl Pts',(4.97813523052996,-0.352179016385168,
3.7470915236456));
#57942=CARTESIAN_POINT('Ctrl Pts',(5.00199314856139,-0.187940789307144,
3.60926861310034));
#57943=CARTESIAN_POINT('Ctrl Pts',(5.0258510665928,0.0222540801607904,3.56699016996131));
#57944=CARTESIAN_POINT('Ctrl Pts',(5.04970898462423,0.227007220840439,3.63059442521772));
#57945=CARTESIAN_POINT('Ctrl Pts',(5.07356690265564,0.376250912472057,3.7845284059142));
#57946=CARTESIAN_POINT('Ctrl Pts',(5.09742482068706,0.433491007135177,3.99115106069306));
#57947=CARTESIAN_POINT('Ctrl Pts',(5.12128273871848,0.384730742495793,4.19993752217271));
#57948=CARTESIAN_POINT('Ctrl Pts',(5.1451406567499,0.241893331461176,4.35983381329239));
#57949=CARTESIAN_POINT('Ctrl Pts',(5.16251285848421,0.0948160588051851,
4.41219316122439));
#57950=CARTESIAN_POINT('Ctrl Pts',(5.17193242087471,0.0127860645481494,
4.41589818594594));
#57951=CARTESIAN_POINT('Ctrl Pts',(5.1733993439214,1.02299162792474E-5,
4.4158851107878));
#57952=CARTESIAN_POINT('Origin',(3.42660065607856,0.,4.));
#57953=CARTESIAN_POINT('',(4.47660065607858,-1.72413508574122E-6,4.41591032029986));
#57954=CARTESIAN_POINT('',(4.5733993439214,2.6062779713001E-6,4.4159095790646));
#57955=CARTESIAN_POINT('',(3.42660065607856,4.87367679877478E-13,4.415875));
#57956=CARTESIAN_POINT('Ctrl Pts',(4.47660065607858,-1.72413508575881E-6,
4.41591032029986));
#57957=CARTESIAN_POINT('Ctrl Pts',(4.47678655759518,-0.00162050728124812,
4.41591069657345));
#57958=CARTESIAN_POINT('Ctrl Pts',(4.48492509845559,-0.0724886630755744,
4.4155056303295));
#57959=CARTESIAN_POINT('Ctrl Pts',(4.5010162786598,-0.212178818846594,4.37811758201071));
#57960=CARTESIAN_POINT('Ctrl Pts',(4.52487419669122,-0.367409789343613,
4.23022337776645));
#57961=CARTESIAN_POINT('Ctrl Pts',(4.54873211472264,-0.432799058467291,
4.02603328640456));
#57962=CARTESIAN_POINT('Ctrl Pts',(4.57259003275406,-0.392357168499796,
3.8154773474345));
#57963=CARTESIAN_POINT('Ctrl Pts',(4.59644795078547,-0.255973263285106,
3.65004222328625));
#57964=CARTESIAN_POINT('Ctrl Pts',(4.6203058688169,-0.0569969226013119,
3.57018130821703));
#57965=CARTESIAN_POINT('Ctrl Pts',(4.64416378684831,0.155916718210686,3.59542277130738));
#57966=CARTESIAN_POINT('Ctrl Pts',(4.66802170487973,0.330704474340828,3.71959438727947));
#57967=CARTESIAN_POINT('Ctrl Pts',(4.69187962291115,0.424625978282027,3.91233281365517));
#57968=CARTESIAN_POINT('Ctrl Pts',(4.71573754094257,0.41471486395576,4.1265082550995));
#57969=CARTESIAN_POINT('Ctrl Pts',(4.73959545897399,0.303394668785218,4.30974898215573));
#57970=CARTESIAN_POINT('Ctrl Pts',(4.75988316401932,0.145646585585232,4.40116103141851));
#57971=CARTESIAN_POINT('Ctrl Pts',(4.77221822972086,0.0381762104768988,
4.41583012037823));
#57972=CARTESIAN_POINT('Ctrl Pts',(4.77660065607858,-3.27394476113199E-6,
4.41584059078717));
#57973=CARTESIAN_POINT('Ctrl Pts',(4.5733993439214,2.60627797130011E-6,
4.4159095790646));
#57974=CARTESIAN_POINT('Ctrl Pts',(4.58106907662335,-0.0667838229435618,
4.4158868274511));
#57975=CARTESIAN_POINT('Ctrl Pts',(4.59669144866912,-0.202842099803805,
4.38250385602613));
#57976=CARTESIAN_POINT('Ctrl Pts',(4.62026646005868,-0.360469908510665,
4.24094439618412));
#57977=CARTESIAN_POINT('Ctrl Pts',(4.6441243780901,-0.431844582779732,4.03876871570463));
#57978=CARTESIAN_POINT('Ctrl Pts',(4.66798229612152,-0.397621493350665,
3.82711302819544));
#57979=CARTESIAN_POINT('Ctrl Pts',(4.69184021415294,-0.266169117804412,
3.65773291463971));
#57980=CARTESIAN_POINT('Ctrl Pts',(4.71569813218436,-0.0696311426542753,
3.57204642662242));
#57981=CARTESIAN_POINT('Ctrl Pts',(4.73955605021577,0.143933543589337,3.59100624451743));
#57982=CARTESIAN_POINT('Ctrl Pts',(4.76341396824719,0.322302557754209,3.70997617639404));
#57983=CARTESIAN_POINT('Ctrl Pts',(4.78727188627862,0.421859817202848,3.8998648332327));
#57984=CARTESIAN_POINT('Ctrl Pts',(4.81112980431003,0.41826086011465,4.11423926597311));
#57985=CARTESIAN_POINT('Ctrl Pts',(4.83498772234146,0.312385729531365,4.30067908636799));
#57986=CARTESIAN_POINT('Ctrl Pts',(4.85574423554524,0.15381688120809,4.39891624198015));
#57987=CARTESIAN_POINT('Ctrl Pts',(4.86854810940522,0.04225549351942,4.41582193963064));
#57988=CARTESIAN_POINT('Ctrl Pts',(4.8733993439214,-6.67049670157252E-6,
4.41584593494091));
#57989=CARTESIAN_POINT('Origin',(3.42660065607856,0.,4.));
#57990=CARTESIAN_POINT('',(4.17660065607858,5.88453344125852E-6,4.41584444980552));
#57991=CARTESIAN_POINT('',(4.2733993439214,2.51014653358805E-6,4.41583996132385));
#57992=CARTESIAN_POINT('',(3.42660065607856,4.87367679877478E-13,4.415875));
#57993=CARTESIAN_POINT('Ctrl Pts',(4.17660065607858,5.88453344126799E-6,
4.41584444980552));
#57994=CARTESIAN_POINT('Ctrl Pts',(4.18135488546951,-0.0414115481342504,
4.41582334930757));
#57995=CARTESIAN_POINT('Ctrl Pts',(4.19406175420423,-0.152126265423154,
4.3993918905015));
#57996=CARTESIAN_POINT('Ctrl Pts',(4.21472126228278,-0.310547447266788,
4.30257739619942));
#57997=CARTESIAN_POINT('Ctrl Pts',(4.23857918031418,-0.417556725585918,
4.11678647978038));
#57998=CARTESIAN_POINT('Ctrl Pts',(4.26243709834561,-0.422462345057068,
3.90243789311793));
#57999=CARTESIAN_POINT('Ctrl Pts',(4.28629501637703,-0.324064236326554,
3.71194600226016));
#58000=CARTESIAN_POINT('Ctrl Pts',(4.31015293440845,-0.146423688323203,
3.59189110566319));
#58001=CARTESIAN_POINT('Ctrl Pts',(4.33401085243986,0.0670214896752265,
3.5716299793216));
#58002=CARTESIAN_POINT('Ctrl Pts',(4.35786877047129,0.264078061498623,3.65611697628114));
#58003=CARTESIAN_POINT('Ctrl Pts',(4.38172668850271,0.396560367883193,3.82469274783887));
#58004=CARTESIAN_POINT('Ctrl Pts',(4.40558460653412,0.432072854850341,4.03613591352675));
#58005=CARTESIAN_POINT('Ctrl Pts',(4.42944252456555,0.361931763288092,4.23874286631049));
#58006=CARTESIAN_POINT('Ctrl Pts',(4.45311454108036,0.204524647174786,4.38184685695289));
#58007=CARTESIAN_POINT('Ctrl Pts',(4.46883391825138,0.0676290543833733,
4.4158946000499));
#58008=CARTESIAN_POINT('Ctrl Pts',(4.47660065607858,-1.72413508575881E-6,
4.41591032029986));
#58009=CARTESIAN_POINT('Ctrl Pts',(4.2733993439214,2.51014653359152E-6,
4.41583996132385));
#58010=CARTESIAN_POINT('Ctrl Pts',(4.27768476515387,-0.0373320337329404,
4.41583213221101));
#58011=CARTESIAN_POINT('Ctrl Pts',(4.28992282573015,-0.143955736965383,
4.40160880992953));
#58012=CARTESIAN_POINT('Ctrl Pts',(4.31011352565024,-0.301501118270308,
4.3115924136571));
#58013=CARTESIAN_POINT('Ctrl Pts',(4.33397144368164,-0.413936097932681,
4.12903358037428));
#58014=CARTESIAN_POINT('Ctrl Pts',(4.35782936171308,-0.425152419412173,
3.91492252699502));
#58015=CARTESIAN_POINT('Ctrl Pts',(4.38168727974448,-0.332407397051365,
3.72161523052345));
#58016=CARTESIAN_POINT('Ctrl Pts',(4.40554519777592,-0.158379709595794,
3.5963805946708));
#58017=CARTESIAN_POINT('Ctrl Pts',(4.42940311580732,0.0543761300157755,
3.56984189703405));
#58018=CARTESIAN_POINT('Ctrl Pts',(4.45326103383876,0.25383552520097,3.64848857324589));
#58019=CARTESIAN_POINT('Ctrl Pts',(4.47711895187016,0.39122521984844,3.81308936806525));
#58020=CARTESIAN_POINT('Ctrl Pts',(4.50097686990159,0.432949691632991,4.02339490384879));
#58021=CARTESIAN_POINT('Ctrl Pts',(4.524834787933,0.368806170420464,4.22797974831721));
#58022=CARTESIAN_POINT('Ctrl Pts',(4.54869270596443,0.214479494504121,4.37681733431002));
#58023=CARTESIAN_POINT('Ctrl Pts',(4.56488089129389,0.0741790848482271,
4.4152866170047));
#58024=CARTESIAN_POINT('Ctrl Pts',(4.57311643727954,0.0024660981813593,
4.41591041828323));
#58025=CARTESIAN_POINT('Ctrl Pts',(4.5733993439214,2.60627797130011E-6,
4.4159095790646));
#58026=CARTESIAN_POINT('Origin',(4.,0.,4.));
#58027=CARTESIAN_POINT('',(4.,-7.34788079488412E-17,4.6));
#58028=CARTESIAN_POINT('Origin',(4.,0.,4.));
#58029=CARTESIAN_POINT('',(4.,-0.219892372742957,4.3529863453938));
#58030=CARTESIAN_POINT('Ctrl Pts',(4.,-0.219914231356238,4.35301468169996));
#58031=CARTESIAN_POINT('Ctrl Pts',(4.,-0.219843051329574,4.3531167999744));
#58032=CARTESIAN_POINT('Ctrl Pts',(4.,-0.219771822781512,4.35321888245988));
#58033=CARTESIAN_POINT('Ctrl Pts',(4.,-0.21970054575756,4.3533209291203));
#58034=CARTESIAN_POINT('Ctrl Pts',(4.,-0.207925336055227,4.3701793886806));
#58035=CARTESIAN_POINT('Ctrl Pts',(4.,-0.194831304039315,4.38605734350833));
#58036=CARTESIAN_POINT('Ctrl Pts',(4.,-0.18064579384139,4.40088380688851));
#58037=CARTESIAN_POINT('Ctrl Pts',(4.,-0.168975273508986,4.41308164397169));
#58038=CARTESIAN_POINT('Ctrl Pts',(4.,-0.156565051628872,4.42456888924957));
#58039=CARTESIAN_POINT('Ctrl Pts',(4.,-0.143515931303371,4.43531683418355));
#58040=CARTESIAN_POINT('Ctrl Pts',(4.,-0.133182439541062,4.44382804395605));
#58041=CARTESIAN_POINT('Ctrl Pts',(4.,-0.122447811630206,4.45187590303098));
#58042=CARTESIAN_POINT('Ctrl Pts',(4.,-0.111352162047151,4.45944712768208));
#58043=CARTESIAN_POINT('Ctrl Pts',(4.,-0.105068105051177,4.46373511522897));
#58044=CARTESIAN_POINT('Ctrl Pts',(4.,-0.0986661212125077,4.46787107983396));
#58045=CARTESIAN_POINT('Ctrl Pts',(4.,-0.0921733602714696,4.47184061613108));
#58046=CARTESIAN_POINT('Ctrl Pts',(4.,-0.0718171345235072,4.48428598070136));
#58047=CARTESIAN_POINT('Ctrl Pts',(4.,-0.0505350523745213,4.49512244469223));
#58048=CARTESIAN_POINT('Ctrl Pts',(4.,-0.0285775088988711,4.50429938857761));
#58049=CARTESIAN_POINT('Ctrl Pts',(4.,-0.00645956782426854,4.51354336909515));
#58050=CARTESIAN_POINT('Ctrl Pts',(4.,0.0163444141029789,4.52110543571878));
#58051=CARTESIAN_POINT('Ctrl Pts',(4.,0.0396343143342583,4.52702898180467));
#58052=CARTESIAN_POINT('Ctrl Pts',(4.,0.0479455316904685,4.52914285427945));
#58053=CARTESIAN_POINT('Ctrl Pts',(4.,0.0563191235587283,4.53104786585874));
#58054=CARTESIAN_POINT('Ctrl Pts',(4.,0.0647475081636451,4.53274519105122));
#58055=CARTESIAN_POINT('Ctrl Pts',(4.,0.0709442475001029,4.53399310299165));
#58056=CARTESIAN_POINT('Ctrl Pts',(4.,0.0771669940275102,4.53512789739638));
#58057=CARTESIAN_POINT('Ctrl Pts',(4.,0.0834037601527001,4.53614909266968));
#58058=CARTESIAN_POINT('Ctrl Pts',(4.,0.108500755516298,4.54025842313435));
#58059=CARTESIAN_POINT('Ctrl Pts',(4.,0.133859781029961,4.54253781872753));
#58060=CARTESIAN_POINT('Ctrl Pts',(3.99999999999999,0.159256593756596,4.54305292380224));
#58061=CARTESIAN_POINT('Ctrl Pts',(3.99999999999999,0.185497795908202,4.5435851550133));
#58062=CARTESIAN_POINT('Ctrl Pts',(3.99999999999998,0.211780221987087,4.54223483664603));
#58063=CARTESIAN_POINT('Ctrl Pts',(3.99999999999998,0.237902321580844,4.5390442708621));
#58064=CARTESIAN_POINT('Ctrl Pts',(3.99999999999998,0.243507595489062,4.53835964001621));
#58065=CARTESIAN_POINT('Ctrl Pts',(3.99999999999998,0.249105619801251,4.53759013757336));
#58066=CARTESIAN_POINT('Ctrl Pts',(3.99999999999998,0.254694598474614,4.53673594206822));
#58067=CARTESIAN_POINT('',(4.,-0.219892372743086,3.64701365460628));
#58068=CARTESIAN_POINT('Ctrl Pts',(4.,0.254721014554616,3.46322028700966));
#58069=CARTESIAN_POINT('Ctrl Pts',(4.,0.254552373521139,3.46319452321125));
#58070=CARTESIAN_POINT('Ctrl Pts',(4.,0.254383724765285,3.46316883668624));
#58071=CARTESIAN_POINT('Ctrl Pts',(4.,0.254215068323085,3.46314322746093));
#58072=CARTESIAN_POINT('Ctrl Pts',(4.,0.228435861761457,3.4592288468388));
#58073=CARTESIAN_POINT('Ctrl Pts',(4.,0.202474691352968,3.45711700011808));
#58074=CARTESIAN_POINT('Ctrl Pts',(4.,0.176517231963435,3.45683380906617));
#58075=CARTESIAN_POINT('Ctrl Pts',(4.,0.151199179447316,3.45655759382427));
#58076=CARTESIAN_POINT('Ctrl Pts',(4.,0.125883695414598,3.45802192769867));
#58077=CARTESIAN_POINT('Ctrl Pts',(4.,0.1007794950383,3.46128259448669));
#58078=CARTESIAN_POINT('Ctrl Pts',(4.,0.0854593772715275,3.46327245269535));
#58079=CARTESIAN_POINT('Ctrl Pts',(4.,0.0702187270328167,3.46593187194604));
#58080=CARTESIAN_POINT('Ctrl Pts',(4.,0.0551140352340102,3.4692772918897));
#58081=CARTESIAN_POINT('Ctrl Pts',(4.,0.0468842919617017,3.47110003330284));
#58082=CARTESIAN_POINT('Ctrl Pts',(4.,0.0386923719445779,3.47312744960567));
#58083=CARTESIAN_POINT('Ctrl Pts',(4.,0.0305707631998946,3.47535548770785));
#58084=CARTESIAN_POINT('Ctrl Pts',(4.,0.0102648423897012,3.48092610391051));
#58085=CARTESIAN_POINT('Ctrl Pts',(4.,-0.00963556638195036,3.48775588581666));
#58086=CARTESIAN_POINT('Ctrl Pts',(4.,-0.0289965775380143,3.49587186612014));
#58087=CARTESIAN_POINT('Ctrl Pts',(4.,-0.047965755796229,3.50382359322137));
#58088=CARTESIAN_POINT('Ctrl Pts',(4.,-0.0664174073931304,3.51301096346156));
#58089=CARTESIAN_POINT('Ctrl Pts',(4.,-0.0841982143338667,3.52340033683134));
#58090=CARTESIAN_POINT('Ctrl Pts',(4.,-0.0930898199841631,3.5285957259532));
#58091=CARTESIAN_POINT('Ctrl Pts',(4.,-0.101813128894432,3.53409169793663));
#58092=CARTESIAN_POINT('Ctrl Pts',(4.,-0.110345561972859,3.53988353361915));
#58093=CARTESIAN_POINT('Ctrl Pts',(4.,-0.11586100642067,3.5436274303089));
#58094=CARTESIAN_POINT('Ctrl Pts',(4.,-0.121288652521606,3.54748953413154));
#58095=CARTESIAN_POINT('Ctrl Pts',(4.,-0.126621987542688,3.55146681430013));
#58096=CARTESIAN_POINT('Ctrl Pts',(4.,-0.143297831161627,3.56390265451229));
#58097=CARTESIAN_POINT('Ctrl Pts',(4.,-0.159061930875806,3.57746928852925));
#58098=CARTESIAN_POINT('Ctrl Pts',(4.,-0.173743808224101,3.59211536896244));
#58099=CARTESIAN_POINT('Ctrl Pts',(4.,-0.187864697165731,3.60620182877415));
#58100=CARTESIAN_POINT('Ctrl Pts',(4.,-0.200984288190684,3.62128798311348));
#58101=CARTESIAN_POINT('Ctrl Pts',(4.,-0.212904831975564,3.63731335989365));
#58102=CARTESIAN_POINT('Ctrl Pts',(4.,-0.21528245268753,3.64050971304978));
#58103=CARTESIAN_POINT('Ctrl Pts',(4.,-0.217612227418936,3.64374335030505));
#58104=CARTESIAN_POINT('Ctrl Pts',(4.,-0.219892372743211,3.64701365460636));
#58105=CARTESIAN_POINT('Origin',(4.,0.,4.));
#58106=CARTESIAN_POINT('Origin',(2.,0.,4.));
#58107=CARTESIAN_POINT('',(2.,-7.34788079488412E-17,4.6));
#58108=CARTESIAN_POINT('',(2.,-7.34788079488412E-17,4.6));
#58109=CARTESIAN_POINT('Origin',(2.,0.,4.));
#58110=CARTESIAN_POINT('Origin',(2.,0.,4.));
#58111=CARTESIAN_POINT('Ctrl Pts',(3.95224475517895,0.178288362465424,4.37571967666652));
#58112=CARTESIAN_POINT('Ctrl Pts',(3.96019739452275,0.115708609995841,4.40541533085819));
#58113=CARTESIAN_POINT('Ctrl Pts',(3.97610267321037,-0.0245105356436035,
4.43290545314371));
#58114=CARTESIAN_POINT('Ctrl Pts',(3.99996059124178,-0.228962993402626,
4.36819499612132));
#58115=CARTESIAN_POINT('Ctrl Pts',(4.0238185092732,-0.377374743411151,4.21349068386271));
#58116=CARTESIAN_POINT('Ctrl Pts',(4.04767642730463,-0.433534992178268,
4.00656196868444));
#58117=CARTESIAN_POINT('Ctrl Pts',(4.07153434533603,-0.383670022685343,
3.79803920418254));
#58118=CARTESIAN_POINT('Ctrl Pts',(4.09539226336747,-0.239994733226421,
3.63889579340969));
#58119=CARTESIAN_POINT('Ctrl Pts',(4.11925018139887,-0.0376302499649443,
3.56805514133307));
#58120=CARTESIAN_POINT('Ctrl Pts',(4.1431080994303,0.173933765839147,3.60283521426327));
#58121=CARTESIAN_POINT('Ctrl Pts',(4.16696601746172,0.342967344134064,3.73473372141871));
#58122=CARTESIAN_POINT('Ctrl Pts',(4.19082393549313,0.428135478754777,3.93149662217858));
#58123=CARTESIAN_POINT('Ctrl Pts',(4.21468185352456,0.40861313688017,4.1450106963618));
#58124=CARTESIAN_POINT('Ctrl Pts',(4.23853977155597,0.289173588337559,4.32306558264197));
#58125=CARTESIAN_POINT('Ctrl Pts',(4.2623976895874,0.0990233075312312,4.42212219878201));
#58126=CARTESIAN_POINT('Ctrl Pts',(4.28625560761881,-0.115340915390822,
4.41795840454656));
#58127=CARTESIAN_POINT('Ctrl Pts',(4.31011352565024,-0.301501118270308,
4.3115924136571));
#58128=CARTESIAN_POINT('Ctrl Pts',(4.33397144368164,-0.413936097932681,
4.12903358037428));
#58129=CARTESIAN_POINT('Ctrl Pts',(4.35782936171308,-0.425152419412173,
3.91492252699502));
#58130=CARTESIAN_POINT('Ctrl Pts',(4.38168727974448,-0.332407397051365,
3.72161523052345));
#58131=CARTESIAN_POINT('Ctrl Pts',(4.40554519777592,-0.158379709595794,
3.5963805946708));
#58132=CARTESIAN_POINT('Ctrl Pts',(4.42940311580732,0.0543761300157755,
3.56984189703405));
#58133=CARTESIAN_POINT('Ctrl Pts',(4.45326103383876,0.25383552520097,3.64848857324589));
#58134=CARTESIAN_POINT('Ctrl Pts',(4.47711895187016,0.39122521984844,3.81308936806525));
#58135=CARTESIAN_POINT('Ctrl Pts',(4.50097686990159,0.432949691632991,4.02339490384879));
#58136=CARTESIAN_POINT('Ctrl Pts',(4.524834787933,0.368806170420464,4.22797974831721));
#58137=CARTESIAN_POINT('Ctrl Pts',(4.54869270596443,0.214479494504121,4.37681733431002));
#58138=CARTESIAN_POINT('Ctrl Pts',(4.57255062399584,0.00770673985495463,
4.4335128177492));
#58139=CARTESIAN_POINT('Ctrl Pts',(4.59640854202726,-0.200950522604244,
4.38420260860549));
#58140=CARTESIAN_POINT('Ctrl Pts',(4.62026646005868,-0.360469908510665,
4.24094439618412));
#58141=CARTESIAN_POINT('Ctrl Pts',(4.6441243780901,-0.431844582779732,4.03876871570463));
#58142=CARTESIAN_POINT('Ctrl Pts',(4.66798229612152,-0.397621493350665,
3.82711302819544));
#58143=CARTESIAN_POINT('Ctrl Pts',(4.69184021415294,-0.266169117804412,
3.65773291463971));
#58144=CARTESIAN_POINT('Ctrl Pts',(4.71569813218436,-0.0696311426542753,
3.57204642662242));
#58145=CARTESIAN_POINT('Ctrl Pts',(4.73955605021577,0.143933543589337,3.59100624451743));
#58146=CARTESIAN_POINT('Ctrl Pts',(4.76341396824719,0.322302557754209,3.70997617639404));
#58147=CARTESIAN_POINT('Ctrl Pts',(4.78727188627862,0.421859817202848,3.8998648332327));
#58148=CARTESIAN_POINT('Ctrl Pts',(4.81112980431003,0.41826086011465,4.11423926597311));
#58149=CARTESIAN_POINT('Ctrl Pts',(4.83498772234146,0.312385729531365,4.30067908636799));
#58150=CARTESIAN_POINT('Ctrl Pts',(4.85884564037287,0.130123778861223,4.41359467981201));
#58151=CARTESIAN_POINT('Ctrl Pts',(4.88270355840429,-0.0839569802410516,
4.42537510794913));
#58152=CARTESIAN_POINT('Ctrl Pts',(4.90656147643571,-0.277507970732168,
4.33313973520738));
#58153=CARTESIAN_POINT('Ctrl Pts',(4.93041939446713,-0.403200703213916,
4.15944262266324));
#58154=CARTESIAN_POINT('Ctrl Pts',(4.95427731249855,-0.430299880793222,
3.94675744574809));
#58155=CARTESIAN_POINT('Ctrl Pts',(4.97813523052996,-0.352179016385168,
3.7470915236456));
#58156=CARTESIAN_POINT('Ctrl Pts',(5.00199314856139,-0.187940789307144,
3.60926861310034));
#58157=CARTESIAN_POINT('Ctrl Pts',(5.0258510665928,0.0222540801607904,3.56699016996131));
#58158=CARTESIAN_POINT('Ctrl Pts',(5.04970898462423,0.227007220840439,3.63059442521772));
#58159=CARTESIAN_POINT('Ctrl Pts',(5.07356690265564,0.376250912472057,3.7845284059142));
#58160=CARTESIAN_POINT('Ctrl Pts',(5.09742482068706,0.433491007135177,3.99115106069306));
#58161=CARTESIAN_POINT('Ctrl Pts',(5.12128273871848,0.384730742495793,4.19993752217271));
#58162=CARTESIAN_POINT('Ctrl Pts',(5.1451406567499,0.241893331461176,4.35983381329239));
#58163=CARTESIAN_POINT('Ctrl Pts',(5.16899857478132,0.0399064118422473,
4.43174093538579));
#58164=CARTESIAN_POINT('Ctrl Pts',(5.19285649281273,-0.171838712500945,
4.39807563839043));
#58165=CARTESIAN_POINT('Ctrl Pts',(5.21671441084416,-0.341564590845109,
4.26707000444592));
#58166=CARTESIAN_POINT('Ctrl Pts',(5.24057232887557,-0.427768622694993,
4.07075847957352));
#58167=CARTESIAN_POINT('Ctrl Pts',(5.264430246907,-0.409371574112622,3.85714457902312));
#58168=CARTESIAN_POINT('Ctrl Pts',(5.2882881649384,-0.290872024601924,3.6784627202051));
#58169=CARTESIAN_POINT('Ctrl Pts',(5.31214608296984,-0.101246341881189,
3.57840548479658));
#58170=CARTESIAN_POINT('Ctrl Pts',(5.33600400100125,0.113136829324483,3.58143959235932));
#58171=CARTESIAN_POINT('Ctrl Pts',(5.35986191903268,0.299854963974951,3.68682312094679));
#58172=CARTESIAN_POINT('Ctrl Pts',(5.38371983706408,0.413250392048343,3.8687869272297));
#58173=CARTESIAN_POINT('Ctrl Pts',(5.40757775509551,0.425594842551202,4.08283590397723));
#58174=CARTESIAN_POINT('Ctrl Pts',(5.43143567312693,0.333869761079625,4.27662924579771));
#58175=CARTESIAN_POINT('Ctrl Pts',(5.45529359115834,0.160504428594232,4.4027792017911));
#58176=CARTESIAN_POINT('Ctrl Pts',(5.47915150918977,-0.0521086087350157,
4.43043867146175));
#58177=CARTESIAN_POINT('Ctrl Pts',(5.50300942722118,-0.251979671819092,
4.35284416104532));
#58178=CARTESIAN_POINT('Ctrl Pts',(5.52686734525261,-0.390234841353927,
4.18896964197264));
#58179=CARTESIAN_POINT('Ctrl Pts',(5.55072526328402,-0.433066962396004,
3.97888689800548));
#58180=CARTESIAN_POINT('Ctrl Pts',(5.57458318131544,-0.370002414621403,
3.77396688259));
#58181=CARTESIAN_POINT('Ctrl Pts',(5.59844109934686,-0.21646219781534,3.62431812139094));
#58182=CARTESIAN_POINT('Ctrl Pts',(5.62229901737828,-0.00999107731853999,
3.56653381289738));
#58183=CARTESIAN_POINT('Ctrl Pts',(5.64615693540971,0.198923133709572,3.61474379450078));
#58184=CARTESIAN_POINT('Ctrl Pts',(5.67001485344111,0.359195220034686,3.75715941257656));
#58185=CARTESIAN_POINT('Ctrl Pts',(5.69387277147254,0.431634290692432,3.95895616900985));
#58186=CARTESIAN_POINT('Ctrl Pts',(5.71773068950395,0.398527019959163,4.1707892603438));
#58187=CARTESIAN_POINT('Ctrl Pts',(5.74158860753538,0.267969036875697,4.34085972491723));
#58188=CARTESIAN_POINT('Ctrl Pts',(5.76544652556679,0.0718853255354575,
4.42758070267197));
#58189=CARTESIAN_POINT('Ctrl Pts',(5.78930444359821,-0.141776307127955,
4.40974655013133));
#58190=CARTESIAN_POINT('Ctrl Pts',(5.81316236162963,-0.320769768688322,
4.29171820750724));
#58191=CARTESIAN_POINT('Ctrl Pts',(5.83702027966105,-0.421326288178809,
4.10235681181338));
#58192=CARTESIAN_POINT('Ctrl Pts',(5.86087819769247,-0.418857046020503,
3.88796639709818));
#58193=CARTESIAN_POINT('Ctrl Pts',(5.88473611572389,-0.313965860818636,
3.70097123187977));
#58194=CARTESIAN_POINT('Ctrl Pts',(5.90859403375531,-0.132301443679057,
3.58709678011166));
#58195=CARTESIAN_POINT('Ctrl Pts',(5.93245195178673,0.0817142298265842,
3.57418834816524));
#58196=CARTESIAN_POINT('Ctrl Pts',(5.95630986981814,0.275748643515392,3.66540258613358));
#58197=CARTESIAN_POINT('Ctrl Pts',(5.98016778784957,0.402354822815078,3.83843477537114));
#58198=CARTESIAN_POINT('Ctrl Pts',(6.00402570588098,0.430574627524036,4.05097449853386));
#58199=CARTESIAN_POINT('Ctrl Pts',(6.02788362391241,0.353506566116634,4.25104874587108));
#58200=CARTESIAN_POINT('Ctrl Pts',(6.05174154194382,0.189997730437525,4.38973628930191));
#58201=CARTESIAN_POINT('Ctrl Pts',(6.07559945997525,-0.0199730113800777,
4.43311976162365));
#58202=CARTESIAN_POINT('Ctrl Pts',(6.09945737800665,-0.2250554921608,4.3705991908187));
#58203=CARTESIAN_POINT('Ctrl Pts',(6.12331529603809,-0.375113923638194,
4.21744656883549));
#58204=CARTESIAN_POINT('Ctrl Pts',(6.1471732140695,-0.433431396087355,4.01114207710762));
#58205=CARTESIAN_POINT('Ctrl Pts',(6.17103113210093,-0.385792139046387,
3.80207577201042));
#58206=CARTESIAN_POINT('Ctrl Pts',(6.19488905013233,-0.243761337718234,
3.64147770828707));
#58207=CARTESIAN_POINT('Ctrl Pts',(6.21874696816376,-0.042227823444436,
3.56841523311022));
#58208=CARTESIAN_POINT('Ctrl Pts',(6.24260488619517,0.16982704650124,3.60113783246665));
#58209=CARTESIAN_POINT('Ctrl Pts',(6.2664628042266,0.339985970990829,3.73091992247201));
#58210=CARTESIAN_POINT('Ctrl Pts',(6.29032072225801,0.427700638223926,3.92738904240251));
#58211=CARTESIAN_POINT('Ctrl Pts',(6.31417864028943,0.409561128158778,4.13996490148311));
#58212=CARTESIAN_POINT('Ctrl Pts',(6.34598919766466,0.254661277208374,4.38159318714805));
#58213=CARTESIAN_POINT('Ctrl Pts',(6.38575239438369,-0.125272905304917,
4.47558432627151));
#58214=CARTESIAN_POINT('Ctrl Pts',(6.43346823044653,-0.468271923807345,
4.15124960425567));
#58215=CARTESIAN_POINT('Ctrl Pts',(6.48118406650937,-0.380227249479543,
3.6882349865083));
#58216=CARTESIAN_POINT('Ctrl Pts',(6.52889990257221,0.0564566449812287,
3.51140415777354));
#58217=CARTESIAN_POINT('Ctrl Pts',(6.57661573863504,0.441574375138847,3.78331933667001));
#58218=CARTESIAN_POINT('Ctrl Pts',(6.62433157469789,0.421040068198854,4.25418342072721));
#58219=CARTESIAN_POINT('Ctrl Pts',(6.67204741076071,0.0139362792425842,
4.49164405688148));
#58220=CARTESIAN_POINT('Ctrl Pts',(6.71976324682356,-0.406006764042365,
4.27761133505345));
#58221=CARTESIAN_POINT('Ctrl Pts',(6.76747908288639,-0.453085647428837,
3.80864864857145));
#58222=CARTESIAN_POINT('Ctrl Pts',(6.81519491894923,-0.0841006081168706,
3.51540431248109));
#58223=CARTESIAN_POINT('Ctrl Pts',(6.86291075501207,0.362121456530253,3.66717299786736));
#58224=CARTESIAN_POINT('Ctrl Pts',(6.91062659107491,0.475798562415156,4.124581128109));
#58225=CARTESIAN_POINT('Ctrl Pts',(6.95834242713775,0.152544250279933,4.46758486877347));
#58226=CARTESIAN_POINT('Ctrl Pts',(7.00605826320058,-0.310794706562241,
4.38119802990972));
#58227=CARTESIAN_POINT('Ctrl Pts',(7.05377409926342,-0.488725618924084,
3.94475128051735));
#58228=CARTESIAN_POINT('Ctrl Pts',(7.10148993532626,-0.21785253135038,3.55904022429238));
#58229=CARTESIAN_POINT('Ctrl Pts',(7.14920577138909,0.253078023397415,3.57826934481931));
#58230=CARTESIAN_POINT('Ctrl Pts',(7.19692160745195,0.491603063369337,3.98478019943955));
#58231=CARTESIAN_POINT('Ctrl Pts',(7.24463744351477,0.278681483980911,4.40526763942622));
#58232=CARTESIAN_POINT('Ctrl Pts',(7.29235327957762,-0.190157610347023,
4.45359156587464));
#58233=CARTESIAN_POINT('Ctrl Pts',(7.34006911564044,-0.484372034479295,
4.08537538031203));
#58234=CARTESIAN_POINT('Ctrl Pts',(7.3877849517033,-0.333780171974684,3.63875766810317));
#58235=CARTESIAN_POINT('Ctrl Pts',(7.43550078776612,0.123327161313159,3.52387434835784));
#58236=CARTESIAN_POINT('Ctrl Pts',(7.48321662382897,0.467181263150904,3.84622454030349));
#58237=CARTESIAN_POINT('Ctrl Pts',(7.5309324598918,0.382015623368301,4.30978910321172));
#58238=CARTESIAN_POINT('Ctrl Pts',(7.57864829595465,-0.0539608418635878,
4.4888695658253));
#58239=CARTESIAN_POINT('Ctrl Pts',(7.62636413201748,-0.440384235482588,
4.21901358396786));
#58240=CARTESIAN_POINT('Ctrl Pts',(7.67407996808031,-0.422396009600076,
3.7480340579683));
#58241=CARTESIAN_POINT('Ctrl Pts',(7.72179580414317,-0.0165150286377962,
3.50843873354525));
#58242=CARTESIAN_POINT('Ctrl Pts',(7.76951164020598,0.404531957204003,3.72025168374225));
#58243=CARTESIAN_POINT('Ctrl Pts',(7.81722747626884,0.454091022239626,4.18896181724392));
#58244=CARTESIAN_POINT('Ctrl Pts',(7.86494331233166,0.0866513144543145,
4.48414540641706));
#58245=CARTESIAN_POINT('Ctrl Pts',(7.91265914839452,-0.360361628691054,
4.33473081934393));
#58246=CARTESIAN_POINT('Ctrl Pts',(7.96037498445733,-0.476448943335793,
3.87792777037096));
#58247=CARTESIAN_POINT('Ctrl Pts',(8.0080908205202,-0.1550058622045,3.53322552818936));
#58248=CARTESIAN_POINT('Ctrl Pts',(8.05580665658301,0.308781487260178,3.61716946571973));
#58249=CARTESIAN_POINT('Ctrl Pts',(8.10352249264587,0.489010045760349,4.0526725734847));
#58250=CARTESIAN_POINT('Ctrl Pts',(8.1512383287087,0.220173154851853,4.43980564654689));
#58251=CARTESIAN_POINT('Ctrl Pts',(8.19895416477154,-0.250852131956433,
4.4230584271054));
#58252=CARTESIAN_POINT('Ctrl Pts',(8.24667000083438,-0.491516046133,4.01781014446235));
#58253=CARTESIAN_POINT('Ctrl Pts',(8.29438583689722,-0.280813212199106,
3.59620653211525));
#58254=CARTESIAN_POINT('Ctrl Pts',(8.34210167296004,0.187764715363875,3.54541267448783));
#58255=CARTESIAN_POINT('Ctrl Pts',(8.38981750902289,0.483915415676709,3.91207335260334));
#58256=CARTESIAN_POINT('Ctrl Pts',(8.43753334508573,0.335679143777854,4.35947842394856));
#58257=CARTESIAN_POINT('Ctrl Pts',(8.48524918114857,-0.120816450939738,
4.4767689272953));
#58258=CARTESIAN_POINT('Ctrl Pts',(8.5329650172114,-0.466364439759318,4.15623518867385));
#58259=CARTESIAN_POINT('Ctrl Pts',(8.58068085327425,-0.383642787608637,
3.69222827230584));
#58260=CARTESIAN_POINT('Ctrl Pts',(8.62839668933707,0.0513839395061145,
3.51085286915611));
#58261=CARTESIAN_POINT('Ctrl Pts',(8.67611252539993,0.439224004328866,3.77866880275638));
#58262=CARTESIAN_POINT('Ctrl Pts',(8.72382836146275,0.42371790764641,4.24973658040369));
#58263=CARTESIAN_POINT('Ctrl Pts',(8.7715441975256,0.0191051366342138,4.49146741357506));
#58264=CARTESIAN_POINT('Ctrl Pts',(8.81926003358843,-0.403052175319494,
4.28187615866228));
#58265=CARTESIAN_POINT('Ctrl Pts',(8.86697586965126,-0.455080472922433,
3.81343369002772));
#58266=CARTESIAN_POINT('Ctrl Pts',(8.91469170571412,-0.0892013699275644,
3.51631793453238));
#58267=CARTESIAN_POINT('Ctrl Pts',(8.96240754177693,0.358592723611288,3.66337486216116));
#58268=CARTESIAN_POINT('Ctrl Pts',(9.0101233778398,0.477085601399612,4.11955983351088));
#58269=CARTESIAN_POINT('Ctrl Pts',(9.05783921390261,0.157463430517111,4.46595117008304));
#58270=CARTESIAN_POINT('Ctrl Pts',(9.10555504996547,-0.306759831495564,
4.38445237758765));
#58271=CARTESIAN_POINT('Ctrl Pts',(9.1532708860283,-0.489280820139143,3.94990505119329));
#58272=CARTESIAN_POINT('Ctrl Pts',(9.20098672209113,-0.222487703095825,
3.56136068709803));
#58273=CARTESIAN_POINT('Ctrl Pts',(9.24870255815399,0.248619295113741,3.57562555337399));
#58274=CARTESIAN_POINT('Ctrl Pts',(9.29641839421681,0.49141536912078,3.97960000382683));
#58275=CARTESIAN_POINT('Ctrl Pts',(9.34413423027966,0.282937148266828,4.40230808465976));
#58276=CARTESIAN_POINT('Ctrl Pts',(9.39185006634249,-0.185366609388173,
4.45557046104408));
#58277=CARTESIAN_POINT('Ctrl Pts',(9.43956590240532,-0.483445357410111,
4.09047547319903));
#58278=CARTESIAN_POINT('Ctrl Pts',(9.48728173846818,-0.337568794959357,
3.64229546617122));
#58279=CARTESIAN_POINT('Ctrl Pts',(9.53499757453099,0.118302386066128,3.5226010365501));
#58280=CARTESIAN_POINT('Ctrl Pts',(9.58271341059386,0.465534665650901,3.84130942079228));
#58281=CARTESIAN_POINT('Ctrl Pts',(9.63042924665667,0.385259298596883,4.30574580568933));
#58282=CARTESIAN_POINT('Ctrl Pts',(9.67814508271952,-0.0488056103349303,
4.48941111271794));
#58283=CARTESIAN_POINT('Ctrl Pts',(9.72586091878235,-0.438051576325333,
4.22364266437974));
#58284=CARTESIAN_POINT('Ctrl Pts',(9.77357675484519,-0.425028039486299,
3.75249971615691));
#58285=CARTESIAN_POINT('Ctrl Pts',(9.82129259090803,-0.0216947140899849,
3.50864008686857));
#58286=CARTESIAN_POINT('Ctrl Pts',(9.86900842697087,0.401561201071248,3.7160038263529));
#58287=CARTESIAN_POINT('Ctrl Pts',(9.91672426303371,0.456057286475463,4.18416562194019));
#58288=CARTESIAN_POINT('Ctrl Pts',(9.96444009909655,0.0917489483659128,
4.48320529314746));
#58289=CARTESIAN_POINT('Ctrl Pts',(10.0121559351594,-0.356813860767086,
4.3385101085883));
#58290=CARTESIAN_POINT('Ctrl Pts',(10.0598717712222,-0.477709011270712,
3.88295588266498));
#58291=CARTESIAN_POINT('Ctrl Pts',(10.1075876072851,-0.159916626226494,
3.53488507064564));
#58292=CARTESIAN_POINT('Ctrl Pts',(10.1553034433479,0.304729657315094,3.61393645496551));
#58293=CARTESIAN_POINT('Ctrl Pts',(10.2030192794107,0.489538007675758,4.04751593304174));
#58294=CARTESIAN_POINT('Ctrl Pts',(10.2507351154736,0.224796073077312,4.43746079867915));
#58295=CARTESIAN_POINT('Ctrl Pts',(10.2984509515364,-0.246379554360218,
4.42567868168988));
#58296=CARTESIAN_POINT('Ctrl Pts',(10.3461667875993,-0.491301045992024,
4.02298928139638));
#58297=CARTESIAN_POINT('Ctrl Pts',(10.3938826236621,-0.285053227451061,
3.599188470261));
#58298=CARTESIAN_POINT('Ctrl Pts',(10.4415984597249,0.182963355965895,3.54345905416307));
#58299=CARTESIAN_POINT('Ctrl Pts',(10.4893142957878,0.482961874346273,3.9069782134126));
#58300=CARTESIAN_POINT('Ctrl Pts',(10.5370301318506,0.339449072190825,4.35592071060949));
#58301=CARTESIAN_POINT('Ctrl Pts',(10.5847459679134,-0.115785036052801,
4.47801574270962));
#58302=CARTESIAN_POINT('Ctrl Pts',(10.6324618039763,-0.464691964107356,
4.16114156306187));
#58303=CARTESIAN_POINT('Ctrl Pts',(10.6801776400391,-0.386865111317189,
3.69628860657276));
#58304=CARTESIAN_POINT('Ctrl Pts',(10.7278934761019,0.0462259258804368,
3.51033849586834));
#58305=CARTESIAN_POINT('Ctrl Pts',(10.7756093121648,0.436866984064762,3.77405207881873));
#58306=CARTESIAN_POINT('Ctrl Pts',(10.8233251482276,0.426326368719826,4.24525711444552));
#58307=CARTESIAN_POINT('Ctrl Pts',(10.8710409842905,0.0242836891050981,
4.49123876811122));
#58308=CARTESIAN_POINT('Ctrl Pts',(10.9187568203533,-0.400059075867425,
4.28610830234036));
#58309=CARTESIAN_POINT('Ctrl Pts',(10.9664726564161,-0.45702143577077,3.81824018018824));
#58310=CARTESIAN_POINT('Ctrl Pts',(11.014188492479,-0.0942939790271268,
3.51728489730359));
#58311=CARTESIAN_POINT('Ctrl Pts',(11.0619043285418,0.355025089556487,3.65961432075161));
#58312=CARTESIAN_POINT('Ctrl Pts',(11.1096201646047,0.478319155637209,4.11452515096033));
#58313=CARTESIAN_POINT('Ctrl Pts',(11.1573360006675,0.16236538121005,4.46426577284621));
#58314=CARTESIAN_POINT('Ctrl Pts',(11.2050518367304,-0.302691021094817,
4.38766399188028));
#58315=CARTESIAN_POINT('Ctrl Pts',(11.2527676727932,-0.489781601228288,
3.95506440219344));
#58316=CARTESIAN_POINT('Ctrl Pts',(11.300483508856,-0.227098200695192,3.56372986339542));
#58317=CARTESIAN_POINT('Ctrl Pts',(11.3481993449188,0.244132971891272,3.57302890392028));
#58318=CARTESIAN_POINT('Ctrl Pts',(11.3959151809817,0.491173079921361,3.97442207176994));
#58319=CARTESIAN_POINT('Ctrl Pts',(11.4436310170445,0.287161390990383,4.39930384468027));
#58320=CARTESIAN_POINT('Ctrl Pts',(11.4913468531074,-0.180555021833016,
4.45749875294131));
#58321=CARTESIAN_POINT('Ctrl Pts',(11.5390626891702,-0.482464979911041,
4.09556551685319));
#58322=CARTESIAN_POINT('Ctrl Pts',(11.586778525233,-0.341319923258817,3.64587299617429));
#58323=CARTESIAN_POINT('Ctrl Pts',(11.6344943612959,0.113264470804062,3.5213807520529));
#58324=CARTESIAN_POINT('Ctrl Pts',(11.6822101973587,0.463836358529674,3.83641192782507));
#58325=CARTESIAN_POINT('Ctrl Pts',(11.7299260334216,0.38846018117773,4.30166854740152));
#58326=CARTESIAN_POINT('Ctrl Pts',(11.7776418694844,-0.0436449577779122,
4.48989829813191));
#58327=CARTESIAN_POINT('Ctrl Pts',(11.8253577055472,-0.435670260442099,
4.22824690363353));
#58328=CARTESIAN_POINT('Ctrl Pts',(11.8730735416101,-0.427612859293677,
3.75699286549843));
#58329=CARTESIAN_POINT('Ctrl Pts',(11.9207893776729,-0.0268719897862959,
3.50889601812151));
#58330=CARTESIAN_POINT('Ctrl Pts',(11.9685052137357,0.398545841420554,3.71178751390968));
#58331=CARTESIAN_POINT('Ctrl Pts',(12.0162210497986,0.457972894034889,4.17934897039372));
#58332=CARTESIAN_POINT('Ctrl Pts',(12.0639368858614,0.0968363912382316,
4.48221150772657));
#58333=CARTESIAN_POINT('Ctrl Pts',(12.1116527219243,-0.353226459651896,
4.34225179773635));
#58334=CARTESIAN_POINT('Ctrl Pts',(12.1593685579871,-0.478916017555994,
3.88799699566402));
#58335=CARTESIAN_POINT('Ctrl Pts',(12.2070843940499,-0.164809627468288,
3.53659627586117));
#58336=CARTESIAN_POINT('Ctrl Pts',(12.2548002301128,0.300643979445627,3.61074632631782));
#58337=CARTESIAN_POINT('Ctrl Pts',(12.3025160661756,0.490011594032383,4.04235401475446));
#58338=CARTESIAN_POINT('Ctrl Pts',(12.3502319022385,0.229394022021679,4.43506735974179));
#58339=CARTESIAN_POINT('Ctrl Pts',(12.3979477383013,-0.241879610092261,
4.42825165390643));
#58340=CARTESIAN_POINT('Ctrl Pts',(12.4456635743641,-0.491031474462283,
4.0281658647901));
#58341=CARTESIAN_POINT('Ctrl Pts',(12.493379410427,-0.289261580343189,3.60221492864948));
#58342=CARTESIAN_POINT('Ctrl Pts',(12.5410952464898,0.178141673866572,3.54155614424011));
#58343=CARTESIAN_POINT('Ctrl Pts',(12.5888110825527,0.481954687902679,3.90189340664049));
#58344=CARTESIAN_POINT('Ctrl Pts',(12.6365269186155,0.343181296211668,4.35232346328687));
#58345=CARTESIAN_POINT('Ctrl Pts',(12.6842427546783,-0.110740760313508,
4.47920946240362));
#58346=CARTESIAN_POINT('Ctrl Pts',(12.7319585907412,-0.462967872677167,
4.16603003860975));
#58347=CARTESIAN_POINT('Ctrl Pts',(12.779674426804,-0.390044463885,3.70038267566003));
#58348=CARTESIAN_POINT('Ctrl Pts',(12.8273902628668,0.0410627776982723,
3.50987851185683));
#58349=CARTESIAN_POINT('Ctrl Pts',(12.8751060989297,0.434461438689172,3.76946045210395));
#58350=CARTESIAN_POINT('Ctrl Pts',(12.9228219349925,0.42888747548329,4.24075040649094));
#58351=CARTESIAN_POINT('Ctrl Pts',(12.9705377710553,0.0294595442590321,
4.49095555817611));
#58352=CARTESIAN_POINT('Ctrl Pts',(13.0182536071182,-0.397021539751646,
4.29030866646591));
#58353=CARTESIAN_POINT('Ctrl Pts',(13.065969443181,-0.458911634846768,3.82306685936703));
#58354=CARTESIAN_POINT('Ctrl Pts',(13.1136852792439,-0.0993761143989603,
3.51830547777773));
#58355=CARTESIAN_POINT('Ctrl Pts',(13.1614011153067,0.351418020999476,3.65589158776806));
#58356=CARTESIAN_POINT('Ctrl Pts',(13.2091169513695,0.479499580452807,4.10947774749948));
#58357=CARTESIAN_POINT('Ctrl Pts',(13.2568327874324,0.167249297126924,4.46252880717046));
#58358=CARTESIAN_POINT('Ctrl Pts',(13.3045486234952,-0.298588589211839,
4.39083254629632));
#58359=CARTESIAN_POINT('Ctrl Pts',(13.352264459558,-0.490227979701372,3.96022874442655));
#58360=CARTESIAN_POINT('Ctrl Pts',(13.3999802956209,-0.23168347330409,3.56614749850931));
#58361=CARTESIAN_POINT('Ctrl Pts',(13.4476961316837,0.239619531536799,3.57047968038978));
#58362=CARTESIAN_POINT('Ctrl Pts',(13.4954119677466,0.490876233547033,3.96924698078795));
#58363=CARTESIAN_POINT('Ctrl Pts',(13.5431278038094,0.291353737189313,4.39625525192456));
#58364=CARTESIAN_POINT('Ctrl Pts',(13.5908436398722,-0.175723379082843,
4.45937622804808));
#58365=CARTESIAN_POINT('Ctrl Pts',(13.6385594759351,-0.481431012491488,
4.10064494554323));
#58366=CARTESIAN_POINT('Ctrl Pts',(13.6862753119979,-0.345033139360895,
3.64948986092447));
#58367=CARTESIAN_POINT('Ctrl Pts',(13.7339911480608,0.108213974662067,3.52021363031051));
#58368=CARTESIAN_POINT('Ctrl Pts',(13.7817069841236,0.462086530666827,3.83153260544464));
#58369=CARTESIAN_POINT('Ctrl Pts',(13.8294228201864,0.391617915445045,4.297557781203));
#58370=CARTESIAN_POINT('Ctrl Pts',(13.8771386562493,-0.0384794573460961,
4.49033106796769));
#58371=CARTESIAN_POINT('Ctrl Pts',(13.9248544923121,-0.433240552373761,
4.23282579030437));
#58372=CARTESIAN_POINT('Ctrl Pts',(13.9725703283749,-0.430150181893835,
3.76151300691929));
#58373=CARTESIAN_POINT('Ctrl Pts',(14.0202861644378,-0.032046280669499,
3.50920649887429));
#58374=CARTESIAN_POINT('Ctrl Pts',(14.0680020005006,0.39548621318905,3.70760321474174));
#58375=CARTESIAN_POINT('Ctrl Pts',(14.1157178365634,0.459837632138507,4.1745123976147));
#58376=CARTESIAN_POINT('Ctrl Pts',(14.1634336726263,0.101913077983734,4.48116416053968));
#58377=CARTESIAN_POINT('Ctrl Pts',(14.2111495086891,-0.349599823817769,
4.34595547117883));
#58378=CARTESIAN_POINT('Ctrl Pts',(14.258865344752,-0.480069828122688,3.8930505494253));
#58379=CARTESIAN_POINT('Ctrl Pts',(14.3065811808148,-0.169684322438749,
3.53835895376334));
#58380=CARTESIAN_POINT('Ctrl Pts',(14.3542970168777,0.296524907469595,3.60759943412104));
#58381=CARTESIAN_POINT('Ctrl Pts',(14.4020128529405,0.49043075222644,4.0371873919842));
#58382=CARTESIAN_POINT('Ctrl Pts',(14.4497286890033,0.233966490966644,4.43262559558668));
#58383=CARTESIAN_POINT('Ctrl Pts',(14.4974445250662,-0.237352798985028,
4.43077705796148));
#58384=CARTESIAN_POINT('Ctrl Pts',(14.545160361129,-0.490707361486496,4.03333931965322));
#58385=CARTESIAN_POINT('Ctrl Pts',(14.5928761971918,-0.293437803431633,
3.60528557111603));
#58386=CARTESIAN_POINT('Ctrl Pts',(14.6405920332547,0.173300204635467,3.53970415608515));
#58387=CARTESIAN_POINT('Ctrl Pts',(14.6883078693175,0.480893968219416,3.89681949708321));
#58388=CARTESIAN_POINT('Ctrl Pts',(14.7360237053804,0.346875401282657,4.34868708154587));
#58389=CARTESIAN_POINT('Ctrl Pts',(14.7837395414432,-0.10568418401607,4.48034995378457));
#58390=CARTESIAN_POINT('Ctrl Pts',(14.831455377506,-0.461192356972643,4.17090007232882));
#58391=CARTESIAN_POINT('Ctrl Pts',(14.8791712135689,-0.393180492164677,
3.7045100248179));
#58392=CARTESIAN_POINT('Ctrl Pts',(14.9268870496317,0.0358950684576197,
3.50947296821438));
#58393=CARTESIAN_POINT('Ctrl Pts',(14.9746028856945,0.432007635398663,3.76489443262817));
#58394=CARTESIAN_POINT('Ctrl Pts',(15.0223187217574,0.431400943461215,4.23621695712364));
#58395=CARTESIAN_POINT('Ctrl Pts',(15.0700345578202,0.0346321271865876,
4.4906178152274));
#58396=CARTESIAN_POINT('Ctrl Pts',(15.1177503938831,-0.393939904367254,
4.2944767844824));
#58397=CARTESIAN_POINT('Ctrl Pts',(15.1654662299459,-0.46075086019608,3.82791319143947));
#58398=CARTESIAN_POINT('Ctrl Pts',(15.2131820660087,-0.104447211543591,
3.51937956259357));
#58399=CARTESIAN_POINT('Ctrl Pts',(15.2608979020716,0.347771918596306,3.652207076714));
#58400=CARTESIAN_POINT('Ctrl Pts',(15.3086137381344,0.480626744730421,4.10441818376995));
#58401=CARTESIAN_POINT('Ctrl Pts',(15.3563295741973,0.172114635785536,4.46074046598969));
#58402=CARTESIAN_POINT('Ctrl Pts',(15.4040454102601,-0.294452991525291,
4.39395768888776));
#58403=CARTESIAN_POINT('Ctrl Pts',(15.4517612463229,-0.490619905976795,
3.96539750426199));
#58404=CARTESIAN_POINT('Ctrl Pts',(15.4994770823858,-0.236243011612202,
3.56861332390027));
#58405=CARTESIAN_POINT('Ctrl Pts',(15.5471929184486,0.235079475381852,3.56797816593814));
#58406=CARTESIAN_POINT('Ctrl Pts',(15.5949087545115,0.490524862970081,3.9640753057054));
#58407=CARTESIAN_POINT('Ctrl Pts',(15.6426245905743,0.295513721197704,4.39316264501585));
#58408=CARTESIAN_POINT('Ctrl Pts',(15.6903404266371,-0.170872217813597,
4.46120267782338));
#58409=CARTESIAN_POINT('Ctrl Pts',(15.7380562626999,-0.480343569999647,
4.1057131950703));
#58410=CARTESIAN_POINT('Ctrl Pts',(15.7857720987628,-0.348708030819167,
3.6531456586776));
#58411=CARTESIAN_POINT('Ctrl Pts',(15.8334879348256,0.103151458625294,3.5190998009613));
#58412=CARTESIAN_POINT('Ctrl Pts',(15.8812037708885,0.460285376424935,3.82667199562295));
#58413=CARTESIAN_POINT('Ctrl Pts',(15.9289196069513,0.39473215065269,4.29341396369818));
#58414=CARTESIAN_POINT('Ctrl Pts',(15.9766354430142,-0.033309682798763,
4.49070937415524));
#58415=CARTESIAN_POINT('Ctrl Pts',(16.024351279077,-0.430762722000766,4.23737881579128));
#58416=CARTESIAN_POINT('Ctrl Pts',(16.0720671151398,-0.432639725453012,
3.76605963834362));
#58417=CARTESIAN_POINT('Ctrl Pts',(16.1197829512026,-0.0372170120039125,
3.50957149464017));
#58418=CARTESIAN_POINT('Ctrl Pts',(16.1674987872655,0.392382656225717,3.70345139362117));
#58419=CARTESIAN_POINT('Ctrl Pts',(16.2152146233283,0.461651293660056,4.16965644082667));
#58420=CARTESIAN_POINT('Ctrl Pts',(16.2629304593912,0.106978444708158,4.48006336792116));
#58421=CARTESIAN_POINT('Ctrl Pts',(16.310646295454,-0.345934356094203,4.34962071752925));
#58422=CARTESIAN_POINT('Ctrl Pts',(16.3583621315169,-0.481170314810987,
3.89811598262401));
#58423=CARTESIAN_POINT('Ctrl Pts',(16.4060779675797,-0.174540169679895,
3.54017290856226));
#58424=CARTESIAN_POINT('Ctrl Pts',(16.4537938036425,0.292372898913969,3.60449612791703));
#58425=CARTESIAN_POINT('Ctrl Pts',(16.5015096397054,0.490795435699827,4.0320166386149));
#58426=CARTESIAN_POINT('Ctrl Pts',(16.5492254757682,0.238512972024049,4.4301357774334));
#58427=CARTESIAN_POINT('Ctrl Pts',(16.596941311831,-0.23279962385521,4.43325461334514));
#58428=CARTESIAN_POINT('Ctrl Pts',(16.6446571478939,-0.490328743065594,
4.03850907134293));
#58429=CARTESIAN_POINT('Ctrl Pts',(16.6923729839567,-0.297581432841348,
3.60840005658827));
#58430=CARTESIAN_POINT('Ctrl Pts',(16.7400888200196,0.168439486040012,3.53790329540825));
#58431=CARTESIAN_POINT('Ctrl Pts',(16.7878046560824,0.479779833116189,3.89175704832657));
#58432=CARTESIAN_POINT('Ctrl Pts',(16.8355204921452,0.350530977080134,4.3450119692985));
#58433=CARTESIAN_POINT('Ctrl Pts',(16.8832363282081,-0.100615868820984,
4.4814370901721));
#58434=CARTESIAN_POINT('Ctrl Pts',(16.9309521642709,-0.459365614209645,
4.17575112327883));
#58435=CARTESIAN_POINT('Ctrl Pts',(16.9786680003337,-0.396272847821079,
3.70867019559999));
#58436=CARTESIAN_POINT('Ctrl Pts',(17.0263838363966,0.0307233721630972,
3.5091219099869));
#58437=CARTESIAN_POINT('Ctrl Pts',(17.0740996724594,0.429505846750062,3.76035452756312));
#58438=CARTESIAN_POINT('Ctrl Pts',(17.1218155085223,0.433866493469502,4.23165726989771));
#58439=CARTESIAN_POINT('Ctrl Pts',(17.1695313445851,0.039800863341802,4.49022557677993));
#58440=CARTESIAN_POINT('Ctrl Pts',(17.217247180648,-0.390814512007675,4.29861219341511));
#58441=CARTESIAN_POINT('Ctrl Pts',(17.2649630167107,-0.462538907526291,
3.83277863809798));
#58442=CARTESIAN_POINT('Ctrl Pts',(17.3126788527736,-0.109506707187599,
3.52050703244687));
#58443=CARTESIAN_POINT('Ctrl Pts',(17.3603946888365,0.344087187338735,3.64856119684745));
#58444=CARTESIAN_POINT('Ctrl Pts',(17.4081105248993,0.481700523269991,4.09934702176407));
#58445=CARTESIAN_POINT('Ctrl Pts',(17.4558263609621,0.176960856767158,4.45890094794434));
#58446=CARTESIAN_POINT('Ctrl Pts',(17.503542197025,-0.290284687397741,4.39703907252861));
#58447=CARTESIAN_POINT('Ctrl Pts',(17.5512580330878,-0.490957336521241,
3.97057010757845));
#58448=CARTESIAN_POINT('Ctrl Pts',(17.5989738691507,-0.240776309167652,
3.57112706567612));
#58449=CARTESIAN_POINT('Ctrl Pts',(17.6466897052135,0.230513307714322,3.56552463842171));
#58450=CARTESIAN_POINT('Ctrl Pts',(17.6944055412763,0.490119007219086,3.95890762096741));
#58451=CARTESIAN_POINT('Ctrl Pts',(17.7421213773392,0.299640880944266,4.39002636746625));
#58452=CARTESIAN_POINT('Ctrl Pts',(17.789837213402,-0.166002076869247,4.46297789939377));
#58453=CARTESIAN_POINT('Ctrl Pts',(17.8375530494648,-0.479202773223469,
4.11076970247734));
#58454=CARTESIAN_POINT('Ctrl Pts',(17.8852688855277,-0.352344189444135,
3.65683998336499));
#58455=CARTESIAN_POINT('Ctrl Pts',(17.9329847215905,0.0980774850139738,
3.51803938772416));
#58456=CARTESIAN_POINT('Ctrl Pts',(17.9807005576534,0.458433095867658,3.82183063825345));
#58457=CARTESIAN_POINT('Ctrl Pts',(18.0284163937162,0.397802540886209,4.28923755516265));
#58458=CARTESIAN_POINT('Ctrl Pts',(18.076132229779,-0.0281362083699241,
4.49103317467411));
#58459=CARTESIAN_POINT('Ctrl Pts',(18.1238480658419,-0.428237044548737,
4.24190547436581));
#58460=CARTESIAN_POINT('Ctrl Pts',(18.1715639019047,-0.435081213444543,
3.7706322547532));
#58461=CARTESIAN_POINT('Ctrl Pts',(18.2192797379675,-0.0423836094492617,
3.50999096487715));
#58462=CARTESIAN_POINT('Ctrl Pts',(18.2669955740304,0.389235515258945,3.69933251171255));
#58463=CARTESIAN_POINT('Ctrl Pts',(18.3147114100932,0.463413677146622,4.16478163940629));
#58464=CARTESIAN_POINT('Ctrl Pts',(18.3624272461561,0.112031928774586,4.4789092521418));
#58465=CARTESIAN_POINT('Ctrl Pts',(18.4101430822189,-0.342230463623947,
4.35324712966946));
#58466=CARTESIAN_POINT('Ctrl Pts',(18.4578589182817,-0.482217355384067,
3.90319273261591));
#58467=CARTESIAN_POINT('Ctrl Pts',(18.5055747543446,-0.179376629827252,
3.54203793877243));
#58468=CARTESIAN_POINT('Ctrl Pts',(18.5532905904074,0.288188414964166,3.60143675240633));
#58469=CARTESIAN_POINT('Ctrl Pts',(18.6010064264702,0.491105603945206,4.02684232898929));
#58470=CARTESIAN_POINT('Ctrl Pts',(18.6487222625331,0.243032960192409,4.42759818183915));
#58471=CARTESIAN_POINT('Ctrl Pts',(18.6964380985959,-0.228220590447982,
4.43568404486223));
#58472=CARTESIAN_POINT('Ctrl Pts',(18.7441539346588,-0.489895661254576,
4.0436745456279));
#58473=CARTESIAN_POINT('Ctrl Pts',(18.7918697707216,-0.301692008317894,
3.6115580391236));
#58474=CARTESIAN_POINT('Ctrl Pts',(18.8395856067845,0.163560057986223,3.53615376224111));
#58475=CARTESIAN_POINT('Ctrl Pts',(18.8873014428472,0.478612406344963,3.88670662268212));
#58476=CARTESIAN_POINT('Ctrl Pts',(18.9350172789101,0.35414761756175,4.34129853476112));
#58477=CARTESIAN_POINT('Ctrl Pts',(18.982733114973,-0.0955363776958117,
4.48247075080787));
#58478=CARTESIAN_POINT('Ctrl Pts',(19.0304489510358,-0.457487847288108,
4.18058265263639));
#58479=CARTESIAN_POINT('Ctrl Pts',(19.0781647870987,-0.399321187381313,
3.71286272589862));
#58480=CARTESIAN_POINT('Ctrl Pts',(19.1258806231614,0.0255482632835279,
3.50882537619781));
#58481=CARTESIAN_POINT('Ctrl Pts',(19.1735964592243,0.426956350589889,3.75584124112414));
#58482=CARTESIAN_POINT('Ctrl Pts',(19.2213122952871,0.436283851722622,4.22707185138688));
#58483=CARTESIAN_POINT('Ctrl Pts',(19.26902813135,0.0449651784623906,4.48977888620274));
#58484=CARTESIAN_POINT('Ctrl Pts',(19.3167439674128,-0.387645709555542,
4.3027144342981));
#58485=CARTESIAN_POINT('Ctrl Pts',(19.3644598034757,-0.464275578741542,
3.8376626582024));
#58486=CARTESIAN_POINT('Ctrl Pts',(19.4121756395385,-0.114554038379521,
3.52168776344319));
#58487=CARTESIAN_POINT('Ctrl Pts',(19.4598914756013,0.340364234683876,3.64495435060606));
#58488=CARTESIAN_POINT('Ctrl Pts',(19.5076073116642,0.482720800247919,4.09426482953845));
#58489=CARTESIAN_POINT('Ctrl Pts',(19.555323147727,0.181787415268628,4.45701044834135));
#58490=CARTESIAN_POINT('Ctrl Pts',(19.6030389837899,-0.28608412753634,4.40007637198121));
#58491=CARTESIAN_POINT('Ctrl Pts',(19.6507548198527,-0.491240257057309,
3.97574594767572));
#58492=CARTESIAN_POINT('Ctrl Pts',(19.6984706559155,-0.245282818621706,
3.57368850533185));
#58493=CARTESIAN_POINT('Ctrl Pts',(19.7461864919783,0.225921452997342,3.56311925573479));
#58494=CARTESIAN_POINT('Ctrl Pts',(19.7939023280412,0.489658867576397,3.95374471702426));
#58495=CARTESIAN_POINT('Ctrl Pts',(19.841618164104,0.303734463062876,4.38684635894002));
#58496=CARTESIAN_POINT('Ctrl Pts',(19.8893340001669,-0.161112940293692,
4.46470246728215));
#58497=CARTESIAN_POINT('Ctrl Pts',(19.9370498362297,-0.47800980043334,4.11581244897344));
#58498=CARTESIAN_POINT('Ctrl Pts',(19.9847656722926,-0.355939225796451,
3.66057517601247));
#58499=CARTESIAN_POINT('Ctrl Pts',(20.0324815083554,0.0929888682922082,
3.51702731322357));
#58500=CARTESIAN_POINT('Ctrl Pts',(20.0801973444182,0.456536973876988,3.81701888067549));
#58501=CARTESIAN_POINT('Ctrl Pts',(20.1279131804811,0.400815378068436,4.28501049648274));
#58502=CARTESIAN_POINT('Ctrl Pts',(20.1756290165439,-0.022934367574535,
4.49133741301101));
#58503=CARTESIAN_POINT('Ctrl Pts',(20.2233448526067,-0.425711472830213,
4.24633918020534));
#58504=CARTESIAN_POINT('Ctrl Pts',(20.2710606886696,-0.437384262562023,
3.77535541015343));
#58505=CARTESIAN_POINT('Ctrl Pts',(20.3187765247324,-0.0477164433392854,
3.51022640082505));
#58506=CARTESIAN_POINT('Ctrl Pts',(20.3664923607953,0.386374384143037,3.69571627142296));
#58507=CARTESIAN_POINT('Ctrl Pts',(20.4062555575143,0.45143962727185,4.08165775845481));
#58508=CARTESIAN_POINT('Ctrl Pts',(20.4380661148895,0.291471375703242,4.31996082336987));
#58509=CARTESIAN_POINT('Ctrl Pts',(20.461924032921,0.103697252552815,4.42124466395835));
#58510=CARTESIAN_POINT('Ctrl Pts',(20.4857819509523,-0.111451542568667,
4.41901444157942));
#58511=CARTESIAN_POINT('Ctrl Pts',(20.5096398689838,-0.298255971346869,
4.31460392554555));
#58512=CARTESIAN_POINT('Ctrl Pts',(20.5334977870152,-0.412709509332759,
4.13311446574462));
#58513=CARTESIAN_POINT('Ctrl Pts',(20.5573557050466,-0.425936384696969,
3.91915434697803));
#58514=CARTESIAN_POINT('Ctrl Pts',(20.581213623078,-0.335173342752607,3.72492109335083));
#58515=CARTESIAN_POINT('Ctrl Pts',(20.6050715411095,-0.162364888615448,
3.59797442377207));
#58516=CARTESIAN_POINT('Ctrl Pts',(20.6289294591408,0.0501004451364318,
3.56932214892951));
#58517=CARTESIAN_POINT('Ctrl Pts',(20.6527873771723,0.250339089241223,3.64598859455508));
#58518=CARTESIAN_POINT('Ctrl Pts',(20.6766452952037,0.389350172549011,3.80921715950176));
#58519=CARTESIAN_POINT('Ctrl Pts',(20.7005032132352,0.433161330121289,4.01909908002448));
#58520=CARTESIAN_POINT('Ctrl Pts',(20.7243611312665,0.371049143609512,4.22430982617278));
#58521=CARTESIAN_POINT('Ctrl Pts',(20.748219049298,0.218207240773441,4.37467120177868));
#58522=CARTESIAN_POINT('Ctrl Pts',(20.7720769673293,0.01200671405148,4.43341500212799));
#58523=CARTESIAN_POINT('Ctrl Pts',(20.7959348853608,-0.197129246586683,
4.38617716647524));
#58524=CARTESIAN_POINT('Ctrl Pts',(20.8197928033922,-0.358062019934396,
4.24450842127602));
#58525=CARTESIAN_POINT('Ctrl Pts',(20.8436507214237,-0.431438726014498,
4.04305074550709));
#58526=CARTESIAN_POINT('Ctrl Pts',(20.867508639455,-0.399316990859146,3.83106596928302));
#58527=CARTESIAN_POINT('Ctrl Pts',(20.8913665574865,-0.269551332195825,
3.66039017609669));
#58528=CARTESIAN_POINT('Ctrl Pts',(20.9152244755179,-0.0738730526583281,
3.57275822989076));
#58529=CARTESIAN_POINT('Ctrl Pts',(20.9390823935493,0.139869212314499,3.58959853735383));
#58530=CARTESIAN_POINT('Ctrl Pts',(20.9629403115807,0.319409638666883,3.70679317993256));
#58531=CARTESIAN_POINT('Ctrl Pts',(20.9867982296122,0.420845711130686,3.8956848776653));
#58532=CARTESIAN_POINT('Ctrl Pts',(21.0106561476436,0.419373541863394,4.11008446384341));
#58533=CARTESIAN_POINT('Ctrl Pts',(21.034514065675,0.315353119032788,4.29756540021079));
#58534=CARTESIAN_POINT('Ctrl Pts',(21.0583719837064,0.134220268060588,4.41228349058099));
#58535=CARTESIAN_POINT('Ctrl Pts',(21.0822299017379,-0.079733094278782,
4.42618703719455));
#58536=CARTESIAN_POINT('Ctrl Pts',(21.1060878197692,-0.274189543318984,
4.33587624407661));
#58537=CARTESIAN_POINT('Ctrl Pts',(21.1299457378007,-0.401599180171465,
4.16343456021562));
#58538=CARTESIAN_POINT('Ctrl Pts',(21.1538036558321,-0.430806878168669,
3.95102867450389));
#58539=CARTESIAN_POINT('Ctrl Pts',(21.1776615738635,-0.354670559489406,
3.75059761183336));
#58540=CARTESIAN_POINT('Ctrl Pts',(21.2015194918949,-0.191807627993766,
3.61115222665144));
#58541=CARTESIAN_POINT('Ctrl Pts',(21.2253774099264,0.0179574932869785,
3.56679071405539));
#58542=CARTESIAN_POINT('Ctrl Pts',(21.2492353279577,0.223331518303719,3.62836067225603));
#58543=CARTESIAN_POINT('Ctrl Pts',(21.2730932459892,0.374094903668402,3.78080656934254));
#58544=CARTESIAN_POINT('Ctrl Pts',(21.2969511640206,0.433381894944723,3.98685123093373));
#58545=CARTESIAN_POINT('Ctrl Pts',(21.320809082052,0.386695207821707,4.19611112472705));
#58546=CARTESIAN_POINT('Ctrl Pts',(21.3446670000834,0.245451009020076,4.35741650656472));
#58547=CARTESIAN_POINT('Ctrl Pts',(21.3685249181149,0.0441873525619181,
4.43132381671722));
#58548=CARTESIAN_POINT('Ctrl Pts',(21.3923828361462,-0.167881315237013,
4.39976070465745));
#58549=CARTESIAN_POINT('Ctrl Pts',(21.4162407541777,-0.338898428465248,
4.27044521104599));
#58550=CARTESIAN_POINT('Ctrl Pts',(21.4400986722091,-0.427045644525908,
4.07499849655415));
#58551=CARTESIAN_POINT('Ctrl Pts',(21.4639565902406,-0.410768568010174,
3.86121260673678));
#58552=CARTESIAN_POINT('Ctrl Pts',(21.4878145082719,-0.294047387504818,
3.68136401506497));
#58553=CARTESIAN_POINT('Ctrl Pts',(21.5116724263034,-0.105423611064507,
3.57943060117972));
#58554=CARTESIAN_POINT('Ctrl Pts',(21.5355303443348,0.108979109962582,3.58033786138646));
#58555=CARTESIAN_POINT('Ctrl Pts',(21.5593882623662,0.296733470072461,3.68386394585134));
#58556=CARTESIAN_POINT('Ctrl Pts',(21.5832461803976,0.411928413892185,3.86469390692879));
#58557=CARTESIAN_POINT('Ctrl Pts',(21.6071040984291,0.426395639810567,4.07860989342611));
#58558=CARTESIAN_POINT('Ctrl Pts',(21.6309620164605,0.33659751701124,4.27330361969026));
#58559=CARTESIAN_POINT('Ctrl Pts',(21.6548199344919,0.164492132570386,4.401167166299));
#58560=CARTESIAN_POINT('Ctrl Pts',(21.6786778525233,-0.0478360589596606,
4.43093441317345));
#58561=CARTESIAN_POINT('Ctrl Pts',(21.7025357705547,-0.248467031045983,
4.35532645760922));
#58562=CARTESIAN_POINT('Ctrl Pts',(21.7263936885861,-0.388341045935521,
4.1928315042612));
#58563=CARTESIAN_POINT('Ctrl Pts',(21.7502516066176,-0.433255096896122,
3.98318399549658));
#58564=CARTESIAN_POINT('Ctrl Pts',(21.774109524649,-0.372226475033738,3.77764845789182));
#58565=CARTESIAN_POINT('Ctrl Pts',(21.7979674426804,-0.220178340780001,
3.62648392906691));
#58566=CARTESIAN_POINT('Ctrl Pts',(21.8218253607118,-0.0142906046679706,
3.56665425395863));
#58567=CARTESIAN_POINT('Ctrl Pts',(21.8456832787432,0.195091573553633,3.61278941785858));
#58568=CARTESIAN_POINT('Ctrl Pts',(21.8695411967747,0.356768547853618,3.75360811649661));
#58569=CARTESIAN_POINT('Ctrl Pts',(21.8933991148061,0.431205894023261,3.95467634223136));
#58570=CARTESIAN_POINT('Ctrl Pts',(21.9172570328375,0.400201653291494,4.16682743688221));
#58571=CARTESIAN_POINT('Ctrl Pts',(21.941114950869,0.271337207055788,4.33818467892719));
#58572=CARTESIAN_POINT('Ctrl Pts',(21.9649728689003,0.0761234226178432,
4.4268465550088));
#58573=CARTESIAN_POINT('Ctrl Pts',(21.9888307869318,-0.137704612210607,
4.41113282132402));
#58574=CARTESIAN_POINT('Ctrl Pts',(22.0126887049632,-0.317860118355158,
4.29488591379237));
#58575=CARTESIAN_POINT('Ctrl Pts',(22.0365466229946,-0.420290167226249,
4.10653136780738));
#58576=CARTESIAN_POINT('Ctrl Pts',(22.060404541026,-0.419947821735935,3.89212700053744));
#58577=CARTESIAN_POINT('Ctrl Pts',(22.0842624590574,-0.316916794682727,
3.70410052003731));
#58578=CARTESIAN_POINT('Ctrl Pts',(22.1081203770888,-0.136390978688423,
3.58842952252864));
#58579=CARTESIAN_POINT('Ctrl Pts',(22.1319782951203,0.0774861468089536,
3.57339871771534));
#58580=CARTESIAN_POINT('Ctrl Pts',(22.1558362131517,0.27241579873489,3.66268354680831));
#58581=CARTESIAN_POINT('Ctrl Pts',(22.1796941311831,0.400732367405962,3.83445143701846));
#58582=CARTESIAN_POINT('Ctrl Pts',(22.2035520492145,0.431058956528623,4.04670046033727));
#58583=CARTESIAN_POINT('Ctrl Pts',(22.227409967246,0.355979888945518,4.24752994899471));
#58584=CARTESIAN_POINT('Ctrl Pts',(22.2512678852773,0.193854041863619,4.38783162256878));
#58585=CARTESIAN_POINT('Ctrl Pts',(22.2751258033088,-0.0156743990186396,
4.43329790005389));
#58586=CARTESIAN_POINT('Ctrl Pts',(22.2989837213402,-0.221370022215225,
4.37281103827166));
#58587=CARTESIAN_POINT('Ctrl Pts',(22.3228416393716,-0.372934645290675,
4.22116172228637));
#58588=CARTESIAN_POINT('Ctrl Pts',(22.346699557403,-0.43330658847365,4.01543234121164));
#58589=CARTESIAN_POINT('Ctrl Pts',(22.3705574754345,-0.387723268841402,
3.80592933171158));
#58590=CARTESIAN_POINT('Ctrl Pts',(22.3944153934659,-0.247331046528593,
3.64388188817752));
#58591=CARTESIAN_POINT('Ctrl Pts',(22.4182733114973,-0.0464596501027702,
3.56891502119853));
#58592=CARTESIAN_POINT('Ctrl Pts',(22.4421312295287,0.165772403721094,3.59936017830047));
#58593=CARTESIAN_POINT('Ctrl Pts',(22.4659891475602,0.337468575289321,3.7277726770023));
#58594=CARTESIAN_POINT('Ctrl Pts',(22.4898470655915,0.426644514167594,3.92275218663495));
#58595=CARTESIAN_POINT('Ctrl Pts',(22.513704983623,0.411494197867752,4.13662086224655));
#58596=CARTESIAN_POINT('Ctrl Pts',(22.5375629016544,0.295722435535401,4.31708206952049));
#58597=CARTESIAN_POINT('Ctrl Pts',(22.5614208196858,0.107638304484935,4.42000797176855));
#58598=CARTESIAN_POINT('Ctrl Pts',(22.5852787377172,-0.106765988085903,
4.42023067651324));
#58599=CARTESIAN_POINT('Ctrl Pts',(22.6091366557487,-0.295063722636797,
4.31769517074077));
#58600=CARTESIAN_POINT('Ctrl Pts',(22.6329945737801,-0.411209141905604,
4.13747522778479));
#58601=CARTESIAN_POINT('Ctrl Pts',(22.6568524918115,-0.426804986482714,
3.92363755172126));
#58602=CARTESIAN_POINT('Ctrl Pts',(22.6807104098429,-0.33803111495158,3.72847502015617));
#58603=CARTESIAN_POINT('Ctrl Pts',(22.7045683278743,-0.16660749730952,3.59970312177549));
#58604=CARTESIAN_POINT('Ctrl Pts',(22.7284262459057,0.0455714674079685,
3.56882345794434));
#58605=CARTESIAN_POINT('Ctrl Pts',(22.7522841639372,0.246577802732478,3.64336153500176));
#58606=CARTESIAN_POINT('Ctrl Pts',(22.7761420819686,0.387346815298129,3.80514019809748));
#58607=CARTESIAN_POINT('Ctrl Pts',(22.7920473606562,0.417963038852713,3.94471011778788));
#58608=CARTESIAN_POINT('Ctrl Pts',(22.8,0.415641328671541,4.01393920819689));
#58609=CARTESIAN_POINT('Ctrl Pts',(3.96816317011929,0.203757107801821,4.42939176513376));
#58610=CARTESIAN_POINT('Ctrl Pts',(3.9761158094631,0.132237748973037,4.46332948562603));
#58611=CARTESIAN_POINT('Ctrl Pts',(3.99202108815071,-0.0280119004087947,
4.49474661085258));
#58612=CARTESIAN_POINT('Ctrl Pts',(4.01587900618213,-0.261670681609628,
4.42079217330492));
#58613=CARTESIAN_POINT('Ctrl Pts',(4.03973692421355,-0.431283260509235,
4.24398813071681));
#58614=CARTESIAN_POINT('Ctrl Pts',(4.06359484224497,-0.495466080430727,
4.00749935521381));
#58615=CARTESIAN_POINT('Ctrl Pts',(4.08745276027639,-0.438477829352452,
3.76918881818141));
#58616=CARTESIAN_POINT('Ctrl Pts',(4.11131067830781,-0.274278321106756,
3.5873115455631));
#58617=CARTESIAN_POINT('Ctrl Pts',(4.13516859633923,-0.0430057845205295,
3.50635120590702));
#58618=CARTESIAN_POINT('Ctrl Pts',(4.15902651437064,0.198780450874126,3.54609966156282));
#58619=CARTESIAN_POINT('Ctrl Pts',(4.18288443240206,0.391960715466274,3.69684005745713));
#58620=CARTESIAN_POINT('Ctrl Pts',(4.20674235043348,0.489295238859844,3.92171081754005));
#58621=CARTESIAN_POINT('Ctrl Pts',(4.2306002684649,0.466984102771714,4.16572567991789));
#58622=CARTESIAN_POINT('Ctrl Pts',(4.25445818649632,0.330482445391075,4.36921595913043));
#58623=CARTESIAN_POINT('Ctrl Pts',(4.27831610452774,0.113168927396708,4.48242295331799));
#58624=CARTESIAN_POINT('Ctrl Pts',(4.30217402255916,-0.131817528672551,
4.47766435517297));
#58625=CARTESIAN_POINT('Ctrl Pts',(4.32603194059057,-0.344570980451485,
4.35610383169054));
#58626=CARTESIAN_POINT('Ctrl Pts',(4.349889858622,-0.473067456356951,4.14746621026076));
#58627=CARTESIAN_POINT('Ctrl Pts',(4.37374777665341,-0.485886045261059,
3.9027690893624));
#58628=CARTESIAN_POINT('Ctrl Pts',(4.39760569468484,-0.379892264971952,
3.68184757153936));
#58629=CARTESIAN_POINT('Ctrl Pts',(4.42146361271625,-0.181004475645389,
3.53872299041084));
#58630=CARTESIAN_POINT('Ctrl Pts',(4.44532153074767,0.0621438372772935,
3.50839320219298));
#58631=CARTESIAN_POINT('Ctrl Pts',(4.46917944877909,0.290096289836991,3.5982746675986));
#58632=CARTESIAN_POINT('Ctrl Pts',(4.49303736681051,0.447112297141319,3.78638891931142));
#58633=CARTESIAN_POINT('Ctrl Pts',(4.51689528484194,0.494797168872773,4.02673689903048));
#58634=CARTESIAN_POINT('Ctrl Pts',(4.54075320287334,0.421490654719143,4.26054697856981));
#58635=CARTESIAN_POINT('Ctrl Pts',(4.56461112090478,0.245118194360182,4.43064622472778));
#58636=CARTESIAN_POINT('Ctrl Pts',(4.58846903893618,0.00880765856895839,
4.49544073835303));
#58637=CARTESIAN_POINT('Ctrl Pts',(4.61232695696761,-0.229656589644598,
4.43908649592634));
#58638=CARTESIAN_POINT('Ctrl Pts',(4.63618487499902,-0.411963545977342,
4.2753636447643));
#58639=CARTESIAN_POINT('Ctrl Pts',(4.66004279303045,-0.493534193653132,
4.04430688170513));
#58640=CARTESIAN_POINT('Ctrl Pts',(4.68390071106186,-0.454422287381232,
3.80241587917234));
#58641=CARTESIAN_POINT('Ctrl Pts',(4.70775862909328,-0.304191753628974,
3.60883957626609));
#58642=CARTESIAN_POINT('Ctrl Pts',(4.7316165471247,-0.0795780500979935,
3.51091265195837));
#58643=CARTESIAN_POINT('Ctrl Pts',(4.75547446515612,0.164494654344808,3.53258090671894));
#58644=CARTESIAN_POINT('Ctrl Pts',(4.77933238318754,0.368343935055725,3.66854586202706));
#58645=CARTESIAN_POINT('Ctrl Pts',(4.80319030121895,0.482123090158262,3.88556038269908));
#58646=CARTESIAN_POINT('Ctrl Pts',(4.82704821925038,0.478010016947761,4.13055850707372));
#58647=CARTESIAN_POINT('Ctrl Pts',(4.85090613728179,0.357010473862124,4.34363152012653));
#58648=CARTESIAN_POINT('Ctrl Pts',(4.87476405531322,0.14871214514713,4.47267726617372));
#58649=CARTESIAN_POINT('Ctrl Pts',(4.89862197334463,-0.0959503538938319,
4.48614054517122));
#58650=CARTESIAN_POINT('Ctrl Pts',(4.92247989137606,-0.317150377772593,
4.38072921867179));
#58651=CARTESIAN_POINT('Ctrl Pts',(4.94633780940747,-0.460798495283114,
4.1822192273514));
#58652=CARTESIAN_POINT('Ctrl Pts',(4.97019572743889,-0.49176882879792,3.93915167139151));
#58653=CARTESIAN_POINT('Ctrl Pts',(4.99405364547031,-0.40248828815769,3.71096318925158));
#58654=CARTESIAN_POINT('Ctrl Pts',(5.01791156350173,-0.214788397502062,
3.55345208054429));
#58655=CARTESIAN_POINT('Ctrl Pts',(5.04176948153314,0.0254331070612992,
3.50513410186502));
#58656=CARTESIAN_POINT('Ctrl Pts',(5.06562739956457,0.259435524164246,3.57782431515618));
#58657=CARTESIAN_POINT('Ctrl Pts',(5.08948531759598,0.429998888727244,3.75374798322641));
#58658=CARTESIAN_POINT('Ctrl Pts',(5.11334323562741,0.495415812061873,3.98988697716804));
#58659=CARTESIAN_POINT('Ctrl Pts',(5.13720115365882,0.439690074491602,4.2284988806653));
#58660=CARTESIAN_POINT('Ctrl Pts',(5.16105907169025,0.276448136790977,4.41123658365534));
#58661=CARTESIAN_POINT('Ctrl Pts',(5.18491698972166,0.0456070993489057,
4.49341574008204));
#58662=CARTESIAN_POINT('Ctrl Pts',(5.20877490775308,-0.196386116196418,
4.45494130768376));
#58663=CARTESIAN_POINT('Ctrl Pts',(5.2326328257845,-0.390357576881318,4.3052213332044));
#58664=CARTESIAN_POINT('Ctrl Pts',(5.25649074381592,-0.488875976891831,
4.08086642869437));
#58665=CARTESIAN_POINT('Ctrl Pts',(5.28034866184734,-0.467850883838054,
3.83673747961128));
#58666=CARTESIAN_POINT('Ctrl Pts',(5.30420657987876,-0.332423505683668,
3.632530663945));
#58667=CARTESIAN_POINT('Ctrl Pts',(5.32806449791017,-0.115709525355139,
3.5181801106079));
#58668=CARTESIAN_POINT('Ctrl Pts',(5.3519224159416,0.129298585786916,3.52164764473745));
#58669=CARTESIAN_POINT('Ctrl Pts',(5.37578033397301,0.342689670681295,3.64208535978523));
#58670=CARTESIAN_POINT('Ctrl Pts',(5.39963825200445,0.472283796414913,3.85004295376459));
#58671=CARTESIAN_POINT('Ctrl Pts',(5.42349617003584,0.48639166917272,4.09466913029638));
#58672=CARTESIAN_POINT('Ctrl Pts',(5.44735408806728,0.381563529774833,4.31614612573549));
#58673=CARTESIAN_POINT('Ctrl Pts',(5.47121200609869,0.183432713764955,4.46031678178449));
#58674=CARTESIAN_POINT('Ctrl Pts',(5.49506992413012,-0.059552397366927,
4.49192744591021));
#58675=CARTESIAN_POINT('Ctrl Pts',(5.51892784216153,-0.287975325168481,
4.40324844967551));
#58676=CARTESIAN_POINT('Ctrl Pts',(5.54278576019295,-0.445980441674811,
4.21596422322942));
#58677=CARTESIAN_POINT('Ctrl Pts',(5.56664367822437,-0.494931191930538,
3.97587086145358));
#58678=CARTESIAN_POINT('Ctrl Pts',(5.59050159625579,-0.422857784100094,
3.74167773132221));
#58679=CARTESIAN_POINT('Ctrl Pts',(5.61435951428721,-0.247384129650275,
3.57065143242979));
#58680=CARTESIAN_POINT('Ctrl Pts',(5.63821743231862,-0.0114183168777074,
3.50461255354752));
#58681=CARTESIAN_POINT('Ctrl Pts',(5.66207535035005,0.227339585372105,3.55970939936999));
#58682=CARTESIAN_POINT('Ctrl Pts',(5.68593326838146,0.410506766445453,3.72246929038963));
#58683=CARTESIAN_POINT('Ctrl Pts',(5.70979118641288,0.493293861043031,3.9530929995654));
#58684=CARTESIAN_POINT('Ctrl Pts',(5.73364910444431,0.455457169749513,4.19518674831082));
#58685=CARTESIAN_POINT('Ctrl Pts',(5.75750702247572,0.306248793691327,4.38955201985635));
#58686=CARTESIAN_POINT('Ctrl Pts',(5.78136494050715,0.0821542461994931,
4.48866121222712));
#58687=CARTESIAN_POINT('Ctrl Pts',(5.80522285853855,-0.162029253596618,
4.46827942571263));
#58688=CARTESIAN_POINT('Ctrl Pts',(5.82908077656998,-0.366592184898752,
4.33339056701663));
#58689=CARTESIAN_POINT('Ctrl Pts',(5.85293869460139,-0.481513345756758,
4.11697862749145));
#58690=CARTESIAN_POINT('Ctrl Pts',(5.87679661263282,-0.478691368855474,
3.87196223809426));
#58691=CARTESIAN_POINT('Ctrl Pts',(5.90065453066423,-0.358816329143926,
3.65825454842257));
#58692=CARTESIAN_POINT('Ctrl Pts',(5.92451244869565,-0.151200892471453,
3.52811296978032));
#58693=CARTESIAN_POINT('Ctrl Pts',(5.94837036672708,0.093387223403125,3.5133605500302));
#58694=CARTESIAN_POINT('Ctrl Pts',(5.97222828475848,0.315139728168714,3.61760487120619));
#58695=CARTESIAN_POINT('Ctrl Pts',(5.99608620278992,0.459831779670103,3.81535495398299));
#58696=CARTESIAN_POINT('Ctrl Pts',(6.01994412082132,0.492082823488737,4.05825627791571));
#58697=CARTESIAN_POINT('Ctrl Pts',(6.04380203885276,0.404005480250355,4.28691141512903));
#58698=CARTESIAN_POINT('Ctrl Pts',(6.06765995688416,0.21713917558903,4.44541067075535));
#58699=CARTESIAN_POINT('Ctrl Pts',(6.09151787491559,-0.0228261843714051,
4.49499153360272));
#58700=CARTESIAN_POINT('Ctrl Pts',(6.11537579294701,-0.257204988275768,
4.42353981062321));
#58701=CARTESIAN_POINT('Ctrl Pts',(6.13923371097843,-0.428699479426561,
4.24850911946619));
#58702=CARTESIAN_POINT('Ctrl Pts',(6.16309162900984,-0.49534768549136,4.01273373861842));
#58703=CARTESIAN_POINT('Ctrl Pts',(6.18694954704127,-0.440903093044182,
3.77380201544612));
#58704=CARTESIAN_POINT('Ctrl Pts',(6.21080746507268,-0.278582990390117,
3.59026229064107));
#58705=CARTESIAN_POINT('Ctrl Pts',(6.23466538310411,-0.048260127889517,
3.50676273730504));
#58706=CARTESIAN_POINT('Ctrl Pts',(6.25852330113552,0.194087080856728,3.5441598063702));
#58707=CARTESIAN_POINT('Ctrl Pts',(6.28238121916694,0.388553448942855,3.69248145192407));
#58708=CARTESIAN_POINT('Ctrl Pts',(6.30623913719837,0.488798280742691,3.9170164641697));
#58709=CARTESIAN_POINT('Ctrl Pts',(6.33009705522977,0.468067515948433,4.15995908608738));
#58710=CARTESIAN_POINT('Ctrl Pts',(6.36190761260502,0.291040001689194,4.43610431491443));
#58711=CARTESIAN_POINT('Ctrl Pts',(6.40167080932402,-0.143168317426403,
4.54352222151223));
#58712=CARTESIAN_POINT('Ctrl Pts',(6.44938664538688,-0.535165231989368,
4.17285582464912));
#58713=CARTESIAN_POINT('Ctrl Pts',(6.49710248144971,-0.434543251113388,
3.64369891234367));
#58714=CARTESIAN_POINT('Ctrl Pts',(6.54481831751255,0.0645215567551043,
3.4416075490323));
#58715=CARTESIAN_POINT('Ctrl Pts',(6.59253415357539,0.504653900644641,3.75236619672659));
#58716=CARTESIAN_POINT('Ctrl Pts',(6.64024998963822,0.481186238846835,4.29049388273239));
#58717=CARTESIAN_POINT('Ctrl Pts',(6.68796582570107,0.01592709648968,4.56187610740764));
#58718=CARTESIAN_POINT('Ctrl Pts',(6.7356816617639,-0.464005405879062,4.31726850783359));
#58719=CARTESIAN_POINT('Ctrl Pts',(6.78339749782674,-0.517809574500644,
3.78131383674221));
#58720=CARTESIAN_POINT('Ctrl Pts',(6.83111333388957,-0.0961144992151805,
3.44617913151078));
#58721=CARTESIAN_POINT('Ctrl Pts',(6.87882916995242,0.413851019972934,3.61962818876606));
#58722=CARTESIAN_POINT('Ctrl Pts',(6.92654500601525,0.543767061592725,4.14237771887731));
#58723=CARTESIAN_POINT('Ctrl Pts',(6.97426084207809,0.174335412693353,4.53438003016987));
#58724=CARTESIAN_POINT('Ctrl Pts',(7.02197667814094,-0.355192171006393,
4.43565270890428));
#58725=CARTESIAN_POINT('Ctrl Pts',(7.06969251420376,-0.558540766450571,
3.93685892261342));
#58726=CARTESIAN_POINT('Ctrl Pts',(7.11740835026661,-0.248973074301851,
3.49604849518665));
#58727=CARTESIAN_POINT('Ctrl Pts',(7.16512418632944,0.289230577826905,3.51802452284194));
#58728=CARTESIAN_POINT('Ctrl Pts',(7.21284002239229,0.561829257914175,3.98260602935256));
#58729=CARTESIAN_POINT('Ctrl Pts',(7.26055585845511,0.318491529052478,4.46316069626365));
#58730=CARTESIAN_POINT('Ctrl Pts',(7.30827169451797,-0.217321894570402,
4.51838776411367));
#58731=CARTESIAN_POINT('Ctrl Pts',(7.35598753058078,-0.553565266295818,
4.09757137442565));
#58732=CARTESIAN_POINT('Ctrl Pts',(7.40370336664365,-0.381461142739227,
3.58715368886071));
#58733=CARTESIAN_POINT('Ctrl Pts',(7.45141920270646,0.140944621146953,3.45585912402047));
#58734=CARTESIAN_POINT('Ctrl Pts',(7.49913503876933,0.533918768911932,3.82425749787944));
#58735=CARTESIAN_POINT('Ctrl Pts',(7.54685087483214,0.436587096747522,4.3540429157916));
#58736=CARTESIAN_POINT('Ctrl Pts',(7.594566710895,-0.0616692246238245,4.5587052763707));
#58737=CARTESIAN_POINT('Ctrl Pts',(7.64228254695782,-0.503293747851232,
4.25029998493175));
#58738=CARTESIAN_POINT('Ctrl Pts',(7.68999838302067,-0.482735878399531,
3.7120403659385));
#58739=CARTESIAN_POINT('Ctrl Pts',(7.7377142190835,-0.0188742238918736,
3.43821850974892));
#58740=CARTESIAN_POINT('Ctrl Pts',(7.78543005514633,0.462319920793015,3.6802892401675));
#58741=CARTESIAN_POINT('Ctrl Pts',(7.83314589120918,0.518958568528469,4.21595528072725));
#58742=CARTESIAN_POINT('Ctrl Pts',(7.88086172727202,0.099029577569048,4.55330626409362));
#58743=CARTESIAN_POINT('Ctrl Pts',(7.92857756333485,-0.411839798232008,
4.38254759143289));
#58744=CARTESIAN_POINT('Ctrl Pts',(7.9762933993977,-0.544510350349916,3.86048957930736));
#58745=CARTESIAN_POINT('Ctrl Pts',(8.02400923546053,-0.177148669371157,
3.466546133148));
#58746=CARTESIAN_POINT('Ctrl Pts',(8.07172507152338,0.352891360472903,3.56248158116143));
#58747=CARTESIAN_POINT('Ctrl Pts',(8.1194409075862,0.558865824063627,4.06019692528064));
#58748=CARTESIAN_POINT('Ctrl Pts',(8.16715674364906,0.251625202160443,4.50263250666582));
#58749=CARTESIAN_POINT('Ctrl Pts',(8.21487257971187,-0.286686714637947,
4.48349292318459));
#58750=CARTESIAN_POINT('Ctrl Pts',(8.26258841577472,-0.561729810142263,
4.02035434884804));
#58751=CARTESIAN_POINT('Ctrl Pts',(8.31030425183756,-0.32092777766878,3.53852406277244));
#58752=CARTESIAN_POINT('Ctrl Pts',(8.3580200879004,0.21458717114652,3.4804742305729));
#58753=CARTESIAN_POINT('Ctrl Pts',(8.40573592396324,0.553043418849938,3.89951290636976));
#58754=CARTESIAN_POINT('Ctrl Pts',(8.45345176002607,0.383631385356639,4.41083042643994));
#58755=CARTESIAN_POINT('Ctrl Pts',(8.50116759608892,-0.13807525223727,4.54487604447167));
#58756=CARTESIAN_POINT('Ctrl Pts',(8.54888343215175,-0.532985261140852,
4.17855360686946));
#58757=CARTESIAN_POINT('Ctrl Pts',(8.59659926821459,-0.43844670370641,3.64826264467864));
#58758=CARTESIAN_POINT('Ctrl Pts',(8.64431510427743,0.0587242081113278,
3.4409775080543));
#58759=CARTESIAN_POINT('Ctrl Pts',(8.69203094034026,0.501967776032349,3.74705132745037));
#58760=CARTESIAN_POINT('Ctrl Pts',(8.73974677640311,0.484246611455832,4.28541180496438));
#58761=CARTESIAN_POINT('Ctrl Pts',(8.78746261246592,0.021834332487559,4.56167423035448));
#58762=CARTESIAN_POINT('Ctrl Pts',(8.83517844852879,-0.460628749968427,
4.32214256754115));
#58763=CARTESIAN_POINT('Ctrl Pts',(8.88289428459161,-0.520089363644054,
3.78678242815423));
#58764=CARTESIAN_POINT('Ctrl Pts',(8.93061012065447,-0.101943912081849,
3.44722326576734));
#58765=CARTESIAN_POINT('Ctrl Pts',(8.97832595671729,0.409818202553832,3.61528748398963));
#58766=CARTESIAN_POINT('Ctrl Pts',(9.02604179278014,0.545237955920739,4.1366391252272));
#58767=CARTESIAN_POINT('Ctrl Pts',(9.07375762884296,0.179957304801303,4.53251295530543));
#58768=CARTESIAN_POINT('Ctrl Pts',(9.12147346490582,-0.350580908316224,
4.43937194476168));
#58769=CARTESIAN_POINT('Ctrl Pts',(9.16918930096864,-0.559175278946307,
3.94274891673689));
#58770=CARTESIAN_POINT('Ctrl Pts',(9.21690513703149,-0.254270386902387,
3.49870043939378));
#58771=CARTESIAN_POINT('Ctrl Pts',(9.26462097309432,0.284134913886797,3.51500306204057));
#58772=CARTESIAN_POINT('Ctrl Pts',(9.31233680915716,0.56161475127612,3.97668583545263));
#58773=CARTESIAN_POINT('Ctrl Pts',(9.36005264522,0.323355121014866,4.45977836490307));
#58774=CARTESIAN_POINT('Ctrl Pts',(9.40776848128284,-0.211846492332409,
4.52064934726353));
#58775=CARTESIAN_POINT('Ctrl Pts',(9.45548431734568,-0.552506212093558,
4.10340002281193));
#58776=CARTESIAN_POINT('Ctrl Pts',(9.50320015340851,-0.385790975888367,
3.59119686639829));
#58777=CARTESIAN_POINT('Ctrl Pts',(9.55091598947136,0.135202049632292,3.45440391781584));
#58778=CARTESIAN_POINT('Ctrl Pts',(9.59863182553417,0.532036952624682,3.81864024657791));
#58779=CARTESIAN_POINT('Ctrl Pts',(9.64634766159704,0.440294135581046,4.34942202748599));
#58780=CARTESIAN_POINT('Ctrl Pts',(9.69406349765985,-0.0557775609627595,
4.55932418400469));
#58781=CARTESIAN_POINT('Ctrl Pts',(9.74177933372271,-0.500627865026369,
4.25559033604309));
#58782=CARTESIAN_POINT('Ctrl Pts',(9.78949516978553,-0.485743897486414,
3.71714394973028));
#58783=CARTESIAN_POINT('Ctrl Pts',(9.83721100584839,-0.0247938347541151,
3.43844862667992));
#58784=CARTESIAN_POINT('Ctrl Pts',(9.88492684191122,0.458924787935076,3.67543457032792));
#58785=CARTESIAN_POINT('Ctrl Pts',(9.93264267797406,0.521205716397956,4.21047394212484));
#58786=CARTESIAN_POINT('Ctrl Pts',(9.98035851403688,0.104855415711801,4.55223185431066));
#58787=CARTESIAN_POINT('Ctrl Pts',(10.0280743500997,-0.407785226630454,
4.3868667575037));
#58788=CARTESIAN_POINT('Ctrl Pts',(10.0757901861625,-0.54595042077573,3.86623596457089));
#58789=CARTESIAN_POINT('Ctrl Pts',(10.1235060222254,-0.182760942995651,
3.46844274359687));
#58790=CARTESIAN_POINT('Ctrl Pts',(10.1712218582882,0.34826072087591,3.55878673023755));
#58791=CARTESIAN_POINT('Ctrl Pts',(10.2189376943511,0.559469206087141,4.05430365143988));
#58792=CARTESIAN_POINT('Ctrl Pts',(10.2666535304139,0.256908510808291,4.49995269395588));
#58793=CARTESIAN_POINT('Ctrl Pts',(10.3143693664768,-0.281575222991369,
4.4864874848512));
#58794=CARTESIAN_POINT('Ctrl Pts',(10.3620852025396,-0.561484096926345,
4.02627333283551));
#58795=CARTESIAN_POINT('Ctrl Pts',(10.4098010386024,-0.325773485110519,
3.5419319750098));
#58796=CARTESIAN_POINT('Ctrl Pts',(10.4575168746653,0.209099930751681,3.47824153281512));
#58797=CARTESIAN_POINT('Ctrl Pts',(10.5052327107281,0.55195366278862,3.89368991932227));
#58798=CARTESIAN_POINT('Ctrl Pts',(10.552948546791,0.387939853388008,4.40676448870664));
#58799=CARTESIAN_POINT('Ctrl Pts',(10.6006643828538,-0.13232509260073,4.54630096923553));
#58800=CARTESIAN_POINT('Ctrl Pts',(10.6483802189166,-0.531073869970951,
4.18416086379456));
#58801=CARTESIAN_POINT('Ctrl Pts',(10.6960960549795,-0.442129340924997,
3.6529030034519));
#58802=CARTESIAN_POINT('Ctrl Pts',(10.7438118910423,0.0528293649267388,
3.44038965581316));
#58803=CARTESIAN_POINT('Ctrl Pts',(10.7915277271051,0.499274052081986,3.74177509795313));
#58804=CARTESIAN_POINT('Ctrl Pts',(10.839243563168,0.487227694891584,4.28029244094358));
#58805=CARTESIAN_POINT('Ctrl Pts',(10.8869593992308,0.0277526485205102,
4.56141292256198));
#58806=CARTESIAN_POINT('Ctrl Pts',(10.9346752352937,-0.457208082016334,
4.32697927894352));
#58807=CARTESIAN_POINT('Ctrl Pts',(10.9823910713565,-0.522307595786967,
3.79227553224832));
#58808=CARTESIAN_POINT('Ctrl Pts',(11.0301069074193,-0.107764007611043,
3.44832836054127));
#58809=CARTESIAN_POINT('Ctrl Pts',(11.0778227434822,0.405740926916492,3.61098974390844));
#58810=CARTESIAN_POINT('Ctrl Pts',(11.125538579545,0.54664772512998,4.13088523113667));
#58811=CARTESIAN_POINT('Ctrl Pts',(11.1732544156078,0.185559506100192,4.53058679668394));
#58812=CARTESIAN_POINT('Ctrl Pts',(11.2209702516707,-0.345930862581405,
4.4430423427091));
#58813=CARTESIAN_POINT('Ctrl Pts',(11.2686860877335,-0.559747597323992,
3.94864528834179));
#58814=CARTESIAN_POINT('Ctrl Pts',(11.3164019237964,-0.259539500620097,
3.50140805588402));
#58815=CARTESIAN_POINT('Ctrl Pts',(11.3641177598592,0.279007713031768,3.51203547753114));
#58816=CARTESIAN_POINT('Ctrl Pts',(11.411833595922,0.561337850721073,3.97076822846069));
#58817=CARTESIAN_POINT('Ctrl Pts',(11.4595494319849,0.328182802800164,4.45634496498341));
#58818=CARTESIAN_POINT('Ctrl Pts',(11.5072652680477,-0.206347562673641,
4.52285309839201));
#58819=CARTESIAN_POINT('Ctrl Pts',(11.5549811041106,-0.551385786278872,
4.10921718641821));
#58820=CARTESIAN_POINT('Ctrl Pts',(11.6026969401734,-0.390077958183356,
3.59528545163414));
#58821=CARTESIAN_POINT('Ctrl Pts',(11.6504127762362,0.129444461032819,3.45300931394821));
#58822=CARTESIAN_POINT('Ctrl Pts',(11.6981286122991,0.530096039923511,3.8130431397972));
#58823=CARTESIAN_POINT('Ctrl Pts',(11.7458444483619,0.443952268776438,4.34476232707146));
#58824=CARTESIAN_POINT('Ctrl Pts',(11.7935602844247,-0.0498797018717475,
4.55988096454574));
#58825=CARTESIAN_POINT('Ctrl Pts',(11.8412761204876,-0.497906374793238,
4.26085229740167));
#58826=CARTESIAN_POINT('Ctrl Pts',(11.8889919565504,-0.48869796246776,3.72227895182515));
#58827=CARTESIAN_POINT('Ctrl Pts',(11.9367077926133,-0.0307106916234339,
3.43874111807518));
#58828=CARTESIAN_POINT('Ctrl Pts',(11.9844236286761,0.455478679883424,3.67061595167475));
#58829=CARTESIAN_POINT('Ctrl Pts',(12.0321394647389,0.523394971212992,4.20496922507643));
#58830=CARTESIAN_POINT('Ctrl Pts',(12.0798553008018,0.110669607010866,4.5510961052335));
#58831=CARTESIAN_POINT('Ctrl Pts',(12.1275711368646,-0.403685360180124,
4.39114295225112));
#58832=CARTESIAN_POINT('Ctrl Pts',(12.1752869729274,-0.547329849620031,
3.8719972077086));
#58833=CARTESIAN_POINT('Ctrl Pts',(12.2230028089903,-0.188352916401613,
3.4703983969034));
#58834=CARTESIAN_POINT('Ctrl Pts',(12.2707186450531,0.34359139813055,3.55514088718992));
#58835=CARTESIAN_POINT('Ctrl Pts',(12.318434481116,0.560010444926212,4.04840434580723));
#58836=CARTESIAN_POINT('Ctrl Pts',(12.3661503171788,0.262163283277844,4.49721734887317));
#58837=CARTESIAN_POINT('Ctrl Pts',(12.4138661532417,-0.276432455305192,
4.48942800979656));
#58838=CARTESIAN_POINT('Ctrl Pts',(12.4615819893045,-0.561176016721412,
4.03218939850585));
#58839=CARTESIAN_POINT('Ctrl Pts',(12.5092978253673,-0.330583007179444,
3.54539076726965));
#58840=CARTESIAN_POINT('Ctrl Pts',(12.5570136614301,0.203589464528802,3.47606678951191));
#58841=CARTESIAN_POINT('Ctrl Pts',(12.604729497493,0.550802598333678,3.88787874069406));
#58842=CARTESIAN_POINT('Ctrl Pts',(12.6524453335558,0.392205230901379,4.40265336950419));
#58843=CARTESIAN_POINT('Ctrl Pts',(12.7001611696187,-0.126560234920843,
4.54766521348015));
#58844=CARTESIAN_POINT('Ctrl Pts',(12.7478770056815,-0.529103489635726,
4.18974766500481));
#58845=CARTESIAN_POINT('Ctrl Pts',(12.7955928417443,-0.44576286851447,3.65758191611243));
#58846=CARTESIAN_POINT('Ctrl Pts',(12.8433086778072,0.0469286537069902,
3.43986396243348));
#58847=CARTESIAN_POINT('Ctrl Pts',(12.89102451387,0.496524871139168,3.73652755085263));
#58848=CARTESIAN_POINT('Ctrl Pts',(12.9387403499328,0.490154659387074,4.27514194336855));
#58849=CARTESIAN_POINT('Ctrl Pts',(12.9864561859957,0.0336678819209607,
4.56108925568614));
#58850=CARTESIAN_POINT('Ctrl Pts',(13.0341720220585,-0.45373662956012,4.33177967103923));
#58851=CARTESIAN_POINT('Ctrl Pts',(13.0818878581214,-0.524467812480695,
3.79779170939055));
#58852=CARTESIAN_POINT('Ctrl Pts',(13.1296036941842,-0.113572133225654,
3.44949473238301));
#58853=CARTESIAN_POINT('Ctrl Pts',(13.177319530247,0.401618583502394,3.60673521324049));
#58854=CARTESIAN_POINT('Ctrl Pts',(13.2250353663099,0.547996775303968,4.12511679893576));
#58855=CARTESIAN_POINT('Ctrl Pts',(13.2727512023727,0.191141096329688,4.52860170299893));
#58856=CARTESIAN_POINT('Ctrl Pts',(13.3204670384356,-0.341242392487953,
4.4466635296155));
#58857=CARTESIAN_POINT('Ctrl Pts',(13.3681828744984,-0.560257741594785,
3.95454736418435));
#58858=CARTESIAN_POINT('Ctrl Pts',(13.4158987105612,-0.264779785921688,
3.5041710536014));
#58859=CARTESIAN_POINT('Ctrl Pts',(13.4636145466241,0.273849521323983,3.50912209380529));
#58860=CARTESIAN_POINT('Ctrl Pts',(13.5113303826869,0.560998599421335,3.96485386839523));
#58861=CARTESIAN_POINT('Ctrl Pts',(13.5590462187498,0.332974031597074,4.45286087643057));
#58862=CARTESIAN_POINT('Ctrl Pts',(13.6067620548126,-0.200825712906817,
4.52499877347948));
#58863=CARTESIAN_POINT('Ctrl Pts',(13.6544778908754,-0.550204115147588,
4.11502221869768));
#58864=CARTESIAN_POINT('Ctrl Pts',(13.7021937269383,-0.394321612469819,
3.5994189906415));
#58865=CARTESIAN_POINT('Ctrl Pts',(13.7499095630011,0.123672494356884,3.45167546721031));
#58866=CARTESIAN_POINT('Ctrl Pts',(13.7976253990639,0.528096246669736,3.80746679929733));
#58867=CARTESIAN_POINT('Ctrl Pts',(13.8453412351268,0.44756108986054,4.34006433209368));
#58868=CARTESIAN_POINT('Ctrl Pts',(13.8930570711896,-0.0439763023801491,
4.56037555616609));
#58869=CARTESIAN_POINT('Ctrl Pts',(13.9407729072525,-0.495129579482757,
4.26608528452492));
#58870=CARTESIAN_POINT('Ctrl Pts',(13.9884887433153,-0.491597745198497,
3.72744480185615));
#58871=CARTESIAN_POINT('Ctrl Pts',(14.0362045793781,-0.0366241372948624,
3.43909595144367));
#58872=CARTESIAN_POINT('Ctrl Pts',(14.083920415441,0.451981979421435,3.66583391943861));
#58873=CARTESIAN_POINT('Ctrl Pts',(14.1316362515038,0.525526089798339,4.19944174101915));
#58874=CARTESIAN_POINT('Ctrl Pts',(14.1793520875667,0.11647150565515,4.54989914301615));
#58875=CARTESIAN_POINT('Ctrl Pts',(14.2270679236295,-0.399540654275635,
4.39537570069553));
#58876=CARTESIAN_POINT('Ctrl Pts',(14.2747837596924,-0.548648483661927,
3.87777266878906));
#58877=CARTESIAN_POINT('Ctrl Pts',(14.3224995957551,-0.193923968459428,
3.47241287584284));
#58878=CARTESIAN_POINT('Ctrl Pts',(14.370215431818,0.338883910883161,3.5515444569815));
#58879=CARTESIAN_POINT('Ctrl Pts',(14.4179312678808,0.560489480462528,4.04249966364955));
#58880=CARTESIAN_POINT('Ctrl Pts',(14.4656471039437,0.267388935893957,4.49442677524682));
#58881=CARTESIAN_POINT('Ctrl Pts',(14.5133629400065,-0.271258982813659,
4.49231417140114));
#58882=CARTESIAN_POINT('Ctrl Pts',(14.5610787760694,-0.560805603747543,
4.03810188873054));
#58883=CARTESIAN_POINT('Ctrl Pts',(14.6087946121322,-0.335355809656676,
3.54890005536578));
#58884=CARTESIAN_POINT('Ctrl Pts',(14.656510448195,0.198056384554314,3.47395024222346));
#58885=CARTESIAN_POINT('Ctrl Pts',(14.7042262842579,0.549590353339887,3.88208001596329));
#58886=CARTESIAN_POINT('Ctrl Pts',(14.7519421203207,0.396427044118869,4.3984975254762));
#58887=CARTESIAN_POINT('Ctrl Pts',(14.7996579563836,-0.120781319530639,
4.54896862567174));
#58888=CARTESIAN_POINT('Ctrl Pts',(14.8473737924464,-0.527074338995675,
4.19531338994486));
#58889=CARTESIAN_POINT('Ctrl Pts',(14.8950896285092,-0.449346882879826,
3.66229886294881));
#58890=CARTESIAN_POINT('Ctrl Pts',(14.9428054645721,0.041022729875082,3.43940048630678));
#58891=CARTESIAN_POINT('Ctrl Pts',(14.9905213006349,0.493720538569869,3.73130926902151));
#58892=CARTESIAN_POINT('Ctrl Pts',(15.0382371366977,0.493027179828974,4.2699608843321));
#58893=CARTESIAN_POINT('Ctrl Pts',(15.0859529727606,0.0395793756528551,
4.56070326567839));
#58894=CARTESIAN_POINT('Ctrl Pts',(15.1336688088234,-0.450214778192253,
4.33654321062351));
#58895=CARTESIAN_POINT('Ctrl Pts',(15.1813846448863,-0.526569773778615,
3.80333034687015));
#58896=CARTESIAN_POINT('Ctrl Pts',(15.2291004809491,-0.119367643786657,
3.45072225173751));
#58897=CARTESIAN_POINT('Ctrl Pts',(15.2768163170119,0.397451630201876,3.60252436455885));
#58898=CARTESIAN_POINT('Ctrl Pts',(15.3245321530748,0.549284956596614,4.11933446935456));
#58899=CARTESIAN_POINT('Ctrl Pts',(15.3722479891376,0.196701455513243,4.52655789474516));
#58900=CARTESIAN_POINT('Ctrl Pts',(15.4199638252005,-0.336516018808871,
4.45023510325662));
#58901=CARTESIAN_POINT('Ctrl Pts',(15.4676796612633,-0.560705655094284,
3.96045448869));
#58902=CARTESIAN_POINT('Ctrl Pts',(15.5153954973261,-0.269990660741143,
3.50698912564524));
#58903=CARTESIAN_POINT('Ctrl Pts',(15.5631113333889,0.268660911710894,3.50626323446785));
#58904=CARTESIAN_POINT('Ctrl Pts',(15.6108271694518,0.560597035059331,3.95894341219528));
#58905=CARTESIAN_POINT('Ctrl Pts',(15.6585430055146,0.337728275218647,4.44932648624059));
#58906=CARTESIAN_POINT('Ctrl Pts',(15.7062588415775,-0.1952815563728,4.52708613419449));
#58907=CARTESIAN_POINT('Ctrl Pts',(15.7539746776403,-0.548961329954127,
4.12081447485494));
#58908=CARTESIAN_POINT('Ctrl Pts',(15.8016905137031,-0.398521467382777,
3.60359702428645));
#58909=CARTESIAN_POINT('Ctrl Pts',(15.849406349766,0.117886790727162,3.4504025257595));
#58910=CARTESIAN_POINT('Ctrl Pts',(15.8971221858288,0.526037794990907,3.80191184447176));
#58911=CARTESIAN_POINT('Ctrl Pts',(15.9448380218916,0.451120197982628,4.33532856438364));
#58912=CARTESIAN_POINT('Ctrl Pts',(15.9925538579545,-0.0380680182095728,
4.56080790392885));
#58913=CARTESIAN_POINT('Ctrl Pts',(16.0402696940173,-0.492297787528177,
4.27128871615743));
#58914=CARTESIAN_POINT('Ctrl Pts',(16.0879855300802,-0.494442923584513,
3.73264092602517));
#58915=CARTESIAN_POINT('Ctrl Pts',(16.135701366143,-0.0425335149309099,
3.43951308737216));
#58916=CARTESIAN_POINT('Ctrl Pts',(16.1834172022058,0.448435074945997,3.66108900478495));
#58917=CARTESIAN_POINT('Ctrl Pts',(16.2311330382687,0.52759883543946,4.19389210391969));
#58918=CARTESIAN_POINT('Ctrl Pts',(16.2788488743315,0.122260467197297,4.54864110061148));
#58919=CARTESIAN_POINT('Ctrl Pts',(16.3265647103944,-0.395351569291248,
4.39956453268331));
#58920=CARTESIAN_POINT('Ctrl Pts',(16.3742805464572,-0.549906176433804,
3.88356170630145));
#58921=CARTESIAN_POINT('Ctrl Pts',(16.42199638252,-0.199473480363076,3.47448595665642));
#58922=CARTESIAN_POINT('Ctrl Pts',(16.4697122185829,0.334138782019088,3.54799783908671));
#58923=CARTESIAN_POINT('Ctrl Pts',(16.5174280546457,0.560906259487099,4.0365902608309));
#58924=CARTESIAN_POINT('Ctrl Pts',(16.5651438907085,0.272584888215931,4.49158128304055));
#58925=CARTESIAN_POINT('Ctrl Pts',(16.6128597267714,-0.26605538016154,4.49514564908375));
#58926=CARTESIAN_POINT('Ctrl Pts',(16.6605755628342,-0.560372899148451,
4.04401014677825));
#58927=CARTESIAN_POINT('Ctrl Pts',(16.7082913988971,-0.340091362401967,
3.55245944950311));
#58928=CARTESIAN_POINT('Ctrl Pts',(16.7560072349599,0.19250130541649,3.4718921260458));
#58929=CARTESIAN_POINT('Ctrl Pts',(16.8037230710227,0.548317062457662,3.87629438922476));
#58930=CARTESIAN_POINT('Ctrl Pts',(16.8514389070856,0.400604824101502,4.39429741823411));
#58931=CARTESIAN_POINT('Ctrl Pts',(16.8991547431484,-0.114988988324618,
4.55021106103346));
#58932=CARTESIAN_POINT('Ctrl Pts',(16.9468705792113,-0.524986643439221,
4.20085742040038));
#58933=CARTESIAN_POINT('Ctrl Pts',(16.9945864152741,-0.45288098592576,3.66705332002498));
#58934=CARTESIAN_POINT('Ctrl Pts',(17.0423022513369,0.0351122494330066,
3.4389992789138));
#58935=CARTESIAN_POINT('Ctrl Pts',(17.0900180873998,0.490861365866046,3.72612083208173));
#58936=CARTESIAN_POINT('Ctrl Pts',(17.1377339234626,0.49584493715134,4.26474983932169));
#58937=CARTESIAN_POINT('Ctrl Pts',(17.1854497595254,0.0454864730955262,
4.56025499541263));
#58938=CARTESIAN_POINT('Ctrl Pts',(17.2331655955883,-0.446642919103261,
4.34126936858499));
#58939=CARTESIAN_POINT('Ctrl Pts',(17.2808814316511,-0.528613246204851,
3.80889082948154));
#58940=CARTESIAN_POINT('Ctrl Pts',(17.328597267714,-0.125149895556227,3.45201078225777));
#58941=CARTESIAN_POINT('Ctrl Pts',(17.3763131037768,0.393240529860342,3.59835766558462));
#58942=CARTESIAN_POINT('Ctrl Pts',(17.4240289398397,0.55051212592285,4.1135388846668));
#58943=CARTESIAN_POINT('Ctrl Pts',(17.4717447759024,0.202239966032548,4.52445559893916));
#58944=CARTESIAN_POINT('Ctrl Pts',(17.5194606119653,-0.331752266527324,
4.45375666691904));
#58945=CARTESIAN_POINT('Ctrl Pts',(17.5671764480281,-0.561091288070378,
3.96636600572338));
#58946=CARTESIAN_POINT('Ctrl Pts',(17.614892284091,-0.275171546279217,3.50986195899749));
#58947=CARTESIAN_POINT('Ctrl Pts',(17.6626081201538,0.263442460518632,3.50345921706735));
#58948=CARTESIAN_POINT('Ctrl Pts',(17.7103239562167,0.560133202238927,3.95303751636628));
#58949=CARTESIAN_POINT('Ctrl Pts',(17.7580397922795,0.342445005586054,4.44574218699675));
#58950=CARTESIAN_POINT('Ctrl Pts',(17.8057556283423,-0.189715708890181,
4.52911494868296));
#58951=CARTESIAN_POINT('Ctrl Pts',(17.8534714644052,-0.547657568741173,
4.12659331151364));
#58952=CARTESIAN_POINT('Ctrl Pts',(17.901187300468,-0.402677056422281,3.60781908849286));
#58953=CARTESIAN_POINT('Ctrl Pts',(17.9489031365308,0.112087992792125,3.44919063098808));
#58954=CARTESIAN_POINT('Ctrl Pts',(17.9966189725937,0.523920913530056,3.79637889233847));
#58955=CARTESIAN_POINT('Ctrl Pts',(18.0443348086565,0.454629197813879,4.33055554996792));
#58956=CARTESIAN_POINT('Ctrl Pts',(18.0920506447194,-0.0321555056241734,
4.56117795981091));
#58957=CARTESIAN_POINT('Ctrl Pts',(18.1397664807822,-0.489411313471489,
4.27646201432672));
#58958=CARTESIAN_POINT('Ctrl Pts',(18.1874823168451,-0.497233181596917,
3.73786674717144));
#58959=CARTESIAN_POINT('Ctrl Pts',(18.2351981529079,-0.0484381681459794,
3.43999247952716));
#58960=CARTESIAN_POINT('Ctrl Pts',(18.2829139889707,0.444838360430441,3.65638173475637));
#58961=CARTESIAN_POINT('Ctrl Pts',(18.3306298250336,0.529612977905601,4.18832093020544));
#58962=CARTESIAN_POINT('Ctrl Pts',(18.3783456610964,0.128035848626906,4.54732211775687));
#58963=CARTESIAN_POINT('Ctrl Pts',(18.4260614971592,-0.391118570530631,
4.40370898293889));
#58964=CARTESIAN_POINT('Ctrl Pts',(18.4737773332221,-0.551102788237131,
3.88936367722697));
#58965=CARTESIAN_POINT('Ctrl Pts',(18.5214931692849,-0.205000835699102,
3.47661740907615));
#58966=CARTESIAN_POINT('Ctrl Pts',(18.5692090053478,0.329356538604741,3.54450142744705));
#58967=CARTESIAN_POINT('Ctrl Pts',(18.6169248414106,0.561260735706054,4.03067679373969));
#58968=CARTESIAN_POINT('Ctrl Pts',(18.6646406774734,0.2777505631021,4.48868118831814));
#58969=CARTESIAN_POINT('Ctrl Pts',(18.7123565135363,-0.260822225340423,
4.49792212833724));
#58970=CARTESIAN_POINT('Ctrl Pts',(18.7600723495991,-0.559877950986752,
4.04991351638789));
#58971=CARTESIAN_POINT('Ctrl Pts',(18.8077881856619,-0.344789139412875,
3.55606855432066));
#58972=CARTESIAN_POINT('Ctrl Pts',(18.8555040217248,0.186924844147682,3.46989266958543));
#58973=CARTESIAN_POINT('Ctrl Pts',(18.9032198577876,0.546982867117114,3.87052250311704));
#58974=CARTESIAN_POINT('Ctrl Pts',(18.9509356938504,0.404738106803207,4.39005351430856));
#58975=CARTESIAN_POINT('Ctrl Pts',(18.9986515299133,-0.109183884691052,
4.55139238155646));
#58976=CARTESIAN_POINT('Ctrl Pts',(19.0463673659761,-0.522840634850846,
4.20637914057629));
#58977=CARTESIAN_POINT('Ctrl Pts',(19.094083202039,-0.456364785113784,3.67184475922049));
#58978=CARTESIAN_POINT('Ctrl Pts',(19.1417990381018,0.029197868913272,3.43866038485254));
#58979=CARTESIAN_POINT('Ctrl Pts',(19.1895148741647,0.487947670564988,3.72096281627648));
#58980=CARTESIAN_POINT('Ctrl Pts',(19.2372307102275,0.498607618457993,4.25950938727589));
#58981=CARTESIAN_POINT('Ctrl Pts',(19.2849465462903,0.0513885179525073,
4.55974449445321));
#58982=CARTESIAN_POINT('Ctrl Pts',(19.3326623823531,-0.44302144872845,4.34595762039384));
#58983=CARTESIAN_POINT('Ctrl Pts',(19.380378218416,-0.530598003365269,3.81447253878192));
#58984=CARTESIAN_POINT('Ctrl Pts',(19.4280940544788,-0.130918245164485,
3.45336018235082));
#58985=CARTESIAN_POINT('Ctrl Pts',(19.4758098905417,0.38898574814073,3.59423557624425));
#58986=CARTESIAN_POINT('Ctrl Pts',(19.5235257266045,0.551678150913516,4.10773069407674));
#58987=CARTESIAN_POINT('Ctrl Pts',(19.5712415626673,0.207756005258534,4.52229503878775));
#58988=CARTESIAN_POINT('Ctrl Pts',(19.6189573987302,-0.326951650734615,
4.4572278489044));
#58989=CARTESIAN_POINT('Ctrl Pts',(19.666673234793,-0.561414624206118,3.9722812219163));
#58990=CARTESIAN_POINT('Ctrl Pts',(19.7143890708559,-0.280321816997631,
3.51278930393937));
#58991=CARTESIAN_POINT('Ctrl Pts',(19.7621049069187,0.258194652845487,3.5007102220535));
#58992=CARTESIAN_POINT('Ctrl Pts',(19.8098207429815,0.559607330995945,3.94713708427543));
#58993=CARTESIAN_POINT('Ctrl Pts',(19.8575365790444,0.347123361713752,4.44210790974427));
#58994=CARTESIAN_POINT('Ctrl Pts',(19.9052524151072,-0.184128152223511,
4.53108587353909));
#58995=CARTESIAN_POINT('Ctrl Pts',(19.9529682511701,-0.546294178096705,
4.13235642149579));
#58996=CARTESIAN_POINT('Ctrl Pts',(20.0006840872329,-0.406785648814185,
3.61208785870539));
#58997=CARTESIAN_POINT('Ctrl Pts',(20.0483999232957,0.106272459957556,3.44803398021027));
#58998=CARTESIAN_POINT('Ctrl Pts',(20.0961157593586,0.5217539278249,3.7908797683689));
#58999=CARTESIAN_POINT('Ctrl Pts',(20.1438315954214,0.458072423058868,4.32572464996293));
#59000=CARTESIAN_POINT('Ctrl Pts',(20.1915474314842,-0.0262105744965466,
4.56152565902554));
#59001=CARTESIAN_POINT('Ctrl Pts',(20.2392632675471,-0.486524960252488,
4.28152908133109));
#59002=CARTESIAN_POINT('Ctrl Pts',(20.2869791036099,-0.499865224545849,
3.74326461201656));
#59003=CARTESIAN_POINT('Ctrl Pts',(20.3346949396728,-0.0545328049175168,
3.440261547834));
#59004=CARTESIAN_POINT('Ctrl Pts',(20.3824107757356,0.441568512678419,3.6522489094147));
#59005=CARTESIAN_POINT('Ctrl Pts',(20.4221739724547,0.515928418030698,4.09332268501583));
#59006=CARTESIAN_POINT('Ctrl Pts',(20.4539845298298,0.333108474939506,4.36566768059473));
#59007=CARTESIAN_POINT('Ctrl Pts',(20.4778424478613,0.118510552090848,4.48142006140068));
#59008=CARTESIAN_POINT('Ctrl Pts',(20.5017003658927,-0.127372553428812,
4.47887124859312));
#59009=CARTESIAN_POINT('Ctrl Pts',(20.5255582839241,-0.340862259689409,
4.35954554232165));
#59010=CARTESIAN_POINT('Ctrl Pts',(20.5494162019555,-0.471665647836603,
4.15213005589169));
#59011=CARTESIAN_POINT('Ctrl Pts',(20.5732741199869,-0.486782001098211,
3.90760543082941));
#59012=CARTESIAN_POINT('Ctrl Pts',(20.5971320380184,-0.38305332993788,3.68562568155832));
#59013=CARTESIAN_POINT('Ctrl Pts',(20.6209899560498,-0.185558943137764,
3.54054450025879));
#59014=CARTESIAN_POINT('Ctrl Pts',(20.6448478740812,0.0572573647513246,
3.50779920733485));
#59015=CARTESIAN_POINT('Ctrl Pts',(20.6687057921126,0.28610038304352,3.59541756340761));
#59016=CARTESIAN_POINT('Ctrl Pts',(20.6925637101441,0.444969396676924,3.78196356026503));
#59017=CARTESIAN_POINT('Ctrl Pts',(20.7164216281754,0.495039040219165,4.02182741068269));
#59018=CARTESIAN_POINT('Ctrl Pts',(20.7402795462069,0.424054039808096,4.25635280284423));
#59019=CARTESIAN_POINT('Ctrl Pts',(20.7641374642383,0.249378454468877,4.42819351412177));
#59020=CARTESIAN_POINT('Ctrl Pts',(20.7879953822697,0.0137218901755031,
4.49532894963167));
#59021=CARTESIAN_POINT('Ctrl Pts',(20.8118533003011,-0.22528943893053,4.44134312218709));
#59022=CARTESIAN_POINT('Ctrl Pts',(20.8357112183326,-0.409211687104306,
4.27943679589328));
#59023=CARTESIAN_POINT('Ctrl Pts',(20.859569136364,-0.493070359673604,4.04920060553547));
#59024=CARTESIAN_POINT('Ctrl Pts',(20.8834270543954,-0.456359989112496,
3.80693350349834));
#59025=CARTESIAN_POINT('Ctrl Pts',(20.9072849724268,-0.308057122141145,
3.61187643128937));
#59026=CARTESIAN_POINT('Ctrl Pts',(20.9311428904583,-0.0844259229598539,
3.51172613733272));
#59027=CARTESIAN_POINT('Ctrl Pts',(20.9550008084896,0.159849727585384,3.53097210659131));
#59028=CARTESIAN_POINT('Ctrl Pts',(20.9788587265211,0.365037758375503,3.66490817000854));
#59029=CARTESIAN_POINT('Ctrl Pts',(21.0027166445525,0.480964117596,3.88078331455297));
#59030=CARTESIAN_POINT('Ctrl Pts',(21.026574562584,0.479281646861755,4.12581018556955));
#59031=CARTESIAN_POINT('Ctrl Pts',(21.0504324806153,0.360401759160676,4.34007303948752));
#59032=CARTESIAN_POINT('Ctrl Pts',(21.0742903986468,0.153393823636192,4.47117877170218));
#59033=CARTESIAN_POINT('Ctrl Pts',(21.0981483166782,-0.0911230798336762,
4.48706845966041));
#59034=CARTESIAN_POINT('Ctrl Pts',(21.1220062347096,-0.313357908298923,
4.38385664171252));
#59035=CARTESIAN_POINT('Ctrl Pts',(21.145864152741,-0.458968192403581,4.18678141884249));
#59036=CARTESIAN_POINT('Ctrl Pts',(21.1697220707724,-0.492348251467217,
3.94403305123036));
#59037=CARTESIAN_POINT('Ctrl Pts',(21.1935799888039,-0.405335751726616,
3.71497012710753));
#59038=CARTESIAN_POINT('Ctrl Pts',(21.2174379068353,-0.21920761957706,3.55560477096155));
#59039=CARTESIAN_POINT('Ctrl Pts',(21.2412958248667,0.0205227466613194,
3.50490615340017));
#59040=CARTESIAN_POINT('Ctrl Pts',(21.2651537428981,0.255234742309135,3.57527146741714));
#59041=CARTESIAN_POINT('Ctrl Pts',(21.2890116609295,0.427534891009427,3.74949447702405));
#59042=CARTESIAN_POINT('Ctrl Pts',(21.312869578961,0.495291113040325,3.98497291063177));
#59043=CARTESIAN_POINT('Ctrl Pts',(21.3367274969923,0.441935166474334,4.22412587691986));
#59044=CARTESIAN_POINT('Ctrl Pts',(21.3605854150238,0.280514033632862,4.40847396123464));
#59045=CARTESIAN_POINT('Ctrl Pts',(21.3844433330552,0.0504995785194436,
4.49293903542029));
#59046=CARTESIAN_POINT('Ctrl Pts',(21.4083012510867,-0.191863399122956,
4.45686708805594));
#59047=CARTESIAN_POINT('Ctrl Pts',(21.432159169118,-0.387310549425693,4.3090786928523));
#59048=CARTESIAN_POINT('Ctrl Pts',(21.4560170871495,-0.488049720266331,
4.08571213811173));
#59049=CARTESIAN_POINT('Ctrl Pts',(21.4798750051809,-0.469447440294381,
3.84138663085107));
#59050=CARTESIAN_POINT('Ctrl Pts',(21.5037329232123,-0.336052473678932,
3.63584641288874));
#59051=CARTESIAN_POINT('Ctrl Pts',(21.5275908412437,-0.120483523363382,
3.51935166631968));
#59052=CARTESIAN_POINT('Ctrl Pts',(21.5514487592752,0.124546930319796,3.5203885299332));
#59053=CARTESIAN_POINT('Ctrl Pts',(21.5753066773065,0.339122266949511,3.63870346233219));
#59054=CARTESIAN_POINT('Ctrl Pts',(21.599164595338,0.470772971804989,3.84536523971104));
#59055=CARTESIAN_POINT('Ctrl Pts',(21.6230225133694,0.487306861455871,4.08983942814686));
#59056=CARTESIAN_POINT('Ctrl Pts',(21.6468804314008,0.384680949508402,4.31234542922385));
#59057=CARTESIAN_POINT('Ctrl Pts',(21.6707383494323,0.187990066907445,4.45847446473699));
#59058=CARTESIAN_POINT('Ctrl Pts',(21.6945962674636,-0.0546695077989956,
4.49249400502822));
#59059=CARTESIAN_POINT('Ctrl Pts',(21.7184541854951,-0.283960898681086,
4.40608534582272));
#59060=CARTESIAN_POINT('Ctrl Pts',(21.7423121035264,-0.443816114896065,
4.22037775802082));
#59061=CARTESIAN_POINT('Ctrl Pts',(21.766170021558,-0.495146201710716,3.98078180541326));
#59062=CARTESIAN_POINT('Ctrl Pts',(21.7900279395893,-0.425399554695369,
3.74588522487523));
#59063=CARTESIAN_POINT('Ctrl Pts',(21.8138858576208,-0.25163112890579,3.57312662880273));
#59064=CARTESIAN_POINT('Ctrl Pts',(21.8377437756521,-0.0163320378044167,
3.50475019978512));
#59065=CARTESIAN_POINT('Ctrl Pts',(21.8616016936836,0.222960681415914,3.55747583725374));
#59066=CARTESIAN_POINT('Ctrl Pts',(21.885459611715,0.407733440703041,3.71841068663001));
#59067=CARTESIAN_POINT('Ctrl Pts',(21.9093175297464,0.492804267302335,3.94820179346412));
#59068=CARTESIAN_POINT('Ctrl Pts',(21.9331754477779,0.457371026827486,4.19065897275109));
#59069=CARTESIAN_POINT('Ctrl Pts',(21.9570333658092,0.310098111756678,4.38649483975425));
#59070=CARTESIAN_POINT('Ctrl Pts',(21.9808912838407,0.0869977614584207,
4.48782219052945));
#59071=CARTESIAN_POINT('Ctrl Pts',(22.0047492018721,-0.15737591128791,4.46986372771052));
#59072=CARTESIAN_POINT('Ctrl Pts',(22.0286071199035,-0.363266886890503,
4.33701078463543));
#59073=CARTESIAN_POINT('Ctrl Pts',(22.0524650379349,-0.480329213457224,
4.12174952472744));
#59074=CARTESIAN_POINT('Ctrl Pts',(22.0763229559664,-0.479937963428243,
3.87671718963328));
#59075=CARTESIAN_POINT('Ctrl Pts',(22.1001808739978,-0.362188808094022,
3.66183085982978));
#59076=CARTESIAN_POINT('Ctrl Pts',(22.1240387920292,-0.155874623354616,
3.529636096341));
#59077=CARTESIAN_POINT('Ctrl Pts',(22.1478967100606,0.0885551527323001,
3.51245811975107));
#59078=CARTESIAN_POINT('Ctrl Pts',(22.1717546280921,0.311330781786364,3.61449741325855));
#59079=CARTESIAN_POINT('Ctrl Pts',(22.1956125461234,0.457977554205651,3.81080259009947));
#59080=CARTESIAN_POINT('Ctrl Pts',(22.2194704641549,0.492636339578261,4.05337168730347));
#59081=CARTESIAN_POINT('Ctrl Pts',(22.2433283821863,0.406832120751761,4.28288995313029));
#59082=CARTESIAN_POINT('Ctrl Pts',(22.2671863002177,0.22154636656941,4.44323391967918));
#59083=CARTESIAN_POINT('Ctrl Pts',(22.2910442182491,-0.0179135091400202,
4.49519511936025));
#59084=CARTESIAN_POINT('Ctrl Pts',(22.3149021362805,-0.2529930437236,4.42606762362056));
#59085=CARTESIAN_POINT('Ctrl Pts',(22.338760054312,-0.426208888077552,4.25275498785448));
#59086=CARTESIAN_POINT('Ctrl Pts',(22.3626179723434,-0.495205048933098,
4.01763687303198));
#59087=CARTESIAN_POINT('Ctrl Pts',(22.3864758903748,-0.443110087468167,
3.77820606161377));
#59088=CARTESIAN_POINT('Ctrl Pts',(22.4103338084062,-0.282662637164788,
3.59300991103726));
#59089=CARTESIAN_POINT('Ctrl Pts',(22.4341917264377,-0.0530964769854286,
3.50733392083031));
#59090=CARTESIAN_POINT('Ctrl Pts',(22.458049644469,0.189453226607198,3.5421282117862));
#59091=CARTESIAN_POINT('Ctrl Pts',(22.4819075625005,0.385676439696491,3.6888846179772));
#59092=CARTESIAN_POINT('Ctrl Pts',(22.5057654805319,0.487591287867653,3.9117172269821));
#59093=CARTESIAN_POINT('Ctrl Pts',(22.5296233985634,0.470276727405835,4.15613734610506));
#59094=CARTESIAN_POINT('Ctrl Pts',(22.5534813165947,0.337966804695391,4.36237769267677));
#59095=CARTESIAN_POINT('Ctrl Pts',(22.5773392346262,0.123014588878675,4.48000670597833));
#59096=CARTESIAN_POINT('Ctrl Pts',(22.6011971526576,-0.122017660845505,
4.48026122441149));
#59097=CARTESIAN_POINT('Ctrl Pts',(22.625055070689,-0.337213993725473,4.36307837627545));
#59098=CARTESIAN_POINT('Ctrl Pts',(22.6489129887204,-0.469950950795418,
4.15711375897153));
#59099=CARTESIAN_POINT('Ctrl Pts',(22.6727709067518,-0.487774683880463,
3.912729067726));
#59100=CARTESIAN_POINT('Ctrl Pts',(22.6966288247832,-0.386319338946922,
3.6896872918462));
#59101=CARTESIAN_POINT('Ctrl Pts',(22.7204867428147,-0.190407614498503,
3.54252014522276));
#59102=CARTESIAN_POINT('Ctrl Pts',(22.7443446608461,0.0520814161336476,
3.50722927763546));
#59103=CARTESIAN_POINT('Ctrl Pts',(22.7682025788775,0.281801791424649,3.59241522467272));
#59104=CARTESIAN_POINT('Ctrl Pts',(22.7920604969089,0.442679857002608,3.77730419914427));
#59105=CARTESIAN_POINT('Ctrl Pts',(22.8079657755965,0.477669651496365,3.93681187972983));
#59106=CARTESIAN_POINT('Ctrl Pts',(22.8159184149403,0.475016281724327,4.01593044384941));
#59107=CARTESIAN_POINT('Ctrl Pts',(3.98408158505964,0.229225853138217,4.48306385360099));
#59108=CARTESIAN_POINT('Ctrl Pts',(3.99203422440344,0.148766887950233,4.52124364039387));
#59109=CARTESIAN_POINT('Ctrl Pts',(4.00793950309106,-0.0315132651739855,
4.55658776856145));
#59110=CARTESIAN_POINT('Ctrl Pts',(4.03179742112247,-0.29437836981663,4.47338935048851));
#59111=CARTESIAN_POINT('Ctrl Pts',(4.0556553391539,-0.485191777607318,4.27448557757091));
#59112=CARTESIAN_POINT('Ctrl Pts',(4.07951325718531,-0.557397168683185,
4.00843674174317));
#59113=CARTESIAN_POINT('Ctrl Pts',(4.10337117521674,-0.493285636019562,
3.74033843218029));
#59114=CARTESIAN_POINT('Ctrl Pts',(4.12722909324815,-0.308561908987092,
3.53572729771651));
#59115=CARTESIAN_POINT('Ctrl Pts',(4.15108701127957,-0.0483813190761145,
3.44464727048097));
#59116=CARTESIAN_POINT('Ctrl Pts',(4.17494492931099,0.223627135909104,3.48936410886239));
#59117=CARTESIAN_POINT('Ctrl Pts',(4.19880284734241,0.440954086798485,3.65894639349553));
#59118=CARTESIAN_POINT('Ctrl Pts',(4.22266076537383,0.55045499896491,3.91192501290154));
#59119=CARTESIAN_POINT('Ctrl Pts',(4.24651868340524,0.525355068663259,4.18644066347397));
#59120=CARTESIAN_POINT('Ctrl Pts',(4.27037660143667,0.371791302444591,4.41536633561891));
#59121=CARTESIAN_POINT('Ctrl Pts',(4.29423451946808,0.127314547262185,4.54272370785395));
#59122=CARTESIAN_POINT('Ctrl Pts',(4.31809243749951,-0.14829414195428,4.5373703057994));
#59123=CARTESIAN_POINT('Ctrl Pts',(4.34195035553092,-0.387640842632661,
4.40061524972397));
#59124=CARTESIAN_POINT('Ctrl Pts',(4.36580827356235,-0.53219881478122,4.16589884014724));
#59125=CARTESIAN_POINT('Ctrl Pts',(4.38966619159376,-0.546619671109945,
3.89061565172978));
#59126=CARTESIAN_POINT('Ctrl Pts',(4.41352410962518,-0.427377132892538,
3.64207991255526));
#59127=CARTESIAN_POINT('Ctrl Pts',(4.4373820276566,-0.203629241694984,3.48106538615089));
#59128=CARTESIAN_POINT('Ctrl Pts',(4.46123994568802,0.0699115445388116,
3.44694450735191));
#59129=CARTESIAN_POINT('Ctrl Pts',(4.48509786371944,0.326357054473012,3.54806076195131));
#59130=CARTESIAN_POINT('Ctrl Pts',(4.50895578175085,0.502999374434197,3.7596884705576));
#59131=CARTESIAN_POINT('Ctrl Pts',(4.53281369978229,0.556644646112557,4.03007889421215));
#59132=CARTESIAN_POINT('Ctrl Pts',(4.55667161781369,0.474175139017821,4.29311420882242));
#59133=CARTESIAN_POINT('Ctrl Pts',(4.58052953584512,0.275756894216243,4.48447511514554));
#59134=CARTESIAN_POINT('Ctrl Pts',(4.60438745387653,0.00990857728296194,
4.55736865895685));
#59135=CARTESIAN_POINT('Ctrl Pts',(4.62824537190795,-0.258362656684952,
4.49397038324719));
#59136=CARTESIAN_POINT('Ctrl Pts',(4.65210328993938,-0.463457183444019,
4.30978289334447));
#59137=CARTESIAN_POINT('Ctrl Pts',(4.67596120797079,-0.555223804526532,
4.04984504770563));
#59138=CARTESIAN_POINT('Ctrl Pts',(4.69981912600221,-0.511223081411799,
3.77771873014923));
#59139=CARTESIAN_POINT('Ctrl Pts',(4.72367704403363,-0.342214389453536,
3.55994623789246));
#59140=CARTESIAN_POINT('Ctrl Pts',(4.74753496206505,-0.0895249575417115,
3.44977887729433));
#59141=CARTESIAN_POINT('Ctrl Pts',(4.77139288009647,0.185055765100279,3.47415556892044));
#59142=CARTESIAN_POINT('Ctrl Pts',(4.79525079812788,0.414385312357242,3.62711554766008));
#59143=CARTESIAN_POINT('Ctrl Pts',(4.81910871615931,0.542386363113676,3.87125593216545));
#59144=CARTESIAN_POINT('Ctrl Pts',(4.84296663419071,0.537759173780872,4.14687774817434));
#59145=CARTESIAN_POINT('Ctrl Pts',(4.86682455222215,0.401635218192884,4.38658395388507));
#59146=CARTESIAN_POINT('Ctrl Pts',(4.89068247025356,0.167300511433038,4.53175985253543));
#59147=CARTESIAN_POINT('Ctrl Pts',(4.91454038828499,-0.107943727546613,
4.54690598239331));
#59148=CARTESIAN_POINT('Ctrl Pts',(4.9383983063164,-0.356792784813018,4.42831870213619));
#59149=CARTESIAN_POINT('Ctrl Pts',(4.96225622434782,-0.518396287352312,
4.20499583203957));
#59150=CARTESIAN_POINT('Ctrl Pts',(4.98611414237924,-0.553237776802617,
3.93154589703492));
#59151=CARTESIAN_POINT('Ctrl Pts',(5.00997206041066,-0.452797559930213,
3.67483485485756));
#59152=CARTESIAN_POINT('Ctrl Pts',(5.03382997844208,-0.241636005696979,
3.49763554798826));
#59153=CARTESIAN_POINT('Ctrl Pts',(5.05768789647349,0.0286121339618079,
3.44327803376872));
#59154=CARTESIAN_POINT('Ctrl Pts',(5.08154581450492,0.291863827488053,3.52505420509465));
#59155=CARTESIAN_POINT('Ctrl Pts',(5.10540373253633,0.48374686498243,3.72296756053861));
#59156=CARTESIAN_POINT('Ctrl Pts',(5.12926165056775,0.557340616988569,3.98862289364304));
#59157=CARTESIAN_POINT('Ctrl Pts',(5.15311956859917,0.49464940648741,4.25706023915787));
#59158=CARTESIAN_POINT('Ctrl Pts',(5.17697748663059,0.311002942120779,4.46263935401832));
#59159=CARTESIAN_POINT('Ctrl Pts',(5.20083540466201,0.0513077868555636,
4.55509054477827));
#59160=CARTESIAN_POINT('Ctrl Pts',(5.22469332269342,-0.22093351989189,4.5118069769771));
#59161=CARTESIAN_POINT('Ctrl Pts',(5.24855124072485,-0.439150562917527,
4.34337266196288));
#59162=CARTESIAN_POINT('Ctrl Pts',(5.27240915875626,-0.549983331088669,
4.09097437781523));
#59163=CARTESIAN_POINT('Ctrl Pts',(5.29626707678769,-0.526330193563486,
3.81633038019944));
#59164=CARTESIAN_POINT('Ctrl Pts',(5.32012499481911,-0.373974986765411,
3.5865986076849));
#59165=CARTESIAN_POINT('Ctrl Pts',(5.34398291285052,-0.130172708829089,
3.45795473641922));
#59166=CARTESIAN_POINT('Ctrl Pts',(5.36784083088195,0.145460342249349,3.46185569711558));
#59167=CARTESIAN_POINT('Ctrl Pts',(5.39169874891335,0.385524377387638,3.59734759862366));
#59168=CARTESIAN_POINT('Ctrl Pts',(5.41555666694479,0.531317200781484,3.83129898029949));
#59169=CARTESIAN_POINT('Ctrl Pts',(5.4394145849762,0.547188495794237,4.10650235661553));
#59170=CARTESIAN_POINT('Ctrl Pts',(5.46327250300762,0.42925729847004,4.35566300567327));
#59171=CARTESIAN_POINT('Ctrl Pts',(5.48713042103904,0.206360998935678,4.51785436177788));
#59172=CARTESIAN_POINT('Ctrl Pts',(5.51098833907045,-0.0669961859988386,
4.55341622035867));
#59173=CARTESIAN_POINT('Ctrl Pts',(5.53484625710188,-0.323970978517869,
4.45365273830571));
#59174=CARTESIAN_POINT('Ctrl Pts',(5.55870417513329,-0.501726041995696,
4.2429588044862));
#59175=CARTESIAN_POINT('Ctrl Pts',(5.58256209316472,-0.556795421465071,
3.97285482490167));
#59176=CARTESIAN_POINT('Ctrl Pts',(5.60642001119613,-0.475713153578786,
3.70938858005442));
#59177=CARTESIAN_POINT('Ctrl Pts',(5.63027792922756,-0.27830606148521,3.51698474346866));
#59178=CARTESIAN_POINT('Ctrl Pts',(5.65413584725897,-0.0128455564368745,
3.44269129419766));
#59179=CARTESIAN_POINT('Ctrl Pts',(5.67799376529039,0.255756037034639,3.5046750042392));
#59180=CARTESIAN_POINT('Ctrl Pts',(5.70185168332181,0.46181831285622,3.68777916820271));
#59181=CARTESIAN_POINT('Ctrl Pts',(5.72570960135323,0.554953431393631,3.94722983012095));
#59182=CARTESIAN_POINT('Ctrl Pts',(5.74956751938465,0.512387319539865,4.21958423627784));
#59183=CARTESIAN_POINT('Ctrl Pts',(5.77342543741606,0.344528550506956,4.43824431479549));
#59184=CARTESIAN_POINT('Ctrl Pts',(5.79728335544749,0.0924231668635294,
4.54974172178225));
#59185=CARTESIAN_POINT('Ctrl Pts',(5.82114127347891,-0.182282200065281,
4.52681230129395));
#59186=CARTESIAN_POINT('Ctrl Pts',(5.84499919151032,-0.412414601109181,
4.37506292652603));
#59187=CARTESIAN_POINT('Ctrl Pts',(5.86885710954175,-0.541700403334708,
4.13160044316952));
#59188=CARTESIAN_POINT('Ctrl Pts',(5.89271502757316,-0.538525691690445,
3.85595807909033));
#59189=CARTESIAN_POINT('Ctrl Pts',(5.91657294560459,-0.403666797469215,
3.61553786496538));
#59190=CARTESIAN_POINT('Ctrl Pts',(5.94043086363599,-0.170100341263849,
3.46912915944898));
#59191=CARTESIAN_POINT('Ctrl Pts',(5.96428878166742,0.105060216979666,3.45253275189516));
#59192=CARTESIAN_POINT('Ctrl Pts',(5.98814669969884,0.354530812822036,3.5698071562788));
#59193=CARTESIAN_POINT('Ctrl Pts',(6.01200461773026,0.517308736525128,3.79227513259484));
#59194=CARTESIAN_POINT('Ctrl Pts',(6.03586253576167,0.553591019453439,4.06553805729756));
#59195=CARTESIAN_POINT('Ctrl Pts',(6.0597204537931,0.454504394384077,4.32277408438697));
#59196=CARTESIAN_POINT('Ctrl Pts',(6.08357837182452,0.244280620740535,4.50108505220882));
#59197=CARTESIAN_POINT('Ctrl Pts',(6.10743628985593,-0.0256793573627324,
4.55686330558177));
#59198=CARTESIAN_POINT('Ctrl Pts',(6.13129420788736,-0.289354484390735,
4.47648043042773));
#59199=CARTESIAN_POINT('Ctrl Pts',(6.15515212591877,-0.482285035214929,
4.27957167009689));
#59200=CARTESIAN_POINT('Ctrl Pts',(6.17901004395019,-0.557263974895364,
4.01432540012922));
#59201=CARTESIAN_POINT('Ctrl Pts',(6.20286796198161,-0.496014047041978,
3.74552825888183));
#59202=CARTESIAN_POINT('Ctrl Pts',(6.22672588001303,-0.313404643062,3.53904687299508));
#59203=CARTESIAN_POINT('Ctrl Pts',(6.25058379804445,-0.0542924323345977,
3.44511024149985));
#59204=CARTESIAN_POINT('Ctrl Pts',(6.27444171607587,0.218347115212216,3.48718178027374));
#59205=CARTESIAN_POINT('Ctrl Pts',(6.29829963410728,0.437120926894882,3.65404298137615));
#59206=CARTESIAN_POINT('Ctrl Pts',(6.32215755213871,0.549895923261456,3.90664388593688));
#59207=CARTESIAN_POINT('Ctrl Pts',(6.34601547017011,0.526573903738089,4.17995327069166));
#59208=CARTESIAN_POINT('Ctrl Pts',(6.37782602754536,0.327418726170013,4.4906154426808));
#59209=CARTESIAN_POINT('Ctrl Pts',(6.41758922426438,-0.161063729547888,
4.61146011675295));
#59210=CARTESIAN_POINT('Ctrl Pts',(6.46530506032721,-0.60205854017139,4.19446204504257));
#59211=CARTESIAN_POINT('Ctrl Pts',(6.51302089639007,-0.488859252747234,
3.59916283817905));
#59212=CARTESIAN_POINT('Ctrl Pts',(6.56073673245289,0.0725864685289804,
3.37181094029106));
#59213=CARTESIAN_POINT('Ctrl Pts',(6.60845256851574,0.567733426150434,3.72141305678318));
#59214=CARTESIAN_POINT('Ctrl Pts',(6.65616840457857,0.541332409494817,4.32680434473755));
#59215=CARTESIAN_POINT('Ctrl Pts',(6.70388424064141,0.0179179137367747,
4.6321081579338));
#59216=CARTESIAN_POINT('Ctrl Pts',(6.75160007670425,-0.522004047715759,
4.35692568061372));
#59217=CARTESIAN_POINT('Ctrl Pts',(6.79931591276708,-0.582533501572452,
3.75397902491298));
#59218=CARTESIAN_POINT('Ctrl Pts',(6.84703174882993,-0.10812839031349,3.37695395054049));
#59219=CARTESIAN_POINT('Ctrl Pts',(6.89474758489276,0.465580583415614,3.57208337966475));
#59220=CARTESIAN_POINT('Ctrl Pts',(6.9424634209556,0.611735560770294,4.16017430964564));
#59221=CARTESIAN_POINT('Ctrl Pts',(6.99017925701844,0.196126575106773,4.60117519156627));
#59222=CARTESIAN_POINT('Ctrl Pts',(7.03789509308127,-0.399589635450545,
4.49010738789885));
#59223=CARTESIAN_POINT('Ctrl Pts',(7.08561092914412,-0.628355913977057,
3.92896656470948));
#59224=CARTESIAN_POINT('Ctrl Pts',(7.13332676520695,-0.280093617253323,
3.43305676608093));
#59225=CARTESIAN_POINT('Ctrl Pts',(7.1810426012698,0.325383132256395,3.45777970086456));
#59226=CARTESIAN_POINT('Ctrl Pts',(7.22875843733263,0.632055452459012,3.98043185926557));
#59227=CARTESIAN_POINT('Ctrl Pts',(7.27647427339546,0.358301574124045,4.52105375310108));
#59228=CARTESIAN_POINT('Ctrl Pts',(7.32419010945831,-0.244486178793781,
4.58318396235269));
#59229=CARTESIAN_POINT('Ctrl Pts',(7.37190594552114,-0.622758498112341,
4.10976736853928));
#59230=CARTESIAN_POINT('Ctrl Pts',(7.41962178158399,-0.42914211350377,3.53554970961824));
#59231=CARTESIAN_POINT('Ctrl Pts',(7.46733761764681,0.158562080980748,3.38784389968312));
#59232=CARTESIAN_POINT('Ctrl Pts',(7.51505345370967,0.600656274672958,3.80229045545538));
#59233=CARTESIAN_POINT('Ctrl Pts',(7.56276928977248,0.491158570126743,4.3982967283715));
#59234=CARTESIAN_POINT('Ctrl Pts',(7.61048512583535,-0.0693776073840611,
4.62854098691609));
#59235=CARTESIAN_POINT('Ctrl Pts',(7.65820096189817,-0.566203260219877,
4.28158638589565));
#59236=CARTESIAN_POINT('Ctrl Pts',(7.70591679796101,-0.543075747198986,
3.67604667390869));
#59237=CARTESIAN_POINT('Ctrl Pts',(7.75363263402386,-0.0212334191459514,
3.36799828595259));
#59238=CARTESIAN_POINT('Ctrl Pts',(7.80134847008666,0.520107884382028,3.64032679659274));
#59239=CARTESIAN_POINT('Ctrl Pts',(7.84906430614954,0.583826114817312,4.24294874421058));
#59240=CARTESIAN_POINT('Ctrl Pts',(7.89678014221235,0.111407840683781,4.62246712177016));
#59241=CARTESIAN_POINT('Ctrl Pts',(7.94449597827521,-0.463317967772962,
4.43036436352186));
#59242=CARTESIAN_POINT('Ctrl Pts',(7.99221181433803,-0.612571757364041,
3.84305138824375));
#59243=CARTESIAN_POINT('Ctrl Pts',(8.03992765040088,-0.199291476537812,
3.39986673810663));
#59244=CARTESIAN_POINT('Ctrl Pts',(8.08764348646372,0.397001233685627,3.50779369660314));
#59245=CARTESIAN_POINT('Ctrl Pts',(8.13535932252656,0.628721602366905,4.06772127707659));
#59246=CARTESIAN_POINT('Ctrl Pts',(8.18307515858938,0.283077249469033,4.56545936678474));
#59247=CARTESIAN_POINT('Ctrl Pts',(8.23079099465223,-0.32252129731946,4.54392741926377));
#59248=CARTESIAN_POINT('Ctrl Pts',(8.27850683071506,-0.631943574151527,
4.02289855323374));
#59249=CARTESIAN_POINT('Ctrl Pts',(8.32622266677791,-0.361042343138453,
3.48084159342964));
#59250=CARTESIAN_POINT('Ctrl Pts',(8.37393850284074,0.241409626929164,3.41553578665797));
#59251=CARTESIAN_POINT('Ctrl Pts',(8.42165433890358,0.622171422023167,3.88695246013618));
#59252=CARTESIAN_POINT('Ctrl Pts',(8.46937017496642,0.431583626935426,4.46218242893131));
#59253=CARTESIAN_POINT('Ctrl Pts',(8.51708601102927,-0.155334053534803,
4.61298316164806));
#59254=CARTESIAN_POINT('Ctrl Pts',(8.56480184709209,-0.599606082522386,
4.20087202506506));
#59255=CARTESIAN_POINT('Ctrl Pts',(8.61251768315494,-0.493250619804184,
3.60429701705146));
#59256=CARTESIAN_POINT('Ctrl Pts',(8.66023351921777,0.0660644767165412,
3.37110214695249));
#59257=CARTESIAN_POINT('Ctrl Pts',(8.70794935528061,0.564711547735832,3.71543385214437));
#59258=CARTESIAN_POINT('Ctrl Pts',(8.75566519134344,0.544775315265253,4.32108702952508));
#59259=CARTESIAN_POINT('Ctrl Pts',(8.80338102740629,0.0245635283409047,
4.6318810471339));
#59260=CARTESIAN_POINT('Ctrl Pts',(8.85109686346912,-0.518205324617361,
4.36240897642002));
#59261=CARTESIAN_POINT('Ctrl Pts',(8.89881269953197,-0.585098254365674,
3.76013116628075));
#59262=CARTESIAN_POINT('Ctrl Pts',(8.9465285355948,-0.114686454236133,3.3781285970023));
#59263=CARTESIAN_POINT('Ctrl Pts',(8.99424437165764,0.461043681496376,3.56720010581811));
#59264=CARTESIAN_POINT('Ctrl Pts',(9.04196020772047,0.613390310441866,4.15371841694351));
#59265=CARTESIAN_POINT('Ctrl Pts',(9.08967604378332,0.202451179085494,4.59907474052783));
#59266=CARTESIAN_POINT('Ctrl Pts',(9.13739187984615,-0.394401985136886,
4.49429151193569));
#59267=CARTESIAN_POINT('Ctrl Pts',(9.18510771590899,-0.629069737753471,
3.93559278228048));
#59268=CARTESIAN_POINT('Ctrl Pts',(9.23282355197184,-0.28605307070895,3.43604019168954));
#59269=CARTESIAN_POINT('Ctrl Pts',(9.28053938803466,0.319650532659854,3.45438057070715));
#59270=CARTESIAN_POINT('Ctrl Pts',(9.32825522409751,0.631814133431458,3.97377166707843));
#59271=CARTESIAN_POINT('Ctrl Pts',(9.37597106016033,0.363773093762905,4.51724864514637));
#59272=CARTESIAN_POINT('Ctrl Pts',(9.4236868962232,-0.238326375276645,4.58572823348297));
#59273=CARTESIAN_POINT('Ctrl Pts',(9.47140273228601,-0.621567066777005,
4.11632457242483));
#59274=CARTESIAN_POINT('Ctrl Pts',(9.51911856834886,-0.434013156817378,
3.54009826662536));
#59275=CARTESIAN_POINT('Ctrl Pts',(9.5668344044117,0.152101713198456,3.38620679908157));
#59276=CARTESIAN_POINT('Ctrl Pts',(9.61455024047453,0.598539239598464,3.79597107236355));
#59277=CARTESIAN_POINT('Ctrl Pts',(9.66226607653739,0.495328972565208,4.39309824928265));
#59278=CARTESIAN_POINT('Ctrl Pts',(9.7099819126002,-0.0627495115905886,
4.62923725529147));
#59279=CARTESIAN_POINT('Ctrl Pts',(9.75769774866305,-0.563204153727404,
4.28753800770644));
#59280=CARTESIAN_POINT('Ctrl Pts',(9.80541358472588,-0.54645975548653,3.68178818330365));
#59281=CARTESIAN_POINT('Ctrl Pts',(9.85312942078873,-0.027892955418244,
3.36825716649128));
#59282=CARTESIAN_POINT('Ctrl Pts',(9.90084525685157,0.516288374798902,3.63486531430293));
#59283=CARTESIAN_POINT('Ctrl Pts',(9.9485610929144,0.58635414632045,4.2367822623095));
#59284=CARTESIAN_POINT('Ctrl Pts',(9.99627692897723,0.117961883057689,4.62125841547385));
#59285=CARTESIAN_POINT('Ctrl Pts',(10.0439927650401,-0.458756592493822,
4.4352234064191));
#59286=CARTESIAN_POINT('Ctrl Pts',(10.0917086011029,-0.614191830280748,
3.8495160464768));
#59287=CARTESIAN_POINT('Ctrl Pts',(10.1394244371658,-0.205605259764808,
3.40200041654811));
#59288=CARTESIAN_POINT('Ctrl Pts',(10.1871402732286,0.391791784436726,3.5036370055096));
#59289=CARTESIAN_POINT('Ctrl Pts',(10.2348561092915,0.629400404498524,4.06109136983801));
#59290=CARTESIAN_POINT('Ctrl Pts',(10.2825719453542,0.289020948539269,4.56244458923262));
#59291=CARTESIAN_POINT('Ctrl Pts',(10.3302877814171,-0.316770891622519,
4.54729628801251));
#59292=CARTESIAN_POINT('Ctrl Pts',(10.3780036174799,-0.631667147860668,
4.02955738427466));
#59293=CARTESIAN_POINT('Ctrl Pts',(10.4257194535428,-0.366493742769977,
3.48467547975859));
#59294=CARTESIAN_POINT('Ctrl Pts',(10.4734352896056,0.235236505537468,3.41302401146715));
#59295=CARTESIAN_POINT('Ctrl Pts',(10.5211511256685,0.620945451230968,3.88040162523195));
#59296=CARTESIAN_POINT('Ctrl Pts',(10.5688669617313,0.436430634585191,4.45760826680378));
#59297=CARTESIAN_POINT('Ctrl Pts',(10.6165827977941,-0.148865149148659,
4.61458619576145));
#59298=CARTESIAN_POINT('Ctrl Pts',(10.664298633857,-0.597455775834545,4.20718016452724));
#59299=CARTESIAN_POINT('Ctrl Pts',(10.7120144699198,-0.497393570532806,
3.60951740033105));
#59300=CARTESIAN_POINT('Ctrl Pts',(10.7597303059826,0.059432803973042,3.37044081575797));
#59301=CARTESIAN_POINT('Ctrl Pts',(10.8074461420455,0.56168112009921,3.70949811708754));
#59302=CARTESIAN_POINT('Ctrl Pts',(10.8551619781083,0.548129021063343,4.31532776744164));
#59303=CARTESIAN_POINT('Ctrl Pts',(10.9028778141712,0.0312216079359222,
4.63158707701274));
#59304=CARTESIAN_POINT('Ctrl Pts',(10.950593650234,-0.514357088165242,4.36785025554668));
#59305=CARTESIAN_POINT('Ctrl Pts',(10.9983094862968,-0.587593755803164,
3.7663108843084));
#59306=CARTESIAN_POINT('Ctrl Pts',(11.0460253223597,-0.12123403619496,3.37937182377895));
#59307=CARTESIAN_POINT('Ctrl Pts',(11.0937411584225,0.456456764276497,3.56236516706526));
#59308=CARTESIAN_POINT('Ctrl Pts',(11.1414569944854,0.61497629462275,4.14724531131301));
#59309=CARTESIAN_POINT('Ctrl Pts',(11.1891728305482,0.208753630990335,4.59690782052167));
#59310=CARTESIAN_POINT('Ctrl Pts',(11.236888666611,-0.389170704067994,4.49842069353791));
#59311=CARTESIAN_POINT('Ctrl Pts',(11.2846045026739,-0.629713593419695,
3.94222617449013));
#59312=CARTESIAN_POINT('Ctrl Pts',(11.3323203387367,-0.291980800545002,
3.43908624837263));
#59313=CARTESIAN_POINT('Ctrl Pts',(11.3800361747996,0.313882454172263,3.45104205114199));
#59314=CARTESIAN_POINT('Ctrl Pts',(11.4277520108624,0.631502621520784,3.96711438515144));
#59315=CARTESIAN_POINT('Ctrl Pts',(11.4754678469252,0.369204214609944,4.51338608528654));
#59316=CARTESIAN_POINT('Ctrl Pts',(11.5231836829881,-0.232140103514266,
4.58820744384271));
#59317=CARTESIAN_POINT('Ctrl Pts',(11.5708995190509,-0.620306592646703,
4.12286885598323));
#59318=CARTESIAN_POINT('Ctrl Pts',(11.6186153551137,-0.438835993107895,
3.54469790709399));
#59319=CARTESIAN_POINT('Ctrl Pts',(11.6663311911766,0.145624451261577,3.38463787584353));
#59320=CARTESIAN_POINT('Ctrl Pts',(11.7140470272394,0.596355721317347,3.78967435176932));
#59321=CARTESIAN_POINT('Ctrl Pts',(11.7617628633022,0.499444356375145,4.38785610674141));
#59322=CARTESIAN_POINT('Ctrl Pts',(11.8094786993651,-0.0561144459655822,
4.62986363095956));
#59323=CARTESIAN_POINT('Ctrl Pts',(11.8571945354279,-0.560142489144378,
4.29345769116983));
#59324=CARTESIAN_POINT('Ctrl Pts',(11.9049103714908,-0.549783065641843,
3.68756503815187));
#59325=CARTESIAN_POINT('Ctrl Pts',(11.9526262075536,-0.0345493934605723,
3.36858621802886));
#59326=CARTESIAN_POINT('Ctrl Pts',(12.0003420436164,0.512411518346294,3.62944438943981));
#59327=CARTESIAN_POINT('Ctrl Pts',(12.0480578796793,0.588817048391095,4.23058947975914));
#59328=CARTESIAN_POINT('Ctrl Pts',(12.0957737157421,0.1245028227835,4.61998070274044));
#59329=CARTESIAN_POINT('Ctrl Pts',(12.1434895518049,-0.454144260708352,
4.44003410676589));
#59330=CARTESIAN_POINT('Ctrl Pts',(12.1912053878678,-0.615743681684068,
3.85599741975318));
#59331=CARTESIAN_POINT('Ctrl Pts',(12.2389212239306,-0.211896205334937,
3.40420051794564));
#59332=CARTESIAN_POINT('Ctrl Pts',(12.2866370599935,0.386538816815474,3.49953544806202));
#59333=CARTESIAN_POINT('Ctrl Pts',(12.3343528960563,0.63000929582004,4.05445467686));
#59334=CARTESIAN_POINT('Ctrl Pts',(12.3820687321191,0.294932544534008,4.55936733800455));
#59335=CARTESIAN_POINT('Ctrl Pts',(12.429784568182,-0.310985300518122,4.55060436568669));
#59336=CARTESIAN_POINT('Ctrl Pts',(12.4775004042448,-0.631320558980542,
4.0362129322216));
#59337=CARTESIAN_POINT('Ctrl Pts',(12.5252162403077,-0.371904434015698,
3.48856660588983));
#59338=CARTESIAN_POINT('Ctrl Pts',(12.5729320763705,0.229037255191033,3.41057743478371));
#59339=CARTESIAN_POINT('Ctrl Pts',(12.6206479124333,0.619650508764677,3.87386407474765));
#59340=CARTESIAN_POINT('Ctrl Pts',(12.6683637484962,0.44122916559109,4.4529832757215));
#59341=CARTESIAN_POINT('Ctrl Pts',(12.716079584559,-0.142379709528176,4.61612096455669));
#59342=CARTESIAN_POINT('Ctrl Pts',(12.7637954206218,-0.595239106594286,
4.21346529139986));
#59343=CARTESIAN_POINT('Ctrl Pts',(12.8115112566847,-0.501481273143938,
3.61478115656484));
#59344=CARTESIAN_POINT('Ctrl Pts',(12.8592270927475,0.0527945297157079,
3.36984941301012));
#59345=CARTESIAN_POINT('Ctrl Pts',(12.9069429288104,0.558588303589165,3.70359464960132));
#59346=CARTESIAN_POINT('Ctrl Pts',(12.9546587648732,0.551421843290858,4.30953348024615));
#59347=CARTESIAN_POINT('Ctrl Pts',(13.002374600936,0.0378762195828894,4.63122295319618));
#59348=CARTESIAN_POINT('Ctrl Pts',(13.0500904369989,-0.510451719368595,
4.37325067561256));
#59349=CARTESIAN_POINT('Ctrl Pts',(13.0978062730617,-0.590023990114621,
3.77251655941407));
#59350=CARTESIAN_POINT('Ctrl Pts',(13.1455221091246,-0.127768152052348,
3.38068398698829));
#59351=CARTESIAN_POINT('Ctrl Pts',(13.1932379451874,0.451819146005312,3.55757883871291));
#59352=CARTESIAN_POINT('Ctrl Pts',(13.2409537812502,0.616493970155128,4.14075585037205));
#59353=CARTESIAN_POINT('Ctrl Pts',(13.2886696173131,0.215032895532453,4.59467459882739));
#59354=CARTESIAN_POINT('Ctrl Pts',(13.3363854533759,-0.383896195764066,
4.50249451293469));
#59355=CARTESIAN_POINT('Ctrl Pts',(13.3841012894387,-0.630287503488198,
3.94886598394213));
#59356=CARTESIAN_POINT('Ctrl Pts',(13.4318171255016,-0.297876098539286,
3.4421946086935));
#59357=CARTESIAN_POINT('Ctrl Pts',(13.4795329615644,0.308079511111167,3.44776450722078));
#59358=CARTESIAN_POINT('Ctrl Pts',(13.5272487976272,0.631120965295637,3.96046075600252));
#59359=CARTESIAN_POINT('Ctrl Pts',(13.5749646336901,0.374594326004835,4.50946650093658));
#59360=CARTESIAN_POINT('Ctrl Pts',(13.6226804697529,-0.225928046730791,
4.59062131891086));
#59361=CARTESIAN_POINT('Ctrl Pts',(13.6703963058158,-0.618977217803688,
4.12939949185215));
#59362=CARTESIAN_POINT('Ctrl Pts',(13.7181121418786,-0.443610085578744,
3.54934812035851));
#59363=CARTESIAN_POINT('Ctrl Pts',(13.7658279779415,0.139131014051702,3.38313730411011));
#59364=CARTESIAN_POINT('Ctrl Pts',(13.8135438140043,0.594105962672646,3.78340099315002));
#59365=CARTESIAN_POINT('Ctrl Pts',(13.8612596500671,0.503504264276035,4.38257088298437));
#59366=CARTESIAN_POINT('Ctrl Pts',(13.90897548613,-0.0494731474142026,4.63042004436449));
#59367=CARTESIAN_POINT('Ctrl Pts',(13.9566913221928,-0.557018606591754,
4.29934477874546));
#59368=CARTESIAN_POINT('Ctrl Pts',(14.0044071582556,-0.553045308503159,
3.69337659679301));
#59369=CARTESIAN_POINT('Ctrl Pts',(14.0521229943185,-0.0412019939202257,
3.36898540401303));
#59370=CARTESIAN_POINT('Ctrl Pts',(14.0998388303813,0.50847774565382,3.62406462413548));
#59371=CARTESIAN_POINT('Ctrl Pts',(14.1475546664442,0.591214547458171,4.22437108442359));
#59372=CARTESIAN_POINT('Ctrl Pts',(14.195270502507,0.131029933326566,4.61863412549262));
#59373=CARTESIAN_POINT('Ctrl Pts',(14.2429863385698,-0.4494814847335,4.44479593021223));
#59374=CARTESIAN_POINT('Ctrl Pts',(14.2907021746327,-0.617227139201166,
3.86249478815283));
#59375=CARTESIAN_POINT('Ctrl Pts',(14.3384180106955,-0.218163614480107,
3.40646679792233));
#59376=CARTESIAN_POINT('Ctrl Pts',(14.3861338467583,0.381242914296727,3.49548947984197));
#59377=CARTESIAN_POINT('Ctrl Pts',(14.4338496828212,0.630548208698617,4.0478119353149));
#59378=CARTESIAN_POINT('Ctrl Pts',(14.481565518884,0.300811380821271,4.55622795490698));
#59379=CARTESIAN_POINT('Ctrl Pts',(14.5292813549469,-0.305165166642291,
4.55385128484077));
#59380=CARTESIAN_POINT('Ctrl Pts',(14.5769971910097,-0.630903846008588,
4.04286445780787));
#59381=CARTESIAN_POINT('Ctrl Pts',(14.6247130270726,-0.37727381588172,3.49251453961553));
#59382=CARTESIAN_POINT('Ctrl Pts',(14.6724288631354,0.222812564473163,3.40819632836178));
#59383=CARTESIAN_POINT('Ctrl Pts',(14.7201446991982,0.618286738460357,3.86734053484336));
#59384=CARTESIAN_POINT('Ctrl Pts',(14.7678605352611,0.44597868695508,4.44830796940654));
#59385=CARTESIAN_POINT('Ctrl Pts',(14.8155763713239,-0.135878455045208,
4.6175872975589));
#59386=CARTESIAN_POINT('Ctrl Pts',(14.8632922073867,-0.592956321018707,
4.2197267075609));
#59387=CARTESIAN_POINT('Ctrl Pts',(14.9110080434496,-0.505513273594975,
3.62008770107973));
#59388=CARTESIAN_POINT('Ctrl Pts',(14.9587238795124,0.0461503912925444,
3.36932800439917));
#59389=CARTESIAN_POINT('Ctrl Pts',(15.0064397155752,0.555433441741075,3.69772410541485));
#59390=CARTESIAN_POINT('Ctrl Pts',(15.0541555516381,0.554653416196733,4.30370481154056));
#59391=CARTESIAN_POINT('Ctrl Pts',(15.1018713877009,0.0445266241191229,
4.63078871612938));
#59392=CARTESIAN_POINT('Ctrl Pts',(15.1495872237638,-0.506489652017253,
4.37860963676461));
#59393=CARTESIAN_POINT('Ctrl Pts',(15.1973030598266,-0.592388687361149,
3.77874750230084));
#59394=CARTESIAN_POINT('Ctrl Pts',(15.2450188958894,-0.134288076029725,
3.38206494088146));
#59395=CARTESIAN_POINT('Ctrl Pts',(15.2927347319523,0.447131341807447,3.5528416524037));
#59396=CARTESIAN_POINT('Ctrl Pts',(15.3404505680151,0.617943168462805,4.13425075493917));
#59397=CARTESIAN_POINT('Ctrl Pts',(15.3881664040779,0.221288275240951,4.59237532350063));
#59398=CARTESIAN_POINT('Ctrl Pts',(15.4358822401408,-0.378579046092452,
4.50651251762549));
#59399=CARTESIAN_POINT('Ctrl Pts',(15.4835980762036,-0.630791404211772,
3.95551147311801));
#59400=CARTESIAN_POINT('Ctrl Pts',(15.5313139122665,-0.303738309870084,
3.44536492739022));
#59401=CARTESIAN_POINT('Ctrl Pts',(15.5790297483293,0.302242348039936,3.44454830299756));
#59402=CARTESIAN_POINT('Ctrl Pts',(15.6267455843921,0.630669207148581,3.95381151868517));
#59403=CARTESIAN_POINT('Ctrl Pts',(15.674461420455,0.379942829239589,4.50549032746533));
#59404=CARTESIAN_POINT('Ctrl Pts',(15.7221772565178,-0.219690894932002,
4.59296959056563));
#59405=CARTESIAN_POINT('Ctrl Pts',(15.7698930925806,-0.617579089908608,
4.13591575463957));
#59406=CARTESIAN_POINT('Ctrl Pts',(15.8176089286435,-0.448334903946386,
3.5540483898953));
#59407=CARTESIAN_POINT('Ctrl Pts',(15.8653247647063,0.13262212282903,3.3817052505577));
#59408=CARTESIAN_POINT('Ctrl Pts',(15.9130406007692,0.591790213556878,3.77715169332057));
#59409=CARTESIAN_POINT('Ctrl Pts',(15.960756436832,0.507508245312566,4.37724316506909));
#59410=CARTESIAN_POINT('Ctrl Pts',(16.0084722728949,-0.0428263536203826,
4.63090643370248));
#59411=CARTESIAN_POINT('Ctrl Pts',(16.0561881089577,-0.553832853055588,
4.30519861652357));
#59412=CARTESIAN_POINT('Ctrl Pts',(16.1039039450205,-0.556246121716014,
3.69922221370673));
#59413=CARTESIAN_POINT('Ctrl Pts',(16.1516197810833,-0.0478500178579074,
3.36945468010413));
#59414=CARTESIAN_POINT('Ctrl Pts',(16.1993356171462,0.504487493666278,3.61872661594874));
#59415=CARTESIAN_POINT('Ctrl Pts',(16.247051453209,0.593546377218863,4.21812776701271));
#59416=CARTESIAN_POINT('Ctrl Pts',(16.2947672892719,0.137542489686435,4.61721883330181));
#59417=CARTESIAN_POINT('Ctrl Pts',(16.3424831253347,-0.444768782488292,
4.44950834783736));
#59418=CARTESIAN_POINT('Ctrl Pts',(16.3901989613976,-0.618642038056621,
3.86900742997889));
#59419=CARTESIAN_POINT('Ctrl Pts',(16.4379147974604,-0.224406791046256,
3.40879900475058));
#59420=CARTESIAN_POINT('Ctrl Pts',(16.4856306335233,0.375904665124208,3.49149955025639));
#59421=CARTESIAN_POINT('Ctrl Pts',(16.533346469586,0.631017083274371,4.04116388304691));
#59422=CARTESIAN_POINT('Ctrl Pts',(16.5810623056489,0.306656804407812,4.55302678864769));
#59423=CARTESIAN_POINT('Ctrl Pts',(16.6287781417117,-0.29931113646787,4.55703668482238));
#59424=CARTESIAN_POINT('Ctrl Pts',(16.6764939777746,-0.630417055231307,
4.04951122221356));
#59425=CARTESIAN_POINT('Ctrl Pts',(16.7242098138374,-0.382601291962586,
3.49651884241796));
#59426=CARTESIAN_POINT('Ctrl Pts',(16.7719256499003,0.216563124792967,3.40588095668335));
#59427=CARTESIAN_POINT('Ctrl Pts',(16.8196414859631,0.616854291799135,3.86083173012294));
#59428=CARTESIAN_POINT('Ctrl Pts',(16.8673573220259,0.450678671122871,4.44358286716973));
#59429=CARTESIAN_POINT('Ctrl Pts',(16.9150731580887,-0.129362107828251,
4.61898503189482));
#59430=CARTESIAN_POINT('Ctrl Pts',(16.9627889941516,-0.590607672668797,
4.22596371752193));
#59431=CARTESIAN_POINT('Ctrl Pts',(17.0105048302144,-0.509489124030439,
3.62543644444997));
#59432=CARTESIAN_POINT('Ctrl Pts',(17.0582206662773,0.0395011267029154,
3.3688766478407));
#59433=CARTESIAN_POINT('Ctrl Pts',(17.1059365023401,0.552216884982031,3.69188713660034));
#59434=CARTESIAN_POINT('Ctrl Pts',(17.153652338403,0.557823380833178,4.29784240874569));
#59435=CARTESIAN_POINT('Ctrl Pts',(17.2013681744658,0.0511720828492506,
4.63028441404532));
#59436=CARTESIAN_POINT('Ctrl Pts',(17.2490840105287,-0.502471326198846,
4.38392654375487));
#59437=CARTESIAN_POINT('Ctrl Pts',(17.2967998465914,-0.594687584883411,
3.78500302086511));
#59438=CARTESIAN_POINT('Ctrl Pts',(17.3445156826543,-0.140793083924855,
3.38351453206865));
#59439=CARTESIAN_POINT('Ctrl Pts',(17.3922315187171,0.442393872381948,3.5481541343218));
#59440=CARTESIAN_POINT('Ctrl Pts',(17.43994735478,0.61932372857571,4.1277307475695));
#59441=CARTESIAN_POINT('Ctrl Pts',(17.4876631908428,0.227519075297936,4.590010249934));
#59442=CARTESIAN_POINT('Ctrl Pts',(17.5353790269057,-0.373219845656906,
4.51047426130944));
#59443=CARTESIAN_POINT('Ctrl Pts',(17.5830948629685,-0.631225239619516,
3.96216190386831));
#59444=CARTESIAN_POINT('Ctrl Pts',(17.6308106990313,-0.309566783390781,
3.44859685231885));
#59445=CARTESIAN_POINT('Ctrl Pts',(17.6785265350942,0.29637161332294,3.44139379571298));
#59446=CARTESIAN_POINT('Ctrl Pts',(17.726242371157,0.630147397258769,3.94716741176515));
#59447=CARTESIAN_POINT('Ctrl Pts',(17.7739582072198,0.385249130227842,4.50145800652724));
#59448=CARTESIAN_POINT('Ctrl Pts',(17.8216740432827,-0.213429340911116,
4.59525199797214));
#59449=CARTESIAN_POINT('Ctrl Pts',(17.8693898793456,-0.616112364258878,
4.14241692054995));
#59450=CARTESIAN_POINT('Ctrl Pts',(17.9171057154084,-0.453009923400427,
3.55879819362073));
#59451=CARTESIAN_POINT('Ctrl Pts',(17.9648215514712,0.126098500570276,3.38034187425201));
#59452=CARTESIAN_POINT('Ctrl Pts',(18.012537387534,0.589408731192455,3.77092714642348));
#59453=CARTESIAN_POINT('Ctrl Pts',(18.0602532235969,0.511455854741549,4.3718735447732));
#59454=CARTESIAN_POINT('Ctrl Pts',(18.1079690596597,-0.0361748028784226,
4.6313227449477));
#59455=CARTESIAN_POINT('Ctrl Pts',(18.1556848957226,-0.55058558239424,4.31101855428765));
#59456=CARTESIAN_POINT('Ctrl Pts',(18.2034007317854,-0.559385149749292,
3.70510123958967));
#59457=CARTESIAN_POINT('Ctrl Pts',(18.2511165678482,-0.0544927268426965,
3.36999399417717));
#59458=CARTESIAN_POINT('Ctrl Pts',(18.2988324039111,0.500441205601937,3.6134309578002));
#59459=CARTESIAN_POINT('Ctrl Pts',(18.3465482399739,0.595812278664582,4.21186022100458));
#59460=CARTESIAN_POINT('Ctrl Pts',(18.3942640760367,0.144039768479226,4.61573498337195));
#59461=CARTESIAN_POINT('Ctrl Pts',(18.4419799120996,-0.440006677437314,
4.4541708362083));
#59462=CARTESIAN_POINT('Ctrl Pts',(18.4896957481624,-0.619988221090196,
3.87553462183804));
#59463=CARTESIAN_POINT('Ctrl Pts',(18.5374115842252,-0.230625041570952,
3.41119687937986));
#59464=CARTESIAN_POINT('Ctrl Pts',(18.5851274202881,0.370524662245315,3.48756610248778));
#59465=CARTESIAN_POINT('Ctrl Pts',(18.6328432563509,0.631415867466904,4.03451125849008));
#59466=CARTESIAN_POINT('Ctrl Pts',(18.6805590924138,0.31246816601179,4.54976419479712));
#59467=CARTESIAN_POINT('Ctrl Pts',(18.7282749284766,-0.293423860232864,
4.56016021181225));
#59468=CARTESIAN_POINT('Ctrl Pts',(18.7759907645394,-0.629860240718928,
4.05615248714788));
#59469=CARTESIAN_POINT('Ctrl Pts',(18.8237066006023,-0.387886270507855,
3.50057906951772));
#59470=CARTESIAN_POINT('Ctrl Pts',(18.8714224366651,0.210289630309142,3.40363157692976));
#59471=CARTESIAN_POINT('Ctrl Pts',(18.919138272728,0.615353327889266,3.85433838355196));
#59472=CARTESIAN_POINT('Ctrl Pts',(18.9668541087908,0.455328596044662,4.43880849385601));
#59473=CARTESIAN_POINT('Ctrl Pts',(19.0145699448537,-0.122831391686292,
4.62031401230505));
#59474=CARTESIAN_POINT('Ctrl Pts',(19.0622857809165,-0.588193422413584,
4.2321756285162));
#59475=CARTESIAN_POINT('Ctrl Pts',(19.1100016169793,-0.513408382846255,
3.63082679254236));
#59476=CARTESIAN_POINT('Ctrl Pts',(19.1577174530421,0.0328474745430158,
3.36849539350727));
#59477=CARTESIAN_POINT('Ctrl Pts',(19.205433289105,0.548938990540088,3.68608439142882));
#59478=CARTESIAN_POINT('Ctrl Pts',(19.2531491251678,0.560931385193363,4.2919469231649));
#59479=CARTESIAN_POINT('Ctrl Pts',(19.3008649612307,0.0578118574426247,
4.62971010270368));
#59480=CARTESIAN_POINT('Ctrl Pts',(19.3485807972935,-0.498397187901359,
4.38920080648958));
#59481=CARTESIAN_POINT('Ctrl Pts',(19.3962966333563,-0.596920427988996,
3.79128241936144));
#59482=CARTESIAN_POINT('Ctrl Pts',(19.4440124694192,-0.147282451949449,
3.38503260125846));
#59483=CARTESIAN_POINT('Ctrl Pts',(19.491728305482,0.437607261597584,3.54351680188243));
#59484=CARTESIAN_POINT('Ctrl Pts',(19.5394441415449,0.620635501579114,4.12119655861503));
#59485=CARTESIAN_POINT('Ctrl Pts',(19.5871599776077,0.233724595248439,4.58757962923414));
#59486=CARTESIAN_POINT('Ctrl Pts',(19.6348758136705,-0.367819173932889,
4.51437932582758));
#59487=CARTESIAN_POINT('Ctrl Pts',(19.6825916497334,-0.631588991354928,
3.96881649615688));
#59488=CARTESIAN_POINT('Ctrl Pts',(19.7303074857962,-0.315360815373557,
3.4518901025469));
#59489=CARTESIAN_POINT('Ctrl Pts',(19.778023321859,0.290467852693633,3.43830118837221));
#59490=CARTESIAN_POINT('Ctrl Pts',(19.8257391579219,0.629555794415491,3.94052945152661));
#59491=CARTESIAN_POINT('Ctrl Pts',(19.8734549939847,0.390512260364629,4.49736946054851));
#59492=CARTESIAN_POINT('Ctrl Pts',(19.9211708300476,-0.207143364153331,
4.59746927979605));
#59493=CARTESIAN_POINT('Ctrl Pts',(19.9688866661104,-0.61457855576007,4.14890039401813));
#59494=CARTESIAN_POINT('Ctrl Pts',(20.0166025021732,-0.45763207183192,3.5636005413983));
#59495=CARTESIAN_POINT('Ctrl Pts',(20.0643183382361,0.119556051622903,3.37904064719698));
#59496=CARTESIAN_POINT('Ctrl Pts',(20.1120341742989,0.586970881772813,3.7647406560623));
#59497=CARTESIAN_POINT('Ctrl Pts',(20.1597500103618,0.515329468049299,4.36643880344312));
#59498=CARTESIAN_POINT('Ctrl Pts',(20.2074658464246,-0.029486781418557,
4.63171390504007));
#59499=CARTESIAN_POINT('Ctrl Pts',(20.2551816824874,-0.547338447674763,
4.31671898245684));
#59500=CARTESIAN_POINT('Ctrl Pts',(20.3028975185503,-0.562346186529673,
3.71117381387971));
#59501=CARTESIAN_POINT('Ctrl Pts',(20.3506133546131,-0.0613491664957494,
3.37029669484294));
#59502=CARTESIAN_POINT('Ctrl Pts',(20.398329190676,0.496762641213801,3.60878154740643));
#59503=CARTESIAN_POINT('Ctrl Pts',(20.4380923873949,0.580417208789547,4.10498761157686));
#59504=CARTESIAN_POINT('Ctrl Pts',(20.4699029447702,0.374745574175769,4.41137453781958));
#59505=CARTESIAN_POINT('Ctrl Pts',(20.4937608628016,0.13332385162888,4.54159545884303));
#59506=CARTESIAN_POINT('Ctrl Pts',(20.517618780833,-0.143293564288956,4.53872805560682));
#59507=CARTESIAN_POINT('Ctrl Pts',(20.5414766988645,-0.38346854803195,4.40448715909776));
#59508=CARTESIAN_POINT('Ctrl Pts',(20.5653346168959,-0.530621786340447,
4.17114564603877));
#59509=CARTESIAN_POINT('Ctrl Pts',(20.5891925349273,-0.547627617499454,
3.89605651468078));
#59510=CARTESIAN_POINT('Ctrl Pts',(20.6130504529587,-0.430933317123153,
3.64633026976583));
#59511=CARTESIAN_POINT('Ctrl Pts',(20.6369083709901,-0.208752997660079,
3.48311457674551));
#59512=CARTESIAN_POINT('Ctrl Pts',(20.6607662890215,0.0644142843662171,
3.4462762657402));
#59513=CARTESIAN_POINT('Ctrl Pts',(20.684624207053,0.321861676845817,3.54484653226013));
#59514=CARTESIAN_POINT('Ctrl Pts',(20.7084821250844,0.500588620804837,3.75470996102831));
#59515=CARTESIAN_POINT('Ctrl Pts',(20.7323400431158,0.556916750317041,4.02455574134091));
#59516=CARTESIAN_POINT('Ctrl Pts',(20.7561979611472,0.47705893600668,4.28839577951569));
#59517=CARTESIAN_POINT('Ctrl Pts',(20.7800558791787,0.280549668164313,4.48171582646486));
#59518=CARTESIAN_POINT('Ctrl Pts',(20.8039137972101,0.0154370662995263,
4.55724289713534));
#59519=CARTESIAN_POINT('Ctrl Pts',(20.8277717152415,-0.253449631274377,
4.49650907789895));
#59520=CARTESIAN_POINT('Ctrl Pts',(20.8516296332729,-0.460361354274216,
4.31436517051053));
#59521=CARTESIAN_POINT('Ctrl Pts',(20.8754875513043,-0.554701993332711,
4.05535046556385));
#59522=CARTESIAN_POINT('Ctrl Pts',(20.8993454693358,-0.513402987365846,
3.78280103771366));
#59523=CARTESIAN_POINT('Ctrl Pts',(20.9232033873672,-0.346562912086465,
3.56336268648205));
#59524=CARTESIAN_POINT('Ctrl Pts',(20.9470613053986,-0.0949787932613798,
3.45069404477467));
#59525=CARTESIAN_POINT('Ctrl Pts',(20.97091922343,0.179830242856268,3.47234567582879));
#59526=CARTESIAN_POINT('Ctrl Pts',(20.9947771414614,0.410665878084123,3.62302316008453));
#59527=CARTESIAN_POINT('Ctrl Pts',(21.0186350594928,0.541082524061315,3.86588175144064));
#59528=CARTESIAN_POINT('Ctrl Pts',(21.0424929775243,0.539189751860116,4.14153590729571));
#59529=CARTESIAN_POINT('Ctrl Pts',(21.0663508955557,0.405450399288564,4.38258067876424));
#59530=CARTESIAN_POINT('Ctrl Pts',(21.0902088135871,0.172567379211795,4.53007405282339));
#59531=CARTESIAN_POINT('Ctrl Pts',(21.1140667316185,-0.102513065388571,
4.54794988212627));
#59532=CARTESIAN_POINT('Ctrl Pts',(21.1379246496499,-0.352526273278862,
4.43183703934844));
#59533=CARTESIAN_POINT('Ctrl Pts',(21.1617825676814,-0.516337204635697,
4.21012827746935));
#59534=CARTESIAN_POINT('Ctrl Pts',(21.1856404857128,-0.553889624765765,
3.93703742795684));
#59535=CARTESIAN_POINT('Ctrl Pts',(21.2094984037442,-0.456000943963824,
3.67934264238169));
#59536=CARTESIAN_POINT('Ctrl Pts',(21.2333563217756,-0.246607611160355,
3.50005731527167));
#59537=CARTESIAN_POINT('Ctrl Pts',(21.257214239807,0.0230880000356606,3.44302159274494));
#59538=CARTESIAN_POINT('Ctrl Pts',(21.2810721578385,0.287137966314551,3.52218226257825));
#59539=CARTESIAN_POINT('Ctrl Pts',(21.3049300758698,0.480974878350452,3.71818238470557));
#59540=CARTESIAN_POINT('Ctrl Pts',(21.3287879939013,0.557200331135927,3.9830945903298));
#59541=CARTESIAN_POINT('Ctrl Pts',(21.3526459119327,0.497175125126959,4.25214062911267));
#59542=CARTESIAN_POINT('Ctrl Pts',(21.3765038299641,0.31557705824565,4.45953141590455));
#59543=CARTESIAN_POINT('Ctrl Pts',(21.4003617479955,0.0568118044769688,
4.55455425412338));
#59544=CARTESIAN_POINT('Ctrl Pts',(21.424219666027,-0.215845483008899,4.51397347145443));
#59545=CARTESIAN_POINT('Ctrl Pts',(21.4480775840584,-0.435722670386138,
4.34771217465862));
#59546=CARTESIAN_POINT('Ctrl Pts',(21.4719355020898,-0.549053796006754,
4.0964257796693));
#59547=CARTESIAN_POINT('Ctrl Pts',(21.4957934201212,-0.528126312578589,
3.82156065496534));
#59548=CARTESIAN_POINT('Ctrl Pts',(21.5196513381527,-0.378057559853047,
3.59032881071252));
#59549=CARTESIAN_POINT('Ctrl Pts',(21.543509256184,-0.135543435662257,3.45927273145963));
#59550=CARTESIAN_POINT('Ctrl Pts',(21.5673671742155,0.14011475067701,3.46043919847993));
#59551=CARTESIAN_POINT('Ctrl Pts',(21.5912250922469,0.381511063826562,3.59354297881304));
#59552=CARTESIAN_POINT('Ctrl Pts',(21.6150830102783,0.529617529717794,3.8260365724933));
#59553=CARTESIAN_POINT('Ctrl Pts',(21.6389409283097,0.548218083101175,4.10106896286759));
#59554=CARTESIAN_POINT('Ctrl Pts',(21.6627988463412,0.432764382005563,4.35138723875747));
#59555=CARTESIAN_POINT('Ctrl Pts',(21.6866567643726,0.211488001244504,4.51578176317496));
#59556=CARTESIAN_POINT('Ctrl Pts',(21.710514682404,-0.0615029566383307,
4.55405359688301));
#59557=CARTESIAN_POINT('Ctrl Pts',(21.7343726004354,-0.319454766316188,
4.4568442340362));
#59558=CARTESIAN_POINT('Ctrl Pts',(21.7582305184669,-0.499291183856609,
4.24792401178047));
#59559=CARTESIAN_POINT('Ctrl Pts',(21.7820884364982,-0.557037306525311,
3.97837961532992));
#59560=CARTESIAN_POINT('Ctrl Pts',(21.8059463545297,-0.478572634356998,
3.71412199185867));
#59561=CARTESIAN_POINT('Ctrl Pts',(21.8298042725611,-0.283083917031579,
3.51976932853855));
#59562=CARTESIAN_POINT('Ctrl Pts',(21.8536621905926,-0.018373470940863,
3.44284614561161));
#59563=CARTESIAN_POINT('Ctrl Pts',(21.8775201086239,0.250829789278194,3.5021622566489));
#59564=CARTESIAN_POINT('Ctrl Pts',(21.9013780266554,0.458698333552465,3.68321325676341));
#59565=CARTESIAN_POINT('Ctrl Pts',(21.9252359446868,0.55440264058141,3.94172724469688));
#59566=CARTESIAN_POINT('Ctrl Pts',(21.9490938627182,0.514540400363477,4.21449050861997));
#59567=CARTESIAN_POINT('Ctrl Pts',(21.9729517807496,0.348859016457567,4.4348050005813));
#59568=CARTESIAN_POINT('Ctrl Pts',(21.996809698781,0.0978721002989983,4.54879782605011));
#59569=CARTESIAN_POINT('Ctrl Pts',(22.0206676168125,-0.177047210365213,
4.52859463409701));
#59570=CARTESIAN_POINT('Ctrl Pts',(22.0445255348439,-0.408673655425848,
4.3791356554785));
#59571=CARTESIAN_POINT('Ctrl Pts',(22.0683834528753,-0.540368259688198,
4.13696768164748));
#59572=CARTESIAN_POINT('Ctrl Pts',(22.0922413709067,-0.53992810512055,3.86130737872913));
#59573=CARTESIAN_POINT('Ctrl Pts',(22.1160992889381,-0.407460821505317,
3.61956119962225));
#59574=CARTESIAN_POINT('Ctrl Pts',(22.1399572069695,-0.175358268020808,
3.47084267015335));
#59575=CARTESIAN_POINT('Ctrl Pts',(22.163815125001,0.0996241586556461,3.45151752178681));
#59576=CARTESIAN_POINT('Ctrl Pts',(22.1876730430324,0.350245764837839,3.56631127970877));
#59577=CARTESIAN_POINT('Ctrl Pts',(22.2115309610638,0.51522274100534,3.78715374318048));
#59578=CARTESIAN_POINT('Ctrl Pts',(22.2353888790952,0.554213722627899,4.06004291426965));
#59579=CARTESIAN_POINT('Ctrl Pts',(22.2592467971266,0.457684352558003,4.31824995726588));
#59580=CARTESIAN_POINT('Ctrl Pts',(22.2831047151581,0.249238691275201,4.49863621678958));
#59581=CARTESIAN_POINT('Ctrl Pts',(22.3069626331895,-0.0201526192614011,
4.55709233866662));
#59582=CARTESIAN_POINT('Ctrl Pts',(22.3308205512209,-0.284616065231974,
4.47932420896945));
#59583=CARTESIAN_POINT('Ctrl Pts',(22.3546784692523,-0.479483130864429,
4.28434825342259));
#59584=CARTESIAN_POINT('Ctrl Pts',(22.3785363872838,-0.557103509392546,
4.01984140485232));
#59585=CARTESIAN_POINT('Ctrl Pts',(22.4023943053151,-0.498496906094933,
3.75048279151596));
#59586=CARTESIAN_POINT('Ctrl Pts',(22.4262522233466,-0.317994227800984,
3.542137933897));
#59587=CARTESIAN_POINT('Ctrl Pts',(22.450110141378,-0.0597333038680864,
3.44575282046209));
#59588=CARTESIAN_POINT('Ctrl Pts',(22.4739680594094,0.213134049493302,3.48489624527193));
#59589=CARTESIAN_POINT('Ctrl Pts',(22.4978259774408,0.433884304103661,3.6499965589521));
#59590=CARTESIAN_POINT('Ctrl Pts',(22.5216838954723,0.548538061567711,3.90068226732924));
#59591=CARTESIAN_POINT('Ctrl Pts',(22.5455418135037,0.529059256943919,4.17565382996358));
#59592=CARTESIAN_POINT('Ctrl Pts',(22.5693997315351,0.380211173855379,4.40767331583304));
#59593=CARTESIAN_POINT('Ctrl Pts',(22.5932576495665,0.138390873272415,4.54000544018811));
#59594=CARTESIAN_POINT('Ctrl Pts',(22.6171155675979,-0.137269333605106,
4.54029177230974));
#59595=CARTESIAN_POINT('Ctrl Pts',(22.6409734856293,-0.379364264814148,
4.40846158181013));
#59596=CARTESIAN_POINT('Ctrl Pts',(22.6648314036608,-0.528692759685234,
4.17675229015827));
#59597=CARTESIAN_POINT('Ctrl Pts',(22.6886893216921,-0.54874438127821,3.90182058373076));
#59598=CARTESIAN_POINT('Ctrl Pts',(22.7125472397236,-0.434607562942265,
3.65089956353622));
#59599=CARTESIAN_POINT('Ctrl Pts',(22.736405157755,-0.214207731687487,3.48533716867003));
#59600=CARTESIAN_POINT('Ctrl Pts',(22.7602630757864,0.0585913648593265,
3.44563509732658));
#59601=CARTESIAN_POINT('Ctrl Pts',(22.7841209938179,0.31702578011682,3.5414689143437));
#59602=CARTESIAN_POINT('Ctrl Pts',(22.8079789118493,0.498012898707086,3.74946820019106));
#59603=CARTESIAN_POINT('Ctrl Pts',(22.8238841905369,0.537376264140017,3.92891364167179));
#59604=CARTESIAN_POINT('Ctrl Pts',(22.8318368298807,0.534391234777113,4.01792167950194));
#59605=CARTESIAN_POINT('Ctrl Pts',(3.99999999999998,0.254694598474614,4.53673594206822));
#59606=CARTESIAN_POINT('Ctrl Pts',(4.00795263934379,0.165296026927429,4.57915779516171));
#59607=CARTESIAN_POINT('Ctrl Pts',(4.0238579180314,-0.0350146299391769,
4.61842892627033));
#59608=CARTESIAN_POINT('Ctrl Pts',(4.04771583606282,-0.327086058023631,
4.5259865276721));
#59609=CARTESIAN_POINT('Ctrl Pts',(4.07157375409423,-0.539100294705402,
4.30498302442502));
#59610=CARTESIAN_POINT('Ctrl Pts',(4.09543167212566,-0.619328256935644,
4.00937412827253));
#59611=CARTESIAN_POINT('Ctrl Pts',(4.11928959015708,-0.548093442686671,
3.71148804617917));
#59612=CARTESIAN_POINT('Ctrl Pts',(4.1431475081885,-0.342845496867427,3.48414304986991));
#59613=CARTESIAN_POINT('Ctrl Pts',(4.16700542621991,-0.0537568536316998,
3.38294333505492));
#59614=CARTESIAN_POINT('Ctrl Pts',(4.19086334425134,0.248473820944083,3.43262855616194));
#59615=CARTESIAN_POINT('Ctrl Pts',(4.21472126228276,0.489947458130694,3.62105272953394));
#59616=CARTESIAN_POINT('Ctrl Pts',(4.23857918031417,0.611614759069978,3.90213920826301));
#59617=CARTESIAN_POINT('Ctrl Pts',(4.26243709834559,0.583726034554802,4.20715564703007));
#59618=CARTESIAN_POINT('Ctrl Pts',(4.28629501637702,0.413100159498109,4.46151671210738));
#59619=CARTESIAN_POINT('Ctrl Pts',(4.31015293440843,0.141460167127662,4.60302446238992));
#59620=CARTESIAN_POINT('Ctrl Pts',(4.33401085243986,-0.164770755236008,
4.59707625642582));
#59621=CARTESIAN_POINT('Ctrl Pts',(4.35786877047126,-0.430710704813839,
4.44512666775742));
#59622=CARTESIAN_POINT('Ctrl Pts',(4.38172668850269,-0.59133017320549,4.18433147003372));
#59623=CARTESIAN_POINT('Ctrl Pts',(4.40558460653411,-0.607353296958831,
3.87846221409715));
#59624=CARTESIAN_POINT('Ctrl Pts',(4.42944252456553,-0.474862000813124,
3.60231225357117));
#59625=CARTESIAN_POINT('Ctrl Pts',(4.45330044259694,-0.226254007744579,
3.42340778189093));
#59626=CARTESIAN_POINT('Ctrl Pts',(4.47715836062837,0.0776792518003291,
3.38549581251083));
#59627=CARTESIAN_POINT('Ctrl Pts',(4.50101627865978,0.362617819109035,3.49784685630402));
#59628=CARTESIAN_POINT('Ctrl Pts',(4.5248741966912,0.558886451727075,3.73298802180378));
#59629=CARTESIAN_POINT('Ctrl Pts',(4.54873211472262,0.618492123352341,4.03342088939383));
#59630=CARTESIAN_POINT('Ctrl Pts',(4.57259003275404,0.5268596233165,4.32568143907503));
#59631=CARTESIAN_POINT('Ctrl Pts',(4.59644795078546,0.306395594072305,4.5383040055633));
#59632=CARTESIAN_POINT('Ctrl Pts',(4.62030586881688,0.0110094959969652,
4.61929657956068));
#59633=CARTESIAN_POINT('Ctrl Pts',(4.6441637868483,-0.287068723725306,4.54885427056805));
#59634=CARTESIAN_POINT('Ctrl Pts',(4.66802170487971,-0.514950820910697,
4.34420214192463));
#59635=CARTESIAN_POINT('Ctrl Pts',(4.69187962291114,-0.616913415399932,
4.05538321370614));
#59636=CARTESIAN_POINT('Ctrl Pts',(4.71573754094255,-0.568023875442366,
3.75302158112612));
#59637=CARTESIAN_POINT('Ctrl Pts',(4.73959545897398,-0.380237025278099,
3.51105289951885));
#59638=CARTESIAN_POINT('Ctrl Pts',(4.76345337700539,-0.0994718649854296,
3.38864510263028));
#59639=CARTESIAN_POINT('Ctrl Pts',(4.78731129503681,0.205616875855751,3.41573023112194));
#59640=CARTESIAN_POINT('Ctrl Pts',(4.81116921306823,0.460426689658758,3.5856852332931));
#59641=CARTESIAN_POINT('Ctrl Pts',(4.83502713109965,0.60264963606909,3.85695148163183));
#59642=CARTESIAN_POINT('Ctrl Pts',(4.85888504913107,0.597508330613982,4.16319698927494));
#59643=CARTESIAN_POINT('Ctrl Pts',(4.88274296716248,0.446259962523644,4.42953638764361));
#59644=CARTESIAN_POINT('Ctrl Pts',(4.90660088519391,0.185888877718945,4.59084243889714));
#59645=CARTESIAN_POINT('Ctrl Pts',(4.93045880322533,-0.119937101199393,
4.60767141961541));
#59646=CARTESIAN_POINT('Ctrl Pts',(4.95431672125674,-0.396435191853442,
4.47590818560059));
#59647=CARTESIAN_POINT('Ctrl Pts',(4.97817463928816,-0.575994079421511,
4.22777243672773));
#59648=CARTESIAN_POINT('Ctrl Pts',(5.00203255731958,-0.614706724807315,
3.92394012267834));
#59649=CARTESIAN_POINT('Ctrl Pts',(5.025890475351,-0.503106831702736,3.63870652046354));
#59650=CARTESIAN_POINT('Ctrl Pts',(5.04974839338242,-0.268483613891896,
3.44181901543221));
#59651=CARTESIAN_POINT('Ctrl Pts',(5.07360631141384,0.0317911608623165,
3.38142196567243));
#59652=CARTESIAN_POINT('Ctrl Pts',(5.09746422944526,0.32429213081186,3.47228409503311));
#59653=CARTESIAN_POINT('Ctrl Pts',(5.12132214747667,0.537494841237617,3.69218713785082));
#59654=CARTESIAN_POINT('Ctrl Pts',(5.1451800655081,0.619265421915264,3.98735881011802));
#59655=CARTESIAN_POINT('Ctrl Pts',(5.16903798353952,0.549608738483219,4.28562159765047));
#59656=CARTESIAN_POINT('Ctrl Pts',(5.19289590157094,0.34555774745058,4.51404212438126));
#59657=CARTESIAN_POINT('Ctrl Pts',(5.21675381960235,0.0570084743622218,
4.61676534947452));
#59658=CARTESIAN_POINT('Ctrl Pts',(5.24061173763377,-0.245480923587363,
4.56867264627043));
#59659=CARTESIAN_POINT('Ctrl Pts',(5.26446965566519,-0.487943548953736,
4.38152399072137));
#59660=CARTESIAN_POINT('Ctrl Pts',(5.28832757369661,-0.611090685285508,
4.10108232693608));
#59661=CARTESIAN_POINT('Ctrl Pts',(5.31218549172803,-0.584809503288917,
3.79592328078761));
#59662=CARTESIAN_POINT('Ctrl Pts',(5.33604340975945,-0.415526467847156,
3.5406665514248));
#59663=CARTESIAN_POINT('Ctrl Pts',(5.35990132779088,-0.144635892303038,
3.39772936223054));
#59664=CARTESIAN_POINT('Ctrl Pts',(5.38375924582228,0.161622098711782,3.40206374949372));
#59665=CARTESIAN_POINT('Ctrl Pts',(5.40761716385371,0.428359084093981,3.55260983746209));
#59666=CARTESIAN_POINT('Ctrl Pts',(5.43147508188512,0.590350605148055,3.81255500683439));
#59667=CARTESIAN_POINT('Ctrl Pts',(5.45533299991655,0.607985322415754,4.11833558293467));
#59668=CARTESIAN_POINT('Ctrl Pts',(5.47919091794796,0.476951067165249,4.39517988561105));
#59669=CARTESIAN_POINT('Ctrl Pts',(5.50304883597938,0.2292892841064,4.57539194177126));
#59670=CARTESIAN_POINT('Ctrl Pts',(5.5269067540108,-0.0744399746307492,
4.61490499480714));
#59671=CARTESIAN_POINT('Ctrl Pts',(5.55076467204222,-0.359966631867259,
4.5040570269359));
#59672=CARTESIAN_POINT('Ctrl Pts',(5.57462259007364,-0.55747164231658,4.26995338574299));
#59673=CARTESIAN_POINT('Ctrl Pts',(5.59848050810506,-0.618659650999605,
3.96983878834977));
#59674=CARTESIAN_POINT('Ctrl Pts',(5.62233842613648,-0.528568523057477,
3.67709942878664));
#59675=CARTESIAN_POINT('Ctrl Pts',(5.6461963441679,-0.309227993320144,3.46331805450751));
#59676=CARTESIAN_POINT('Ctrl Pts',(5.67005426219932,-0.0142727959960426,
3.38077003484781));
#59677=CARTESIAN_POINT('Ctrl Pts',(5.69391218023074,0.284172488697173,3.4496406091084));
#59678=CARTESIAN_POINT('Ctrl Pts',(5.71777009826216,0.513129859266986,3.65308904601577));
#59679=CARTESIAN_POINT('Ctrl Pts',(5.74162801629357,0.616613001744231,3.94136666067651));
#59680=CARTESIAN_POINT('Ctrl Pts',(5.765485934325,0.569317469330215,4.24398172424487));
#59681=CARTESIAN_POINT('Ctrl Pts',(5.78934385235641,0.382808307322586,4.48693660973462));
#59682=CARTESIAN_POINT('Ctrl Pts',(5.81320177038783,0.102692087527565,4.61082223133738));
#59683=CARTESIAN_POINT('Ctrl Pts',(5.83705968841925,-0.202535146533943,
4.58534517687525));
#59684=CARTESIAN_POINT('Ctrl Pts',(5.86091760645067,-0.458237017319611,
4.41673528603543));
#59685=CARTESIAN_POINT('Ctrl Pts',(5.88477552448209,-0.601887460912657,
4.14622225884759));
#59686=CARTESIAN_POINT('Ctrl Pts',(5.9086334425135,-0.598360014525416,3.83995392008642));
#59687=CARTESIAN_POINT('Ctrl Pts',(5.93249136054493,-0.448517265794504,
3.57282118150817));
#59688=CARTESIAN_POINT('Ctrl Pts',(5.95634927857635,-0.188999790056246,
3.41014534911766));
#59689=CARTESIAN_POINT('Ctrl Pts',(5.98020719660777,0.116733210556207,3.39170495376011));
#59690=CARTESIAN_POINT('Ctrl Pts',(6.00406511463918,0.393921897475357,3.52200944135141));
#59691=CARTESIAN_POINT('Ctrl Pts',(6.02792303267061,0.574785693380153,3.76919531120668));
#59692=CARTESIAN_POINT('Ctrl Pts',(6.05178095070201,0.61509921541814,4.07281983667942));
#59693=CARTESIAN_POINT('Ctrl Pts',(6.07563886873346,0.505003308517799,4.35863675364492));
#59694=CARTESIAN_POINT('Ctrl Pts',(6.09949678676485,0.27142206589204,4.55675943366228));
#59695=CARTESIAN_POINT('Ctrl Pts',(6.12335470479629,-0.0285325303540597,
4.61873507756083));
#59696=CARTESIAN_POINT('Ctrl Pts',(6.14721262282769,-0.321503980505702,
4.52942105023226));
#59697=CARTESIAN_POINT('Ctrl Pts',(6.17107054085913,-0.535870591003297,
4.31063422072759));
#59698=CARTESIAN_POINT('Ctrl Pts',(6.19492845889052,-0.619180264299368,
4.01591706164003));
#59699=CARTESIAN_POINT('Ctrl Pts',(6.21878637692196,-0.551125001039776,
3.71725450231754));
#59700=CARTESIAN_POINT('Ctrl Pts',(6.24264429495337,-0.348226295733882,
3.48783145534908));
#59701=CARTESIAN_POINT('Ctrl Pts',(6.2665022129848,-0.0603247367796791,
3.38345774569467));
#59702=CARTESIAN_POINT('Ctrl Pts',(6.29036013101621,0.242607149567705,3.43020375417728));
#59703=CARTESIAN_POINT('Ctrl Pts',(6.31421804904763,0.485688404846908,3.61560451082823));
#59704=CARTESIAN_POINT('Ctrl Pts',(6.33807596707905,0.61099356578022,3.89627130770405));
#59705=CARTESIAN_POINT('Ctrl Pts',(6.36193388511046,0.585080291527744,4.19994745529594));
#59706=CARTESIAN_POINT('Ctrl Pts',(6.3937444424857,0.363797450650833,4.54512657044717));
#59707=CARTESIAN_POINT('Ctrl Pts',(6.43350763920472,-0.178959141669374,
4.67939801199369));
#59708=CARTESIAN_POINT('Ctrl Pts',(6.48122347526757,-0.668951848353412,
4.21606826543601));
#59709=CARTESIAN_POINT('Ctrl Pts',(6.5289393113304,-0.543175254381078,3.55462676401443));
#59710=CARTESIAN_POINT('Ctrl Pts',(6.57665514739324,0.0806513803028556,
3.30201433154981));
#59711=CARTESIAN_POINT('Ctrl Pts',(6.62437098345608,0.630812951656228,3.69045991683978));
#59712=CARTESIAN_POINT('Ctrl Pts',(6.67208681951892,0.601478580142798,4.36311480674272));
#59713=CARTESIAN_POINT('Ctrl Pts',(6.71980265558175,0.0199087309838695,
4.70234020845997));
#59714=CARTESIAN_POINT('Ctrl Pts',(6.76751849164459,-0.580002689552455,
4.39658285339385));
#59715=CARTESIAN_POINT('Ctrl Pts',(6.81523432770743,-0.64725742864426,3.72664421308375));
#59716=CARTESIAN_POINT('Ctrl Pts',(6.86295016377027,-0.120142281411799,
3.30772876957018));
#59717=CARTESIAN_POINT('Ctrl Pts',(6.91066599983311,0.517310146858294,3.52453857056345));
#59718=CARTESIAN_POINT('Ctrl Pts',(6.95838183589594,0.679704059947864,4.17797090041396));
#59719=CARTESIAN_POINT('Ctrl Pts',(7.00609767195879,0.217917737520193,4.66797035296266));
#59720=CARTESIAN_POINT('Ctrl Pts',(7.05381350802161,-0.443987099894697,
4.54456206689342));
#59721=CARTESIAN_POINT('Ctrl Pts',(7.10152934408447,-0.698171061503544,
3.92107420680554));
#59722=CARTESIAN_POINT('Ctrl Pts',(7.14924518014729,-0.311214160204793,
3.3700650369752));
#59723=CARTESIAN_POINT('Ctrl Pts',(7.19696101621015,0.361535686685884,3.39753487888718));
#59724=CARTESIAN_POINT('Ctrl Pts',(7.24467685227297,0.702281647003851,3.97825768917858));
#59725=CARTESIAN_POINT('Ctrl Pts',(7.29239268833582,0.398111619195611,4.5789468099385));
#59726=CARTESIAN_POINT('Ctrl Pts',(7.34010852439865,-0.271650463017158,
4.64798016059173));
#59727=CARTESIAN_POINT('Ctrl Pts',(7.38782436046149,-0.691951729928866,
4.1219633626529));
#59728=CARTESIAN_POINT('Ctrl Pts',(7.43554019652432,-0.476823084268312,
3.48394573037578));
#59729=CARTESIAN_POINT('Ctrl Pts',(7.48325603258717,0.17617954081454,3.31982867534575));
#59730=CARTESIAN_POINT('Ctrl Pts',(7.53097186865001,0.667393780433987,3.78032341303133));
#59731=CARTESIAN_POINT('Ctrl Pts',(7.57868770471284,0.545730043505963,4.44255054095139));
#59732=CARTESIAN_POINT('Ctrl Pts',(7.62640354077568,-0.077085990144297,
4.69837669746149));
#59733=CARTESIAN_POINT('Ctrl Pts',(7.67411937683852,-0.629112772588521,
4.31287278685955));
#59734=CARTESIAN_POINT('Ctrl Pts',(7.72183521290136,-0.603415615998442,
3.64005298187887));
#59735=CARTESIAN_POINT('Ctrl Pts',(7.76955104896419,-0.0235926144000291,
3.29777806215626));
#59736=CARTESIAN_POINT('Ctrl Pts',(7.81726688502703,0.577895847971041,3.60036435301798));
#59737=CARTESIAN_POINT('Ctrl Pts',(7.86498272108987,0.648693661106154,4.26994220769392));
#59738=CARTESIAN_POINT('Ctrl Pts',(7.9126985571527,0.123786103798515,4.6916279794467));
#59739=CARTESIAN_POINT('Ctrl Pts',(7.96041439321555,-0.514796137313916,
4.47818113561083));
#59740=CARTESIAN_POINT('Ctrl Pts',(8.00813022927838,-0.680633164378164,
3.82561319718015));
#59741=CARTESIAN_POINT('Ctrl Pts',(8.05584606534123,-0.221434283704469,
3.33318734306526));
#59742=CARTESIAN_POINT('Ctrl Pts',(8.10356190140405,0.441111106898351,3.45310581204486));
#59743=CARTESIAN_POINT('Ctrl Pts',(8.1512777374669,0.698577380670183,4.07524562887252));
#59744=CARTESIAN_POINT('Ctrl Pts',(8.19899357352974,0.314529296777622,4.62828622690367));
#59745=CARTESIAN_POINT('Ctrl Pts',(8.24670940959258,-0.358355880000973,
4.60436191534297));
#59746=CARTESIAN_POINT('Ctrl Pts',(8.29442524565541,-0.70215733816079,4.02544275761943));
#59747=CARTESIAN_POINT('Ctrl Pts',(8.34214108171825,-0.401156908608127,
3.42315912408683));
#59748=CARTESIAN_POINT('Ctrl Pts',(8.3898569177811,0.268232082711808,3.35059734274305));
#59749=CARTESIAN_POINT('Ctrl Pts',(8.43757275384392,0.691299425196396,3.8743920139026));
#59750=CARTESIAN_POINT('Ctrl Pts',(8.48528858990677,0.479535868514212,4.51353443142269));
#59751=CARTESIAN_POINT('Ctrl Pts',(8.53300442596961,-0.172592854832336,
4.68109027882443));
#59752=CARTESIAN_POINT('Ctrl Pts',(8.58072026203244,-0.66622690390392,4.22319044326068));
#59753=CARTESIAN_POINT('Ctrl Pts',(8.62843609809529,-0.548054535901959,
3.56033138942427));
#59754=CARTESIAN_POINT('Ctrl Pts',(8.67615193415812,0.0734047453217555,
3.30122678585069));
#59755=CARTESIAN_POINT('Ctrl Pts',(8.72386777022095,0.627455319439314,3.68381637683837));
#59756=CARTESIAN_POINT('Ctrl Pts',(8.7715836062838,0.605304019074675,4.35676225408577));
#59757=CARTESIAN_POINT('Ctrl Pts',(8.81929944234663,0.0272927241942496,
4.70208786391332));
#59758=CARTESIAN_POINT('Ctrl Pts',(8.86701527840948,-0.575781899266294,
4.40267538529889));
#59759=CARTESIAN_POINT('Ctrl Pts',(8.9147311144723,-0.650107145087294,3.73347990440727));
#59760=CARTESIAN_POINT('Ctrl Pts',(8.96244695053515,-0.127428996390418,
3.30903392823725));
#59761=CARTESIAN_POINT('Ctrl Pts',(9.01016278659798,0.512269160438921,3.51911272764658));
#59762=CARTESIAN_POINT('Ctrl Pts',(9.05787862266082,0.681542664962993,4.17079770865984));
#59763=CARTESIAN_POINT('Ctrl Pts',(9.10559445872366,0.224945053369686,4.66563652575022));
#59764=CARTESIAN_POINT('Ctrl Pts',(9.1533102947865,-0.438223061957547,4.54921107910972));
#59765=CARTESIAN_POINT('Ctrl Pts',(9.20102613084934,-0.698964196560635,
3.92843664782408));
#59766=CARTESIAN_POINT('Ctrl Pts',(9.24874196691217,-0.317835754515511,
3.3733799439853));
#59767=CARTESIAN_POINT('Ctrl Pts',(9.29645780297501,0.355166151432911,3.39375807937372));
#59768=CARTESIAN_POINT('Ctrl Pts',(9.34417363903786,0.702013515586798,3.97085749870423));
#59769=CARTESIAN_POINT('Ctrl Pts',(9.39188947510068,0.404191066510942,4.57471892538967));
#59770=CARTESIAN_POINT('Ctrl Pts',(9.43960531116354,-0.264806258220881,
4.65080711970243));
#59771=CARTESIAN_POINT('Ctrl Pts',(9.48732114722635,-0.690627921460452,
4.12924912203773));
#59772=CARTESIAN_POINT('Ctrl Pts',(9.53503698328922,-0.482235337746388,
3.48899966685243));
#59773=CARTESIAN_POINT('Ctrl Pts',(9.58275281935202,0.169001376764621,3.31800968034731));
#59774=CARTESIAN_POINT('Ctrl Pts',(9.63046865541491,0.665041526572246,3.77330189814918));
#59775=CARTESIAN_POINT('Ctrl Pts',(9.6781844914777,0.550363809549371,4.43677447107931));
#59776=CARTESIAN_POINT('Ctrl Pts',(9.72590032754056,-0.0697214622184181,
4.69915032657822));
#59777=CARTESIAN_POINT('Ctrl Pts',(9.7736161636034,-0.625780442428439,4.31948567936979));
#59778=CARTESIAN_POINT('Ctrl Pts',(9.82133199966623,-0.607175613486645,
3.64643241687702));
#59779=CARTESIAN_POINT('Ctrl Pts',(9.86904783572907,-0.030992076082374,
3.29806570630264));
#59780=CARTESIAN_POINT('Ctrl Pts',(9.91676367179191,0.573651961662729,3.59429605827795));
#59781=CARTESIAN_POINT('Ctrl Pts',(9.96447950785474,0.651502576242943,4.26309058249416));
#59782=CARTESIAN_POINT('Ctrl Pts',(10.0121953439176,0.131068350403577,4.69028497663703));
#59783=CARTESIAN_POINT('Ctrl Pts',(10.0599111799804,-0.50972795835719,4.48358005533451));
#59784=CARTESIAN_POINT('Ctrl Pts',(10.1076270160433,-0.682433239785766,
3.83279612838271));
#59785=CARTESIAN_POINT('Ctrl Pts',(10.1553428521061,-0.228449576533966,
3.33555808949935));
#59786=CARTESIAN_POINT('Ctrl Pts',(10.2030586881689,0.435322847997542,3.44848728078164));
#59787=CARTESIAN_POINT('Ctrl Pts',(10.2507745242318,0.699331602909907,4.06787908823615));
#59788=CARTESIAN_POINT('Ctrl Pts',(10.2984903602946,0.321133386270249,4.62493648450936));
#59789=CARTESIAN_POINT('Ctrl Pts',(10.3462061963575,-0.351966560253669,
4.60810509117381));
#59790=CARTESIAN_POINT('Ctrl Pts',(10.3939220324203,-0.701850198794989,
4.03284143571381));
#59791=CARTESIAN_POINT('Ctrl Pts',(10.4416378684831,-0.407214000429435,
3.42741898450738));
#59792=CARTESIAN_POINT('Ctrl Pts',(10.489353704546,0.261373080323254,3.34780649011919));
#59793=CARTESIAN_POINT('Ctrl Pts',(10.5370695406088,0.689937239673316,3.86711333114163));
#59794=CARTESIAN_POINT('Ctrl Pts',(10.5847853766716,0.484921415782374,4.50845204490092));
#59795=CARTESIAN_POINT('Ctrl Pts',(10.6325012127345,-0.165405205696588,
4.68287142228737));
#59796=CARTESIAN_POINT('Ctrl Pts',(10.6802170487973,-0.66383768169814,4.23019946525991));
#59797=CARTESIAN_POINT('Ctrl Pts',(10.7279328848602,-0.552657800140614,
3.5661317972102));
#59798=CARTESIAN_POINT('Ctrl Pts',(10.775648720923,0.0660362430193439,3.30049197570278));
#59799=CARTESIAN_POINT('Ctrl Pts',(10.8233645569858,0.624088188116435,3.67722113622194));
#59800=CARTESIAN_POINT('Ctrl Pts',(10.8710803930487,0.609030347235101,4.3503630939397));
#59801=CARTESIAN_POINT('Ctrl Pts',(10.9187962291115,0.0346905673513346,
4.70176123146349));
#59802=CARTESIAN_POINT('Ctrl Pts',(10.9665120651743,-0.57150609431415,4.40872123214985));
#59803=CARTESIAN_POINT('Ctrl Pts',(11.0142279012372,-0.65287991581936,3.74034623636848));
#59804=CARTESIAN_POINT('Ctrl Pts',(11.0619437373,-0.134704064778877,3.31041528701663));
#59805=CARTESIAN_POINT('Ctrl Pts',(11.1096595733629,0.507172601636502,3.51374059022208));
#59806=CARTESIAN_POINT('Ctrl Pts',(11.1573754094257,0.68330486411552,4.16360539148934));
#59807=CARTESIAN_POINT('Ctrl Pts',(11.2050912454885,0.231947755880478,4.66322884435941));
#59808=CARTESIAN_POINT('Ctrl Pts',(11.2528070815514,-0.432410545554582,
4.55379904436673));
#59809=CARTESIAN_POINT('Ctrl Pts',(11.3005229176142,-0.699679589515398,
3.93580706063847));
#59810=CARTESIAN_POINT('Ctrl Pts',(11.348238753677,-0.324422100469907,3.37676444086124));
#59811=CARTESIAN_POINT('Ctrl Pts',(11.3959545897399,0.348757195312759,3.39004862475285));
#59812=CARTESIAN_POINT('Ctrl Pts',(11.4436704258027,0.701667392320496,3.9634605418422));
#59813=CARTESIAN_POINT('Ctrl Pts',(11.4913862618656,0.410225626419724,4.57042720558968));
#59814=CARTESIAN_POINT('Ctrl Pts',(11.5391020979284,-0.257932644354891,
4.65356178929341));
#59815=CARTESIAN_POINT('Ctrl Pts',(11.5868179339912,-0.689227399014534,
4.13652052554825));
#59816=CARTESIAN_POINT('Ctrl Pts',(11.6345337700541,-0.487594028032435,
3.49411036255383));
#59817=CARTESIAN_POINT('Ctrl Pts',(11.6822496061169,0.161804441490335,3.31626643773886));
#59818=CARTESIAN_POINT('Ctrl Pts',(11.7299654421798,0.662615402711184,3.76630556374144));
#59819=CARTESIAN_POINT('Ctrl Pts',(11.7776812782426,0.554936443973853,4.43094988641136));
#59820=CARTESIAN_POINT('Ctrl Pts',(11.8253971143054,-0.062349190059417,
4.69984629737339));
#59821=CARTESIAN_POINT('Ctrl Pts',(11.8731129503683,-0.622378603495518,
4.32606308493799));
#59822=CARTESIAN_POINT('Ctrl Pts',(11.9208287864311,-0.610868168815925,
3.65285112447858));
#59823=CARTESIAN_POINT('Ctrl Pts',(11.9685446224939,-0.0383880952977111,
3.29843131798253));
#59824=CARTESIAN_POINT('Ctrl Pts',(12.0162604585568,0.569344356809164,3.58827282720487));
#59825=CARTESIAN_POINT('Ctrl Pts',(12.0639762946196,0.654239125569198,4.25620973444184));
#59826=CARTESIAN_POINT('Ctrl Pts',(12.1116921306825,0.138336038556134,4.68886530024737));
#59827=CARTESIAN_POINT('Ctrl Pts',(12.1594079667453,-0.50460316123658,4.48892526128066));
#59828=CARTESIAN_POINT('Ctrl Pts',(12.2071238028081,-0.684157513748105,
3.83999763179777));
#59829=CARTESIAN_POINT('Ctrl Pts',(12.254839638871,-0.235439494268261,3.33800263898788));
#59830=CARTESIAN_POINT('Ctrl Pts',(12.3025554749338,0.429486235500398,3.44393000893412));
#59831=CARTESIAN_POINT('Ctrl Pts',(12.3502713109967,0.700008146713868,4.06050500791278));
#59832=CARTESIAN_POINT('Ctrl Pts',(12.3979871470595,0.327701805790174,4.62151732713591));
#59833=CARTESIAN_POINT('Ctrl Pts',(12.4457029831223,-0.345538145731053,
4.61178072157682));
#59834=CARTESIAN_POINT('Ctrl Pts',(12.4934188191852,-0.701465101239671,
4.04023646593735));
#59835=CARTESIAN_POINT('Ctrl Pts',(12.541134655248,-0.413225860851952,3.43174244451));
#59836=CARTESIAN_POINT('Ctrl Pts',(12.5888504913108,0.254485045853264,3.34508808005552));
#59837=CARTESIAN_POINT('Ctrl Pts',(12.6365663273737,0.688498419195676,3.85984940880123));
#59838=CARTESIAN_POINT('Ctrl Pts',(12.6842821634365,0.490253100280801,4.50331318193882));
#59839=CARTESIAN_POINT('Ctrl Pts',(12.7319979994994,-0.158199184135511,
4.68457671563321));
#59840=CARTESIAN_POINT('Ctrl Pts',(12.7797138355622,-0.661374723552845,
4.23718291779492));
#59841=CARTESIAN_POINT('Ctrl Pts',(12.827429671625,-0.557199677773407,3.57198039701723));
#59842=CARTESIAN_POINT('Ctrl Pts',(12.8751455076879,0.058660405724426,3.29983486358678));
#59843=CARTESIAN_POINT('Ctrl Pts',(12.9228613437507,0.62065173603916,3.67066174834999));
#59844=CARTESIAN_POINT('Ctrl Pts',(12.9705771798135,0.612689027194643,4.34392501712378));
#59845=CARTESIAN_POINT('Ctrl Pts',(13.0182930158764,0.0420845572448178,
4.7013566507062));
#59846=CARTESIAN_POINT('Ctrl Pts',(13.0660088519392,-0.567166809177069,
4.4147216801859));
#59847=CARTESIAN_POINT('Ctrl Pts',(13.1137246880021,-0.655580167748548,
3.74724140943759));
#59848=CARTESIAN_POINT('Ctrl Pts',(13.1614405240649,-0.141964170879043,
3.31187324159358));
#59849=CARTESIAN_POINT('Ctrl Pts',(13.2091563601277,0.502019708508231,3.50842246418533));
#59850=CARTESIAN_POINT('Ctrl Pts',(13.2568721961906,0.684991165006287,4.15639490180834));
#59851=CARTESIAN_POINT('Ctrl Pts',(13.3045880322534,0.238924694735218,4.66074749465585));
#59852=CARTESIAN_POINT('Ctrl Pts',(13.3523038683163,-0.426549999040181,
4.55832549625387));
#59853=CARTESIAN_POINT('Ctrl Pts',(13.4000197043791,-0.700317265381609,
3.94318460369993));
#59854=CARTESIAN_POINT('Ctrl Pts',(13.4477355404419,-0.330972411156884,
3.38021816378559));
#59855=CARTESIAN_POINT('Ctrl Pts',(13.4954513765048,0.342309500898352,3.3864069206363));
#59856=CARTESIAN_POINT('Ctrl Pts',(13.5431672125676,0.70124333116994,3.95606764360979));
#59857=CARTESIAN_POINT('Ctrl Pts',(13.5908830486304,0.416214620412595,4.5660721254426));
#59858=CARTESIAN_POINT('Ctrl Pts',(13.6385988846933,-0.251030380554765,
4.65624386434224));
#59859=CARTESIAN_POINT('Ctrl Pts',(13.6863147207561,-0.687750320459788,
4.14377676500662));
#59860=CARTESIAN_POINT('Ctrl Pts',(13.734030556819,-0.492898558687668,3.49927725007553));
#59861=CARTESIAN_POINT('Ctrl Pts',(13.7817463928818,0.15458953374652,3.31459914100992));
#59862=CARTESIAN_POINT('Ctrl Pts',(13.8294622289446,0.660115678675556,3.75933518700271));
#59863=CARTESIAN_POINT('Ctrl Pts',(13.8771780650075,0.559447438691528,4.42507743387505));
#59864=CARTESIAN_POINT('Ctrl Pts',(13.9248939010703,-0.0549699924482557,
4.7004645325629));
#59865=CARTESIAN_POINT('Ctrl Pts',(13.9726097371331,-0.61890763370075,4.33260427296601));
#59866=CARTESIAN_POINT('Ctrl Pts',(14.020325573196,-0.614492871807821,3.65930839172987));
#59867=CARTESIAN_POINT('Ctrl Pts',(14.0680414092588,-0.0457798505455885,
3.29887485658241));
#59868=CARTESIAN_POINT('Ctrl Pts',(14.1157572453217,0.564973511886205,3.58229532883235));
#59869=CARTESIAN_POINT('Ctrl Pts',(14.1634730813845,0.656903005118004,4.24930042782804));
#59870=CARTESIAN_POINT('Ctrl Pts',(14.2111889174473,0.145588360997982,4.6873691079691));
#59871=CARTESIAN_POINT('Ctrl Pts',(14.2589047535102,-0.499422315191365,
4.49421615972892));
#59872=CARTESIAN_POINT('Ctrl Pts',(14.306620589573,-0.685805794740406,3.8472169075166));
#59873=CARTESIAN_POINT('Ctrl Pts',(14.3543364256359,-0.242403260500786,
3.34052072000184));
#59874=CARTESIAN_POINT('Ctrl Pts',(14.4020522616987,0.423601917710294,3.43943450270243));
#59875=CARTESIAN_POINT('Ctrl Pts',(14.4497680977615,0.700606936934704,4.05312420698026));
#59876=CARTESIAN_POINT('Ctrl Pts',(14.4974839338244,0.334233825748585,4.61802913456711));
#59877=CARTESIAN_POINT('Ctrl Pts',(14.5451997698872,-0.339071350470923,
4.61538839828042));
#59878=CARTESIAN_POINT('Ctrl Pts',(14.59291560595,-0.701002088269634,4.04762702688518));
#59879=CARTESIAN_POINT('Ctrl Pts',(14.6406314420129,-0.419191822106764,
3.43612902386528));
#59880=CARTESIAN_POINT('Ctrl Pts',(14.6883472780757,0.24756874439201,3.34244241450009));
#59881=CARTESIAN_POINT('Ctrl Pts',(14.7360631141386,0.686983123580828,3.85260105372344));
#59882=CARTESIAN_POINT('Ctrl Pts',(14.7837789502014,0.495530329791292,4.49811841333687));
#59883=CARTESIAN_POINT('Ctrl Pts',(14.8314947862642,-0.150975590559777,
4.68620596944608));
#59884=CARTESIAN_POINT('Ctrl Pts',(14.8792106223271,-0.658838303041738,
4.24414002517693));
#59885=CARTESIAN_POINT('Ctrl Pts',(14.9269264583899,-0.561679664310124,
3.57787653921065));
#59886=CARTESIAN_POINT('Ctrl Pts',(14.9746422944528,0.0512780527100071,
3.29925552249156));
#59887=CARTESIAN_POINT('Ctrl Pts',(15.0223581305156,0.617146344912281,3.6641389418082));
#59888=CARTESIAN_POINT('Ctrl Pts',(15.0700739665784,0.616279652564493,4.337448738749));
#59889=CARTESIAN_POINT('Ctrl Pts',(15.1177898026413,0.0494738725853903,
4.70087416658037));
#59890=CARTESIAN_POINT('Ctrl Pts',(15.1655056387041,-0.562764525842253,
4.42067606290572));
#59891=CARTESIAN_POINT('Ctrl Pts',(15.2132214747669,-0.658207600943685,
3.75416465773151));
#59892=CARTESIAN_POINT('Ctrl Pts',(15.2609373108298,-0.14920850827279,3.31340763002542));
#59893=CARTESIAN_POINT('Ctrl Pts',(15.3086531468926,0.496811053413015,3.50315894024854));
#59894=CARTESIAN_POINT('Ctrl Pts',(15.3563689829554,0.686601380328997,4.14916704052379));
#59895=CARTESIAN_POINT('Ctrl Pts',(15.4040848190183,0.245875094968658,4.6581927522561));
#59896=CARTESIAN_POINT('Ctrl Pts',(15.4518006550811,-0.420642073376032,
4.56278993199436));
#59897=CARTESIAN_POINT('Ctrl Pts',(15.499516491144,-0.700877153329261,3.95056845754601));
#59898=CARTESIAN_POINT('Ctrl Pts',(15.5472323272068,-0.337485958999024,
3.3837407291352));
#59899=CARTESIAN_POINT('Ctrl Pts',(15.5949481632696,0.335823784368978,3.38283337152726));
#59900=CARTESIAN_POINT('Ctrl Pts',(15.6426639993325,0.70074137923783,3.94867962517506));
#59901=CARTESIAN_POINT('Ctrl Pts',(15.6903798353953,0.422157383260532,4.56165416869007));
#59902=CARTESIAN_POINT('Ctrl Pts',(15.7380956714582,-0.244100233491204,
4.65885304693675));
#59903=CARTESIAN_POINT('Ctrl Pts',(15.785811507521,-0.686196849863089,4.15101703442422));
#59904=CARTESIAN_POINT('Ctrl Pts',(15.8335273435838,-0.498148340509996,
3.50449975550414));
#59905=CARTESIAN_POINT('Ctrl Pts',(15.8812431796467,0.147357454930898,3.3130079753559));
#59906=CARTESIAN_POINT('Ctrl Pts',(15.9289590157095,0.657542632122849,3.75239154216938));
#59907=CARTESIAN_POINT('Ctrl Pts',(15.9766748517723,0.563896292642505,4.41915776575455));
#59908=CARTESIAN_POINT('Ctrl Pts',(16.0243906878352,-0.0475846890311933,
4.70100496347609));
#59909=CARTESIAN_POINT('Ctrl Pts',(16.072106523898,-0.615367918582998,4.33910851688972));
#59910=CARTESIAN_POINT('Ctrl Pts',(16.1198223599609,-0.618049319847516,
3.66580350138828));
#59911=CARTESIAN_POINT('Ctrl Pts',(16.1675381960237,-0.0531665207849041,
3.29939627283611));
#59912=CARTESIAN_POINT('Ctrl Pts',(16.2152540320865,0.560539912386559,3.57636422711252));
#59913=CARTESIAN_POINT('Ctrl Pts',(16.2629698681494,0.659493918998266,4.24236343010572));
#59914=CARTESIAN_POINT('Ctrl Pts',(16.3106857042122,0.152824512175573,4.68579656599215));
#59915=CARTESIAN_POINT('Ctrl Pts',(16.358401540275,-0.494185995685336,4.49945216299141));
#59916=CARTESIAN_POINT('Ctrl Pts',(16.4061173763379,-0.687377899679438,
3.85445315365633));
#59917=CARTESIAN_POINT('Ctrl Pts',(16.4538332124007,-0.249340101729437,
3.34311205284473));
#59918=CARTESIAN_POINT('Ctrl Pts',(16.5015490484636,0.417670548229327,3.43500126142608));
#59919=CARTESIAN_POINT('Ctrl Pts',(16.5492648845264,0.701127907061643,4.04573750526291));
#59920=CARTESIAN_POINT('Ctrl Pts',(16.5969807205892,0.340728720599694,4.61447229425484));
#59921=CARTESIAN_POINT('Ctrl Pts',(16.6446965566521,-0.3325668927742,4.61892772056098));
#59922=CARTESIAN_POINT('Ctrl Pts',(16.6924123927149,-0.700461211314163,
4.05501229764889));
#59923=CARTESIAN_POINT('Ctrl Pts',(16.7401282287777,-0.425111221523205,
3.4405782353328));
#59924=CARTESIAN_POINT('Ctrl Pts',(16.7878440648406,0.240624944169445,3.3398697873209));
#59925=CARTESIAN_POINT('Ctrl Pts',(16.8355599009034,0.685391521140609,3.84536907102113));
#59926=CARTESIAN_POINT('Ctrl Pts',(16.8832757369663,0.500752518144239,4.49286831610534));
#59927=CARTESIAN_POINT('Ctrl Pts',(16.9309915730291,-0.143735227331884,
4.68775900275617));
#59928=CARTESIAN_POINT('Ctrl Pts',(16.978707409092,-0.656228701898373,4.25107001464348));
#59929=CARTESIAN_POINT('Ctrl Pts',(17.0264232451548,-0.566097262135119,
3.58381956887496));
#59930=CARTESIAN_POINT('Ctrl Pts',(17.0741390812176,0.0438900039728252,
3.29875401676759));
#59931=CARTESIAN_POINT('Ctrl Pts',(17.1218549172805,0.613572404098014,3.65765344111895));
#59932=CARTESIAN_POINT('Ctrl Pts',(17.1695707533433,0.619801824515016,4.33093497816967));
#59933=CARTESIAN_POINT('Ctrl Pts',(17.2172865894061,0.0568576926029748,
4.70031383267802));
#59934=CARTESIAN_POINT('Ctrl Pts',(17.265002425469,-0.558299733294432,4.42658371892475));
#59935=CARTESIAN_POINT('Ctrl Pts',(17.3127182615318,-0.66076192356197,3.76111521224867));
#59936=CARTESIAN_POINT('Ctrl Pts',(17.3604340975947,-0.156436272293483,
3.31501828187956));
#59937=CARTESIAN_POINT('Ctrl Pts',(17.4081499336575,0.491547214903555,3.49795060305896));
#59938=CARTESIAN_POINT('Ctrl Pts',(17.4558657697204,0.688135331228569,4.14192261047223));
#59939=CARTESIAN_POINT('Ctrl Pts',(17.5035816057831,0.252798184563325,4.65556490092881));
#59940=CARTESIAN_POINT('Ctrl Pts',(17.551297441846,-0.414687424786488,4.56719185569987));
#59941=CARTESIAN_POINT('Ctrl Pts',(17.5990132779088,-0.701359191168653,
3.95795780201324));
#59942=CARTESIAN_POINT('Ctrl Pts',(17.6467291139717,-0.343962020502345,
3.38733174564023));
#59943=CARTESIAN_POINT('Ctrl Pts',(17.6944449500345,0.329300766127249,3.37932837435862));
#59944=CARTESIAN_POINT('Ctrl Pts',(17.7421607860974,0.700161592278611,3.94129730716402));
#59945=CARTESIAN_POINT('Ctrl Pts',(17.7898766221602,0.428053254869629,4.55717382605774));
#59946=CARTESIAN_POINT('Ctrl Pts',(17.837592458223,-0.23714297293205,4.66138904726133));
#59947=CARTESIAN_POINT('Ctrl Pts',(17.8853082942859,-0.684567159776581,
4.15824052958626));
#59948=CARTESIAN_POINT('Ctrl Pts',(17.9330241303487,-0.503342790378573,
3.50977729874859));
#59949=CARTESIAN_POINT('Ctrl Pts',(17.9807399664116,0.140109008348428,3.31149311751593));
#59950=CARTESIAN_POINT('Ctrl Pts',(18.0284558024744,0.654896548854854,3.7454754005085));
#59951=CARTESIAN_POINT('Ctrl Pts',(18.0761716385372,0.568282511669218,4.41319153957849));
#59952=CARTESIAN_POINT('Ctrl Pts',(18.1238874746001,-0.040194100132671,
4.70146753008449));
#59953=CARTESIAN_POINT('Ctrl Pts',(18.1716033106629,-0.611759851316993,
4.34557509424858));
#59954=CARTESIAN_POINT('Ctrl Pts',(18.2193191467258,-0.621537117901666,
3.67233573200791));
#59955=CARTESIAN_POINT('Ctrl Pts',(18.2670349827885,-0.0605472855394143,
3.29999550882718));
#59956=CARTESIAN_POINT('Ctrl Pts',(18.3147508188514,0.556044050773433,3.57048018084402));
#59957=CARTESIAN_POINT('Ctrl Pts',(18.3624666549143,0.662011579423562,4.23539951180373));
#59958=CARTESIAN_POINT('Ctrl Pts',(18.4101824909771,0.160043688331546,4.684147848987));
#59959=CARTESIAN_POINT('Ctrl Pts',(18.4578983270399,-0.488894784343999,
4.50463268947774));
#59960=CARTESIAN_POINT('Ctrl Pts',(18.5056141631028,-0.68887365394326,3.86170556644909));
#59961=CARTESIAN_POINT('Ctrl Pts',(18.5533299991656,-0.256249247442801,
3.34577634968359));
#59962=CARTESIAN_POINT('Ctrl Pts',(18.6010458352284,0.41169278588589,3.4306307775285));
#59963=CARTESIAN_POINT('Ctrl Pts',(18.6487616712913,0.701570999227752,4.03834572324048));
#59964=CARTESIAN_POINT('Ctrl Pts',(18.6964775073541,0.347185768921481,4.6108472012761));
#59965=CARTESIAN_POINT('Ctrl Pts',(18.744193343417,-0.326025495125306,4.62239829528727));
#59966=CARTESIAN_POINT('Ctrl Pts',(18.7919091794798,-0.699842530451103,
4.06239145790787));
#59967=CARTESIAN_POINT('Ctrl Pts',(18.8396250155426,-0.430983401602837,
3.44508958471478));
#59968=CARTESIAN_POINT('Ctrl Pts',(18.8873408516055,0.233654416470602,3.33737048427408));
#59969=CARTESIAN_POINT('Ctrl Pts',(18.9350566876683,0.683723788661416,3.83815426398688));
#59970=CARTESIAN_POINT('Ctrl Pts',(18.9827725237312,0.505919085286118,4.48756347340344));
#59971=CARTESIAN_POINT('Ctrl Pts',(19.030488359794,-0.136478898681533,4.68923564305365));
#59972=CARTESIAN_POINT('Ctrl Pts',(19.0782041958568,-0.653546209976322,
4.2579721164561));
#59973=CARTESIAN_POINT('Ctrl Pts',(19.1259200319197,-0.570451980578726,
3.58980882586423));
#59974=CARTESIAN_POINT('Ctrl Pts',(19.1736358679825,0.0364970801727598,
3.29833040216201));
#59975=CARTESIAN_POINT('Ctrl Pts',(19.2213517040453,0.609930310515188,3.65120596658116));
#59976=CARTESIAN_POINT('Ctrl Pts',(19.2690675401082,0.623255151928734,4.32438445905389));
#59977=CARTESIAN_POINT('Ctrl Pts',(19.316783376171,0.0642351969327414,4.69967571095415));
#59978=CARTESIAN_POINT('Ctrl Pts',(19.3644992122339,-0.553772927074266,
4.43244399258532));
#59979=CARTESIAN_POINT('Ctrl Pts',(19.4122150482967,-0.663242852612724,
3.76809229994096));
#59980=CARTESIAN_POINT('Ctrl Pts',(19.4599308843595,-0.163646658734412,
3.3167050201661));
#59981=CARTESIAN_POINT('Ctrl Pts',(19.5076467204224,0.486228775054438,3.49279802752061));
#59982=CARTESIAN_POINT('Ctrl Pts',(19.5553625564852,0.689592852244711,4.13466242315333));
#59983=CARTESIAN_POINT('Ctrl Pts',(19.6030783925481,0.259693185238344,4.65286421968052));
#59984=CARTESIAN_POINT('Ctrl Pts',(19.6507942286109,-0.408686697131164,
4.57153080275077));
#59985=CARTESIAN_POINT('Ctrl Pts',(19.6985100646738,-0.701763358503738,
3.96535177039745));
#59986=CARTESIAN_POINT('Ctrl Pts',(19.7462259007365,-0.350399813749482,
3.39099090115443));
#59987=CARTESIAN_POINT('Ctrl Pts',(19.7939417367994,0.322741052541778,3.37589215469092));
#59988=CARTESIAN_POINT('Ctrl Pts',(19.8416575728622,0.699504257835039,3.93392181877779));
#59989=CARTESIAN_POINT('Ctrl Pts',(19.8893734089251,0.433901159015506,4.55263101135276));
#59990=CARTESIAN_POINT('Ctrl Pts',(19.9370892449879,-0.23015857608315,4.663852686053));
#59991=CARTESIAN_POINT('Ctrl Pts',(19.9848050810507,-0.682862933423436,
4.16544436654047));
#59992=CARTESIAN_POINT('Ctrl Pts',(20.0325209171136,-0.508478494849655,
3.51511322409123));
#59993=CARTESIAN_POINT('Ctrl Pts',(20.0802367531764,0.132839643288252,3.31004731418368));
#59994=CARTESIAN_POINT('Ctrl Pts',(20.1279525892393,0.652187835720725,3.73860154375571));
#59995=CARTESIAN_POINT('Ctrl Pts',(20.1756684253021,0.572586513039731,4.4071529569233));
#59996=CARTESIAN_POINT('Ctrl Pts',(20.2233842613649,-0.0327629883405684,
4.70190215105461));
#59997=CARTESIAN_POINT('Ctrl Pts',(20.2711000974278,-0.608151935097038,
4.35190888358257));
#59998=CARTESIAN_POINT('Ctrl Pts',(20.3188159334906,-0.624827148513498,
3.67908301574286));
#59999=CARTESIAN_POINT('Ctrl Pts',(20.3665317695535,-0.0681655280739813,
3.30033184185188));
#60000=CARTESIAN_POINT('Ctrl Pts',(20.4142476056163,0.551956769749184,3.56531418539817));
#60001=CARTESIAN_POINT('Ctrl Pts',(20.4540108023353,0.644905999548395,4.11665253813788));
#60002=CARTESIAN_POINT('Ctrl Pts',(20.4858213597105,0.416382673412033,4.45708139504444));
#60003=CARTESIAN_POINT('Ctrl Pts',(20.509679277742,0.148137151166912,4.60177085628536));
#60004=CARTESIAN_POINT('Ctrl Pts',(20.5335371957734,-0.159214575149101,
4.59858486262053));
#60005=CARTESIAN_POINT('Ctrl Pts',(20.5573951138048,-0.426074836374489,
4.44942877587387));
#60006=CARTESIAN_POINT('Ctrl Pts',(20.5812530318362,-0.589577924844292,
4.19016123618585));
#60007=CARTESIAN_POINT('Ctrl Pts',(20.6051109498677,-0.608473233900696,
3.88450759853215));
#60008=CARTESIAN_POINT('Ctrl Pts',(20.6289688678991,-0.478813304308425,
3.60703485797333));
#60009=CARTESIAN_POINT('Ctrl Pts',(20.6528267859305,-0.231947052182395,
3.42568465323223));
#60010=CARTESIAN_POINT('Ctrl Pts',(20.6766847039619,0.0715712039811096,
3.38475332414555));
#60011=CARTESIAN_POINT('Ctrl Pts',(20.7005426219933,0.357622970648114,3.49427550111266));
#60012=CARTESIAN_POINT('Ctrl Pts',(20.7244005400248,0.556207844932749,3.72745636179159));
#60013=CARTESIAN_POINT('Ctrl Pts',(20.7482584580561,0.618794460414918,4.02728407199912));
#60014=CARTESIAN_POINT('Ctrl Pts',(20.7721163760876,0.530063832205264,4.32043875618714));
#60015=CARTESIAN_POINT('Ctrl Pts',(20.7959742941189,0.311720881859749,4.53523813880796));
#60016=CARTESIAN_POINT('Ctrl Pts',(20.8198322121505,0.01715224242355,4.619156844639));
#60017=CARTESIAN_POINT('Ctrl Pts',(20.8436901301818,-0.281609823618225,
4.55167503361081));
#60018=CARTESIAN_POINT('Ctrl Pts',(20.8675480482133,-0.511511021444125,
4.34929354512778));
#60019=CARTESIAN_POINT('Ctrl Pts',(20.8914059662447,-0.616333626991818,
4.06150032559224));
#60020=CARTESIAN_POINT('Ctrl Pts',(20.9152638842761,-0.570445985619195,
3.75866857192897));
#60021=CARTESIAN_POINT('Ctrl Pts',(20.9391218023075,-0.385068702031786,
3.51484894167474));
#60022=CARTESIAN_POINT('Ctrl Pts',(20.9629797203389,-0.105531663562905,
3.38966195221662));
#60023=CARTESIAN_POINT('Ctrl Pts',(20.9868376383704,0.199810758127152,3.41371924506628));
#60024=CARTESIAN_POINT('Ctrl Pts',(21.0106955564018,0.456293997792742,3.58113815016051));
#60025=CARTESIAN_POINT('Ctrl Pts',(21.0345534744332,0.60120093052663,3.85098018832832));
#60026=CARTESIAN_POINT('Ctrl Pts',(21.0584113924646,0.599097856858477,4.15726162902184));
#60027=CARTESIAN_POINT('Ctrl Pts',(21.082269310496,0.450499039416452,4.42508831804098));
#60028=CARTESIAN_POINT('Ctrl Pts',(21.1061272285275,0.191740934787398,4.58896933394457));
#60029=CARTESIAN_POINT('Ctrl Pts',(21.1299851465589,-0.113903050943465,
4.60883130459215));
#60030=CARTESIAN_POINT('Ctrl Pts',(21.1538430645903,-0.391694638258801,
4.47981743698434));
#60031=CARTESIAN_POINT('Ctrl Pts',(21.1777009826217,-0.573706216867813,
4.23347513609622));
#60032=CARTESIAN_POINT('Ctrl Pts',(21.2015589006531,-0.615430998064313,
3.9300418046833));
#60033=CARTESIAN_POINT('Ctrl Pts',(21.2254168186846,-0.506666136201032,
3.64371515765586));
#60034=CARTESIAN_POINT('Ctrl Pts',(21.2492747367159,-0.27400760274365,3.44450985958179));
#60035=CARTESIAN_POINT('Ctrl Pts',(21.2731326547474,0.0256532534100022,
3.38113703208972));
#60036=CARTESIAN_POINT('Ctrl Pts',(21.2969905727788,0.319041190319967,3.46909305773936));
#60037=CARTESIAN_POINT('Ctrl Pts',(21.3208484908102,0.534414865691478,3.68687029238709));
#60038=CARTESIAN_POINT('Ctrl Pts',(21.3447064088416,0.619109549231529,3.98121627002784));
#60039=CARTESIAN_POINT('Ctrl Pts',(21.3685643268731,0.552415083779586,4.28015538130547));
#60040=CARTESIAN_POINT('Ctrl Pts',(21.3924222449044,0.350640082858436,4.51058887057447));
#60041=CARTESIAN_POINT('Ctrl Pts',(21.4162801629359,0.0631240304344945,
4.61616947282646));
#60042=CARTESIAN_POINT('Ctrl Pts',(21.4401380809673,-0.239827566894842,
4.57107985485291));
#60043=CARTESIAN_POINT('Ctrl Pts',(21.4639959989987,-0.484134791346583,
4.38634565646493));
#60044=CARTESIAN_POINT('Ctrl Pts',(21.4878539170302,-0.610057871747176,
4.10713942122688));
#60045=CARTESIAN_POINT('Ctrl Pts',(21.5117118350615,-0.586805184862796,
3.80173467907963));
#60046=CARTESIAN_POINT('Ctrl Pts',(21.535569753093,-0.420062646027161,3.5448112085363));
#60047=CARTESIAN_POINT('Ctrl Pts',(21.5594276711244,-0.150603347961132,
3.39919379659958));
#60048=CARTESIAN_POINT('Ctrl Pts',(21.5832855891558,0.155682571034224,3.40048986702667));
#60049=CARTESIAN_POINT('Ctrl Pts',(21.6071435071872,0.423899860703612,3.54838249529388));
#60050=CARTESIAN_POINT('Ctrl Pts',(21.6310014252187,0.588462087630599,3.80670790527556));
#60051=CARTESIAN_POINT('Ctrl Pts',(21.6548593432501,0.609129304746478,4.11229849758833));
#60052=CARTESIAN_POINT('Ctrl Pts',(21.6787172612815,0.480847814502724,4.39042904829107));
#60053=CARTESIAN_POINT('Ctrl Pts',(21.7025751793129,0.234985935581564,4.57308906161293));
#60054=CARTESIAN_POINT('Ctrl Pts',(21.7264330973443,-0.0683364054776661,
4.61561318873779));
#60055=CARTESIAN_POINT('Ctrl Pts',(21.7502910153758,-0.35494863395129,4.5076031222497));
#60056=CARTESIAN_POINT('Ctrl Pts',(21.7741489334072,-0.554766252817153,
4.2754702655401));
#60057=CARTESIAN_POINT('Ctrl Pts',(21.7980068514386,-0.618928411339905,
3.9759774252466));
#60058=CARTESIAN_POINT('Ctrl Pts',(21.82186476947,-0.531745714018629,3.68235875884208));
#60059=CARTESIAN_POINT('Ctrl Pts',(21.8457226875014,-0.314536705157368,
3.46641202827438));
#60060=CARTESIAN_POINT('Ctrl Pts',(21.8695806055329,-0.0204149040773093,
3.3809420914381));
#60061=CARTESIAN_POINT('Ctrl Pts',(21.8934385235643,0.278698897140474,3.44684867604406));
#60062=CARTESIAN_POINT('Ctrl Pts',(21.9172964415957,0.509663226401888,3.6480158268968));
#60063=CARTESIAN_POINT('Ctrl Pts',(21.9411543596271,0.616001013860485,3.93525269592965));
#60064=CARTESIAN_POINT('Ctrl Pts',(21.9650122776585,0.571709773899469,4.23832204448885));
#60065=CARTESIAN_POINT('Ctrl Pts',(21.98887019569,0.387619921158457,4.48311516140836));
#60066=CARTESIAN_POINT('Ctrl Pts',(22.0127281137213,0.108746439139576,4.60977346157076));
#60067=CARTESIAN_POINT('Ctrl Pts',(22.0365860317528,-0.196718509442517,
4.5873255404835));
#60068=CARTESIAN_POINT('Ctrl Pts',(22.0604439497842,-0.454080423961193,
4.42126052632156));
#60069=CARTESIAN_POINT('Ctrl Pts',(22.0843018678156,-0.600407305919173,
4.15218583856754));
#60070=CARTESIAN_POINT('Ctrl Pts',(22.1081597858471,-0.599918246812857,
3.84589756782496));
#60071=CARTESIAN_POINT('Ctrl Pts',(22.1320177038785,-0.452732834916613,
3.57729153941473));
#60072=CARTESIAN_POINT('Ctrl Pts',(22.1558756219099,-0.194841912687001,
3.41204924396571));
#60073=CARTESIAN_POINT('Ctrl Pts',(22.1797335399413,0.110693164578993,3.39057692382254));
#60074=CARTESIAN_POINT('Ctrl Pts',(22.2035914579728,0.389160747889314,3.51812514615901));
#60075=CARTESIAN_POINT('Ctrl Pts',(22.2274493760041,0.572467927805029,3.76350489626149));
#60076=CARTESIAN_POINT('Ctrl Pts',(22.2513072940356,0.615791105677536,4.06671414123586));
#60077=CARTESIAN_POINT('Ctrl Pts',(22.2751652120669,0.508536584364246,4.35360996140145));
#60078=CARTESIAN_POINT('Ctrl Pts',(22.2990231300984,0.276931015980992,4.55403851389998));
#60079=CARTESIAN_POINT('Ctrl Pts',(22.3228810481298,-0.0223917293827815,
4.61898955797298));
#60080=CARTESIAN_POINT('Ctrl Pts',(22.3467389661613,-0.31623908674035,4.53258079431836));
#60081=CARTESIAN_POINT('Ctrl Pts',(22.3705968841927,-0.532757373651304,
4.31594151899069));
#60082=CARTESIAN_POINT('Ctrl Pts',(22.3944548022241,-0.619001969851995,
4.02204593667267));
#60083=CARTESIAN_POINT('Ctrl Pts',(22.4183127202555,-0.553883724721699,
3.72275952141814));
#60084=CARTESIAN_POINT('Ctrl Pts',(22.4421706382869,-0.35332581843718,3.49126595675675));
#60085=CARTESIAN_POINT('Ctrl Pts',(22.4660285563184,-0.0663701307507445,
3.38417172009386));
#60086=CARTESIAN_POINT('Ctrl Pts',(22.4898864743497,0.236814872379406,3.42766427875767));
#60087=CARTESIAN_POINT('Ctrl Pts',(22.5137443923812,0.482092168510832,3.61110849992699));
#60088=CARTESIAN_POINT('Ctrl Pts',(22.5376023104126,0.609484835267769,3.88964730767638));
#60089=CARTESIAN_POINT('Ctrl Pts',(22.561460228444,0.587841786482003,4.19517031382209));
#60090=CARTESIAN_POINT('Ctrl Pts',(22.5853181464754,0.422455543015367,4.45296893898932));
#60091=CARTESIAN_POINT('Ctrl Pts',(22.6091760645069,0.153767157666155,4.60000417439789));
#60092=CARTESIAN_POINT('Ctrl Pts',(22.6330339825383,-0.152521006364708,
4.60032232020799));
#60093=CARTESIAN_POINT('Ctrl Pts',(22.6568919005697,-0.421514535902825,
4.45384478734481));
#60094=CARTESIAN_POINT('Ctrl Pts',(22.6807498186011,-0.587434568575047,
4.19639082134502));
#60095=CARTESIAN_POINT('Ctrl Pts',(22.7046077366325,-0.60971407867596,3.89091209973551));
#60096=CARTESIAN_POINT('Ctrl Pts',(22.728465654664,-0.482895786937606,3.61211183522625));
#60097=CARTESIAN_POINT('Ctrl Pts',(22.7523235726954,-0.23800784887647,3.4281541921173));
#60098=CARTESIAN_POINT('Ctrl Pts',(22.7761814907268,0.0651013135850054,
3.38404091701771));
#60099=CARTESIAN_POINT('Ctrl Pts',(22.8000394087582,0.352249768808992,3.49052260401466));
#60100=CARTESIAN_POINT('Ctrl Pts',(22.8238973267896,0.553345940411564,3.72163220123786));
#60101=CARTESIAN_POINT('Ctrl Pts',(22.8398026054772,0.597082876783669,3.92101540361374));
#60102=CARTESIAN_POINT('Ctrl Pts',(22.847755244821,0.593766187829899,4.01991291515446));
#60103=CARTESIAN_POINT('',(22.8,0.337479661717902,3.51106003648017));
#60104=CARTESIAN_POINT('Ctrl Pts',(22.8,0.337504360408405,3.51101527402275));
#60105=CARTESIAN_POINT('Ctrl Pts',(22.8,0.337610992569967,3.51114843896934));
#60106=CARTESIAN_POINT('Ctrl Pts',(22.8,0.337717562131928,3.51128164981369));
#60107=CARTESIAN_POINT('Ctrl Pts',(22.8,0.337824069051012,3.51141490653789));
#60108=CARTESIAN_POINT('Ctrl Pts',(22.8,0.354145371784291,3.53183539523119));
#60109=CARTESIAN_POINT('Ctrl Pts',(22.8,0.368999739942303,3.55333386321799));
#60110=CARTESIAN_POINT('Ctrl Pts',(22.8,0.382262544471458,3.57576050230915));
#60111=CARTESIAN_POINT('Ctrl Pts',(22.8,0.395177725624396,3.59759933027929));
#60112=CARTESIAN_POINT('Ctrl Pts',(22.8,0.406583379369087,3.62031953557487));
#60113=CARTESIAN_POINT('Ctrl Pts',(22.8,0.416319965152677,3.64376476659274));
#60114=CARTESIAN_POINT('Ctrl Pts',(22.8,0.420499854003763,3.65382973822867));
#60115=CARTESIAN_POINT('Ctrl Pts',(22.8,0.424371599987778,3.66402799385056));
#60116=CARTESIAN_POINT('Ctrl Pts',(22.8,0.42792023461967,3.67434527679585));
#60117=CARTESIAN_POINT('Ctrl Pts',(22.8,0.430015882150509,3.68043815216119));
#60118=CARTESIAN_POINT('Ctrl Pts',(22.8,0.431995626466768,3.68656321156818));
#60119=CARTESIAN_POINT('Ctrl Pts',(22.8,0.433857425300493,3.69271766785326));
#60120=CARTESIAN_POINT('Ctrl Pts',(22.8,0.440667704273582,3.71523007009016));
#60121=CARTESIAN_POINT('Ctrl Pts',(22.8,0.445903532435623,3.73813926926309));
#60122=CARTESIAN_POINT('Ctrl Pts',(22.8,0.449441836754149,3.76130640751661));
#60123=CARTESIAN_POINT('Ctrl Pts',(22.8,0.450038513826676,3.76521316594877));
#60124=CARTESIAN_POINT('Ctrl Pts',(22.8,0.450586822418701,3.76912718643627));
#60125=CARTESIAN_POINT('Ctrl Pts',(22.8,0.451086059471329,3.77304770583064));
#60126=CARTESIAN_POINT('Ctrl Pts',(22.8,0.453684096906641,3.79345015011803));
#60127=CARTESIAN_POINT('Ctrl Pts',(22.8,0.454954433743694,3.81403106227893));
#60128=CARTESIAN_POINT('Ctrl Pts',(22.8,0.45484641916779,3.83463783350426));
#60129=CARTESIAN_POINT('Ctrl Pts',(22.8,0.454808390965019,3.84189276616533));
#60130=CARTESIAN_POINT('Ctrl Pts',(22.8,0.454599381710613,3.84915061719132));
#60131=CARTESIAN_POINT('Ctrl Pts',(22.8,0.454216814112443,3.8564037154462));
#60132=CARTESIAN_POINT('Ctrl Pts',(22.8,0.453866695925276,3.86304160538904));
#60133=CARTESIAN_POINT('Ctrl Pts',(22.8,0.453371644107099,3.86966645154658));
#60134=CARTESIAN_POINT('Ctrl Pts',(22.8,0.452731182295137,3.87626933737115));
#60135=CARTESIAN_POINT('Ctrl Pts',(22.8,0.450713457978438,3.89707120727158));
#60136=CARTESIAN_POINT('Ctrl Pts',(22.8,0.447253508643,3.9176725514372));
#60137=CARTESIAN_POINT('Ctrl Pts',(22.8,0.442312061254715,3.9379035771693));
#60138=CARTESIAN_POINT('Ctrl Pts',(22.8,0.437564183511961,3.95734209977996));
#60139=CARTESIAN_POINT('Ctrl Pts',(22.8,0.431447509288203,3.97643919003209));
#60140=CARTESIAN_POINT('Ctrl Pts',(22.8,0.423915075143768,3.9949978423605));
#60141=CARTESIAN_POINT('Ctrl Pts',(22.8,0.421325190817866,4.00137888225459));
#60142=CARTESIAN_POINT('Ctrl Pts',(22.8,0.418567902041021,4.00769582483512));
#60143=CARTESIAN_POINT('Ctrl Pts',(22.8,0.415641328671541,4.01393920819689));
#60144=CARTESIAN_POINT('Ctrl Pts',(22.6211545887425,-1.51173456864708E-7,
4.59404872180247));
#60145=CARTESIAN_POINT('Ctrl Pts',(22.6251143866744,-0.0492822808754852,
4.59404929162283));
#60146=CARTESIAN_POINT('Ctrl Pts',(22.6290741846063,-0.0985642856931001,
4.58798571459226));
#60147=CARTESIAN_POINT('Ctrl Pts',(22.6330339825383,-0.14630523394925,4.57585637376244));
#60148=CARTESIAN_POINT('Ctrl Pts',(22.6409866218821,-0.242185516210759,
4.55149647592026));
#60149=CARTESIAN_POINT('Ctrl Pts',(22.6489392612259,-0.331850026056775,
4.50267063163255));
#60150=CARTESIAN_POINT('Ctrl Pts',(22.6568919005697,-0.404335619758509,
4.43534871515538));
#60151=CARTESIAN_POINT('Ctrl Pts',(22.6648445399135,-0.476821213460227,
4.36802679867822));
#60152=CARTESIAN_POINT('Ctrl Pts',(22.6727971792573,-0.532127891017642,
4.28220881001161));
#60153=CARTESIAN_POINT('Ctrl Pts',(22.6807498186011,-0.563494481479829,
4.18838669541007));
#60154=CARTESIAN_POINT('Ctrl Pts',(22.6887024579449,-0.594861071942019,
4.09456458080851));
#60155=CARTESIAN_POINT('Ctrl Pts',(22.6966550972887,-0.602287575308989,
3.99273834027202));
#60156=CARTESIAN_POINT('Ctrl Pts',(22.7046077366325,-0.584864445036083,
3.89535850925222));
#60157=CARTESIAN_POINT('Ctrl Pts',(22.7125603759763,-0.567441314763176,
3.79797867823242));
#60158=CARTESIAN_POINT('Ctrl Pts',(22.7205130153201,-0.525168550850394,
3.70504525672934));
#60159=CARTESIAN_POINT('Ctrl Pts',(22.7284656546639,-0.463217512550482,
3.62791893879298));
#60160=CARTESIAN_POINT('Ctrl Pts',(22.7364182940078,-0.401266474250563,
3.5507926208566));
#60161=CARTESIAN_POINT('Ctrl Pts',(22.7443709333516,-0.319637161563486,
3.48947340648693));
#60162=CARTESIAN_POINT('Ctrl Pts',(22.7523235726954,-0.228304311476372,
3.45146158678551));
#60163=CARTESIAN_POINT('Ctrl Pts',(22.7602762120392,-0.136971461389268,
3.41344976708409));
#60164=CARTESIAN_POINT('Ctrl Pts',(22.768228851383,-0.0359350739021178,
3.3987453420509));
#60165=CARTESIAN_POINT('Ctrl Pts',(22.7761814907268,0.062441195712126,3.40914007736714));
#60166=CARTESIAN_POINT('Ctrl Pts',(22.7841209938178,0.160654966376612,3.41951764255099));
#60167=CARTESIAN_POINT('Ctrl Pts',(22.7920604969089,0.256217399931083,3.45491151845628));
#60168=CARTESIAN_POINT('Ctrl Pts',(22.8,0.337504360408238,3.51101527402264));
#60169=CARTESIAN_POINT('Ctrl Pts',(4.,-0.219914231356244,4.35301468169996));
#60170=CARTESIAN_POINT('Ctrl Pts',(4.00793950309107,-0.278596966840389,
4.31645650682028));
#60171=CARTESIAN_POINT('Ctrl Pts',(4.02383164552594,-0.377405665439666,
4.21337674819164));
#60172=CARTESIAN_POINT('Ctrl Pts',(4.04767642730463,-0.433534992178268,
4.00656196868444));
#60173=CARTESIAN_POINT('Ctrl Pts',(4.07153434533603,-0.383670022685343,
3.79803920418254));
#60174=CARTESIAN_POINT('Ctrl Pts',(4.09539226336747,-0.239994733226421,
3.63889579340969));
#60175=CARTESIAN_POINT('Ctrl Pts',(4.11925018139887,-0.0376302499649443,
3.56805514133307));
#60176=CARTESIAN_POINT('Ctrl Pts',(4.1431080994303,0.173933765839147,3.60283521426327));
#60177=CARTESIAN_POINT('Ctrl Pts',(4.16696601746172,0.342967344134064,3.73473372141871));
#60178=CARTESIAN_POINT('Ctrl Pts',(4.19082393549313,0.428135478754777,3.93149662217858));
#60179=CARTESIAN_POINT('Ctrl Pts',(4.21468185352456,0.40861313688017,4.1450106963618));
#60180=CARTESIAN_POINT('Ctrl Pts',(4.23853977155597,0.289173588337559,4.32306558264197));
#60181=CARTESIAN_POINT('Ctrl Pts',(4.25811226835493,0.13317859508208,4.40432939198872));
#60182=CARTESIAN_POINT('Ctrl Pts',(4.26973212581007,0.0319512750557707,
4.41584666103033));
#60183=CARTESIAN_POINT('Ctrl Pts',(4.2733993439214,2.51014653359152E-6,
4.41583996132385));
#60184=CARTESIAN_POINT('Origin',(3.42660065607856,0.,4.));
#60185=CARTESIAN_POINT('Ctrl Pts',(4.,-0.219892372743211,3.64701365460636));
#60186=CARTESIAN_POINT('Ctrl Pts',(4.00795263934381,-0.161099076858729,
3.61038844940468));
#60187=CARTESIAN_POINT('Ctrl Pts',(4.02385791803142,-0.0249198690254346,
3.56711791692558));
#60188=CARTESIAN_POINT('Ctrl Pts',(4.04771583606284,0.185569069288609,3.60813812632505));
#60189=CARTESIAN_POINT('Ctrl Pts',(4.07157375409426,0.350624105231944,3.74494568050885));
#60190=CARTESIAN_POINT('Ctrl Pts',(4.09543167212568,0.429971014252744,3.94413788601839));
#60191=CARTESIAN_POINT('Ctrl Pts',(4.1192895901571,0.40416308778273,4.15698104289539));
#60192=CARTESIAN_POINT('Ctrl Pts',(4.14314750818851,0.279534313346206,4.3314427366163));
#60193=CARTESIAN_POINT('Ctrl Pts',(4.16225119682902,0.125004509401131,4.40624063703925));
#60194=CARTESIAN_POINT('Ctrl Pts',(4.1734022461257,0.0278694809177792,4.41585864517498));
#60195=CARTESIAN_POINT('Ctrl Pts',(4.17660065607858,5.88453344126799E-6,
4.41584444980552));
#60196=CARTESIAN_POINT('Ctrl Pts',(3.95224475517896,-0.314128184302177,
3.49573985500833));
#60197=CARTESIAN_POINT('Ctrl Pts',(3.96019739452277,-0.230138771413741,
3.44341876234755));
#60198=CARTESIAN_POINT('Ctrl Pts',(3.97610267321038,-0.0355993848822847,
3.38160445914153));
#60199=CARTESIAN_POINT('Ctrl Pts',(3.9999605912418,0.265095483172694,3.44020405374152));
#60200=CARTESIAN_POINT('Ctrl Pts',(4.02381850927322,0.500885556761892,3.63564106712445));
#60201=CARTESIAN_POINT('Ctrl Pts',(4.04767642730465,0.614236921112272,3.92019793948569));
#60202=CARTESIAN_POINT('Ctrl Pts',(4.07153434533605,0.577368897990231,4.22425593648149));
#60203=CARTESIAN_POINT('Ctrl Pts',(4.09539226336749,0.399329932212592,4.47348393104611));
#60204=CARTESIAN_POINT('Ctrl Pts',(4.11925018139889,0.123637843932736,4.60692867011962));
#60205=CARTESIAN_POINT('Ctrl Pts',(4.14310809943032,-0.182283847264271,
4.59196468982869));
#60206=CARTESIAN_POINT('Ctrl Pts',(4.16696601746173,-0.443633876576525,
4.43224822622665));
#60207=CARTESIAN_POINT('Ctrl Pts',(4.19082393549315,-0.596502436238336,
4.16683582239239));
#60208=CARTESIAN_POINT('Ctrl Pts',(4.21468185352458,-0.603510379797736,
3.86062723727387));
#60209=CARTESIAN_POINT('Ctrl Pts',(4.23853977155598,-0.462943343075553,
3.58849923641164));
#60210=CARTESIAN_POINT('Ctrl Pts',(4.26239768958742,-0.209174182705692,
3.41699430327496));
#60211=CARTESIAN_POINT('Ctrl Pts',(4.28625560761882,0.0957438341235747,
3.38805018506757));
#60212=CARTESIAN_POINT('Ctrl Pts',(4.31011352565025,0.377249837899377,3.50874444390425));
#60213=CARTESIAN_POINT('Ctrl Pts',(4.33397144368167,0.566508000142931,3.7495640793295));
#60214=CARTESIAN_POINT('Ctrl Pts',(4.35782936171309,0.617239514437223,4.05162211295782));
#60215=CARTESIAN_POINT('Ctrl Pts',(4.3816872797445,0.517039159770137,4.34105713706075));
#60216=CARTESIAN_POINT('Ctrl Pts',(4.40554519777592,0.290408643717306,4.54709439922074));
#60217=CARTESIAN_POINT('Ctrl Pts',(4.42940311580735,-0.00723469473045889,
4.61935217913086));
#60218=CARTESIAN_POINT('Ctrl Pts',(4.45326103383876,-0.303108954077165,
4.54016147994594));
#60219=CARTESIAN_POINT('Ctrl Pts',(4.47711895187019,-0.524864817190473,
4.3288865854667));
#60220=CARTESIAN_POINT('Ctrl Pts',(4.5009768699016,-0.618276935702851,4.03718996201469));
#60221=CARTESIAN_POINT('Ctrl Pts',(4.52483478793302,-0.560503501787052,
3.7363993798876));
#60222=CARTESIAN_POINT('Ctrl Pts',(4.54869270596444,-0.365671693940747,
3.50006632967672));
#60223=CARTESIAN_POINT('Ctrl Pts',(4.57255062399586,-0.0814231961944085,
3.38598067979976));
#60224=CARTESIAN_POINT('Ctrl Pts',(4.59640854202727,0.222735490926488,3.42203947925158));
#60225=CARTESIAN_POINT('Ctrl Pts',(4.6202664600587,0.472429283332598,3.59942536936051));
#60226=CARTESIAN_POINT('Ctrl Pts',(4.64412437809011,0.606601247243452,3.87476266809168));
#60227=CARTESIAN_POINT('Ctrl Pts',(4.66798229612153,0.592442682719785,4.18072390587243));
#60228=CARTESIAN_POINT('Ctrl Pts',(4.69184021415295,0.433415744455024,4.44249322584619));
#60229=CARTESIAN_POINT('Ctrl Pts',(4.71569813218437,0.168406850663934,4.59606089882753));
#60230=CARTESIAN_POINT('Ctrl Pts',(4.7395560502158,-0.1377821054254,4.60387544567241));
#60231=CARTESIAN_POINT('Ctrl Pts',(4.7634139682472,-0.410279583628813,4.46402599681362));
#60232=CARTESIAN_POINT('Ctrl Pts',(4.78727188627863,-0.582452527843622,
4.21070955191949));
#60233=CARTESIAN_POINT('Ctrl Pts',(4.81112980431005,-0.612199963312297,
3.9058688819681));
#60234=CARTESIAN_POINT('Ctrl Pts',(4.83498772234147,-0.492247831758966,
3.62404583445569));
#60235=CARTESIAN_POINT('Ctrl Pts',(4.85884564037289,-0.251927696778831,
3.4341538212047));
#60236=CARTESIAN_POINT('Ctrl Pts',(4.88270355840431,0.0499956224363984,
3.38262661200963));
#60237=CARTESIAN_POINT('Ctrl Pts',(4.90656147643572,0.339693650112522,3.48206401309162));
#60238=CARTESIAN_POINT('Ctrl Pts',(4.93041939446714,0.546327327266884,3.70815087126575));
#60239=CARTESIAN_POINT('Ctrl Pts',(4.95427731249857,0.619369091246891,4.00560279122603));
#60240=CARTESIAN_POINT('Ctrl Pts',(4.97813523052998,0.540958241141728,4.3016846761146));
#60241=CARTESIAN_POINT('Ctrl Pts',(5.00199314856141,0.330268365670778,4.52399643996756));
#60242=CARTESIAN_POINT('Ctrl Pts',(5.02585106659282,0.0388188784636707,
4.61817680087201));
#60243=CARTESIAN_POINT('Ctrl Pts',(5.04970898462424,-0.262122881932824,
4.56119609516527));
#60244=CARTESIAN_POINT('Ctrl Pts',(5.07356690265566,-0.498968457612796,
4.36698765751594));
#60245=CARTESIAN_POINT('Ctrl Pts',(5.09742482068708,-0.613802653778546,
4.08304074106085));
#60246=CARTESIAN_POINT('Ctrl Pts',(5.12128273871849,-0.578545381446849,
3.77878810143205));
#60247=CARTESIAN_POINT('Ctrl Pts',(5.14514065674992,-0.40181800409162,3.52862779669421));
#60248=CARTESIAN_POINT('Ctrl Pts',(5.16899857478133,-0.126835179433317,
3.39373083558568));
#60249=CARTESIAN_POINT('Ctrl Pts',(5.19285649281276,0.179162301517353,3.4070831996169));
#60250=CARTESIAN_POINT('Ctrl Pts',(5.21671441084417,0.441349719463922,3.56541987207117));
#60251=CARTESIAN_POINT('Ctrl Pts',(5.24057232887559,0.595615108876583,3.83002322352904));
#60252=CARTESIAN_POINT('Ctrl Pts',(5.26443024690701,0.604236379939102,4.13619052690848));
#60253=CARTESIAN_POINT('Ctrl Pts',(5.28828816493843,0.465105397037983,4.40905553670335));
#60254=CARTESIAN_POINT('Ctrl Pts',(5.31214608296985,0.21224347534444,4.58189532532512));
#60255=CARTESIAN_POINT('Ctrl Pts',(5.33600400100126,-0.0925177574670201,
4.61244585639451));
#60256=CARTESIAN_POINT('Ctrl Pts',(5.35986191903269,-0.37465587844466,4.49323669288525));
#60257=CARTESIAN_POINT('Ctrl Pts',(5.3837198370641,-0.565180431721392,4.25341772246777));
#60258=CARTESIAN_POINT('Ctrl Pts',(5.40757775509553,-0.617502974236318,
3.95163121594683));
#60259=CARTESIAN_POINT('Ctrl Pts',(5.43143567312694,-0.518829219107294,
3.66167219466597));
#60260=CARTESIAN_POINT('Ctrl Pts',(5.45529359115837,-0.293287587282116,
3.45444353765392));
#60261=CARTESIAN_POINT('Ctrl Pts',(5.47915150918978,0.00397084862654925,
3.38061829634467));
#60262=CARTESIAN_POINT('Ctrl Pts',(5.50300942722121,0.300258303883157,3.45824875319892));
#60263=CARTESIAN_POINT('Ctrl Pts',(5.52686734525262,0.523124424966688,3.66835214690199));
#60264=CARTESIAN_POINT('Ctrl Pts',(5.55072526328404,0.618072374525773,3.95955247459688));
#60265=CARTESIAN_POINT('Ctrl Pts',(5.57458318131546,0.561884792553919,4.26064332401524));
#60266=CARTESIAN_POINT('Ctrl Pts',(5.59844109934688,0.368301073379394,4.49799978094171));
#60267=CARTESIAN_POINT('Ctrl Pts',(5.62229901737829,0.0846577094226282,
4.61358172616469));
#60268=CARTESIAN_POINT('Ctrl Pts',(5.64615693540972,-0.219686770477705,
4.57912622575047));
#60269=CARTESIAN_POINT('Ctrl Pts',(5.67001485344113,-0.470311850924231,
4.40305858798173));
#60270=CARTESIAN_POINT('Ctrl Pts',(5.69387277147256,-0.605932872639677,
4.12843214650112));
#60271=CARTESIAN_POINT('Ctrl Pts',(5.71773068950397,-0.593386801983745,
3.82240054650545));
#60272=CARTESIAN_POINT('Ctrl Pts',(5.74158860753539,-0.435741494202748,
3.55979685111874));
#60273=CARTESIAN_POINT('Ctrl Pts',(5.76544652556682,-0.171545522688555,
3.40483481554927));
#60274=CARTESIAN_POINT('Ctrl Pts',(5.78930444359822,0.134598003740687,3.39540688139736));
#60275=CARTESIAN_POINT('Ctrl Pts',(5.81316236162965,0.407828648458881,3.53381843004554));
#60276=CARTESIAN_POINT('Ctrl Pts',(5.83702027966106,0.58133408605803,3.78622407765735));
#60277=CARTESIAN_POINT('Ctrl Pts',(5.86087819769249,0.612687492198482,4.09090374899912));
#60278=CARTESIAN_POINT('Ctrl Pts',(5.8847361157239,0.494222140250734,4.3733550009975));
#60279=CARTESIAN_POINT('Ctrl Pts',(5.90859403375532,0.254905969192102,4.56451074097759));
#60280=CARTESIAN_POINT('Ctrl Pts',(5.93245195178675,-0.0467415727364197,
4.61762831145024));
#60281=CARTESIAN_POINT('Ctrl Pts',(5.95630986981815,-0.336959681931401,
4.51971877801409));
#60282=CARTESIAN_POINT('Ctrl Pts',(5.98016778784959,-0.544781677596122,
4.29472414464893));
#60283=CARTESIAN_POINT('Ctrl Pts',(6.00402570588099,-0.61939026621187,3.99766086682344));
#60284=CARTESIAN_POINT('Ctrl Pts',(6.02788362391242,-0.542540019317823,
3.70117063377655));
#60285=CARTESIAN_POINT('Ctrl Pts',(6.05174154194384,-0.333025929677459,
3.47775031355921));
#60286=CARTESIAN_POINT('Ctrl Pts',(6.07559945997526,-0.042074208138152,
3.38203805739984));
#60287=CARTESIAN_POINT('Ctrl Pts',(6.09945737800668,0.259158778028439,3.43742717299816));
#60288=CARTESIAN_POINT('Ctrl Pts',(6.12331529603809,0.497033648893269,3.63039418124561));
#60289=CARTESIAN_POINT('Ctrl Pts',(6.14717321406952,0.613345206175343,3.91371436613889));
#60290=CARTESIAN_POINT('Ctrl Pts',(6.17103113210093,0.579724447951105,4.21818191418763));
#60291=CARTESIAN_POINT('Ctrl Pts',(6.19488905013236,0.40425597056565,4.46920707734689));
#60292=CARTESIAN_POINT('Ctrl Pts',(6.21874696816377,0.13010450107023,4.60567007851858));
#60293=CARTESIAN_POINT('Ctrl Pts',(6.24260488619519,-0.176179318911185,
4.59370602015056));
#60294=CARTESIAN_POINT('Ctrl Pts',(6.26646280422661,-0.438782409775579,
4.43717629804221));
#60295=CARTESIAN_POINT('Ctrl Pts',(6.29032072225803,-0.595217424383659,
4.17259489198797));
#60296=CARTESIAN_POINT('Ctrl Pts',(6.31417864028945,-0.604035436411749,
3.86794272465182));
#60297=CARTESIAN_POINT('Ctrl Pts',(6.34598919766468,-0.423477061217623,
3.4998212904071));
#60298=CARTESIAN_POINT('Ctrl Pts',(6.3857523943837,0.100470573235224,3.30464850830547));
#60299=CARTESIAN_POINT('Ctrl Pts',(6.43346823044655,0.640013163212275,3.70919899990029));
#60300=CARTESIAN_POINT('Ctrl Pts',(6.48118406650937,0.590335835129396,4.3806576914582));
#60301=CARTESIAN_POINT('Ctrl Pts',(6.52889990257223,-0.000686065451295705,
4.70262946694599));
#60302=CARTESIAN_POINT('Ctrl Pts',(6.57661573863505,-0.591483599613884,
4.37932465573422));
#60303=CARTESIAN_POINT('Ctrl Pts',(6.6243315746979,-0.638898060441451,3.70770201230499));
#60304=CARTESIAN_POINT('Ctrl Pts',(6.67204741076074,-0.0997162142428727,
3.30448953810453));
#60305=CARTESIAN_POINT('Ctrl Pts',(6.71976324682356,0.531096731682035,3.53998115137447));
#60306=CARTESIAN_POINT('Ctrl Pts',(6.76747908288643,0.674163513320998,4.19791190586338));
#60307=CARTESIAN_POINT('Ctrl Pts',(6.81519491894923,0.19815244237474,4.67409883091767));
#60308=CARTESIAN_POINT('Ctrl Pts',(6.86291075501209,-0.459834002450772,
4.53124951681343));
#60309=CARTESIAN_POINT('Ctrl Pts',(6.91062659107492,-0.695543074258338,
3.90054607923755));
#60310=CARTESIAN_POINT('Ctrl Pts',(6.95834242713776,-0.292526745343327,
3.36117245204842));
#60311=CARTESIAN_POINT('Ctrl Pts',(7.00605826320061,0.379122722467859,3.40844412700009));
#60312=CARTESIAN_POINT('Ctrl Pts',(7.05377409926343,0.702617257610868,3.99895059076549));
#60313=CARTESIAN_POINT('Ctrl Pts',(7.10148993532628,0.380887926283931,4.59042078110798));
#60314=CARTESIAN_POINT('Ctrl Pts',(7.14920577138911,-0.290616845661789,
4.63969846327979));
#60315=CARTESIAN_POINT('Ctrl Pts',(7.19692160745196,-0.695243592084394,
4.10153121423426));
#60316=CARTESIAN_POINT('Ctrl Pts',(7.24463744351478,-0.461417505508394,
3.47012628326466));
#60317=CARTESIAN_POINT('Ctrl Pts',(7.29235327957764,0.196135405489393,3.32531254251214));
#60318=CARTESIAN_POINT('Ctrl Pts',(7.34006911564046,0.673574140181709,3.80007467379138));
#60319=CARTESIAN_POINT('Ctrl Pts',(7.38778495170331,0.532459385890787,4.45843130921146));
#60320=CARTESIAN_POINT('Ctrl Pts',(7.43550078776614,-0.0976210197556089,
4.69580341906706));
#60321=CARTESIAN_POINT('Ctrl Pts',(7.48321662382899,-0.638054538563543,
4.29420854311633));
#60322=CARTESIAN_POINT('Ctrl Pts',(7.53093245989182,-0.592552758097988,
3.62243743491725));
#60323=CARTESIAN_POINT('Ctrl Pts',(7.57864829595465,-0.00290066162856385,
3.29738783984629));
#60324=CARTESIAN_POINT('Ctrl Pts',(7.6263641320175,0.589415156704478,3.61755780248734));
#60325=CARTESIAN_POINT('Ctrl Pts',(7.67407996808033,0.64046196749915,4.28893031975233));
#60326=CARTESIAN_POINT('Ctrl Pts',(7.72179580414318,0.103362698669259,4.69497367861456));
#60327=CARTESIAN_POINT('Ctrl Pts',(7.769511640206,-0.528656126737314,4.46281201486565));
#60328=CARTESIAN_POINT('Ctrl Pts',(7.81722747626886,-0.675201896567852,
3.80564295658466));
#60329=CARTESIAN_POINT('Ctrl Pts',(7.86494331233168,-0.201699375449268,
3.32695496184095));
#60330=CARTESIAN_POINT('Ctrl Pts',(7.91265914839452,0.457026785680635,3.46633458176699));
#60331=CARTESIAN_POINT('Ctrl Pts',(7.96037498445737,0.696058217263005,4.09578736675475));
#60332=CARTESIAN_POINT('Ctrl Pts',(8.0080908205202,0.295888677698302,4.63727713897333));
#60333=CARTESIAN_POINT('Ctrl Pts',(8.05580665658303,-0.375999987428149,
4.59354550870361));
#60334=CARTESIAN_POINT('Ctrl Pts',(8.10352249264589,-0.702602078596463,
4.00475190491975));
#60335=CARTESIAN_POINT('Ctrl Pts',(8.1512383287087,-0.383993870066737,3.41159455373064));
#60336=CARTESIAN_POINT('Ctrl Pts',(8.19895416477156,0.287241817850264,3.35877897763223));
#60337=CARTESIAN_POINT('Ctrl Pts',(8.24667000083438,0.694698924651979,3.89480653282778));
#60338=CARTESIAN_POINT('Ctrl Pts',(8.29438583689724,0.464203319628796,4.52743486753713));
#60339=CARTESIAN_POINT('Ctrl Pts',(8.34210167296006,-0.192577336495663,
4.67571164775853));
#60340=CARTESIAN_POINT('Ctrl Pts',(8.3898175090229,-0.672511261332963,4.20347202468314));
#60341=CARTESIAN_POINT('Ctrl Pts',(8.43753334508575,-0.534867746972347,
3.54438091052171));
#60342=CARTESIAN_POINT('Ctrl Pts',(8.48524918114857,0.0939530494311211,
3.303691816829));
#60343=CARTESIAN_POINT('Ctrl Pts',(8.53296501721143,0.636495314888509,3.70243324182078));
#60344=CARTESIAN_POINT('Ctrl Pts',(8.58068085327425,0.594534138944492,4.37443479950165));
#60345=CARTESIAN_POINT('Ctrl Pts',(8.6283966893371,0.00660311512414562,
4.7025871193802));
#60346=CARTESIAN_POINT('Ctrl Pts',(8.67611252539993,-0.58739165091669,4.3855428768395));
#60347=CARTESIAN_POINT('Ctrl Pts',(8.72382836146277,-0.64197562573843,3.71444867815739));
#60348=CARTESIAN_POINT('Ctrl Pts',(8.77154419752561,-0.107023505379864,
3.30558065209521));
#60349=CARTESIAN_POINT('Ctrl Pts',(8.81926003358845,0.526209946737336,3.53440859822909));
#60350=CARTESIAN_POINT('Ctrl Pts',(8.86697586965128,0.676216707984864,4.19079629265377));
#60351=CARTESIAN_POINT('Ctrl Pts',(8.91469170571413,0.20524326135842,4.67197281575615));
#60352=CARTESIAN_POINT('Ctrl Pts',(8.96240754177695,-0.45420823024697,4.53606636251889));
#60353=CARTESIAN_POINT('Ctrl Pts',(9.0101233778398,-0.69655331512461,3.90788192013928));
#60354=CARTESIAN_POINT('Ctrl Pts',(9.05783921390263,-0.299242772872918,
3.36429092791464));
#60355=CARTESIAN_POINT('Ctrl Pts',(9.10555504996548,0.37286701214988,3.40448135822736));
#60356=CARTESIAN_POINT('Ctrl Pts',(9.15327088602831,0.702567282619003,3.99154572051203));
#60357=CARTESIAN_POINT('Ctrl Pts',(9.20098672209116,0.387089207071907,4.58637377773631));
#60358=CARTESIAN_POINT('Ctrl Pts',(9.24870255815397,-0.28385884346236,4.64272577234503));
#60359=CARTESIAN_POINT('Ctrl Pts',(9.29641839421684,-0.694134950315416,
4.10885280060212));
#60360=CARTESIAN_POINT('Ctrl Pts',(9.34413423027966,-0.46697625165475,3.47501862715065));
#60361=CARTESIAN_POINT('Ctrl Pts',(9.39185006634251,0.189013924253689,3.32328292626348));
#60362=CARTESIAN_POINT('Ctrl Pts',(9.43956590240535,0.671429705166911,3.79298692681914));
#60363=CARTESIAN_POINT('Ctrl Pts',(9.48728173846818,0.537261256551386,4.45279421778236));
#60364=CARTESIAN_POINT('Ctrl Pts',(9.53499757453101,-0.090282470782305,
4.69679361142145));
#60365=CARTESIAN_POINT('Ctrl Pts',(9.58271341059386,-0.634918416022234,
4.30091671014441));
#60366=CARTESIAN_POINT('Ctrl Pts',(9.63042924665669,-0.596499010353368,
3.62870336374299));
#60367=CARTESIAN_POINT('Ctrl Pts',(9.67814508271953,-0.0103053851599677,
3.29745743154951));
#60368=CARTESIAN_POINT('Ctrl Pts',(9.72586091878236,0.585351833794561,3.61136714997101));
#60369=CARTESIAN_POINT('Ctrl Pts',(9.77357675484522,0.643471456979869,4.28216439445919));
#60370=CARTESIAN_POINT('Ctrl Pts',(9.82129259090803,0.110681340139534,4.69384573385819));
#60371=CARTESIAN_POINT('Ctrl Pts',(9.8690084269709,-0.523749154402255,4.46835785966634));
#60372=CARTESIAN_POINT('Ctrl Pts',(9.91672426303372,-0.677212741539845,
3.81276975633088));
#60373=CARTESIAN_POINT('Ctrl Pts',(9.96444009909655,-0.208781447863971,
3.32911806666439));
#60374=CARTESIAN_POINT('Ctrl Pts',(10.0121559351594,0.451377061900895,3.4615475792254));
#60375=CARTESIAN_POINT('Ctrl Pts',(10.0598717712222,0.697029070393332,4.08844623493918));
#60376=CARTESIAN_POINT('Ctrl Pts',(10.1075876072851,0.302588558372737,4.63412335218805));
#60377=CARTESIAN_POINT('Ctrl Pts',(10.1553034433479,-0.369723682724971,
4.5974752378807));
#60378=CARTESIAN_POINT('Ctrl Pts',(10.2030192794108,-0.702512977046242,
4.01215641928927));
#60379=CARTESIAN_POINT('Ctrl Pts',(10.2507351154736,-0.390173794994359,
3.41567417381395));
#60380=CARTESIAN_POINT('Ctrl Pts',(10.2984509515364,0.280467986596366,3.3557873255338));
#60381=CARTESIAN_POINT('Ctrl Pts',(10.3461667875993,0.693551700540965,3.8874908887021));
#60382=CARTESIAN_POINT('Ctrl Pts',(10.3938826236621,0.469736216214169,4.52251329995044));
#60383=CARTESIAN_POINT('Ctrl Pts',(10.441598459725,-0.185445263282835,4.67770370795377));
#60384=CARTESIAN_POINT('Ctrl Pts',(10.4893142957878,-0.670329504065059,
4.21054837313121));
#60385=CARTESIAN_POINT('Ctrl Pts',(10.5370301318506,-0.539639846919137,
3.55004322755915));
#60386=CARTESIAN_POINT('Ctrl Pts',(10.5847459679134,0.0866093850789692,
3.30274030959437));
#60387=CARTESIAN_POINT('Ctrl Pts',(10.6324618039763,0.633323886102378,3.69574169404847));
#60388=CARTESIAN_POINT('Ctrl Pts',(10.6801776400391,0.598447317577389,4.36814816247366));
#60389=CARTESIAN_POINT('Ctrl Pts',(10.727893476102,0.0140073690254923,4.70247850861168));
#60390=CARTESIAN_POINT('Ctrl Pts',(10.7756093121648,-0.583295762033595,
4.39171203127037));
#60391=CARTESIAN_POINT('Ctrl Pts',(10.8233251482277,-0.644949419658282,
3.72123036834915));
#60392=CARTESIAN_POINT('Ctrl Pts',(10.8710409842905,-0.114336101388361,
3.30674714759503));
#60393=CARTESIAN_POINT('Ctrl Pts',(10.9187568203533,0.521273818073547,3.52888868827067));
#60394=CARTESIAN_POINT('Ctrl Pts',(10.9664726564162,0.678189969569843,4.18365899548663));
#60395=CARTESIAN_POINT('Ctrl Pts',(11.014188492479,0.212313836716152,4.66977242119035));
#60396=CARTESIAN_POINT('Ctrl Pts',(11.0619043285418,-0.44853335926228,4.54082352674158));
#60397=CARTESIAN_POINT('Ctrl Pts',(11.1096201646047,-0.697485469857315,
3.91522806604643));
#60398=CARTESIAN_POINT('Ctrl Pts',(11.1573360006675,-0.305925941288932,
3.36747997668469));
#60399=CARTESIAN_POINT('Ctrl Pts',(11.2050518367303,0.36657008644075,3.40058475730499));
#60400=CARTESIAN_POINT('Ctrl Pts',(11.2527676727932,0.702439163386103,3.98414177848112));
#60401=CARTESIAN_POINT('Ctrl Pts',(11.300483508856,0.393247548178179,4.58226164848818));
#60402=CARTESIAN_POINT('Ctrl Pts',(11.3481993449189,-0.277069341413063,
4.64568168744144));
#60403=CARTESIAN_POINT('Ctrl Pts',(11.3959151809817,-0.692949191524882,
4.11616229772746));
#60404=CARTESIAN_POINT('Ctrl Pts',(11.4436310170446,-0.47248313666557,3.47996928262364));
#60405=CARTESIAN_POINT('Ctrl Pts',(11.4913468531074,0.181871452681271,3.32132847698764));
#60406=CARTESIAN_POINT('Ctrl Pts',(11.5390626891702,0.669210688578896,3.78592217363756));
#60407=CARTESIAN_POINT('Ctrl Pts',(11.586778525233,0.54200345202451,4.44710683224685));
#60408=CARTESIAN_POINT('Ctrl Pts',(11.6344943612959,-0.082933894319074,
4.69770640718098));
#60409=CARTESIAN_POINT('Ctrl Pts',(11.6822101973587,-0.631711769407458,
4.30759145280778));
#60410=CARTESIAN_POINT('Ctrl Pts',(11.7299260334216,-0.600379006513997,
3.63501053441836));
#60411=CARTESIAN_POINT('Ctrl Pts',(11.7776418694844,-0.0177089639202829,
3.29760505835735));
#60412=CARTESIAN_POINT('Ctrl Pts',(11.8253577055473,0.581223492728864,3.60521966494218));
#60413=CARTESIAN_POINT('Ctrl Pts',(11.8730735416101,0.646409472732109,4.27536712768685));
#60414=CARTESIAN_POINT('Ctrl Pts',(11.9207893776729,0.11798768763725,4.69264072000881));
#60415=CARTESIAN_POINT('Ctrl Pts',(11.9685052137358,-0.518784006488825,
4.4738516814993));
#60416=CARTESIAN_POINT('Ctrl Pts',(12.0162210497986,-0.679148364938221,
3.81991735272367));
#60417=CARTESIAN_POINT('Ctrl Pts',(12.0639368858614,-0.215840329824027,
3.33135568986959));
#60418=CARTESIAN_POINT('Ctrl Pts',(12.1116527219243,0.445677201297934,3.45682038542343));
#60419=CARTESIAN_POINT('Ctrl Pts',(12.1593685579871,0.697922500842799,4.08109527893561));
#60420=CARTESIAN_POINT('Ctrl Pts',(12.2070843940499,0.309254828945687,4.63089912998995));
#60421=CARTESIAN_POINT('Ctrl Pts',(12.2548002301128,-0.36340631086944,4.60133860234362));
#60422=CARTESIAN_POINT('Ctrl Pts',(12.3025160661756,-0.702345843688318,
4.0195595833814));
#60423=CARTESIAN_POINT('Ctrl Pts',(12.3502319022385,-0.396310381268302,
3.41981869803717));
#60424=CARTESIAN_POINT('Ctrl Pts',(12.3979477383013,0.273663002289436,3.35286722952223));
#60425=CARTESIAN_POINT('Ctrl Pts',(12.4456635743641,0.69232743999824,3.88018774155459));
#60426=CARTESIAN_POINT('Ctrl Pts',(12.493379410427,0.475216936729713,4.51753369406595));
#60427=CARTESIAN_POINT('Ctrl Pts',(12.5410952464898,-0.178292591690169,
4.67962049203707));
#60428=CARTESIAN_POINT('Ctrl Pts',(12.5888110825527,-0.66807328977682,4.21760133486514));
#60429=CARTESIAN_POINT('Ctrl Pts',(12.6365269186155,-0.544352006232531,
3.55575552365962));
#60430=CARTESIAN_POINT('Ctrl Pts',(12.6842427546784,0.0792561005673328,
3.3018662506574));
#60431=CARTESIAN_POINT('Ctrl Pts',(12.7319585907411,0.630082110704352,3.68908394184497));
#60432=CARTESIAN_POINT('Ctrl Pts',(12.779674426804,0.60229402352211,4.36182063329482));
#60433=CARTESIAN_POINT('Ctrl Pts',(12.8273902628668,0.0214100670547408,
4.70229186986395));
#60434=CARTESIAN_POINT('Ctrl Pts',(12.8751060989297,-0.579135083425219,
4.39783767618763));
#60435=CARTESIAN_POINT('Ctrl Pts',(12.9228219349925,-0.647851575657132,
3.7280430229487));
#60436=CARTESIAN_POINT('Ctrl Pts',(12.9705377710554,-0.121635997485283,
3.30799064633195));
#60437=CARTESIAN_POINT('Ctrl Pts',(13.0182536071182,0.516279788787698,3.52342110712114));
#60438=CARTESIAN_POINT('Ctrl Pts',(13.065969443181,0.68008790103128,4.17650129834983));
#60439=CARTESIAN_POINT('Ctrl Pts',(13.1136852792439,0.219360829260397,4.66749763148232));
#60440=CARTESIAN_POINT('Ctrl Pts',(13.1614011153067,-0.44280866732052,4.54552061885334));
#60441=CARTESIAN_POINT('Ctrl Pts',(13.2091169513696,-0.698340151213866,
3.92258362801769));
#60442=CARTESIAN_POINT('Ctrl Pts',(13.2568327874324,-0.31257512890311,3.37073928277739));
#60443=CARTESIAN_POINT('Ctrl Pts',(13.3045486234952,0.36023244386594,3.39675473658331));
#60444=CARTESIAN_POINT('Ctrl Pts',(13.3522644595581,0.702233020544282,3.97673959790624));
#60445=CARTESIAN_POINT('Ctrl Pts',(13.3999802956209,0.39936220921291,4.57808484437918));
#60446=CARTESIAN_POINT('Ctrl Pts',(13.4476961316837,-0.270249063816132,
4.64856588328003));
#60447=CARTESIAN_POINT('Ctrl Pts',(13.4954119677466,-0.691686463226468,
4.123458892096));
#60448=CARTESIAN_POINT('Ctrl Pts',(13.5431278038094,-0.47793754049168,3.48497770064095));
#60449=CARTESIAN_POINT('Ctrl Pts',(13.5908436398723,0.174708779690948,3.31944941132403));
#60450=CARTESIAN_POINT('Ctrl Pts',(13.6385594759351,0.666917339243262,3.77888119920505));
#60451=CARTESIAN_POINT('Ctrl Pts',(13.6862753119979,0.54668544432619,4.44136978420615));
#60452=CARTESIAN_POINT('Ctrl Pts',(13.7339911480608,-0.075576105952426,
4.69854170502367));
#60453=CARTESIAN_POINT('Ctrl Pts',(13.7817069841236,-0.62843495524706,4.31423202967224));
#60454=CARTESIAN_POINT('Ctrl Pts',(13.8294228201864,-0.604192315423611,
3.64135824639153));
#60455=CARTESIAN_POINT('Ctrl Pts',(13.8771386562493,-0.025110575652917,
3.29783070386218));
#60456=CARTESIAN_POINT('Ctrl Pts',(13.9248544923121,0.577030592115723,3.59911603023956));
#60457=CARTESIAN_POINT('Ctrl Pts',(13.972570328375,0.649275688387581,4.26853927444071));
#60458=CARTESIAN_POINT('Ctrl Pts',(14.0202861644378,0.125280929622514,4.69135877091509));
#60459=CARTESIAN_POINT('Ctrl Pts',(14.0680020005006,-0.513761234509794,
4.47929287013608));
#60460=CARTESIAN_POINT('Ctrl Pts',(14.1157178365635,-0.681008551759042,
3.82708495184235));
#60461=CARTESIAN_POINT('Ctrl Pts',(14.1634336726263,-0.222875237264486,
3.33366758291179));
#60462=CARTESIAN_POINT('Ctrl Pts',(14.2111495086891,0.439927836986373,3.45215352543546));
#60463=CARTESIAN_POINT('Ctrl Pts',(14.258865344752,0.698738409372782,4.07373531525328));
#60464=CARTESIAN_POINT('Ctrl Pts',(14.3065811808148,0.315886748959774,4.62760483051036));
#60465=CARTESIAN_POINT('Ctrl Pts',(14.3542970168777,-0.357048573565392,
4.60513517296818));
#60466=CARTESIAN_POINT('Ctrl Pts',(14.4020128529405,-0.702100697086982,
4.02696057488784));
#60467=CARTESIAN_POINT('Ctrl Pts',(14.4497286890033,-0.402402947265751,
3.42402766604624));
#60468=CARTESIAN_POINT('Ctrl Pts',(14.4974445250662,0.266827620794843,3.35001901394789));
#60469=CARTESIAN_POINT('Ctrl Pts',(14.545160361129,0.691026279008849,3.87289790258421));
#60470=CARTESIAN_POINT('Ctrl Pts',(14.5928761971919,0.480644872403009,4.51249660299459));
#60471=CARTESIAN_POINT('Ctrl Pts',(14.6405920332547,-0.171120116202498,
4.6814617871012));
#60472=CARTESIAN_POINT('Ctrl Pts',(14.6883078693176,-0.665742869077823,
4.22463012647536));
#60473=CARTESIAN_POINT('Ctrl Pts',(14.7360237053803,-0.549003701508229,
3.56151716432844));
#60474=CARTESIAN_POINT('Ctrl Pts',(14.7837395414432,0.0718940126641393,
3.30106973710437));
#60475=CARTESIAN_POINT('Ctrl Pts',(14.831455377506,0.626770348775451,3.68246072472179));
#60476=CARTESIAN_POINT('Ctrl Pts',(14.8791712135689,0.606073829504824,4.35545291479698));
#60477=CARTESIAN_POINT('Ctrl Pts',(14.9268870496317,0.0288103869553486,
4.70202722386799));
#60478=CARTESIAN_POINT('Ctrl Pts',(14.9746028856946,-0.574910077240004,
4.4039191311837));
#60479=CARTESIAN_POINT('Ctrl Pts',(15.0223187217574,-0.650681771377263,
3.73488588523872));
#60480=CARTESIAN_POINT('Ctrl Pts',(15.0700345578202,-0.128922382832804,
3.30931101018402));
#60481=CARTESIAN_POINT('Ctrl Pts',(15.1177503938831,0.511228413592865,3.51800646209349));
#60482=CARTESIAN_POINT('Ctrl Pts',(15.1654662299459,0.681910291555949,4.16932399628639));
#60483=CARTESIAN_POINT('Ctrl Pts',(15.2131820660088,0.226383456244684,4.6651486993049));
#60484=CARTESIAN_POINT('Ctrl Pts',(15.2608979020716,-0.437034790293287,
4.55015711712348));
#60485=CARTESIAN_POINT('Ctrl Pts',(15.3086137381344,-0.699117264260319,
3.92994778903219));
#60486=CARTESIAN_POINT('Ctrl Pts',(15.3563295741972,-0.319189597155267,
3.37406848416447));
#60487=CARTESIAN_POINT('Ctrl Pts',(15.4040454102601,0.353854788380711,3.39299172148285));
#60488=CARTESIAN_POINT('Ctrl Pts',(15.4517612463229,0.70194887699091,3.96934000098645));
#60489=CARTESIAN_POINT('Ctrl Pts',(15.4994770823858,0.40543251098856,4.57384382934891));
#60490=CARTESIAN_POINT('Ctrl Pts',(15.5471929184486,-0.263398768235635,
4.65137803949801));
#60491=CARTESIAN_POINT('Ctrl Pts',(15.5949087545115,-0.690346905678043,
4.13074177323664));
#60492=CARTESIAN_POINT('Ctrl Pts',(15.6426245905743,-0.483338857283784,
3.4900433248913));
#60493=CARTESIAN_POINT('Ctrl Pts',(15.6903404266371,0.167526700878456,3.31764593799033));
#60494=CARTESIAN_POINT('Ctrl Pts',(15.7380562627,0.664549911894371,3.77186478559966));
#60495=CARTESIAN_POINT('Ctrl Pts',(15.7857720987628,0.551306713402943,4.43558371090429));
#60496=CARTESIAN_POINT('Ctrl Pts',(15.8334879348256,-0.0682099229505586,
4.69929941216862));
#60497=CARTESIAN_POINT('Ctrl Pts',(15.8812037708885,-0.625088337514006,
4.32083770313399));
#60498=CARTESIAN_POINT('Ctrl Pts',(15.9289196069513,-0.607938513517956,
3.64774579458877));
#60499=CARTESIAN_POINT('Ctrl Pts',(15.9766354430142,-0.0325093982219456,
3.29813434300035));
#60500=CARTESIAN_POINT('Ctrl Pts',(16.024351279077,0.572773597682653,3.59305692382598));
#60501=CARTESIAN_POINT('Ctrl Pts',(16.0720671151399,0.652069785580651,4.2616815931263));
#60502=CARTESIAN_POINT('Ctrl Pts',(16.1197829512026,0.132560255996602,4.69000002896988));
#60503=CARTESIAN_POINT('Ctrl Pts',(16.1674987872655,-0.508681396370837,
4.48468082119526));
#60504=CARTESIAN_POINT('Ctrl Pts',(16.2152146233283,-0.682793095381579,
3.83427175754402));
#60505=CARTESIAN_POINT('Ctrl Pts',(16.2629304593912,-0.229885388781225,
3.33605348899688));
#60506=CARTESIAN_POINT('Ctrl Pts',(16.310646295454,0.434129607578297,3.44754751763412));
#60507=CARTESIAN_POINT('Ctrl Pts',(16.3583621315168,0.699476705356048,4.06636716140204));
#60508=CARTESIAN_POINT('Ctrl Pts',(16.4060779675797,0.322483581772784,4.62424081966442));
#60509=CARTESIAN_POINT('Ctrl Pts',(16.4537938036425,-0.350651177000141,
4.60886452804932));
#60510=CARTESIAN_POINT('Ctrl Pts',(16.5015096397054,-0.701777564471952,
4.03435857174156));
#60511=CARTESIAN_POINT('Ctrl Pts',(16.5492254757682,-0.408450816253369,
3.42830061032894));
#60512=CARTESIAN_POINT('Ctrl Pts',(16.596941311831,0.259962601354342,3.34724299517707));
#60513=CARTESIAN_POINT('Ctrl Pts',(16.6446571478939,0.689648362099571,3.86562218151166));
#60514=CARTESIAN_POINT('Ctrl Pts',(16.6923729839567,0.486019420324727,4.50740258623259));
#60515=CARTESIAN_POINT('Ctrl Pts',(16.7400888200196,-0.163928633504336,
4.6832273886238));
#60516=CARTESIAN_POINT('Ctrl Pts',(16.7878046560824,-0.663338500820136,
4.23163396723712));
#60517=CARTESIAN_POINT('Ctrl Pts',(16.8355204921452,-0.553594416058007,
3.56732750958986));
#60518=CARTESIAN_POINT('Ctrl Pts',(16.8832363282081,0.064523939115192,3.30035085740826));
#60519=CARTESIAN_POINT('Ctrl Pts',(16.9309521642709,0.623388968170475,3.67587277835446));
#60520=CARTESIAN_POINT('Ctrl Pts',(16.9786680003338,0.609786315682611,4.34904571427615));
#60521=CARTESIAN_POINT('Ctrl Pts',(17.0263838363966,0.0362075067348799,
4.70168460001938));
#60522=CARTESIAN_POINT('Ctrl Pts',(17.0740996724594,-0.570621212771584,
4.40995572075944));
#60523=CARTESIAN_POINT('Ctrl Pts',(17.1218155085223,-0.653439692453966,
3.74175819514654));
#60524=CARTESIAN_POINT('Ctrl Pts',(17.1695313445851,-0.136194448093839,
3.31070809249149));
#60525=CARTESIAN_POINT('Ctrl Pts',(17.2172471806479,0.50612025357182,3.51264535462077));
#60526=CARTESIAN_POINT('Ctrl Pts',(17.2649630167108,0.683656938721366,4.16212788651693));
#60527=CARTESIAN_POINT('Ctrl Pts',(17.3126788527736,0.233380937628925,4.66272588556639));
#60528=CARTESIAN_POINT('Ctrl Pts',(17.3603946888365,-0.431212369515449,
4.55473250655174));
#60529=CARTESIAN_POINT('Ctrl Pts',(17.4081105248993,-0.699816722678643,
3.93731973111387));
#60530=CARTESIAN_POINT('Ctrl Pts',(17.4558263609621,-0.325768611341644,
3.37746721105403));
#60531=CARTESIAN_POINT('Ctrl Pts',(17.503542197025,0.347437828384778,3.38929612998149));
#60532=CARTESIAN_POINT('Ctrl Pts',(17.5512580330878,0.701586764287296,3.96194380963385));
#60533=CARTESIAN_POINT('Ctrl Pts',(17.5989738691507,0.411457779244836,4.56953907446917));
#60534=CARTESIAN_POINT('Ctrl Pts',(17.6466897052135,-0.256519215569882,
4.65411784373439));
#60535=CARTESIAN_POINT('Ctrl Pts',(17.6944055412764,-0.688930667671302,
4.13801013220155));
#60536=CARTESIAN_POINT('Ctrl Pts',(17.7421213773391,-0.488686487089258,
3.49516559270919));
#60537=CARTESIAN_POINT('Ctrl Pts',(17.789837213402,0.160326013994967,3.3159182573078));
#60538=CARTESIAN_POINT('Ctrl Pts',(17.8375530494648,0.662108669494809,3.76487371217125));
#60539=CARTESIAN_POINT('Ctrl Pts',(17.8852688855277,0.555866745946156,4.42974925503083));
#60540=CARTESIAN_POINT('Ctrl Pts',(17.9329847215905,-0.060836163514142,
4.69997944445332));
#60541=CARTESIAN_POINT('Ctrl Pts',(17.9807005576534,-0.621672287934692,
4.32740773946617));
#60542=CARTESIAN_POINT('Ctrl Pts',(18.0284163937162,-0.611617184687133,
3.65417246951162));
#60543=CARTESIAN_POINT('Ctrl Pts',(18.0761322297791,-0.0399046098013318,
3.29851594204507));
#60544=CARTESIAN_POINT('Ctrl Pts',(18.1238480658419,0.568452982276385,3.58704301871817));
#60545=CARTESIAN_POINT('Ctrl Pts',(18.1715639019047,0.65479145395626,4.25479484546229));
#60546=CARTESIAN_POINT('Ctrl Pts',(18.2192797379675,0.139824858206545,4.68856464509573));
#60547=CARTESIAN_POINT('Ctrl Pts',(18.2669955740304,-0.503545056316242,
4.49001493620888));
#60548=CARTESIAN_POINT('Ctrl Pts',(18.3147114100932,-0.684501797587214,
3.84147697155243));
#60549=CARTESIAN_POINT('Ctrl Pts',(18.3624272461561,-0.236870005719869,
3.33851314310973));
#60550=CARTESIAN_POINT('Ctrl Pts',(18.4101430822189,0.42828315711354,3.44300287363294));
#60551=CARTESIAN_POINT('Ctrl Pts',(18.4578589182817,0.70013730678616,4.05899163580144));
#60552=CARTESIAN_POINT('Ctrl Pts',(18.5055747543446,0.32904459463985,4.62080747111051));
#60553=CARTESIAN_POINT('Ctrl Pts',(18.5532905904074,-0.34421483176614,4.61252625334797));
#60554=CARTESIAN_POINT('Ctrl Pts',(18.6010064264702,-0.701376481735239,
4.0417527522082));
#60555=CARTESIAN_POINT('Ctrl Pts',(18.6487222625331,-0.414453316462639,
3.43263705626685));
#60556=CARTESIAN_POINT('Ctrl Pts',(18.6964380985959,0.253068706501803,3.34453948155689));
#60557=CARTESIAN_POINT('Ctrl Pts',(18.7441539346588,0.68819384232267,3.85836138648927));
#60558=CARTESIAN_POINT('Ctrl Pts',(18.7918697707216,0.491339983515996,4.50225220959958));
#60559=CARTESIAN_POINT('Ctrl Pts',(18.8395856067844,-0.156718942392259,
4.68491710048942));
#60560=CARTESIAN_POINT('Ctrl Pts',(18.8873014428473,-0.660860452068119,
4.23861207919858));
#60561=CARTESIAN_POINT('Ctrl Pts',(18.9350172789101,-0.558123639969822,
3.57318591405529));
#60562=CARTESIAN_POINT('Ctrl Pts',(18.9827331149729,0.0571466985584877,
3.29970969142451));
#60563=CARTESIAN_POINT('Ctrl Pts',(19.0304489510358,0.619938344467307,3.66932083449001));
#60564=CARTESIAN_POINT('Ctrl Pts',(19.0781647870986,0.613431069708698,4.3425997434341));
#60565=CARTESIAN_POINT('Ctrl Pts',(19.1258806231615,0.0436006047213211,
4.70126403633668));
#60566=CARTESIAN_POINT('Ctrl Pts',(19.1735964592243,-0.566268966340429,
4.41594677447179));
#60567=CARTESIAN_POINT('Ctrl Pts',(19.2213122952871,-0.656125032675529,
3.74865918919138));
#60568=CARTESIAN_POINT('Ctrl Pts',(19.26902813135,-0.143451385285705,3.31218173833215));
#60569=CARTESIAN_POINT('Ctrl Pts',(19.3167439674128,0.500955875668841,3.50733837970023));
#60570=CARTESIAN_POINT('Ctrl Pts',(19.3644598034757,0.68532764936022,4.15491376927485));
#60571=CARTESIAN_POINT('Ctrl Pts',(19.4121756395385,0.240352494576274,4.66022945763735));
#60572=CARTESIAN_POINT('Ctrl Pts',(19.4598914756013,-0.425342048711971,
4.55924628221868));
#60573=CARTESIAN_POINT('Ctrl Pts',(19.5076073116642,-0.700438454444525,
3.94469862920436));
#60574=CARTESIAN_POINT('Ctrl Pts',(19.555323147727,-0.332311429993836,3.3809350976725));
#60575=CARTESIAN_POINT('Ctrl Pts',(19.6030389837899,0.340982256434611,3.38566835039883));
#60576=CARTESIAN_POINT('Ctrl Pts',(19.6507548198527,0.701146760813864,3.95455188724214));
#60577=CARTESIAN_POINT('Ctrl Pts',(19.6984706559155,0.417437272672218,4.56517097885182));
#60578=CARTESIAN_POINT('Ctrl Pts',(19.7461864919784,-0.249611033919464,
4.6567851409082));
#60579=CARTESIAN_POINT('Ctrl Pts',(19.7939023280412,-0.687438163400574,
4.14526287985386));
#60580=CARTESIAN_POINT('Ctrl Pts',(19.841618164104,-0.493979350866992,3.5003444672369));
#60581=CARTESIAN_POINT('Ctrl Pts',(19.8893340001669,0.153106602982307,3.31426555646693));
#60582=CARTESIAN_POINT('Ctrl Pts',(19.9370498362297,0.659595612567133,3.75791065255607));
#60583=CARTESIAN_POINT('Ctrl Pts',(19.9847656722925,0.560361770063263,4.42386348253578));
#60584=CARTESIAN_POINT('Ctrl Pts',(20.0324815083554,-0.0534494809679074,
4.70058849011268));
#60585=CARTESIAN_POINT('Ctrl Pts',(20.0801973444182,-0.618198828117398,
4.33392863744107));
#60586=CARTESIAN_POINT('Ctrl Pts',(20.1279131804811,-0.615205937201001,
3.66066167313574));
#60587=CARTESIAN_POINT('Ctrl Pts',(20.1756290165439,-0.0473369003220797,
3.29892991724937));
#60588=CARTESIAN_POINT('Ctrl Pts',(20.2233448526068,0.564147630203746,3.58116102158214));
#60589=CARTESIAN_POINT('Ctrl Pts',(20.2710606886696,0.657292163719816,4.24771695100806));
#60590=CARTESIAN_POINT('Ctrl Pts',(20.3187765247324,0.147355317357748,4.68736342730055));
#60591=CARTESIAN_POINT('Ctrl Pts',(20.3664923607953,-0.498896366832293,
4.49468216892218));
#60592=CARTESIAN_POINT('Ctrl Pts',(20.4062555575143,-0.653992183610565,
3.9575054511282));
#60593=CARTESIAN_POINT('Ctrl Pts',(20.4380661148895,-0.465699721472375,
3.59327933193152));
#60594=CARTESIAN_POINT('Ctrl Pts',(20.461924032921,-0.215665100260693,3.41899970433759));
#60595=CARTESIAN_POINT('Ctrl Pts',(20.4857819509523,0.0900520562992202,
3.38718375849312));
#60596=CARTESIAN_POINT('Ctrl Pts',(20.5096398689838,0.372154449079436,3.50499792242313));
#60597=CARTESIAN_POINT('Ctrl Pts',(20.5334977870152,0.564103623124681,3.74397162737493));
#60598=CARTESIAN_POINT('Ctrl Pts',(20.5573557050466,0.61766411855396,4.04548854604559));
#60599=CARTESIAN_POINT('Ctrl Pts',(20.581213623078,0.520427284318709,4.33591550271974));
#60600=CARTESIAN_POINT('Ctrl Pts',(20.6050715411094,0.295805552416038,4.5441843692251));
#60601=CARTESIAN_POINT('Ctrl Pts',(20.6289294591409,-0.00108183093298003,
4.61939465531364));
#60602=CARTESIAN_POINT('Ctrl Pts',(20.6527873771723,-0.297740088546312,
4.543141139652));
#60603=CARTESIAN_POINT('Ctrl Pts',(20.6766452952037,-0.521574030203058,
4.33407743490148));
#60604=CARTESIAN_POINT('Ctrl Pts',(20.7005032132351,-0.617878846294169,
4.04332131262121));
#60605=CARTESIAN_POINT('Ctrl Pts',(20.7243611312665,-0.563090193646282,
3.74197268265107));
#60606=CARTESIAN_POINT('Ctrl Pts',(20.748219049298,-0.370613436173077,3.50371837193987));
#60607=CARTESIAN_POINT('Ctrl Pts',(20.7720769673294,-0.0875101228827464,
3.38681864340431));
#60608=CARTESIAN_POINT('Ctrl Pts',(20.7959348853608,0.216991017820888,3.41985835035499));
#60609=CARTESIAN_POINT('Ctrl Pts',(20.8197928033922,0.468432357761717,3.59475855107288));
#60610=CARTESIAN_POINT('Ctrl Pts',(20.8436507214236,0.605329007232586,3.86875129405724));
#60611=CARTESIAN_POINT('Ctrl Pts',(20.8675086394551,0.594206341669864,4.17483793696784));
#60612=CARTESIAN_POINT('Ctrl Pts',(20.8913665574864,0.437783978244149,4.43817193323088));
#60613=CARTESIAN_POINT('Ctrl Pts',(20.9152244755179,0.174311539695801,4.5943609607934));
#60614=CARTESIAN_POINT('Ctrl Pts',(20.9390823935493,-0.13178483570001,4.60521254097096));
#60615=CARTESIAN_POINT('Ctrl Pts',(20.9629403115808,-0.405656219889506,
4.46807317049539));
#60616=CARTESIAN_POINT('Ctrl Pts',(20.9867982296121,-0.580333613298163,
4.21647715910241));
#60617=CARTESIAN_POINT('Ctrl Pts',(21.0106561476436,-0.613103627724174,
3.91194658594648));
#60618=CARTESIAN_POINT('Ctrl Pts',(21.034514065675,-0.495953105920446,3.62894747086441));
#60619=CARTESIAN_POINT('Ctrl Pts',(21.0583719837064,-0.257528539509485,
3.43668080652407));
#60620=CARTESIAN_POINT('Ctrl Pts',(21.0822299017379,0.0438687693677006,
3.38216102944232));
#60621=CARTESIAN_POINT('Ctrl Pts',(21.1060878197692,0.334538969374667,3.47871971028568));
#60622=CARTESIAN_POINT('Ctrl Pts',(21.1299457378007,0.543405278604256,3.7027456213393));
#60623=CARTESIAN_POINT('Ctrl Pts',(21.153803655832,0.619394195209021,3.99945832503004));
#60624=CARTESIAN_POINT('Ctrl Pts',(21.1776615738635,0.543924359096133,4.29630348300169));
#60625=CARTESIAN_POINT('Ctrl Pts',(21.2015194918949,0.33545020099803,4.52069436823682));
#60626=CARTESIAN_POINT('Ctrl Pts',(21.2253774099264,0.0449493312674926,
4.61776129700707));
#60627=CARTESIAN_POINT('Ctrl Pts',(21.2492353279577,-0.256542874348706,
4.56376876117982));
#60628=CARTESIAN_POINT('Ctrl Pts',(21.2730932459892,-0.495303359101402,
4.37191940649105));
#60629=CARTESIAN_POINT('Ctrl Pts',(21.2969511640206,-0.612948680759938,
4.08912562603418));
#60630=CARTESIAN_POINT('Ctrl Pts',(21.320809082052,-0.580711353586496,3.78453820227854));
#60631=CARTESIAN_POINT('Ctrl Pts',(21.3446670000834,-0.406474282201139,
3.53263705712739));
#60632=CARTESIAN_POINT('Ctrl Pts',(21.3685249181149,-0.132843176680646,
3.39501888221951));
#60633=CARTESIAN_POINT('Ctrl Pts',(21.3923828361463,0.17327170411384,3.40533506996376));
#60634=CARTESIAN_POINT('Ctrl Pts',(21.4162407541777,0.437016933425986,3.56106303144932));
#60635=CARTESIAN_POINT('Ctrl Pts',(21.4400986722091,0.593899618413251,3.82412303814848));
#60636=CARTESIAN_POINT('Ctrl Pts',(21.4639565902405,0.605557669197671,4.13018975281259));
#60637=CARTESIAN_POINT('Ctrl Pts',(21.4878145082719,0.469140374803543,4.40442152661638));
#60638=CARTESIAN_POINT('Ctrl Pts',(21.5116724263034,0.218005479642704,4.57976122094124));
#60639=CARTESIAN_POINT('Ctrl Pts',(21.5355303443348,-0.0864376936408111,
4.61333350436739));
#60640=CARTESIAN_POINT('Ctrl Pts',(21.5593882623662,-0.369744496313637,
4.49692903910649));
#60641=CARTESIAN_POINT('Ctrl Pts',(21.5832461803976,-0.562638697999917,
4.2590118877088));
#60642=CARTESIAN_POINT('Ctrl Pts',(21.607104098429,-0.617952412054802,3.95775927442416));
#60643=CARTESIAN_POINT('Ctrl Pts',(21.6309620164605,-0.522159928676552,
3.66683566915707));
#60644=CARTESIAN_POINT('Ctrl Pts',(21.6548199344919,-0.298685119385998,
3.45737981799522));
#60645=CARTESIAN_POINT('Ctrl Pts',(21.6786778525233,-0.00217366238626178,
3.38060938201055));
#60646=CARTESIAN_POINT('Ctrl Pts',(21.7025357705547,0.294869314276287,3.45529682398599));
#60647=CARTESIAN_POINT('Ctrl Pts',(21.7263936885862,0.519808711519421,3.66317902991346));
#60648=CARTESIAN_POINT('Ctrl Pts',(21.7502516066175,0.617640719491047,3.95342313784609));
#60649=CARTESIAN_POINT('Ctrl Pts',(21.774109524649,0.564442747351711,4.25505655730362));
#60650=CARTESIAN_POINT('Ctrl Pts',(21.7979674426804,0.373223148373148,4.49432170089927));
#60651=CARTESIAN_POINT('Ctrl Pts',(21.8218253607118,0.0907403232229101,
4.61271172357229));
#60652=CARTESIAN_POINT('Ctrl Pts',(21.8456832787432,-0.213930982672105,
4.58127703989962));
#60653=CARTESIAN_POINT('Ctrl Pts',(21.8695411967746,-0.466290335940828,
4.40770428630285));
#60654=CARTESIAN_POINT('Ctrl Pts',(21.8933991148061,-0.604629000578284,
4.13443672906324));
#60655=CARTESIAN_POINT('Ctrl Pts',(21.9172570328375,-0.595119404811066,
3.82829572958469));
#60656=CARTESIAN_POINT('Ctrl Pts',(21.9411149508689,-0.440086903840403,
3.56414110135311));
#60657=CARTESIAN_POINT('Ctrl Pts',(21.9649728689003,-0.177441167154219,
3.40656584639871));
#60658=CARTESIAN_POINT('Ctrl Pts',(21.9888307869318,0.128593768301574,3.39410140682164));
#60659=CARTESIAN_POINT('Ctrl Pts',(22.0126887049631,0.403184024583593,3.52979567762293));
#60660=CARTESIAN_POINT('Ctrl Pts',(22.0365466229946,0.579184804342829,3.7804677133541));
#60661=CARTESIAN_POINT('Ctrl Pts',(22.060404541026,0.613559122762511,4.08482137310942));
#60662=CARTESIAN_POINT('Ctrl Pts',(22.0842624590574,0.497901522652627,4.36843389665204));
#60663=CARTESIAN_POINT('Ctrl Pts',(22.1081203770888,0.260493437687466,4.56195429652472));
#60664=CARTESIAN_POINT('Ctrl Pts',(22.1319782951203,-0.0406123884881684,
4.61806156357065));
#60665=CARTESIAN_POINT('Ctrl Pts',(22.1558362131517,-0.33178737942464,4.52303594266224));
#60666=CARTESIAN_POINT('Ctrl Pts',(22.1796941311831,-0.541831318374727,
4.30011378656432));
#60667=CARTESIAN_POINT('Ctrl Pts',(22.2035520492145,-0.619382740812877,
4.00380563470766));
#60668=CARTESIAN_POINT('Ctrl Pts',(22.2274099672459,-0.545478211438426,
3.70656690151735));
#60669=CARTESIAN_POINT('Ctrl Pts',(22.2512678852774,-0.338189400908512,
3.48108055383335));
#60670=CARTESIAN_POINT('Ctrl Pts',(22.2751258033088,-0.0482040696311437,
3.38248414587532));
#60671=CARTESIAN_POINT('Ctrl Pts',(22.2989837213402,0.253568469476171,3.43488718493857));
#60672=CARTESIAN_POINT('Ctrl Pts',(22.3228416393716,0.493336611197201,3.62547570084914));
#60673=CARTESIAN_POINT('Ctrl Pts',(22.346699557403,0.612470512379129,3.90764560936005));
#60674=CARTESIAN_POINT('Ctrl Pts',(22.3705574754344,0.581838691587799,4.21239868278141));
#60675=CARTESIAN_POINT('Ctrl Pts',(22.3944153934659,0.408931458591185,4.46521449128699));
#60676=CARTESIAN_POINT('Ctrl Pts',(22.4182733114973,0.13602935083686,4.60427268703701));
#60677=CARTESIAN_POINT('Ctrl Pts',(22.4421312295287,-0.170135649772668,
4.59556974592947));
#60678=CARTESIAN_POINT('Ctrl Pts',(22.4659891475601,-0.434697828443077,
4.44123378804823));
#60679=CARTESIAN_POINT('Ctrl Pts',(22.4898470655916,-0.592964587096883,
4.17900413283907));
#60680=CARTESIAN_POINT('Ctrl Pts',(22.513704983623,-0.606235276705168,3.87300312362118));
#60681=CARTESIAN_POINT('Ctrl Pts',(22.5375629016543,-0.471265070143009,
3.59805624874041));
#60682=CARTESIAN_POINT('Ctrl Pts',(22.5614208196858,-0.22105744785653,3.4213956854475));
#60683=CARTESIAN_POINT('Ctrl Pts',(22.5852787377172,0.0832042338527798,
3.38621941950615));
#60684=CARTESIAN_POINT('Ctrl Pts',(22.6091366557487,0.36712117327337,3.50112963696785));
#60685=CARTESIAN_POINT('Ctrl Pts',(22.63299457378,0.561265174232679,3.7380264683998));
#60686=CARTESIAN_POINT('Ctrl Pts',(22.6568524918115,0.618167971965146,4.03898443479498));
#60687=CARTESIAN_POINT('Ctrl Pts',(22.6807104098429,0.523905402647805,4.33040686810369));
#60688=CARTESIAN_POINT('Ctrl Pts',(22.7045683278744,0.301545895245711,4.54104106792393));
#60689=CARTESIAN_POINT('Ctrl Pts',(22.7284262459057,0.00542710047790416,
4.61936606261506));
#60690=CARTESIAN_POINT('Ctrl Pts',(22.7522841639372,-0.291974666000346,
4.54625809930836));
#60691=CARTESIAN_POINT('Ctrl Pts',(22.7761420819686,-0.518067845615496,
4.33953802216683));
#60692=CARTESIAN_POINT('Ctrl Pts',(22.7920473606562,-0.584213376873476,
4.14642833911731));
#60693=CARTESIAN_POINT('Ctrl Pts',(22.8,-0.592174260192535,4.04779597854866));
#60694=CARTESIAN_POINT('Ctrl Pts',(3.96816317011931,-0.282716247115855,
3.54616445487434));
#60695=CARTESIAN_POINT('Ctrl Pts',(3.97611580946312,-0.207125539895404,
3.49907532469992));
#60696=CARTESIAN_POINT('Ctrl Pts',(3.99202108815073,-0.0320395462633344,
3.44344227840288));
#60697=CARTESIAN_POINT('Ctrl Pts',(4.01587900618214,0.238586678544665,3.49618207793602));
#60698=CARTESIAN_POINT('Ctrl Pts',(4.03973692421357,0.450798406251909,3.67207593825259));
#60699=CARTESIAN_POINT('Ctrl Pts',(4.06359484224498,0.552814952159096,3.92817792166325));
#60700=CARTESIAN_POINT('Ctrl Pts',(4.0874527602764,0.519633627921064,4.20183097195279));
#60701=CARTESIAN_POINT('Ctrl Pts',(4.11131067830782,0.359398059257131,4.42613686623617));
#60702=CARTESIAN_POINT('Ctrl Pts',(4.13516859633924,0.11127440638865,4.54623750576341));
#60703=CARTESIAN_POINT('Ctrl Pts',(4.15902651437066,-0.164055973910312,
4.53276988152218));
#60704=CARTESIAN_POINT('Ctrl Pts',(4.18288443240208,-0.399271733473279,
4.38902461621758));
#60705=CARTESIAN_POINT('Ctrl Pts',(4.2067423504335,-0.536853866020863,4.15015270818839));
#60706=CARTESIAN_POINT('Ctrl Pts',(4.23060026846491,-0.543161034884179,
3.87456412255522));
#60707=CARTESIAN_POINT('Ctrl Pts',(4.25445818649634,-0.416650307492554,
3.62964815836115));
#60708=CARTESIAN_POINT('Ctrl Pts',(4.27831610452775,-0.188257351244862,
3.47529323740438));
#60709=CARTESIAN_POINT('Ctrl Pts',(4.30217402255918,0.0861697193074588,
3.44924344981891));
#60710=CARTESIAN_POINT('Ctrl Pts',(4.32603194059059,0.339525912432458,3.55786862136322));
#60711=CARTESIAN_POINT('Ctrl Pts',(4.34988985862202,0.509858789389686,3.77460696883261));
#60712=CARTESIAN_POINT('Ctrl Pts',(4.37374777665342,0.555517294574929,4.0464600464808));
#60713=CARTESIAN_POINT('Ctrl Pts',(4.39760569468486,0.465336694276122,4.30695238014399));
#60714=CARTESIAN_POINT('Ctrl Pts',(4.42146361271626,0.261368594047533,4.4923864940975));
#60715=CARTESIAN_POINT('Ctrl Pts',(4.4453215307477,-0.00651124555331369,
4.55741869872598));
#60716=CARTESIAN_POINT('Ctrl Pts',(4.4691794487791,-0.272798909000308,4.48614684730087));
#60717=CARTESIAN_POINT('Ctrl Pts',(4.49303736681053,-0.472379807908186,
4.29599884956661));
#60718=CARTESIAN_POINT('Ctrl Pts',(4.51689528484195,-0.55645097662433,4.03347107014466));
#60719=CARTESIAN_POINT('Ctrl Pts',(4.54075320287336,-0.504454724024634,
3.76275870240323));
#60720=CARTESIAN_POINT('Ctrl Pts',(4.56461112090479,-0.329105550388866,
3.55005829421323));
#60721=CARTESIAN_POINT('Ctrl Pts',(4.5884690389362,-0.0732811049967102,
3.44738088927219));
#60722=CARTESIAN_POINT('Ctrl Pts',(4.61232695696762,0.200462566687888,3.47983390993684));
#60723=CARTESIAN_POINT('Ctrl Pts',(4.63618487499904,0.425187680335341,3.63948170866684));
#60724=CARTESIAN_POINT('Ctrl Pts',(4.66004279303046,0.54594282425631,3.88728604994618));
#60725=CARTESIAN_POINT('Ctrl Pts',(4.68390071106188,0.533200076465109,4.16265202228146));
#60726=CARTESIAN_POINT('Ctrl Pts',(4.7077586290933,0.390075385898422,4.39824514461603));
#60727=CARTESIAN_POINT('Ctrl Pts',(4.73161654712472,0.151566638040082,4.53645648111246));
#60728=CARTESIAN_POINT('Ctrl Pts',(4.75547446515614,-0.124004281411749,
4.54348959519552));
#60729=CARTESIAN_POINT('Ctrl Pts',(4.77933238318755,-0.369252776249408,
4.41762469889406));
#60730=CARTESIAN_POINT('Ctrl Pts',(4.80319030121898,-0.524208909050512,
4.18963918784455));
#60731=CARTESIAN_POINT('Ctrl Pts',(4.82704821925039,-0.550981684424725,
3.91528172969931));
#60732=CARTESIAN_POINT('Ctrl Pts',(4.85090613728181,-0.443024429517375,
3.66164019632193));
#60733=CARTESIAN_POINT('Ctrl Pts',(4.87476405531323,-0.226735633849849,
3.49073685167984));
#60734=CARTESIAN_POINT('Ctrl Pts',(4.89862197334465,0.0449962004486201,
3.44436221885167));
#60735=CARTESIAN_POINT('Ctrl Pts',(4.92247989137607,0.305725238065515,3.53385615878353));
#60736=CARTESIAN_POINT('Ctrl Pts',(4.94633780940749,0.491696127187109,3.73733496539613));
#60737=CARTESIAN_POINT('Ctrl Pts',(4.9701957274389,0.557433919677865,4.00504252782125));
#60738=CARTESIAN_POINT('Ctrl Pts',(4.99405364547033,0.486863934612277,4.27151705483839));
#60739=CARTESIAN_POINT('Ctrl Pts',(5.01791156350174,0.297242455626679,4.47159826597145));
#60740=CARTESIAN_POINT('Ctrl Pts',(5.04176948153317,0.0349370995184326,
4.55636085499566));
#60741=CARTESIAN_POINT('Ctrl Pts',(5.06562739956458,-0.235911329089554,
4.505078060008));
#60742=CARTESIAN_POINT('Ctrl Pts',(5.08948531759601,-0.449073011639563,
4.33028992129829));
#60743=CARTESIAN_POINT('Ctrl Pts',(5.11334323562741,-0.552424110340463,
4.07473689991432));
#60744=CARTESIAN_POINT('Ctrl Pts',(5.13720115365885,-0.520692466332485,
3.80090867070902));
#60745=CARTESIAN_POINT('Ctrl Pts',(5.16105907169026,-0.361637330928202,
3.57576369465428));
#60746=CARTESIAN_POINT('Ctrl Pts',(5.18491698972168,-0.114152017308863,
3.45435605122152));
#60747=CARTESIAN_POINT('Ctrl Pts',(5.2087749077531,0.161246573981014,3.46637321630784));
#60748=CARTESIAN_POINT('Ctrl Pts',(5.23263282578452,0.397215985664045,3.60887666570863));
#60749=CARTESIAN_POINT('Ctrl Pts',(5.25649074381594,0.536055268906009,3.84702042432939));
#60750=CARTESIAN_POINT('Ctrl Pts',(5.28034866184735,0.543814437048104,4.12257185628156));
#60751=CARTESIAN_POINT('Ctrl Pts',(5.30420657987878,0.418596162124088,4.3681511305826));
#60752=CARTESIAN_POINT('Ctrl Pts',(5.32806449791019,0.191019723230217,4.5237074252207));
#60753=CARTESIAN_POINT('Ctrl Pts',(5.35192241594161,-0.0832662412662402,
4.55120298888854));
#60754=CARTESIAN_POINT('Ctrl Pts',(5.37578033397303,-0.337191341646214,
4.44391440730515));
#60755=CARTESIAN_POINT('Ctrl Pts',(5.39963825200445,-0.508663974085987,
4.22807666114996));
#60756=CARTESIAN_POINT('Ctrl Pts',(5.42349617003587,-0.555754409133215,
3.95646795866016));
#60757=CARTESIAN_POINT('Ctrl Pts',(5.4473540880673,-0.466947752701331,3.69550402606682));
#60758=CARTESIAN_POINT('Ctrl Pts',(5.47121200609871,-0.263959651332346,
3.50899765340418));
#60759=CARTESIAN_POINT('Ctrl Pts',(5.49506992413013,0.00357377490351851,
3.44255472911916));
#60760=CARTESIAN_POINT('Ctrl Pts',(5.51892784216155,0.270233315828591,3.51242235806964));
#60761=CARTESIAN_POINT('Ctrl Pts',(5.54278576019296,0.470813450024345,3.70151600181885));
#60762=CARTESIAN_POINT('Ctrl Pts',(5.56664367822439,0.556266870991092,3.96359711366712));
#60763=CARTESIAN_POINT('Ctrl Pts',(5.5905015962558,0.505697889589837,4.23457972281303));
#60764=CARTESIAN_POINT('Ctrl Pts',(5.61435951428722,0.331471999260015,4.4482011999181));
#60765=CARTESIAN_POINT('Ctrl Pts',(5.63821743231864,0.0761921759760934,
4.55222527486821));
#60766=CARTESIAN_POINT('Ctrl Pts',(5.66207535035006,-0.197718709731212,
4.52121522783523));
#60767=CARTESIAN_POINT('Ctrl Pts',(5.68593326838148,-0.423281985227643,
4.3627538599096));
#60768=CARTESIAN_POINT('Ctrl Pts',(5.70979118641289,-0.545341285237878,
4.11558929214995));
#60769=CARTESIAN_POINT('Ctrl Pts',(5.73364910444432,-0.534049786451273,
3.84015999362387));
#60770=CARTESIAN_POINT('Ctrl Pts',(5.75750702247573,-0.392168567195948,
3.6038159310769));
#60771=CARTESIAN_POINT('Ctrl Pts',(5.78136494050716,-0.154391451667357,
3.46434966433946));
#60772=CARTESIAN_POINT('Ctrl Pts',(5.80522285853857,0.121138580962943,3.45586449715393));
#60773=CARTESIAN_POINT('Ctrl Pts',(5.82908077656999,0.367046927720705,3.58043527923202));
#60774=CARTESIAN_POINT('Ctrl Pts',(5.85293869460141,0.523202308305842,3.80760107017232));
#60775=CARTESIAN_POINT('Ctrl Pts',(5.87679661263283,0.551420461789987,4.08181362911724));
#60776=CARTESIAN_POINT('Ctrl Pts',(5.90065453066425,0.44480131269862,4.33602054829434));
#60777=CARTESIAN_POINT('Ctrl Pts',(5.92451244869567,0.229416087376931,4.50806125053784));
#60778=CARTESIAN_POINT('Ctrl Pts',(5.94837036672709,-0.042067546589846,
4.55586721297736));
#60779=CARTESIAN_POINT('Ctrl Pts',(5.97222828475851,-0.30326465903273,4.46774835821298));
#60780=CARTESIAN_POINT('Ctrl Pts',(5.99608620278993,-0.490305038147314,
4.26525255699254));
#60781=CARTESIAN_POINT('Ctrl Pts',(6.01994412082133,-0.557452977205748,
3.99789477357902));
#60782=CARTESIAN_POINT('Ctrl Pts',(6.04380203885278,-0.488287539408226,
3.73105273207384));
#60783=CARTESIAN_POINT('Ctrl Pts',(6.06765995688417,-0.299724270968661,
3.52997381710292));
#60784=CARTESIAN_POINT('Ctrl Pts',(6.09151787491561,-0.0378669053578504,
3.44383251805177));
#60785=CARTESIAN_POINT('Ctrl Pts',(6.11537579294702,0.233243627260218,3.49368287747685));
#60786=CARTESIAN_POINT('Ctrl Pts',(6.13923371097844,0.447331678364145,3.6673537262422));
#60787=CARTESIAN_POINT('Ctrl Pts',(6.16309162900986,0.552012406214274,3.92234268746235));
#60788=CARTESIAN_POINT('Ctrl Pts',(6.18694954704127,0.521753629494025,4.19636433484848));
#60789=CARTESIAN_POINT('Ctrl Pts',(6.2108074650727,0.363831507594212,4.42228768590875));
#60790=CARTESIAN_POINT('Ctrl Pts',(6.23466538310411,0.117094415953721,4.54510476979165));
#60791=CARTESIAN_POINT('Ctrl Pts',(6.25852330113554,-0.158561881267111,
4.53433708369694));
#60792=CARTESIAN_POINT('Ctrl Pts',(6.28238121916695,-0.394905399742298,
4.39345989467659));
#60793=CARTESIAN_POINT('Ctrl Pts',(6.30623913719837,-0.535697351746728,
4.1553358869807));
#60794=CARTESIAN_POINT('Ctrl Pts',(6.33009705522979,-0.543633587309765,
3.88114808171798));
#60795=CARTESIAN_POINT('Ctrl Pts',(6.36190761260502,-0.381130543103143,
3.54983775818315));
#60796=CARTESIAN_POINT('Ctrl Pts',(6.40167080932404,0.0904237977681596,
3.37418170676098));
#60797=CARTESIAN_POINT('Ctrl Pts',(6.4493866453869,0.576013642360818,3.73827828410759));
#60798=CARTESIAN_POINT('Ctrl Pts',(6.49710248144972,0.531303907723303,4.34259299019566));
#60799=CARTESIAN_POINT('Ctrl Pts',(6.54481831751257,-0.000617460830772086,
4.63236849138271));
#60800=CARTESIAN_POINT('Ctrl Pts',(6.5925341535754,-0.532336898979176,4.34139325430452));
#60801=CARTESIAN_POINT('Ctrl Pts',(6.64024998963824,-0.575010046738857,
3.73693099107234));
#60802=CARTESIAN_POINT('Ctrl Pts',(6.68796582570108,-0.0897448725589052,
3.37403863313417));
#60803=CARTESIAN_POINT('Ctrl Pts',(6.73568166176391,0.477988548433368,3.58598174571673));
#60804=CARTESIAN_POINT('Ctrl Pts',(6.78339749782676,0.606749053262868,4.17812127049189));
#60805=CARTESIAN_POINT('Ctrl Pts',(6.83111333388958,0.178337754027021,4.60669083891839));
#60806=CARTESIAN_POINT('Ctrl Pts',(6.87882916995244,-0.413851892207341,
4.47812605548031));
#60807=CARTESIAN_POINT('Ctrl Pts',(6.92654500601527,-0.625990718083913,
3.91049119230943));
#60808=CARTESIAN_POINT('Ctrl Pts',(6.97426084207811,-0.263274891453005,
3.42505341469988));
#60809=CARTESIAN_POINT('Ctrl Pts',(7.02197667814094,0.341211513798207,3.46759805477058));
#60810=CARTESIAN_POINT('Ctrl Pts',(7.06969251420378,0.63235750294684,3.99905552874491));
#60811=CARTESIAN_POINT('Ctrl Pts',(7.11740835026662,0.342800202184808,4.53138035934227));
#60812=CARTESIAN_POINT('Ctrl Pts',(7.16512418632946,-0.261555976381552,
4.57573041153878));
#60813=CARTESIAN_POINT('Ctrl Pts',(7.2128400223923,-0.625721183287191,4.0913783776429));
#60814=CARTESIAN_POINT('Ctrl Pts',(7.26055585845514,-0.41527704940159,3.52311216844965));
#60815=CARTESIAN_POINT('Ctrl Pts',(7.30827169451797,0.176522415171576,3.39277939551711));
#60816=CARTESIAN_POINT('Ctrl Pts',(7.35598753058081,0.606218615784068,3.8200666455489));
#60817=CARTESIAN_POINT('Ctrl Pts',(7.40370336664364,0.479214941044062,4.4125894643569));
#60818=CARTESIAN_POINT('Ctrl Pts',(7.4514192027065,-0.0878591916424711,
4.62622502914213));
#60819=CARTESIAN_POINT('Ctrl Pts',(7.49913503876932,-0.574250874682306,
4.26478851416677));
#60820=CARTESIAN_POINT('Ctrl Pts',(7.54685087483217,-0.53329914461431,3.6601926322252));
#60821=CARTESIAN_POINT('Ctrl Pts',(7.594566710895,-0.00261060360317682,
3.36764708477891));
#60822=CARTESIAN_POINT('Ctrl Pts',(7.64228254695784,0.530475294557976,3.65580094934904));
#60823=CARTESIAN_POINT('Ctrl Pts',(7.68999838302067,0.576417567478113,4.26003809833172));
#60824=CARTESIAN_POINT('Ctrl Pts',(7.73771421908353,0.093026718772369,4.62547826040714));
#60825=CARTESIAN_POINT('Ctrl Pts',(7.78543005514634,-0.475791997136335,
4.41653211173522));
#60826=CARTESIAN_POINT('Ctrl Pts',(7.8331458912092,-0.607683601098078,3.82507811568403));
#60827=CARTESIAN_POINT('Ctrl Pts',(7.88086172727203,-0.181530003744534,
3.39425757752065));
#60828=CARTESIAN_POINT('Ctrl Pts',(7.92857756333487,0.411325389238953,3.51969962646458));
#60829=CARTESIAN_POINT('Ctrl Pts',(7.97629339939771,0.626454348233276,4.08620889879763));
#60830=CARTESIAN_POINT('Ctrl Pts',(8.02400923546054,0.266300640003926,4.57355121287022));
#60831=CARTESIAN_POINT('Ctrl Pts',(8.07172507152339,-0.338401043502061,
4.5341926229444));
#60832=CARTESIAN_POINT('Ctrl Pts',(8.11944090758622,-0.632343841791292,
4.00427672775865));
#60833=CARTESIAN_POINT('Ctrl Pts',(8.16715674364906,-0.345595560302635,
3.47043344766624));
#60834=CARTESIAN_POINT('Ctrl Pts',(8.2148725797119,0.258518441882999,3.42289928101069));
#60835=CARTESIAN_POINT('Ctrl Pts',(8.26258841577473,0.625230981070026,3.90532558443901));
#60836=CARTESIAN_POINT('Ctrl Pts',(8.31030425183758,0.417784289925175,4.47469286043008));
#60837=CARTESIAN_POINT('Ctrl Pts',(8.35802008790041,-0.173320143095541,
4.60814237859973));
#60838=CARTESIAN_POINT('Ctrl Pts',(8.40573592396325,-0.605262021838435,
4.18312539302794));
#60839=CARTESIAN_POINT('Ctrl Pts',(8.45345176002609,-0.481382472773795,
3.58994154129225));
#60840=CARTESIAN_POINT('Ctrl Pts',(8.50116759608892,0.0845580080604409,
3.37332068174828));
#60841=CARTESIAN_POINT('Ctrl Pts',(8.54888343215178,0.572847569000584,3.73218908285563));
#60842=CARTESIAN_POINT('Ctrl Pts',(8.59659926821459,0.535082392934658,4.33699236997728));
#60843=CARTESIAN_POINT('Ctrl Pts',(8.64431510427745,0.00594282213592907,
4.6323303784547));
#60844=CARTESIAN_POINT('Ctrl Pts',(8.69203094034027,-0.528654133672296,
4.34698967074364));
#60845=CARTESIAN_POINT('Ctrl Pts',(8.73974677640312,-0.577779864139828,
3.74300300926635));
#60846=CARTESIAN_POINT('Ctrl Pts',(8.78746261246595,-0.0963214550818077,
3.37502063878676));
#60847=CARTESIAN_POINT('Ctrl Pts',(8.8351784485288,0.473590428273928,3.58096643225285));
#60848=CARTESIAN_POINT('Ctrl Pts',(8.88289428459164,0.608596934220305,4.17171719864135));
#60849=CARTESIAN_POINT('Ctrl Pts',(8.93061012065447,0.184719511004659,4.60477741930878));
#60850=CARTESIAN_POINT('Ctrl Pts',(8.97832595671731,-0.408788681441581,
4.48246123012823));
#60851=CARTESIAN_POINT('Ctrl Pts',(9.02604179278014,-0.626899937697651,
3.91709346970068));
#60852=CARTESIAN_POINT('Ctrl Pts',(9.07375762884299,-0.269319335070538,
3.42786005172794));
#60853=CARTESIAN_POINT('Ctrl Pts',(9.12147346490582,0.335581356962483,3.46403155175812));
#60854=CARTESIAN_POINT('Ctrl Pts',(9.16918930096866,0.632312525313962,3.99239112474344));
#60855=CARTESIAN_POINT('Ctrl Pts',(9.21690513703149,0.348381372290835,4.52773804495445));
#60856=CARTESIAN_POINT('Ctrl Pts',(9.26462097309434,-0.255473755443411,
4.5784549981902));
#60857=CARTESIAN_POINT('Ctrl Pts',(9.31233680915717,-0.624723402584967,
4.09796782591368));
#60858=CARTESIAN_POINT('Ctrl Pts',(9.36005264522002,-0.420279936527615,
3.52751529167185));
#60859=CARTESIAN_POINT('Ctrl Pts',(9.40776848128285,0.170113062081096,3.39095273519949));
#60860=CARTESIAN_POINT('Ctrl Pts',(9.45548431734569,0.604288618254829,3.81368765339017));
#60861=CARTESIAN_POINT('Ctrl Pts',(9.50320015340853,0.483536638109595,4.40751606625661));
#60862=CARTESIAN_POINT('Ctrl Pts',(9.55091598947137,-0.0812544769791981,
4.62711620503893));
#60863=CARTESIAN_POINT('Ctrl Pts',(9.5986318255342,-0.571428355597161,4.27082588331087));
#60864=CARTESIAN_POINT('Ctrl Pts',(9.64634766159704,-0.536850782714826,
3.66583198574659));
#60865=CARTESIAN_POINT('Ctrl Pts',(9.69406349765987,-0.0092748755543832,
3.36770971750703));
#60866=CARTESIAN_POINT('Ctrl Pts',(9.74177933372272,0.52681829253995,3.65022934471732));
#60867=CARTESIAN_POINT('Ctrl Pts',(9.78949516978555,0.579126116453474,4.253948746587));
#60868=CARTESIAN_POINT('Ctrl Pts',(9.83721100584839,0.099613516627068,4.62446310696212));
#60869=CARTESIAN_POINT('Ctrl Pts',(9.88492684191123,-0.471375708268938,
4.42152338761395));
#60870=CARTESIAN_POINT('Ctrl Pts',(9.93264267797408,-0.609493367214024,
3.83149225544889));
#60871=CARTESIAN_POINT('Ctrl Pts',(9.9803585140369,-0.187903888785556,3.39620437793004));
#60872=CARTESIAN_POINT('Ctrl Pts',(10.0280743500997,0.406240621987656,3.51539131074786));
#60873=CARTESIAN_POINT('Ctrl Pts',(10.0757901861626,0.627328118774167,4.07960185956908));
#60874=CARTESIAN_POINT('Ctrl Pts',(10.1235060222254,0.27233055140652,4.57071279591595));
#60875=CARTESIAN_POINT('Ctrl Pts',(10.1712218582883,-0.332752351661881,
4.5377293902281));
#60876=CARTESIAN_POINT('Ctrl Pts',(10.2189376943511,-0.632263650146131,
4.01094081146358));
#60877=CARTESIAN_POINT('Ctrl Pts',(10.2666535304139,-0.351157510074434,
3.47410511718603));
#60878=CARTESIAN_POINT('Ctrl Pts',(10.3143693664768,0.252421974751429,3.42020678572945));
#60879=CARTESIAN_POINT('Ctrl Pts',(10.3620852025396,0.624198476151732,3.89874148420283));
#60880=CARTESIAN_POINT('Ctrl Pts',(10.4098010386024,0.422763912373798,4.47026343579529));
#60881=CARTESIAN_POINT('Ctrl Pts',(10.4575168746653,-0.166901257195935,
4.60993523836389));
#60882=CARTESIAN_POINT('Ctrl Pts',(10.5052327107281,-0.603298434176698,
4.18949412648294));
#60883=CARTESIAN_POINT('Ctrl Pts',(10.552948546791,-0.485677376113382,3.5950376425108));
#60884=CARTESIAN_POINT('Ctrl Pts',(10.6006643828538,0.0779486895418537,
3.3724643225678));
#60885=CARTESIAN_POINT('Ctrl Pts',(10.6483802189166,0.569993274196054,3.72616667108832));
#60886=CARTESIAN_POINT('Ctrl Pts',(10.6960960549795,0.538604264682155,4.3313343790158));
#60887=CARTESIAN_POINT('Ctrl Pts',(10.7438118910423,0.0126066714187673,
4.63223262845832));
#60888=CARTESIAN_POINT('Ctrl Pts',(10.7915277271052,-0.524967822187051,
4.35254192703816));
#60889=CARTESIAN_POINT('Ctrl Pts',(10.839243563168,-0.580456287010268,3.74910654946403));
#60890=CARTESIAN_POINT('Ctrl Pts',(10.8869593992308,-0.102902812003948,
3.37607048800905));
#60891=CARTESIAN_POINT('Ctrl Pts',(10.9346752352937,0.469147898628881,3.5759984978049));
#60892=CARTESIAN_POINT('Ctrl Pts',(10.9823910713565,0.610372875182502,4.16529361116822));
#60893=CARTESIAN_POINT('Ctrl Pts',(11.0301069074193,0.191083048662156,4.60279705802663));
#60894=CARTESIAN_POINT('Ctrl Pts',(11.0778227434822,-0.403681281635282,
4.48674269127424));
#60895=CARTESIAN_POINT('Ctrl Pts',(11.125538579545,-0.627738879572117,3.92370502162571));
#60896=CARTESIAN_POINT('Ctrl Pts',(11.1732544156079,-0.275334205393669,
3.43073020456744));
#60897=CARTESIAN_POINT('Ctrl Pts',(11.2209702516707,0.329914106159097,3.46052459999659));
#60898=CARTESIAN_POINT('Ctrl Pts',(11.2686860877335,0.632197217644931,3.98572755614488));
#60899=CARTESIAN_POINT('Ctrl Pts',(11.3164019237964,0.353923896562866,4.52403711709511));
#60900=CARTESIAN_POINT('Ctrl Pts',(11.3641177598592,-0.24936318455202,4.58111533006939));
#60901=CARTESIAN_POINT('Ctrl Pts',(11.411833595922,-0.623656216347001,4.10454639383227));
#60902=CARTESIAN_POINT('Ctrl Pts',(11.4595494319849,-0.425236148486169,
3.53197089548594));
#60903=CARTESIAN_POINT('Ctrl Pts',(11.5072652680477,0.163684817628688,3.3891937253683));
#60904=CARTESIAN_POINT('Ctrl Pts',(11.5549811041106,0.602291497100466,3.80732935570755));
#60905=CARTESIAN_POINT('Ctrl Pts',(11.6026969401734,0.487804627338989,4.40239740331947));
#60906=CARTESIAN_POINT('Ctrl Pts',(11.6504127762363,-0.0746407375468588,
4.62793772378323));
#60907=CARTESIAN_POINT('Ctrl Pts',(11.6981286122991,-0.568542364648052,
4.276833170433));
#60908=CARTESIAN_POINT('Ctrl Pts',(11.7458444483619,-0.540342790144192,
3.67150845704832));
#60909=CARTESIAN_POINT('Ctrl Pts',(11.7935602844247,-0.0159381172083995,
3.36784258204823));
#60910=CARTESIAN_POINT('Ctrl Pts',(11.8412761204876,0.523102773999324,3.64469659094542));
#60911=CARTESIAN_POINT('Ctrl Pts',(11.8889919565504,0.581770338872691,4.24783118742311));
#60912=CARTESIAN_POINT('Ctrl Pts',(11.9367077926133,0.106189249871976,4.62337859111715));
#60913=CARTESIAN_POINT('Ctrl Pts',(11.9844236286761,-0.466907061217805,
4.4264678426758));
#60914=CARTESIAN_POINT('Ctrl Pts',(12.0321394647389,-0.611235433702689,
3.83792511225401));
#60915=CARTESIAN_POINT('Ctrl Pts',(12.0798553008018,-0.19425690235234,3.39821824509208));
#60916=CARTESIAN_POINT('Ctrl Pts',(12.1275711368646,0.401110731454808,3.51113682306459));
#60917=CARTESIAN_POINT('Ctrl Pts',(12.1752869729275,0.628132208685083,4.07298597854376));
#60918=CARTESIAN_POINT('Ctrl Pts',(12.2230028089903,0.27833021362349,4.56781098689255));
#60919=CARTESIAN_POINT('Ctrl Pts',(12.2707186450531,-0.327066699269377,
4.54120642908287));
#60920=CARTESIAN_POINT('Ctrl Pts',(12.3184344811159,-0.632113229655128,
4.01760367991507));
#60921=CARTESIAN_POINT('Ctrl Pts',(12.3661503171788,-0.356680454936339,
3.47783520061383));
#60922=CARTESIAN_POINT('Ctrl Pts',(12.4138661532416,0.246297469784735,3.4175786911271));
#60923=CARTESIAN_POINT('Ctrl Pts',(12.4615819893045,0.623096638228782,3.89216863128209));
#60924=CARTESIAN_POINT('Ctrl Pts',(12.5092978253673,0.427696576213203,4.46578177652963));
#60925=CARTESIAN_POINT('Ctrl Pts',(12.5570136614302,-0.16046383269669,4.61166034941614));
#60926=CARTESIAN_POINT('Ctrl Pts',(12.604729497493,-0.601267834987779,4.1958418118296));
#60927=CARTESIAN_POINT('Ctrl Pts',(12.6524453335558,-0.489918332714758,
3.60017872502631));
#60928=CARTESIAN_POINT('Ctrl Pts',(12.7001611696187,0.0713307128527425,
3.37167766707246));
#60929=CARTESIAN_POINT('Ctrl Pts',(12.7478770056815,0.56707566724347,3.72017467542775));
#60930=CARTESIAN_POINT('Ctrl Pts',(12.7955928417444,0.542066310823814,4.32563958500381));
#60931=CARTESIAN_POINT('Ctrl Pts',(12.8433086778072,0.0192691204123526,
4.63206465306178));
#60932=CARTESIAN_POINT('Ctrl Pts',(12.89102451387,-0.521223199767296,4.35805502464836));
#60933=CARTESIAN_POINT('Ctrl Pts',(12.9387403499329,-0.583068235550835,
3.7552379577156));
#60934=CARTESIAN_POINT('Ctrl Pts',(12.9864561859957,-0.109472738970043,
3.37718964036075));
#60935=CARTESIAN_POINT('Ctrl Pts',(13.0341720220585,0.464653258261548,3.57107765943178));
#60936=CARTESIAN_POINT('Ctrl Pts',(13.0818878581214,0.612081018822183,4.15885166366515));
#60937=CARTESIAN_POINT('Ctrl Pts',(13.1296036941842,0.197425361721354,4.6007497409078));
#60938=CARTESIAN_POINT('Ctrl Pts',(13.177319530247,-0.398529042827853,4.49097008735187));
#60939=CARTESIAN_POINT('Ctrl Pts',(13.2250353663099,-0.628508095190705,
3.93032504803489));
#60940=CARTESIAN_POINT('Ctrl Pts',(13.2727512023727,-0.281318492899819,
3.4336635891944));
#60941=CARTESIAN_POINT('Ctrl Pts',(13.3204670384356,0.324210210062374,3.45707757060249));
#60942=CARTESIAN_POINT('Ctrl Pts',(13.3681828744984,0.632011688508986,3.97906557286167));
#60943=CARTESIAN_POINT('Ctrl Pts',(13.4158987105612,0.359427108647973,4.52027798167956));
#60944=CARTESIAN_POINT('Ctrl Pts',(13.4636145466241,-0.243224915581421,
4.58371111441534));
#60945=CARTESIAN_POINT('Ctrl Pts',(13.5113303826869,-0.622519757336015,
4.11111334923356));
#60946=CARTESIAN_POINT('Ctrl Pts',(13.5590462187498,-0.430145127231255,
3.53647848575196));
#60947=CARTESIAN_POINT('Ctrl Pts',(13.6067620548126,0.157238391843492,3.38750256099959));
#60948=CARTESIAN_POINT('Ctrl Pts',(13.6544778908755,0.600227476264717,3.8009924589658));
#60949=CARTESIAN_POINT('Ctrl Pts',(13.7021937269383,0.492018433545193,4.39723404398833));
#60950=CARTESIAN_POINT('Ctrl Pts',(13.7499095630011,-0.0680187073756014,
4.62868949418496));
#60951=CARTESIAN_POINT('Ctrl Pts',(13.797625399064,-0.565593222711038,4.28280970824024));
#60952=CARTESIAN_POINT('Ctrl Pts',(13.8453412351268,-0.543774778860562,
3.67722141563181));
#60953=CARTESIAN_POINT('Ctrl Pts',(13.8930570711896,-0.0225995885319848,
3.36804566363559));
#60954=CARTESIAN_POINT('Ctrl Pts',(13.9407729072525,0.519329151684885,3.63920330259016));
#60955=CARTESIAN_POINT('Ctrl Pts',(13.9884887433153,0.584349941003394,4.24168610034696));
#60956=CARTESIAN_POINT('Ctrl Pts',(14.0362045793781,0.112753188118911,4.62222483333648));
#60957=CARTESIAN_POINT('Ctrl Pts',(14.083920415441,-0.462386552345973,4.43136492771341));
#60958=CARTESIAN_POINT('Ctrl Pts',(14.1316362515038,-0.612909607059929,
3.84437597156854));
#60959=CARTESIAN_POINT('Ctrl Pts',(14.1793520875667,-0.200588338784227,
3.40029895531576));
#60960=CARTESIAN_POINT('Ctrl Pts',(14.2270679236295,0.395936287445344,3.50693663598317));
#60961=CARTESIAN_POINT('Ctrl Pts',(14.2747837596923,0.628866528650988,4.06636199058228));
#60962=CARTESIAN_POINT('Ctrl Pts',(14.3224995957552,0.284298960241116,4.5648461081192));
#60963=CARTESIAN_POINT('Ctrl Pts',(14.370215431818,-0.321344717859966,4.54462335329573));
#60964=CARTESIAN_POINT('Ctrl Pts',(14.4179312678809,-0.631892597026201,
4.02426459303334));
#60965=CARTESIAN_POINT('Ctrl Pts',(14.4656471039437,-0.362163781425906,
3.48162328362967));
#60966=CARTESIAN_POINT('Ctrl Pts',(14.5133629400065,0.240145607263868,3.41501528911991));
#60967=CARTESIAN_POINT('Ctrl Pts',(14.5610787760693,0.6219255896881,3.8856077557581));
#60968=CARTESIAN_POINT('Ctrl Pts',(14.6087946121322,0.432581733546503,4.46124838043455));
#60969=CARTESIAN_POINT('Ctrl Pts',(14.656510448195,-0.154008584636381,4.61331752013935));
#60970=CARTESIAN_POINT('Ctrl Pts',(14.7042262842579,-0.599170449821005,
4.20216774399712));
#60971=CARTESIAN_POINT('Ctrl Pts',(14.7519421203207,-0.494104871512583,
3.60536421779174));
#60972=CARTESIAN_POINT('Ctrl Pts',(14.7996579563836,0.0647048130865326,
3.37096080264023));
#60973=CARTESIAN_POINT('Ctrl Pts',(14.8473737924464,0.564095072216763,3.71421376143635));
#60974=CARTESIAN_POINT('Ctrl Pts',(14.8950896285093,0.545468146811986,4.319908620492));
#60975=CARTESIAN_POINT('Ctrl Pts',(14.942805464572,0.0259294290834894,4.63182647092298));
#60976=CARTESIAN_POINT('Ctrl Pts',(14.9905213006349,-0.517420682347921,
4.36352835120552));
#60977=CARTESIAN_POINT('Ctrl Pts',(15.0382371366977,-0.585615419638682,
3.76139655297334));
#60978=CARTESIAN_POINT('Ctrl Pts',(15.0859529727606,-0.116030506223773,
3.3783779715317));
#60979=CARTESIAN_POINT('Ctrl Pts',(15.1336688088234,0.460107006415252,3.56620446371685));
#60980=CARTESIAN_POINT('Ctrl Pts',(15.1813846448862,0.613721175406852,4.15239207167311));
#60981=CARTESIAN_POINT('Ctrl Pts',(15.2291004809491,0.203745745708236,4.59863569535852));
#60982=CARTESIAN_POINT('Ctrl Pts',(15.2768163170119,-0.393332537305518,
4.49514294880206));
#60983=CARTESIAN_POINT('Ctrl Pts',(15.3245321530748,-0.629207499112597,
3.93695281360709));
#60984=CARTESIAN_POINT('Ctrl Pts',(15.3722479891376,-0.287271532882751,
3.43665987978239));
#60985=CARTESIAN_POINT('Ctrl Pts',(15.4199638252004,0.318470302234025,3.45369084645546));
#60986=CARTESIAN_POINT('Ctrl Pts',(15.4676796612633,0.631755958513824,3.97240591487529));
#60987=CARTESIAN_POINT('Ctrl Pts',(15.5153954973261,0.364890397275464,4.51646105625472));
#60988=CARTESIAN_POINT('Ctrl Pts',(15.563111333389,-0.237059630341402,4.58624206290064));
#60989=CARTESIAN_POINT('Ctrl Pts',(15.6108271694518,-0.621314151784485,
4.11766796269128));
#60990=CARTESIAN_POINT('Ctrl Pts',(15.6585430055147,-0.435006327496808,
3.54103756178819));
#60991=CARTESIAN_POINT('Ctrl Pts',(15.7062588415774,0.150774500763906,3.38587942993986));
#60992=CARTESIAN_POINT('Ctrl Pts',(15.7539746776403,0.598096785009218,3.79467766703735));
#60993=CARTESIAN_POINT('Ctrl Pts',(15.8016905137032,0.496177588678611,4.39202656178461));
#60994=CARTESIAN_POINT('Ctrl Pts',(15.849406349766,-0.0613891220090978,
4.62937143274106));
#60995=CARTESIAN_POINT('Ctrl Pts',(15.8971221858288,-0.562581257362808,
4.28875483288714));
#60996=CARTESIAN_POINT('Ctrl Pts',(15.9448380218917,-0.547146367654922,
3.68297022692873));
#60997=CARTESIAN_POINT('Ctrl Pts',(15.9925538579545,-0.0292585496004989,
3.36831893971177));
#60998=CARTESIAN_POINT('Ctrl Pts',(16.0402696940173,0.515497844752703,3.63375008981994));
#60999=CARTESIAN_POINT('Ctrl Pts',(16.0879855300802,0.586864636315616,4.23551416792571));
#61000=CARTESIAN_POINT('Ctrl Pts',(16.135701366143,0.119304602276749,4.62100196177401));
#61001=CARTESIAN_POINT('Ctrl Pts',(16.1834172022059,-0.457814683770117,
4.43621409878185));
#61002=CARTESIAN_POINT('Ctrl Pts',(16.2311330382687,-0.614515701326505,
3.85084411686165));
#61003=CARTESIAN_POINT('Ctrl Pts',(16.2788488743316,-0.206897494815317,
3.40244627748567));
#61004=CARTESIAN_POINT('Ctrl Pts',(16.3265647103943,0.390717864711932,3.50279121604045));
#61005=CARTESIAN_POINT('Ctrl Pts',(16.3742805464572,0.629530997107116,4.05973063144581));
#61006=CARTESIAN_POINT('Ctrl Pts',(16.42199638252,0.290236128279341,4.56181848892059));
#61007=CARTESIAN_POINT('Ctrl Pts',(16.4697122185829,-0.315587043004215,
4.54797978333095));
#61008=CARTESIAN_POINT('Ctrl Pts',(16.5174280546457,-0.631601776766168,
4.03092281095576));
#61009=CARTESIAN_POINT('Ctrl Pts',(16.5651438907086,-0.367606880481235,
3.48546894547127));
#61010=CARTESIAN_POINT('Ctrl Pts',(16.6128597267714,0.233967070508539,3.41251686443844));
#61011=CARTESIAN_POINT('Ctrl Pts',(16.6605755628343,0.620685460604191,3.87905958638177));
#61012=CARTESIAN_POINT('Ctrl Pts',(16.7082913988971,0.437418841753611,4.45666375105816));
#61013=CARTESIAN_POINT('Ctrl Pts',(16.7560072349599,-0.147536230033309,
4.61490656646286));
#61014=CARTESIAN_POINT('Ctrl Pts',(16.8037230710227,-0.597006511643959,
4.20847122033102));
#61015=CARTESIAN_POINT('Ctrl Pts',(16.8514389070856,-0.498236527486006,
3.61059354482716));
#61016=CARTESIAN_POINT('Ctrl Pts',(16.8991547431484,0.058071726216741,3.37031380889701));
#61017=CARTESIAN_POINT('Ctrl Pts',(16.9468705792113,0.561051820186282,3.70828459122417));
#61018=CARTESIAN_POINT('Ctrl Pts',(16.9945864152741,0.548809394786867,4.31414212204871));
#61019=CARTESIAN_POINT('Ctrl Pts',(17.0423022513369,0.0325868576366809,
4.63151810849805));
#61020=CARTESIAN_POINT('Ctrl Pts',(17.0900180873998,-0.513560692294518,
4.3689612987585));
#61021=CARTESIAN_POINT('Ctrl Pts',(17.1377339234626,-0.588097556344686,
3.76758165116972));
#61022=CARTESIAN_POINT('Ctrl Pts',(17.1854497595255,-0.122575385359494,
3.37963534952775));
#61023=CARTESIAN_POINT('Ctrl Pts',(17.2331655955883,0.455509648066065,3.56137945195155));
#61024=CARTESIAN_POINT('Ctrl Pts',(17.2808814316511,0.615293162755707,4.14591555269289));
#61025=CARTESIAN_POINT('Ctrl Pts',(17.328597267714,0.210043498584534,4.59645515619697));
#61026=CARTESIAN_POINT('Ctrl Pts',(17.3763131037768,-0.388092342271454,
4.49926081212312));
#61027=CARTESIAN_POINT('Ctrl Pts',(17.4240289398397,-0.629837013651323,
3.94358758216158));
#61028=CARTESIAN_POINT('Ctrl Pts',(17.4717447759025,-0.293192664107019,
3.43971874351766));
#61029=CARTESIAN_POINT('Ctrl Pts',(17.5194606119653,0.312695020235776,3.45036480373676));
#61030=CARTESIAN_POINT('Ctrl Pts',(17.5671764480282,0.631430056064715,3.96574932190893));
#61031=CARTESIAN_POINT('Ctrl Pts',(17.614892284091,0.370313155609181,4.51258676478657));
#61032=CARTESIAN_POINT('Ctrl Pts',(17.6626081201539,-0.230868013642575,
4.58870789439952));
#61033=CARTESIAN_POINT('Ctrl Pts',(17.7103239562166,-0.620039533605355,
4.12420950615009));
#61034=CARTESIAN_POINT('Ctrl Pts',(17.7580397922796,-0.43981920932378,3.54564761719411));
#61035=CARTESIAN_POINT('Ctrl Pts',(17.8057556283423,0.144293862368219,3.38432451247882));
#61036=CARTESIAN_POINT('Ctrl Pts',(17.8534714644052,0.595899660001039,3.78838568133928));
#61037=CARTESIAN_POINT('Ctrl Pts',(17.901187300468,0.500281630760053,4.38677553513073));
#61038=CARTESIAN_POINT('Ctrl Pts',(17.9489031365309,-0.0547527178302441,
4.62998346370502));
#61039=CARTESIAN_POINT('Ctrl Pts',(17.9966189725937,-0.559506803158163,
4.29466788401745));
#61040=CARTESIAN_POINT('Ctrl Pts',(18.0443348086565,-0.550457182027191,
3.68875425238845));
#61041=CARTESIAN_POINT('Ctrl Pts',(18.0920506447194,-0.0359142607682062,
3.36866237992255));
#61042=CARTESIAN_POINT('Ctrl Pts',(18.1397664807822,0.511609278766163,3.62833755835171));
#61043=CARTESIAN_POINT('Ctrl Pts',(18.187482316845,0.589314145488933,4.22931607570827));
#61044=CARTESIAN_POINT('Ctrl Pts',(18.2351981529079,0.12584276464555,4.61971011226051));
#61045=CARTESIAN_POINT('Ctrl Pts',(18.2829139889707,-0.453191963311679,
4.44101481725822));
#61046=CARTESIAN_POINT('Ctrl Pts',(18.3306298250336,-0.616053538105107,
3.85732882968247));
#61047=CARTESIAN_POINT('Ctrl Pts',(18.3783456610964,-0.213183669654489,
3.40465997308746));
#61048=CARTESIAN_POINT('Ctrl Pts',(18.4260614971592,0.385456042892229,3.49870102369));
#61049=CARTESIAN_POINT('Ctrl Pts',(18.4737773332221,0.630125540247444,4.05309263771424));
#61050=CARTESIAN_POINT('Ctrl Pts',(18.5214931692849,0.296141058265729,4.55872846559028));
#61051=CARTESIAN_POINT('Ctrl Pts',(18.5692090053478,-0.309794314237323,
4.55127534637221));
#61052=CARTESIAN_POINT('Ctrl Pts',(18.6169248414106,-0.631240801177943,
4.0375775941191));
#61053=CARTESIAN_POINT('Ctrl Pts',(18.6646406774734,-0.373009147508776,
3.4893717589807));
#61054=CARTESIAN_POINT('Ctrl Pts',(18.7123565135363,0.227762545801372,3.41008369459593));
#61055=CARTESIAN_POINT('Ctrl Pts',(18.7600723495991,0.619376388724522,3.87252485049244));
#61056=CARTESIAN_POINT('Ctrl Pts',(18.8077881856619,0.442207363551868,4.45202839763978));
#61057=CARTESIAN_POINT('Ctrl Pts',(18.8555040217248,-0.141047487806633,
4.61642731188217));
#61058=CARTESIAN_POINT('Ctrl Pts',(18.9032198577876,-0.594776260815313,
4.21475154067248));
#61059=CARTESIAN_POINT('Ctrl Pts',(18.9509356938505,-0.502312841712761,
3.615866125281));
#61060=CARTESIAN_POINT('Ctrl Pts',(18.9986515299133,0.0514321890198641,
3.36973675771293));
#61061=CARTESIAN_POINT('Ctrl Pts',(19.0463673659762,0.557946249173174,3.70238782336559));
#61062=CARTESIAN_POINT('Ctrl Pts',(19.0940832020389,0.552089683635207,4.30834073020757));
#61063=CARTESIAN_POINT('Ctrl Pts',(19.1417990381018,0.0392406665648073,
4.63113960000379));
#61064=CARTESIAN_POINT('Ctrl Pts',(19.1895148741646,-0.509643658296843,
4.3743532639067));
#61065=CARTESIAN_POINT('Ctrl Pts',(19.2372307102275,-0.590514370077448,
3.77379256516987));
#61066=CARTESIAN_POINT('Ctrl Pts',(19.2849465462903,-0.129106649190522,
3.38096163491845));
#61067=CARTESIAN_POINT('Ctrl Pts',(19.3326623823532,0.450861693465423,3.55660315963506));
#61068=CARTESIAN_POINT('Ctrl Pts',(19.380378218416,0.616796807017627,4.1394228269368));
#61069=CARTESIAN_POINT('Ctrl Pts',(19.4280940544789,0.216317919394901,4.59420836405745));
#61070=CARTESIAN_POINT('Ctrl Pts',(19.4758098905416,-0.382809037079938,
4.50332322288615));
#61071=CARTESIAN_POINT('Ctrl Pts',(19.5235257266046,-0.630396573984801,
3.95022861114352));
#61072=CARTESIAN_POINT('Ctrl Pts',(19.5712415626673,-0.299081219248977,
3.44283985120298));
#61073=CARTESIAN_POINT('Ctrl Pts',(19.6189573987302,0.306884987370396,3.44709979193512));
#61074=CARTESIAN_POINT('Ctrl Pts',(19.666673234793,0.631034051704256,3.95909657101937));
#61075=CARTESIAN_POINT('Ctrl Pts',(19.7143890708559,0.375694716468479,4.50865546647685));
#61076=CARTESIAN_POINT('Ctrl Pts',(19.7621049069187,-0.224650630777236,
4.59110846933868));
#61077=CARTESIAN_POINT('Ctrl Pts',(19.8098207429815,-0.618696275574682,
4.13073699938377));
#61078=CARTESIAN_POINT('Ctrl Pts',(19.8575365790444,-0.44458280157215,3.55030861879767));
#61079=CARTESIAN_POINT('Ctrl Pts',(19.9052524151072,0.13779637220375,3.3828370770856));
#61080=CARTESIAN_POINT('Ctrl Pts',(19.9529682511701,0.593637901716091,3.7821189081517));
#61081=CARTESIAN_POINT('Ctrl Pts',(20.0006840872329,0.504327165075627,4.38147832337345));
#61082=CARTESIAN_POINT('Ctrl Pts',(20.0483999232957,-0.0481046828163007,
4.63053160650705));
#61083=CARTESIAN_POINT('Ctrl Pts',(20.0961157593586,-0.556380679578279,
4.30053671048834));
#61084=CARTESIAN_POINT('Ctrl Pts',(20.1438315954214,-0.553687069357429,
3.69459455385474));
#61085=CARTESIAN_POINT('Ctrl Pts',(20.1915474314843,-0.0426033430871586,
3.36903495876776));
#61086=CARTESIAN_POINT('Ctrl Pts',(20.2392632675471,0.507734449822709,3.62304374442814));
#61087=CARTESIAN_POINT('Ctrl Pts',(20.2869791036099,0.591564791291533,4.22294595084339));
#61088=CARTESIAN_POINT('Ctrl Pts',(20.3346949396728,0.132620199007312,4.618629012875));
#61089=CARTESIAN_POINT('Ctrl Pts',(20.3824107757356,-0.449008129734859,
4.44521533979349));
#61090=CARTESIAN_POINT('Ctrl Pts',(20.4221739724547,-0.588594799935545,
3.96175478680276));
#61091=CARTESIAN_POINT('Ctrl Pts',(20.4539845298298,-0.419131055782338,
3.63395025773895));
#61092=CARTESIAN_POINT('Ctrl Pts',(20.4778424478613,-0.194099195253748,
3.47709810398663));
#61093=CARTESIAN_POINT('Ctrl Pts',(20.5017003658927,0.0810471032980313,
3.44846366347126));
#61094=CARTESIAN_POINT('Ctrl Pts',(20.5255582839241,0.334940048200093,3.55449674151986));
#61095=CARTESIAN_POINT('Ctrl Pts',(20.5494162019556,0.507694843328107,3.76957374638464));
#61096=CARTESIAN_POINT('Ctrl Pts',(20.5732741199869,0.555899439471162,4.04093981905292));
#61097=CARTESIAN_POINT('Ctrl Pts',(20.5971320380184,0.468386015874758,4.30232489481291));
#61098=CARTESIAN_POINT('Ctrl Pts',(20.6209899560498,0.266225827016684,4.48976745893774));
#61099=CARTESIAN_POINT('Ctrl Pts',(20.6448478740812,-0.000973650874560818,
4.55745692740964));
#61100=CARTESIAN_POINT('Ctrl Pts',(20.6687057921126,-0.267966914960919,
4.48882854939535));
#61101=CARTESIAN_POINT('Ctrl Pts',(20.6925637101441,-0.469418090387657,
4.30067062862012));
#61102=CARTESIAN_POINT('Ctrl Pts',(20.7164216281755,-0.556092695039732,
4.03898930289119));
#61103=CARTESIAN_POINT('Ctrl Pts',(20.7402795462069,-0.506782753954552,
3.7677746905255));
#61104=CARTESIAN_POINT('Ctrl Pts',(20.7641374642383,-0.333553132261349,
3.55334514249538));
#61105=CARTESIAN_POINT('Ctrl Pts',(20.7879953822697,-0.0787593560922578,
3.44813505886707));
#61106=CARTESIAN_POINT('Ctrl Pts',(20.8118533003012,0.19529252477751,3.47787088781106));
#61107=CARTESIAN_POINT('Ctrl Pts',(20.8357112183325,0.421590436108717,3.63528155911584));
#61108=CARTESIAN_POINT('Ctrl Pts',(20.859569136364,0.544797804677434,3.8818757964511));
#61109=CARTESIAN_POINT('Ctrl Pts',(20.8834270543954,0.534787374467886,4.15735463375504));
#61110=CARTESIAN_POINT('Ctrl Pts',(20.9072849724269,0.394006808563119,4.39435596913946));
#61111=CARTESIAN_POINT('Ctrl Pts',(20.9311428904582,0.156880874733563,4.53492653211281));
#61112=CARTESIAN_POINT('Ctrl Pts',(20.9550008084897,-0.118606721834374,
4.54469298471526));
#61113=CARTESIAN_POINT('Ctrl Pts',(20.9788587265211,-0.365091735913813,
4.42126716656144));
#61114=CARTESIAN_POINT('Ctrl Pts',(21.0027166445525,-0.522301880015273,
4.19483005048941));
#61115=CARTESIAN_POINT('Ctrl Pts',(21.0265745625839,-0.55179498493052,3.92075168033001));
#61116=CARTESIAN_POINT('Ctrl Pts',(21.0504324806153,-0.446359186657349,
3.66605168284066));
#61117=CARTESIAN_POINT('Ctrl Pts',(21.0742903986468,-0.231776408019839,
3.49301114555638));
#61118=CARTESIAN_POINT('Ctrl Pts',(21.0981483166782,0.0394820154987394,
3.44394319323497));
#61119=CARTESIAN_POINT('Ctrl Pts',(21.1220062347096,0.301086010940692,3.5308462768762));
#61120=CARTESIAN_POINT('Ctrl Pts',(21.145864152741,0.489066275193333,3.73247022529863));
#61121=CARTESIAN_POINT('Ctrl Pts',(21.1697220707724,0.557456513314207,3.9995124910074));
#61122=CARTESIAN_POINT('Ctrl Pts',(21.1935799888039,0.489533449092281,4.26667396594056));
#61123=CARTESIAN_POINT('Ctrl Pts',(21.2174379068352,0.30190612195814,4.46862639215028));
#61124=CARTESIAN_POINT('Ctrl Pts',(21.2412958248667,0.0404545242400231,
4.55598690035157));
#61125=CARTESIAN_POINT('Ctrl Pts',(21.2651537428981,-0.230889306609896,
4.50739346663836));
#61126=CARTESIAN_POINT('Ctrl Pts',(21.2890116609295,-0.445774412697373,
4.33472850921124));
#61127=CARTESIAN_POINT('Ctrl Pts',(21.312869578961,-0.551655532228011,4.08021331346062));
#61128=CARTESIAN_POINT('Ctrl Pts',(21.3367274969923,-0.522641847334507,
3.80608377760199));
#61129=CARTESIAN_POINT('Ctrl Pts',(21.3605854150238,-0.365827994289322,
3.57937204029158));
#61130=CARTESIAN_POINT('Ctrl Pts',(21.3844433330552,-0.119559231686077,
3.45551529680541));
#61131=CARTESIAN_POINT('Ctrl Pts',(21.4083012510867,0.155945019792583,3.46479989471587));
#61132=CARTESIAN_POINT('Ctrl Pts',(21.432159169118,0.393316466074861,3.60495549692644));
#61133=CARTESIAN_POINT('Ctrl Pts',(21.4560170871495,0.534511322676435,3.84171024093472));
#61134=CARTESIAN_POINT('Ctrl Pts',(21.4798750051809,0.545003601087511,4.11717114276091));
#61135=CARTESIAN_POINT('Ctrl Pts',(21.5037329232123,0.422227653432673,4.36398050850424));
#61136=CARTESIAN_POINT('Ctrl Pts',(21.5275908412437,0.196205543263173,4.52178672528827));
#61137=CARTESIAN_POINT('Ctrl Pts',(21.5514487592751,-0.0777941667658609,
4.5520018745543));
#61138=CARTESIAN_POINT('Ctrl Pts',(21.5753066773066,-0.332771083950078,
4.44723752926263));
#61139=CARTESIAN_POINT('Ctrl Pts',(21.5991645953379,-0.506376406606172,
4.23311142556056));
#61140=CARTESIAN_POINT('Ctrl Pts',(21.6230225133694,-0.556158904430687,
3.96198322848119));
#61141=CARTESIAN_POINT('Ctrl Pts',(21.6468804314008,-0.469945400657515,
3.70015116759423));
#61142=CARTESIAN_POINT('Ctrl Pts',(21.6707383494323,-0.268817445367881,
3.51164031394868));
#61143=CARTESIAN_POINT('Ctrl Pts',(21.6945962674636,-0.00195630224560004,
3.44254670619344));
#61144=CARTESIAN_POINT('Ctrl Pts',(21.7184541854951,0.26538321006433,3.50976561349676));
#61145=CARTESIAN_POINT('Ctrl Pts',(21.7423121035264,0.467829298620023,3.6968601820167));
#61146=CARTESIAN_POINT('Ctrl Pts',(21.766170021558,0.555878380248887,3.95808069339639));
#61147=CARTESIAN_POINT('Ctrl Pts',(21.7900279395893,0.508000056083844,4.22955161709966));
#61148=CARTESIAN_POINT('Ctrl Pts',(21.8138858576208,0.335901880562604,4.44489091756156));
#61149=CARTESIAN_POINT('Ctrl Pts',(21.8377437756521,0.0816665454602928,
4.55144227009437));
#61150=CARTESIAN_POINT('Ctrl Pts',(21.8616016936836,-0.192538484559094,
4.52315096660328));
#61151=CARTESIAN_POINT('Ctrl Pts',(21.885459611715,-0.419662610460766,4.36693500143146));
#61152=CARTESIAN_POINT('Ctrl Pts',(21.9093175297464,-0.544167796724789,
4.12099343330092));
#61153=CARTESIAN_POINT('Ctrl Pts',(21.9331754477779,-0.535609133856441,
3.84546567493331));
#61154=CARTESIAN_POINT('Ctrl Pts',(21.9570333658092,-0.396079448060293,
3.60772576847503));
#61155=CARTESIAN_POINT('Ctrl Pts',(21.9808912838407,-0.159697548225882,
3.46590759696012));
#61156=CARTESIAN_POINT('Ctrl Pts',(22.0047492018721,0.115734752223676,3.45468956637345));
#61157=CARTESIAN_POINT('Ctrl Pts',(22.0286071199035,0.362866753203085,3.5768147907664));
#61158=CARTESIAN_POINT('Ctrl Pts',(22.0524650379349,0.521267948732644,3.80242032615069));
#61159=CARTESIAN_POINT('Ctrl Pts',(22.0763229559664,0.552204931742854,4.07633947375325));
#61160=CARTESIAN_POINT('Ctrl Pts',(22.1001808739978,0.448112767182329,4.33159154057792));
#61161=CARTESIAN_POINT('Ctrl Pts',(22.1240387920292,0.23444482469764,4.5057604433585));
#61162=CARTESIAN_POINT('Ctrl Pts',(22.1478967100606,-0.0365512635718279,
4.55625714110116));
#61163=CARTESIAN_POINT('Ctrl Pts',(22.171754628092,-0.298609572266455,4.47073381570218));
#61164=CARTESIAN_POINT('Ctrl Pts',(22.1956125461234,-0.487649706571227,
4.2701032498363));
#61165=CARTESIAN_POINT('Ctrl Pts',(22.2194704641549,-0.557446204325542,
4.00342508191314));
#61166=CARTESIAN_POINT('Ctrl Pts',(22.2433283821863,-0.490931920559466,
3.73590938817905));
#61167=CARTESIAN_POINT('Ctrl Pts',(22.2671863002177,-0.304371409562025,
3.53297104269219));
#61168=CARTESIAN_POINT('Ctrl Pts',(22.2910442182491,-0.0433837978980346,
3.44423399893113));
#61169=CARTESIAN_POINT('Ctrl Pts',(22.3149021362806,0.228212333880327,3.49139688109763));
#61170=CARTESIAN_POINT('Ctrl Pts',(22.3387600543119,0.444004334066149,3.66292708008725));
#61171=CARTESIAN_POINT('Ctrl Pts',(22.3626179723434,0.551225179343846,3.91688078933633));
#61172=CARTESIAN_POINT('Ctrl Pts',(22.3864758903748,0.523656454698273,4.19115941035881));
#61173=CARTESIAN_POINT('Ctrl Pts',(22.4103338084062,0.368039459933637,4.41869434725418));
#61174=CARTESIAN_POINT('Ctrl Pts',(22.4341917264376,0.122426797365049,4.54384711353805));
#61175=CARTESIAN_POINT('Ctrl Pts',(22.458049644469,-0.153122562087755,4.53601444212637));
#61176=CARTESIAN_POINT('Ctrl Pts',(22.4819075625005,-0.391229265084309,
4.39711164706476));
#61177=CARTESIAN_POINT('Ctrl Pts',(22.5057654805319,-0.533669791868601,
4.16110422172694));
#61178=CARTESIAN_POINT('Ctrl Pts',(22.5296233985633,-0.545613449745194,
3.88570245498666));
#61179=CARTESIAN_POINT('Ctrl Pts',(22.5534813165947,-0.424139885198736,
3.63824949626794));
#61180=CARTESIAN_POINT('Ctrl Pts',(22.5773392346261,-0.198952323217499,
3.47925449370713));
#61181=CARTESIAN_POINT('Ctrl Pts',(22.6011971526576,0.0748840438856019,
3.44759575567767));
#61182=CARTESIAN_POINT('Ctrl Pts',(22.625055070689,0.330410085854462,3.55101527375816));
#61183=CARTESIAN_POINT('Ctrl Pts',(22.6489129887204,0.505140231362423,3.7642230866287));
#61184=CARTESIAN_POINT('Ctrl Pts',(22.6727709067518,0.556352908954721,4.03508610068096));
#61185=CARTESIAN_POINT('Ctrl Pts',(22.6966288247833,0.471516332128332,4.29736710820476));
#61186=CARTESIAN_POINT('Ctrl Pts',(22.7204867428146,0.27139215166714,4.48693847894857));
#61187=CARTESIAN_POINT('Ctrl Pts',(22.7443446608461,0.00488440565515616,
4.55743119390072));
#61188=CARTESIAN_POINT('Ctrl Pts',(22.7682025788775,-0.262778018495442,
4.49163382183027));
#61189=CARTESIAN_POINT('Ctrl Pts',(22.7920604969089,-0.466262514422727,
4.30558517247789));
#61190=CARTESIAN_POINT('Ctrl Pts',(22.8079657755965,-0.525793678117208,
4.1317859159904));
#61191=CARTESIAN_POINT('Ctrl Pts',(22.8159184149403,-0.532958495437544,
4.04301651477895));
#61192=CARTESIAN_POINT('Ctrl Pts',(3.98408158505965,-0.251304309929533,
3.59658905474035));
#61193=CARTESIAN_POINT('Ctrl Pts',(3.99203422440346,-0.184112308377066,
3.5547318870523));
#61194=CARTESIAN_POINT('Ctrl Pts',(4.00793950309107,-0.0284797076443847,
3.50528009766423));
#61195=CARTESIAN_POINT('Ctrl Pts',(4.03179742112249,0.212077873916637,3.55216010213054));
#61196=CARTESIAN_POINT('Ctrl Pts',(4.05565533915392,0.400711255741927,3.70851080938071));
#61197=CARTESIAN_POINT('Ctrl Pts',(4.07951325718533,0.49139298320592,3.93615790384083));
#61198=CARTESIAN_POINT('Ctrl Pts',(4.10337117521676,0.461898357851897,4.17940600742409));
#61199=CARTESIAN_POINT('Ctrl Pts',(4.12722909324816,0.319466186301668,4.37878980142624));
#61200=CARTESIAN_POINT('Ctrl Pts',(4.15108701127959,0.0989109688445654,
4.48554634140719));
#61201=CARTESIAN_POINT('Ctrl Pts',(4.174944929311,-0.145828100556353,4.47357507321567));
#61202=CARTESIAN_POINT('Ctrl Pts',(4.19880284734243,-0.354909590370033,
4.34580100620849));
#61203=CARTESIAN_POINT('Ctrl Pts',(4.22266076537384,-0.477205295803391,
4.13346959398438));
#61204=CARTESIAN_POINT('Ctrl Pts',(4.24651868340526,-0.482811689970624,
3.88850100783657));
#61205=CARTESIAN_POINT('Ctrl Pts',(4.27037660143669,-0.370357271909554,
3.67079708031066));
#61206=CARTESIAN_POINT('Ctrl Pts',(4.2942345194681,-0.167340519784032,3.53359217153378));
#61207=CARTESIAN_POINT('Ctrl Pts',(4.31809243749953,0.0765956044913427,
3.51043671457025));
#61208=CARTESIAN_POINT('Ctrl Pts',(4.34195035553093,0.301801986965541,3.60699279882218));
#61209=CARTESIAN_POINT('Ctrl Pts',(4.36580827356237,0.453209578636439,3.79964985833574));
#61210=CARTESIAN_POINT('Ctrl Pts',(4.38966619159377,0.493795074712635,4.04129798000377));
#61211=CARTESIAN_POINT('Ctrl Pts',(4.4135241096252,0.413634228782107,4.27284762322724));
#61212=CARTESIAN_POINT('Ctrl Pts',(4.43738202765661,0.23232854437776,4.43767858897425));
#61213=CARTESIAN_POINT('Ctrl Pts',(4.46123994568804,-0.00578779637616802,
4.49548521832112));
#61214=CARTESIAN_POINT('Ctrl Pts',(4.48509786371945,-0.242488863923451,
4.43213221465579));
#61215=CARTESIAN_POINT('Ctrl Pts',(4.50895578175088,-0.419894798625899,
4.26311111366653));
#61216=CARTESIAN_POINT('Ctrl Pts',(4.53281369978229,-0.494625017545811,
4.02975217827461));
#61217=CARTESIAN_POINT('Ctrl Pts',(4.55667161781372,-0.448405946262215,
3.78911802491887));
#61218=CARTESIAN_POINT('Ctrl Pts',(4.58052953584513,-0.292539406836986,
3.60005025874973));
#61219=CARTESIAN_POINT('Ctrl Pts',(4.60438745387655,-0.0651390137990107,
3.50878109874461));
#61220=CARTESIAN_POINT('Ctrl Pts',(4.62824537190797,0.178189642449287,3.53762834062211));
#61221=CARTESIAN_POINT('Ctrl Pts',(4.65210328993938,0.377946077338085,3.67953804797316));
#61222=CARTESIAN_POINT('Ctrl Pts',(4.67596120797081,0.485284401269169,3.89980943180067));
#61223=CARTESIAN_POINT('Ctrl Pts',(4.69981912600222,0.473957470210434,4.14458013869048));
#61224=CARTESIAN_POINT('Ctrl Pts',(4.72367704403364,0.34673502734182,4.35399706338589));
#61225=CARTESIAN_POINT('Ctrl Pts',(4.74753496206506,0.134726425416229,4.47685206339739));
#61226=CARTESIAN_POINT('Ctrl Pts',(4.77139288009648,-0.110226457398098,
4.48310374471865));
#61227=CARTESIAN_POINT('Ctrl Pts',(4.7952507981279,-0.328225968870003,4.37122340097448));
#61228=CARTESIAN_POINT('Ctrl Pts',(4.81910871615932,-0.465965290257402,
4.16856882376961));
#61229=CARTESIAN_POINT('Ctrl Pts',(4.84296663419074,-0.489763405537152,
3.92469457743051));
#61230=CARTESIAN_POINT('Ctrl Pts',(4.86682455222216,-0.393801027275785,
3.69923455818817));
#61231=CARTESIAN_POINT('Ctrl Pts',(4.89068247025357,-0.201543570920867,
3.54731988215497));
#61232=CARTESIAN_POINT('Ctrl Pts',(4.914540388285,0.039996778460842,3.50609782569371));
#61233=CARTESIAN_POINT('Ctrl Pts',(4.93839830631641,0.271756826018508,3.58564830447545));
#61234=CARTESIAN_POINT('Ctrl Pts',(4.96225622434784,0.437064927107334,3.76651905952651));
#61235=CARTESIAN_POINT('Ctrl Pts',(4.98611414237925,0.495498748108838,4.00448226441646));
#61236=CARTESIAN_POINT('Ctrl Pts',(5.00997206041068,0.432769628082826,4.24134943356216));
#61237=CARTESIAN_POINT('Ctrl Pts',(5.03382997844209,0.26421654558258,4.41920009197534));
#61238=CARTESIAN_POINT('Ctrl Pts',(5.05768789647352,0.031055320573195,4.49454490911931));
#61239=CARTESIAN_POINT('Ctrl Pts',(5.08154581450493,-0.209699776246285,
4.44896002485074));
#61240=CARTESIAN_POINT('Ctrl Pts',(5.10540373253635,-0.399177565666329,
4.29359218508065));
#61241=CARTESIAN_POINT('Ctrl Pts',(5.12926165056777,-0.491045566902382,
4.06643305876778));
#61242=CARTESIAN_POINT('Ctrl Pts',(5.15311956859918,-0.462839551218119,
3.823029239986));
#61243=CARTESIAN_POINT('Ctrl Pts',(5.17697748663061,-0.321456657764784,
3.62289959261435));
#61244=CARTESIAN_POINT('Ctrl Pts',(5.20083540466202,-0.101468855184408,
3.51498126685736));
#61245=CARTESIAN_POINT('Ctrl Pts',(5.22469332269345,0.143330846444675,3.52566323299877));
#61246=CARTESIAN_POINT('Ctrl Pts',(5.24855124072486,0.353082251864168,3.6523334593461));
#61247=CARTESIAN_POINT('Ctrl Pts',(5.27240915875629,0.476495428935435,3.86401762512973));
#61248=CARTESIAN_POINT('Ctrl Pts',(5.2962670767877,0.483392494157105,4.10895318565465));
#61249=CARTESIAN_POINT('Ctrl Pts',(5.32012499481913,0.372086927210194,4.32724672446184));
#61250=CARTESIAN_POINT('Ctrl Pts',(5.34398291285054,0.169795971115995,4.46551952511629));
#61251=CARTESIAN_POINT('Ctrl Pts',(5.36784083088196,-0.0740147250654609,
4.48996012138256));
#61252=CARTESIAN_POINT('Ctrl Pts',(5.39169874891337,-0.299726804847767,
4.39459212172504));
#61253=CARTESIAN_POINT('Ctrl Pts',(5.4155566669448,-0.452147516450583,4.20273559983216));
#61254=CARTESIAN_POINT('Ctrl Pts',(5.43941458497621,-0.494005844030112,
3.96130470137348));
#61255=CARTESIAN_POINT('Ctrl Pts',(5.46327250300764,-0.415066286295368,
3.72933585746768));
#61256=CARTESIAN_POINT('Ctrl Pts',(5.48713042103905,-0.234631715382576,
3.56355176915442));
#61257=CARTESIAN_POINT('Ctrl Pts',(5.51098833907048,0.00317670118048804,
3.50449116189365));
#61258=CARTESIAN_POINT('Ctrl Pts',(5.53484625710188,0.240208327774024,3.56659596294035));
#61259=CARTESIAN_POINT('Ctrl Pts',(5.55870417513332,0.418502475082003,3.73467985673571));
#61260=CARTESIAN_POINT('Ctrl Pts',(5.58256209316472,0.494461367456411,3.96764175273735));
#61261=CARTESIAN_POINT('Ctrl Pts',(5.60642001119615,0.449510986625754,4.20851612161082));
#61262=CARTESIAN_POINT('Ctrl Pts',(5.63027792922757,0.294642925140636,4.39840261889448));
#61263=CARTESIAN_POINT('Ctrl Pts',(5.65413584725899,0.0677266425295592,
4.49086882357174));
#61264=CARTESIAN_POINT('Ctrl Pts',(5.6779937652904,-0.17575064898472,4.46330422991997));
#61265=CARTESIAN_POINT('Ctrl Pts',(5.70185168332183,-0.376252119531055,
4.32244913183746));
#61266=CARTESIAN_POINT('Ctrl Pts',(5.72570960135325,-0.48474969783608,4.10274643779879));
#61267=CARTESIAN_POINT('Ctrl Pts',(5.74956751938466,-0.474712770918799,
3.85791944074229));
#61268=CARTESIAN_POINT('Ctrl Pts',(5.77342543741608,-0.348595640189148,
3.64783501103505));
#61269=CARTESIAN_POINT('Ctrl Pts',(5.7972833554475,-0.13723738064616,3.52386451312966));
#61270=CARTESIAN_POINT('Ctrl Pts',(5.82114127347893,0.1076791581852,3.5163221129105));
#61271=CARTESIAN_POINT('Ctrl Pts',(5.84499919151033,0.326265206982528,3.62705212841851));
#61272=CARTESIAN_POINT('Ctrl Pts',(5.86885710954176,0.465070530553655,3.82897806268729));
#61273=CARTESIAN_POINT('Ctrl Pts',(5.89271502757317,0.490153431381492,4.07272350923538));
#61274=CARTESIAN_POINT('Ctrl Pts',(5.9165729456046,0.395380485146506,4.29868609559117));
#61275=CARTESIAN_POINT('Ctrl Pts',(5.94043086363601,0.203926205561759,4.45161176009809));
#61276=CARTESIAN_POINT('Ctrl Pts',(5.96428878166744,-0.0373935204432717,
4.49410611450448));
#61277=CARTESIAN_POINT('Ctrl Pts',(5.98814669969885,-0.26956963613406,4.41577793841189));
#61278=CARTESIAN_POINT('Ctrl Pts',(6.01200461773027,-0.435828398698505,
4.23578096933615));
#61279=CARTESIAN_POINT('Ctrl Pts',(6.0358625357617,-0.495515688199628,3.99812868033461));
#61280=CARTESIAN_POINT('Ctrl Pts',(6.0597204537931,-0.434035059498629,3.76093483037113));
#61281=CARTESIAN_POINT('Ctrl Pts',(6.08357837182454,-0.266422612259865,
3.58219732064663));
#61282=CARTESIAN_POINT('Ctrl Pts',(6.10743628985594,-0.0336596025775484,
3.50562697870369));
#61283=CARTESIAN_POINT('Ctrl Pts',(6.13129420788738,0.207328476491996,3.54993858195554));
#61284=CARTESIAN_POINT('Ctrl Pts',(6.15515212591877,0.397629707835022,3.70431327123879));
#61285=CARTESIAN_POINT('Ctrl Pts',(6.17901004395022,0.490679606253205,3.93097100878581));
#61286=CARTESIAN_POINT('Ctrl Pts',(6.20286796198161,0.463782811036945,4.17454675550933));
#61287=CARTESIAN_POINT('Ctrl Pts',(6.22672588001306,0.323407044622774,4.3753682944706));
#61288=CARTESIAN_POINT('Ctrl Pts',(6.25058379804445,0.104084330837213,4.48453946106473));
#61289=CARTESIAN_POINT('Ctrl Pts',(6.27444171607588,-0.140944443623038,
4.4749681472433));
#61290=CARTESIAN_POINT('Ctrl Pts',(6.29829963410731,-0.351028389709017,
4.349743491311));
#61291=CARTESIAN_POINT('Ctrl Pts',(6.32215755213872,-0.476177279109797,
4.13807688197341));
#61292=CARTESIAN_POINT('Ctrl Pts',(6.34601547017014,-0.483231738207782,
3.89435343878414));
#61293=CARTESIAN_POINT('Ctrl Pts',(6.37782602754537,-0.338784024988664,
3.5998542259592));
#61294=CARTESIAN_POINT('Ctrl Pts',(6.41758922426439,0.0803770223010952,
3.44371490521648));
#61295=CARTESIAN_POINT('Ctrl Pts',(6.46530506032724,0.512014121509362,3.7673575683149));
#61296=CARTESIAN_POINT('Ctrl Pts',(6.51302089639006,0.472271980317209,4.30452828893312));
#61297=CARTESIAN_POINT('Ctrl Pts',(6.56073673245292,-0.000548856210248058,
4.56210751581942));
#61298=CARTESIAN_POINT('Ctrl Pts',(6.60845256851575,-0.473190198344468,
4.30346185287483));
#61299=CARTESIAN_POINT('Ctrl Pts',(6.65616840457859,-0.511122033036262,
3.76615996983968));
#61300=CARTESIAN_POINT('Ctrl Pts',(6.70388424064142,-0.0797735308749388,
3.44358772816382));
#61301=CARTESIAN_POINT('Ctrl Pts',(6.75160007670426,0.424880365184703,3.63198234005898));
#61302=CARTESIAN_POINT('Ctrl Pts',(6.7993159127671,0.539334593204737,4.15833063512042));
#61303=CARTESIAN_POINT('Ctrl Pts',(6.84703174882994,0.158523065679302,4.53928284691909));
#61304=CARTESIAN_POINT('Ctrl Pts',(6.89474758489278,-0.367869781963911,
4.42500259414721));
#61305=CARTESIAN_POINT('Ctrl Pts',(6.94246342095561,-0.556438361909488,
3.92043630538129));
#61306=CARTESIAN_POINT('Ctrl Pts',(6.99017925701846,-0.234023037562683,
3.48893437735136));
#61307=CARTESIAN_POINT('Ctrl Pts',(7.03789509308128,0.303300305128555,3.52675198254107));
#61308=CARTESIAN_POINT('Ctrl Pts',(7.08561092914413,0.562097748282813,3.99916046672433));
#61309=CARTESIAN_POINT('Ctrl Pts',(7.13332676520696,0.304712478085684,4.47233993757656));
#61310=CARTESIAN_POINT('Ctrl Pts',(7.18104260126981,-0.232495107101315,
4.51176235979777));
#61311=CARTESIAN_POINT('Ctrl Pts',(7.22875843733264,-0.556198774489988,
4.08122554105153));
#61312=CARTESIAN_POINT('Ctrl Pts',(7.27647427339549,-0.369136593294786,
3.57609805363465));
#61313=CARTESIAN_POINT('Ctrl Pts',(7.32419010945832,0.156909424853758,3.46024624852207));
#61314=CARTESIAN_POINT('Ctrl Pts',(7.37190594552116,0.538863091386428,3.84005861730642));
#61315=CARTESIAN_POINT('Ctrl Pts',(7.41962178158399,0.425970496197337,4.36674761950234));
#61316=CARTESIAN_POINT('Ctrl Pts',(7.46733761764684,-0.0780973635293338,
4.55664663921719));
#61317=CARTESIAN_POINT('Ctrl Pts',(7.51505345370967,-0.510447210801067,
4.2353684852172));
#61318=CARTESIAN_POINT('Ctrl Pts',(7.56276928977251,-0.474045531130633,
3.69794782953315));
#61319=CARTESIAN_POINT('Ctrl Pts',(7.61048512583535,-0.00232054557778912,
3.43790632971152));
#61320=CARTESIAN_POINT('Ctrl Pts',(7.65820096189818,0.471535432411473,3.69404409621074));
#61321=CARTESIAN_POINT('Ctrl Pts',(7.70591679796103,0.512373167457076,4.23114587691112));
#61322=CARTESIAN_POINT('Ctrl Pts',(7.75363263402387,0.0826907388754792,
4.55598284219971));
#61323=CARTESIAN_POINT('Ctrl Pts',(7.80134847008669,-0.422927867535356,
4.3702522086048));
#61324=CARTESIAN_POINT('Ctrl Pts',(7.84906430614955,-0.540165305628305,
3.84451327478339));
#61325=CARTESIAN_POINT('Ctrl Pts',(7.89678014221237,-0.161360632039799,
3.46156019320034));
#61326=CARTESIAN_POINT('Ctrl Pts',(7.94449597827521,0.365623992797271,3.57306467116217));
#61327=CARTESIAN_POINT('Ctrl Pts',(7.99221181433806,0.556850479203549,4.07663043084052));
#61328=CARTESIAN_POINT('Ctrl Pts',(8.03992765040089,0.236712602309549,4.50982528676712));
#61329=CARTESIAN_POINT('Ctrl Pts',(8.08764348646373,-0.300802099575971,
4.47483973718518));
#61330=CARTESIAN_POINT('Ctrl Pts',(8.13535932252656,-0.562085604986122,
4.00380155059756));
#61331=CARTESIAN_POINT('Ctrl Pts',(8.18307515858941,-0.307197250538534,
3.52927234160183));
#61332=CARTESIAN_POINT('Ctrl Pts',(8.23079099465223,0.229795065915734,3.48701958438918));
#61333=CARTESIAN_POINT('Ctrl Pts',(8.27850683071509,0.555763037488074,3.91584463605021));
#61334=CARTESIAN_POINT('Ctrl Pts',(8.32622266677791,0.371365260221553,4.42195085332305));
#61335=CARTESIAN_POINT('Ctrl Pts',(8.37393850284076,-0.154062949695418,
4.54057310944092));
#61336=CARTESIAN_POINT('Ctrl Pts',(8.4216543389036,-0.538012782343907,4.16277876137275));
#61337=CARTESIAN_POINT('Ctrl Pts',(8.46937017496643,-0.427897198575242,
3.6355021720628));
#61338=CARTESIAN_POINT('Ctrl Pts',(8.51708601102927,0.0751629666897603,
3.44294954666756));
#61339=CARTESIAN_POINT('Ctrl Pts',(8.56480184709211,0.50919982311266,3.76194492389047));
#61340=CARTESIAN_POINT('Ctrl Pts',(8.61251768315494,0.475630646924824,4.29954994045293));
#61341=CARTESIAN_POINT('Ctrl Pts',(8.66023351921779,0.00528252914771292,
4.56207363752918));
#61342=CARTESIAN_POINT('Ctrl Pts',(8.70794935528062,-0.469916616427902,
4.30843646464781));
#61343=CARTESIAN_POINT('Ctrl Pts',(8.75566519134346,-0.513584102541225,
3.7715573403753));
#61344=CARTESIAN_POINT('Ctrl Pts',(8.8033810274063,-0.0856194047837525,
3.44446062547832));
#61345=CARTESIAN_POINT('Ctrl Pts',(8.85109686346913,0.420970909810523,3.6275242662766));
#61346=CARTESIAN_POINT('Ctrl Pts',(8.89881269953199,0.540977160455745,4.15263810462895));
#61347=CARTESIAN_POINT('Ctrl Pts',(8.9465285355948,0.1641957606509,4.5375820228614));
#61348=CARTESIAN_POINT('Ctrl Pts',(8.99424437165766,-0.363369132636193,
4.42885609773758));
#61349=CARTESIAN_POINT('Ctrl Pts',(9.04196020772048,-0.557246560270691,
3.92630501926208));
#61350=CARTESIAN_POINT('Ctrl Pts',(9.08967604378333,-0.239395897268157,
3.49142917554125));
#61351=CARTESIAN_POINT('Ctrl Pts',(9.13739187984617,0.298295701775085,3.52358174528888));
#61352=CARTESIAN_POINT('Ctrl Pts',(9.18510771590899,0.562057768008922,3.99323652897485));
#61353=CARTESIAN_POINT('Ctrl Pts',(9.23282355197185,0.309673537509763,4.46910231217259));
#61354=CARTESIAN_POINT('Ctrl Pts',(9.28053938803466,-0.227088667424462,
4.51418422403538));
#61355=CARTESIAN_POINT('Ctrl Pts',(9.32825522409753,-0.555311854854516,
4.08708285122523));
#61356=CARTESIAN_POINT('Ctrl Pts',(9.37597106016035,-0.373583621400482,
3.58001195619306));
#61357=CARTESIAN_POINT('Ctrl Pts',(9.4236868962232,0.151212199908504,3.45862254413551));
#61358=CARTESIAN_POINT('Ctrl Pts',(9.47140273228603,0.537147531342748,3.83438837996121));
#61359=CARTESIAN_POINT('Ctrl Pts',(9.51911856834887,0.429812019667804,4.36223791473086));
#61360=CARTESIAN_POINT('Ctrl Pts',(9.5668344044117,-0.0722264831760907,
4.5574387986564));
#61361=CARTESIAN_POINT('Ctrl Pts',(9.61455024047456,-0.507938295172089,
4.24073505647735));
#61362=CARTESIAN_POINT('Ctrl Pts',(9.66226607653738,-0.477202555076283,
3.70296060775017));
#61363=CARTESIAN_POINT('Ctrl Pts',(9.70998191260023,-0.00824436594879979,
3.43796200346455));
#61364=CARTESIAN_POINT('Ctrl Pts',(9.75769774866306,0.46828475128534,3.68909153946361));
#61365=CARTESIAN_POINT('Ctrl Pts',(9.80541358472589,0.514780775927077,4.22573309871483));
#61366=CARTESIAN_POINT('Ctrl Pts',(9.85312942078874,0.0885456931146035,
4.55508048006603));
#61367=CARTESIAN_POINT('Ctrl Pts',(9.90084525685159,-0.419002262135622,
4.37468891556157));
#61368=CARTESIAN_POINT('Ctrl Pts',(9.9485610929144,-0.541773992888202,3.8502147545669));
#61369=CARTESIAN_POINT('Ctrl Pts',(9.99627692897727,-0.167026329707142,
3.46329068919569));
#61370=CARTESIAN_POINT('Ctrl Pts',(10.0439927650401,0.361104182074418,3.56923504227033));
#61371=CARTESIAN_POINT('Ctrl Pts',(10.0917086011029,0.557627167155001,4.07075748419897));
#61372=CARTESIAN_POINT('Ctrl Pts',(10.1394244371657,0.242072544440304,4.50730223964386));
#61373=CARTESIAN_POINT('Ctrl Pts',(10.1871402732286,-0.295781020598791,
4.47798354257549));
#61374=CARTESIAN_POINT('Ctrl Pts',(10.2348561092914,-0.56201432324602,4.00972520363789));
#61375=CARTESIAN_POINT('Ctrl Pts',(10.2825719453543,-0.312141225154507,
3.53253606055812));
#61376=CARTESIAN_POINT('Ctrl Pts',(10.3302877814171,0.224375962906492,3.48462624592509));
#61377=CARTESIAN_POINT('Ctrl Pts',(10.37800361748,0.554845251762499,3.90999207970357));
#61378=CARTESIAN_POINT('Ctrl Pts',(10.4257194535428,0.375791608533427,4.41801357164013));
#61379=CARTESIAN_POINT('Ctrl Pts',(10.4734352896056,-0.148357251109035,
4.54216676877402));
#61380=CARTESIAN_POINT('Ctrl Pts',(10.5211511256685,-0.536267364288337,
4.16843987983467));
#61381=CARTESIAN_POINT('Ctrl Pts',(10.5688669617313,-0.431714905307627,
3.64003205746247));
#61382=CARTESIAN_POINT('Ctrl Pts',(10.6165827977942,0.0692879940047382,
3.44218833554121));
#61383=CARTESIAN_POINT('Ctrl Pts',(10.664298633857,0.50666266228973,3.75659164812817));
#61384=CARTESIAN_POINT('Ctrl Pts',(10.7120144699198,0.478761211786921,4.29452059555793));
#61385=CARTESIAN_POINT('Ctrl Pts',(10.7597303059827,0.0112059738120427,
4.56198674830498));
#61386=CARTESIAN_POINT('Ctrl Pts',(10.8074461420455,-0.466639882340508,
4.31337182280594));
#61387=CARTESIAN_POINT('Ctrl Pts',(10.8551619781083,-0.515963154362253,
3.77698273057893));
#61388=CARTESIAN_POINT('Ctrl Pts',(10.9028778141712,-0.0914695226195351,
3.44539382842306));
#61389=CARTESIAN_POINT('Ctrl Pts',(10.950593650234,0.417021979184216,3.62310830733915));
#61390=CARTESIAN_POINT('Ctrl Pts',(10.9983094862969,0.542555780795161,4.14692822684982));
#61391=CARTESIAN_POINT('Ctrl Pts',(11.0460253223597,0.169852260608159,4.53582169486292));
#61392=CARTESIAN_POINT('Ctrl Pts',(11.0937411584225,-0.358829204008283,
4.43266185580689));
#61393=CARTESIAN_POINT('Ctrl Pts',(11.1414569944853,-0.55799228928692,3.93218197720501));
#61394=CARTESIAN_POINT('Ctrl Pts',(11.1891728305482,-0.244742469498405,
3.49398043245019));
#61395=CARTESIAN_POINT('Ctrl Pts',(11.236888666611,0.293258125877444,3.5204644426882));
#61396=CARTESIAN_POINT('Ctrl Pts',(11.2846045026739,0.561955271903759,3.98731333380864));
#61397=CARTESIAN_POINT('Ctrl Pts',(11.3323203387367,0.314600244947554,4.46581258570203));
#61398=CARTESIAN_POINT('Ctrl Pts',(11.3800361747996,-0.221657027690976,
4.51654897269734));
#61399=CARTESIAN_POINT('Ctrl Pts',(11.4277520108624,-0.554363241169119,
4.0929304899371));
#61400=CARTESIAN_POINT('Ctrl Pts',(11.4754678469252,-0.377989160306769,
3.58397250834823));
#61401=CARTESIAN_POINT('Ctrl Pts',(11.5231836829881,0.145498182576105,3.45705897374896));
#61402=CARTESIAN_POINT('Ctrl Pts',(11.5708995190509,0.535372305622036,3.82873653777755));
#61403=CARTESIAN_POINT('Ctrl Pts',(11.6186153551137,0.43360580265347,4.35768797439208));
#61404=CARTESIAN_POINT('Ctrl Pts',(11.6663311911766,-0.0663475807746441,
4.55816904038548));
#61405=CARTESIAN_POINT('Ctrl Pts',(11.7140470272394,-0.505372959888646,
4.24607488805821));
#61406=CARTESIAN_POINT('Ctrl Pts',(11.7617628633023,-0.480306573774387,
3.70800637967828));
#61407=CARTESIAN_POINT('Ctrl Pts',(11.8094786993651,-0.0141672704965164,
3.43808010573911));
#61408=CARTESIAN_POINT('Ctrl Pts',(11.8571945354279,0.464982055269784,3.68417351694868));
#61409=CARTESIAN_POINT('Ctrl Pts',(11.9049103714908,0.517131205013274,4.22029524715934));
#61410=CARTESIAN_POINT('Ctrl Pts',(11.9526262075536,0.0943908121067024,
4.55411646222552));
#61411=CARTESIAN_POINT('Ctrl Pts',(12.0003420436165,-0.415030115946784,
4.37908400385228));
#61412=CARTESIAN_POINT('Ctrl Pts',(12.0480578796793,-0.543322502467158,
3.85593287178435));
#61413=CARTESIAN_POINT('Ctrl Pts',(12.0957737157421,-0.172673474880652,
3.46508080031456));
#61414=CARTESIAN_POINT('Ctrl Pts',(12.143489551805,0.356544261611682,3.56545326070575));
#61415=CARTESIAN_POINT('Ctrl Pts',(12.1912053878678,0.558341916527368,4.06487667815191));
#61416=CARTESIAN_POINT('Ctrl Pts',(12.2389212239306,0.247405598301292,4.50472284379514));
#61417=CARTESIAN_POINT('Ctrl Pts',(12.2866370599935,-0.290727087669313,
4.48107425582212));
#61418=CARTESIAN_POINT('Ctrl Pts',(12.3343528960563,-0.56188061562194,4.01564777644873));
#61419=CARTESIAN_POINT('Ctrl Pts',(12.3820687321191,-0.317050528604376,
3.5358517031905));
#61420=CARTESIAN_POINT('Ctrl Pts',(12.429784568182,0.218931937280033,3.48229015273196));
#61421=CARTESIAN_POINT('Ctrl Pts',(12.4775004042448,0.553865836459325,3.90414952100961));
#61422=CARTESIAN_POINT('Ctrl Pts',(12.5252162403077,0.380176215696692,4.4140298589933));
#61423=CARTESIAN_POINT('Ctrl Pts',(12.5729320763705,-0.142635073703209,
4.54370020679522));
#61424=CARTESIAN_POINT('Ctrl Pts',(12.6206479124333,-0.53446238019874,4.17408228879405));
#61425=CARTESIAN_POINT('Ctrl Pts',(12.6683637484962,-0.435484659196984,
3.644601926393));
#61426=CARTESIAN_POINT('Ctrl Pts',(12.716079584559,0.0634053251381518,3.44148908348752));
#61427=CARTESIAN_POINT('Ctrl Pts',(12.7637954206219,0.504069223782589,3.75126540901054));
#61428=CARTESIAN_POINT('Ctrl Pts',(12.8115112566847,0.481838598125516,4.2894585367128));
#61429=CARTESIAN_POINT('Ctrl Pts',(12.8592270927475,0.0171281737699642,
4.56183743625962));
#61430=CARTESIAN_POINT('Ctrl Pts',(12.9069429288104,-0.463311316109371,
4.31827237310907));
#61431=CARTESIAN_POINT('Ctrl Pts',(12.9546587648732,-0.518284895444539,
3.78243289248252));
#61432=CARTESIAN_POINT('Ctrl Pts',(13.0023746009361,-0.0973094804548018,
3.44638863438952));
#61433=CARTESIAN_POINT('Ctrl Pts',(13.0500904369989,0.413026727735397,3.61873421174243));
#61434=CARTESIAN_POINT('Ctrl Pts',(13.0978062730617,0.544074136613086,4.14120202898048));
#61435=CARTESIAN_POINT('Ctrl Pts',(13.1455221091246,0.17548989418231,4.53400185033327));
#61436=CARTESIAN_POINT('Ctrl Pts',(13.1932379451874,-0.354249418335187,
4.4364195558504));
#61437=CARTESIAN_POINT('Ctrl Pts',(13.2409537812502,-0.558676039167545,
3.93806646805208));
#61438=CARTESIAN_POINT('Ctrl Pts',(13.2886696173131,-0.250061856896528,
3.49658789561142));
#61439=CARTESIAN_POINT('Ctrl Pts',(13.3363854533759,0.288187976258808,3.51740040462167));
#61440=CARTESIAN_POINT('Ctrl Pts',(13.3841012894388,0.56179035647369,3.9813915478171));
#61441=CARTESIAN_POINT('Ctrl Pts',(13.4318171255016,0.319492008083037,4.46247111897993));
#61442=CARTESIAN_POINT('Ctrl Pts',(13.4795329615644,-0.21620076734671,4.51885634555065));
#61443=CARTESIAN_POINT('Ctrl Pts',(13.5272487976273,-0.553353051445561,
4.09876780637113));
#61444=CARTESIAN_POINT('Ctrl Pts',(13.5749646336901,-0.382352713970831,
3.58797927086295));
#61445=CARTESIAN_POINT('Ctrl Pts',(13.6226804697529,0.139768003996038,3.45555571067516));
#61446=CARTESIAN_POINT('Ctrl Pts',(13.6703963058158,0.53353761328617,3.82310371872654));
#61447=CARTESIAN_POINT('Ctrl Pts',(13.7181121418786,0.437351422764197,4.35309830377052));
#61448=CARTESIAN_POINT('Ctrl Pts',(13.7658279779415,-0.0604613087987784,
4.55883728334624));
#61449=CARTESIAN_POINT('Ctrl Pts',(13.8135438140043,-0.502751490175015,
4.25138738680826));
#61450=CARTESIAN_POINT('Ctrl Pts',(13.8612596500671,-0.483357242297515,
3.71308458487209));
#61451=CARTESIAN_POINT('Ctrl Pts',(13.90897548613,-0.0200886014110514,3.43826062340902));
#61452=CARTESIAN_POINT('Ctrl Pts',(13.9566913221928,0.461627711254046,3.67929057494076));
#61453=CARTESIAN_POINT('Ctrl Pts',(14.0044071582557,0.519424193619207,4.21483292625321));
#61454=CARTESIAN_POINT('Ctrl Pts',(14.0521229943185,0.100225446615308,4.55309089575788));
#61455=CARTESIAN_POINT('Ctrl Pts',(14.0998388303813,-0.411011870182152,
4.38343698529073));
#61456=CARTESIAN_POINT('Ctrl Pts',(14.1475546664441,-0.544810662360815,
3.86166699129474));
#61457=CARTESIAN_POINT('Ctrl Pts',(14.195270502507,-0.178301440303968,3.46693032771971));
#61458=CARTESIAN_POINT('Ctrl Pts',(14.2429863385698,0.351944737904315,3.5617197465309));
#61459=CARTESIAN_POINT('Ctrl Pts',(14.2907021746327,0.558994647929194,4.05898866591129));
#61460=CARTESIAN_POINT('Ctrl Pts',(14.3384180106955,0.252711171522458,4.50208738572805));
#61461=CARTESIAN_POINT('Ctrl Pts',(14.3861338467583,-0.28564086215454,4.48411153362329));
#61462=CARTESIAN_POINT('Ctrl Pts',(14.4338496828212,-0.561684496965419,
4.02156861117883));
#61463=CARTESIAN_POINT('Ctrl Pts',(14.481565518884,-0.321924615586062,3.53921890121312));
#61464=CARTESIAN_POINT('Ctrl Pts',(14.5292813549469,0.213463593732893,3.48001156429194));
#61465=CARTESIAN_POINT('Ctrl Pts',(14.5769971910097,0.552824900367352,3.89831760893199));
#61466=CARTESIAN_POINT('Ctrl Pts',(14.6247130270725,0.384518594689996,4.4100001578745));
#61467=CARTESIAN_POINT('Ctrl Pts',(14.6724288631354,-0.136897053070264,
4.54517325317752));
#61468=CARTESIAN_POINT('Ctrl Pts',(14.7201446991982,-0.532598030564186,
4.17970536151887));
#61469=CARTESIAN_POINT('Ctrl Pts',(14.7678605352611,-0.439206041516937,
3.64921127125505));
#61470=CARTESIAN_POINT('Ctrl Pts',(14.8155763713239,0.0575156135089261,
3.44085186817608));
#61471=CARTESIAN_POINT('Ctrl Pts',(14.8632922073868,0.501419795658073,3.74596679815093));
#61472=CARTESIAN_POINT('Ctrl Pts',(14.9110080434496,0.484862464119148,4.284364326187));
#61473=CARTESIAN_POINT('Ctrl Pts',(14.9587238795124,0.0230484712116303,
4.56162571797798));
#61474=CARTESIAN_POINT('Ctrl Pts',(15.0064397155752,-0.459931287455839,
4.32313757122732));
#61475=CARTESIAN_POINT('Ctrl Pts',(15.0541555516381,-0.5205490679001,3.78790722070797));
#61476=CARTESIAN_POINT('Ctrl Pts',(15.1018713877009,-0.103138629614742,
3.44744493287938));
#61477=CARTESIAN_POINT('Ctrl Pts',(15.1495872237638,0.40898559923764,3.61440246534021));
#61478=CARTESIAN_POINT('Ctrl Pts',(15.1973030598266,0.545532059257757,4.13546014705983));
#61479=CARTESIAN_POINT('Ctrl Pts',(15.2450188958894,0.181108035171788,4.53212269141213));
#61480=CARTESIAN_POINT('Ctrl Pts',(15.2927347319523,-0.349630284317748,
4.44012878048063));
#61481=CARTESIAN_POINT('Ctrl Pts',(15.3404505680151,-0.559297733964875,
3.94395783818199));
#61482=CARTESIAN_POINT('Ctrl Pts',(15.3881664040779,-0.255353468610234,
3.49925127540033));
#61483=CARTESIAN_POINT('Ctrl Pts',(15.4358822401408,0.283085816087337,3.51438997142805));
#61484=CARTESIAN_POINT('Ctrl Pts',(15.4835980762036,0.561563040036739,3.97547182876414));
#61485=CARTESIAN_POINT('Ctrl Pts',(15.5313139122665,0.324348283562367,4.45907828316053));
#61486=CARTESIAN_POINT('Ctrl Pts',(15.5790297483293,-0.210720492447169,
4.52110608630326));
#61487=CARTESIAN_POINT('Ctrl Pts',(15.6267455843921,-0.552281397890927,
4.10459415214592));
#61488=CARTESIAN_POINT('Ctrl Pts',(15.674461420455,-0.386673797709831,3.59203179868507));
#61489=CARTESIAN_POINT('Ctrl Pts',(15.7221772565178,0.134022300649356,3.45411292188939));
#61490=CARTESIAN_POINT('Ctrl Pts',(15.7698930925807,0.531643658124066,3.81749054847505));
#61491=CARTESIAN_POINT('Ctrl Pts',(15.8176089286435,0.441048463954279,4.34846941266494));
#61492=CARTESIAN_POINT('Ctrl Pts',(15.8653247647064,-0.054568321067637,
4.5594434533135));
#61493=CARTESIAN_POINT('Ctrl Pts',(15.9130406007692,-0.500074177211609,
4.25667196264028));
#61494=CARTESIAN_POINT('Ctrl Pts',(15.960756436832,-0.486354221791887,3.71819465926869));
#61495=CARTESIAN_POINT('Ctrl Pts',(16.0084722728949,-0.0260077009790528,
3.4385035364232));
#61496=CARTESIAN_POINT('Ctrl Pts',(16.0561881089577,0.458222091822753,3.6744432558139));
#61497=CARTESIAN_POINT('Ctrl Pts',(16.1039039450206,0.52165948705058,4.2093467427251));
#61498=CARTESIAN_POINT('Ctrl Pts',(16.1516197810833,0.106048948556897,4.55200389457816));
#61499=CARTESIAN_POINT('Ctrl Pts',(16.1993356171462,-0.406947971169398,
4.38774737636841));
#61500=CARTESIAN_POINT('Ctrl Pts',(16.247051453209,-0.546238307271431,3.86741647617928));
#61501=CARTESIAN_POINT('Ctrl Pts',(16.2947672892719,-0.183909600849411,
3.46883906597446));
#61502=CARTESIAN_POINT('Ctrl Pts',(16.3424831253347,0.347306121845567,3.55803491444678));
#61503=CARTESIAN_POINT('Ctrl Pts',(16.3901989613975,0.559585288858183,4.05309410148958));
#61504=CARTESIAN_POINT('Ctrl Pts',(16.4379147974604,0.257988674785898,4.49939615817675));
#61505=CARTESIAN_POINT('Ctrl Pts',(16.4856306335232,-0.280522909008289,
4.4870950386126));
#61506=CARTESIAN_POINT('Ctrl Pts',(16.5333464695861,-0.561425989060384,
4.02748705016995));
#61507=CARTESIAN_POINT('Ctrl Pts',(16.5810623056489,-0.326762944709103,
3.54263728061361));
#61508=CARTESIAN_POINT('Ctrl Pts',(16.6287781417117,0.207971539662738,3.4777907336998));
#61509=CARTESIAN_POINT('Ctrl Pts',(16.6764939777746,0.551722559108811,3.89249699125187));
#61510=CARTESIAN_POINT('Ctrl Pts',(16.7242098138374,0.388818263182495,4.40592491588375));
#61511=CARTESIAN_POINT('Ctrl Pts',(16.7719256499003,-0.131143826562283,
4.54658574430191));
#61512=CARTESIAN_POINT('Ctrl Pts',(16.8196414859631,-0.53067452246778,4.18530847342493));
#61513=CARTESIAN_POINT('Ctrl Pts',(16.8673573220259,-0.442878638914007,
3.65385958006445));
#61514=CARTESIAN_POINT('Ctrl Pts',(16.9150731580888,0.0516195133182915,
3.44027676038576));
#61515=CARTESIAN_POINT('Ctrl Pts',(16.9627889941516,0.498714672202087,3.74069640409388));
#61516=CARTESIAN_POINT('Ctrl Pts',(17.0105048302145,0.487832473891125,4.27923852982128));
#61517=CARTESIAN_POINT('Ctrl Pts',(17.0582206662773,0.0289662085384809,
4.56135161697672));
#61518=CARTESIAN_POINT('Ctrl Pts',(17.1059365023401,-0.456500171817451,
4.32796687675757));
#61519=CARTESIAN_POINT('Ctrl Pts',(17.1536523384029,-0.522755420235406,
3.79340510719289));
#61520=CARTESIAN_POINT('Ctrl Pts',(17.2013681744658,-0.108956322625149,
3.44856260656401));
#61521=CARTESIAN_POINT('Ctrl Pts',(17.2490840105286,0.404899042560309,3.61011354928233));
#61522=CARTESIAN_POINT('Ctrl Pts',(17.2967998465915,0.54692938679005,4.12970321886885));
#61523=CARTESIAN_POINT('Ctrl Pts',(17.3445156826543,0.186706059540143,4.53018442682757));
#61524=CARTESIAN_POINT('Ctrl Pts',(17.3922315187172,-0.344972315027459,
4.4437891176945));
#61525=CARTESIAN_POINT('Ctrl Pts',(17.43994735478,-0.559857304624004,3.94985543320929));
#61526=CARTESIAN_POINT('Ctrl Pts',(17.4876631908428,-0.260616716872392,
3.5019702759813));
#61527=CARTESIAN_POINT('Ctrl Pts',(17.5353790269057,0.277952212086773,3.51143347749201));
#61528=CARTESIAN_POINT('Ctrl Pts',(17.5830948629685,0.561273347842132,3.96955483418404));
#61529=CARTESIAN_POINT('Ctrl Pts',(17.6308106990313,0.329168531973526,4.45563445510394));
#61530=CARTESIAN_POINT('Ctrl Pts',(17.6785265350942,-0.205216811715269,
4.52329794506467));
#61531=CARTESIAN_POINT('Ctrl Pts',(17.726242371157,-0.551148399539408,4.11040888009862));
#61532=CARTESIAN_POINT('Ctrl Pts',(17.7739582072198,-0.390951931558304,
3.59612964167903));
#61533=CARTESIAN_POINT('Ctrl Pts',(17.8216740432827,0.128261710741471,3.45273076764982));
#61534=CARTESIAN_POINT('Ctrl Pts',(17.8693898793456,0.529690650507269,3.81189765050732));
#61535=CARTESIAN_POINT('Ctrl Pts',(17.9171057154083,0.44469651557395,4.34380181523062));
#61536=CARTESIAN_POINT('Ctrl Pts',(17.9648215514712,-0.0486692721463468,
4.55998748295674));
#61537=CARTESIAN_POINT('Ctrl Pts',(18.012537387534,-0.497341318381634,4.26192802856871));
#61538=CARTESIAN_POINT('Ctrl Pts',(18.0602532235969,-0.489297179367249,
3.72333603526529));
#61539=CARTESIAN_POINT('Ctrl Pts',(18.1079690596597,-0.0319239117350811,
3.43880881780002));
#61540=CARTESIAN_POINT('Ctrl Pts',(18.1556848957225,0.454765575255941,3.66963209798526));
#61541=CARTESIAN_POINT('Ctrl Pts',(18.2034007317854,0.523836837021606,4.20383730595423));
#61542=CARTESIAN_POINT('Ctrl Pts',(18.2511165678483,0.111860671084556,4.5508555794253));
#61543=CARTESIAN_POINT('Ctrl Pts',(18.298832403911,-0.402838870307115,4.39201469830757));
#61544=CARTESIAN_POINT('Ctrl Pts',(18.346548239974,-0.547605278623001,3.87318068781251));
#61545=CARTESIAN_POINT('Ctrl Pts',(18.3942640760367,-0.189497333589109,
3.47080680306518));
#61546=CARTESIAN_POINT('Ctrl Pts',(18.4419799120997,0.342628928670919,3.55439917374707));
#61547=CARTESIAN_POINT('Ctrl Pts',(18.4896957481624,0.560113773708727,4.04719363962704));
#61548=CARTESIAN_POINT('Ctrl Pts',(18.5374115842253,0.263237521891608,4.49664946007004));
#61549=CARTESIAN_POINT('Ctrl Pts',(18.5851274202881,-0.275373796708506,
4.49002443939646));
#61550=CARTESIAN_POINT('Ctrl Pts',(18.632843256351,-0.561105120620647,4.03340243603));
#61551=CARTESIAN_POINT('Ctrl Pts',(18.6805590924138,-0.331564978554912,
3.54610646169455));
#61552=CARTESIAN_POINT('Ctrl Pts',(18.7282749284766,0.202456385100939,3.47562790763498));
#61553=CARTESIAN_POINT('Ctrl Pts',(18.7759907645394,0.550558935126376,3.8866883144956));
#61554=CARTESIAN_POINT('Ctrl Pts',(18.8237066006023,0.393074743587739,4.40180458567998));
#61555=CARTESIAN_POINT('Ctrl Pts',(18.8714224366651,-0.125376033221007,
4.54793752327491));
#61556=CARTESIAN_POINT('Ctrl Pts',(18.919138272728,-0.528692069562509,4.19089100214638));
#61557=CARTESIAN_POINT('Ctrl Pts',(18.9668541087908,-0.4465020434557,3.6585463365067));
#61558=CARTESIAN_POINT('Ctrl Pts',(19.0145699448537,0.0457176794812401,
3.43976382400136));
#61559=CARTESIAN_POINT('Ctrl Pts',(19.0622857809165,0.495954153879041,3.73545481224116));
#61560=CARTESIAN_POINT('Ctrl Pts',(19.1100016169793,0.490748297561716,4.27408171698104));
#61561=CARTESIAN_POINT('Ctrl Pts',(19.1577174530421,0.0348807284082936,
4.5610151636709));
#61562=CARTESIAN_POINT('Ctrl Pts',(19.205433289105,-0.453018350253257,4.33275975334162));
#61563=CARTESIAN_POINT('Ctrl Pts',(19.2531491251678,-0.524903707479367,
3.79892594114836));
#61564=CARTESIAN_POINT('Ctrl Pts',(19.3008649612307,-0.11476191309534,3.44974153150476));
#61565=CARTESIAN_POINT('Ctrl Pts',(19.3485807972935,0.400767511262006,3.60586793956989));
#61566=CARTESIAN_POINT('Ctrl Pts',(19.3962966333564,0.548265964675035,4.12393188459875));
#61567=CARTESIAN_POINT('Ctrl Pts',(19.4440124694192,0.192283344213529,4.52818727047755));
#61568=CARTESIAN_POINT('Ctrl Pts',(19.491728305482,-0.340276025447905,4.44740016355363));
#61569=CARTESIAN_POINT('Ctrl Pts',(19.5394441415448,-0.560354693525076,
3.95575859308266));
#61570=CARTESIAN_POINT('Ctrl Pts',(19.5871599776077,-0.265851008504119,
3.50474460473346));
#61571=CARTESIAN_POINT('Ctrl Pts',(19.6348758136705,0.272787718306182,3.5085312334714));
#61572=CARTESIAN_POINT('Ctrl Pts',(19.6825916497334,0.560921342594646,3.96364125479661));
#61573=CARTESIAN_POINT('Ctrl Pts',(19.7303074857962,0.33395216026474,4.45213995410186));
#61574=CARTESIAN_POINT('Ctrl Pts',(19.7780233218591,-0.199690227635008,
4.52543179776919));
#61575=CARTESIAN_POINT('Ctrl Pts',(19.8257391579219,-0.549954387748789,
4.11621111891367));
#61576=CARTESIAN_POINT('Ctrl Pts',(19.8734549939848,-0.395186252277308,
3.60027277035845));
#61577=CARTESIAN_POINT('Ctrl Pts',(19.9211708300475,0.122486141425193,3.45140859770427));
#61578=CARTESIAN_POINT('Ctrl Pts',(19.9688866661104,0.527680190865048,3.80632716374734));
#61579=CARTESIAN_POINT('Ctrl Pts',(20.0166025021732,0.448292560087992,4.33909316421112));
#61580=CARTESIAN_POINT('Ctrl Pts',(20.0643183382361,-0.0427598846646947,
4.56047472290141));
#61581=CARTESIAN_POINT('Ctrl Pts',(20.1120341742989,-0.49456253103916,4.26714478353561));
#61582=CARTESIAN_POINT('Ctrl Pts',(20.1597500103618,-0.492168201513856,
3.72852743457374));
#61583=CARTESIAN_POINT('Ctrl Pts',(20.2074658464246,-0.0378697858522375,
3.43914000028616));
#61584=CARTESIAN_POINT('Ctrl Pts',(20.2551816824874,0.451321269441671,3.66492646727415));
#61585=CARTESIAN_POINT('Ctrl Pts',(20.3028975185503,0.52583741886325,4.1981749506787));
#61586=CARTESIAN_POINT('Ctrl Pts',(20.3506133546131,0.117885080656874,4.54989459844945));
#61587=CARTESIAN_POINT('Ctrl Pts',(20.398329190676,-0.399119892637424,4.39574851066478));
#61588=CARTESIAN_POINT('Ctrl Pts',(20.438092387395,-0.523197416260526,3.96600412247733));
#61589=CARTESIAN_POINT('Ctrl Pts',(20.4699029447702,-0.3725623900923,3.67462118354637));
#61590=CARTESIAN_POINT('Ctrl Pts',(20.4937608628016,-0.172533290246804,
3.53519650363565));
#61591=CARTESIAN_POINT('Ctrl Pts',(20.5176187808331,0.0720421502968434,
3.50974356844941));
#61592=CARTESIAN_POINT('Ctrl Pts',(20.5414766988645,0.297725647320748,3.60399556061657));
#61593=CARTESIAN_POINT('Ctrl Pts',(20.5653346168959,0.451286063531533,3.79517586539437));
#61594=CARTESIAN_POINT('Ctrl Pts',(20.5891925349273,0.494134760388362,4.03639109206021));
#61595=CARTESIAN_POINT('Ctrl Pts',(20.6130504529587,0.416344747430809,4.26873428690612));
#61596=CARTESIAN_POINT('Ctrl Pts',(20.6369083709901,0.23664610161733,4.43535054865035));
#61597=CARTESIAN_POINT('Ctrl Pts',(20.6607662890216,-0.000865470816140784,
4.49551919950567));
#61598=CARTESIAN_POINT('Ctrl Pts',(20.684624207053,-0.238193741375527,4.43451595913869));
#61599=CARTESIAN_POINT('Ctrl Pts',(20.7084821250844,-0.417262150572256,
4.26726382233879));
#61600=CARTESIAN_POINT('Ctrl Pts',(20.7323400431158,-0.494306543785295,
4.03465729316116));
#61601=CARTESIAN_POINT('Ctrl Pts',(20.7561979611472,-0.45047531426282,3.79357669839993));
#61602=CARTESIAN_POINT('Ctrl Pts',(20.7800558791787,-0.296492828349621,
3.60297191305088));
#61603=CARTESIAN_POINT('Ctrl Pts',(20.80391379721,-0.0700085893017688,3.50945147432983));
#61604=CARTESIAN_POINT('Ctrl Pts',(20.8277717152415,0.173594031734132,3.53588342526713));
#61605=CARTESIAN_POINT('Ctrl Pts',(20.8516296332729,0.374748514455718,3.6758045671588));
#61606=CARTESIAN_POINT('Ctrl Pts',(20.8754875513043,0.484266602122282,3.89500029884494));
#61607=CARTESIAN_POINT('Ctrl Pts',(20.8993454693358,0.475368407265908,4.13987133054223));
#61608=CARTESIAN_POINT('Ctrl Pts',(20.9232033873671,0.350229638882089,4.35054000504804));
#61609=CARTESIAN_POINT('Ctrl Pts',(20.9470613053986,0.139450209771325,4.47549210343221));
#61610=CARTESIAN_POINT('Ctrl Pts',(20.97091922343,-0.105428607968738,4.48417342845956));
#61611=CARTESIAN_POINT('Ctrl Pts',(20.9947771414615,-0.324527251938122,
4.37446116262749));
#61612=CARTESIAN_POINT('Ctrl Pts',(21.0186350594928,-0.464270146732381,
4.17318294187641));
#61613=CARTESIAN_POINT('Ctrl Pts',(21.0424929775243,-0.490486342136868,
3.92955677471355));
#61614=CARTESIAN_POINT('Ctrl Pts',(21.0663508955557,-0.396765267394252,
3.7031558948169));
#61615=CARTESIAN_POINT('Ctrl Pts',(21.0902088135871,-0.206024276530194,
3.54934148458869));
#61616=CARTESIAN_POINT('Ctrl Pts',(21.1140667316185,0.0350952616297792,
3.50572535702762));
#61617=CARTESIAN_POINT('Ctrl Pts',(21.1379246496499,0.267633052506714,3.58297284346672));
#61618=CARTESIAN_POINT('Ctrl Pts',(21.1617825676814,0.434727271782411,3.76219482925797));
#61619=CARTESIAN_POINT('Ctrl Pts',(21.1856404857128,0.495518831419392,3.99956665698474));
#61620=CARTESIAN_POINT('Ctrl Pts',(21.2094984037442,0.43514253908843,4.23704444887943));
#61621=CARTESIAN_POINT('Ctrl Pts',(21.2333563217756,0.268362042918248,4.41655841606373));
#61622=CARTESIAN_POINT('Ctrl Pts',(21.257214239807,0.0359597172125542,4.49421250369607));
#61623=CARTESIAN_POINT('Ctrl Pts',(21.2810721578384,-0.205235738871087,
4.45101817209691));
#61624=CARTESIAN_POINT('Ctrl Pts',(21.3049300758699,-0.396245466293343,
4.29753761193144));
#61625=CARTESIAN_POINT('Ctrl Pts',(21.3287879939013,-0.490362383696085,
4.07130100088706));
#61626=CARTESIAN_POINT('Ctrl Pts',(21.3526459119327,-0.464572341082516,
3.82762935292545));
#61627=CARTESIAN_POINT('Ctrl Pts',(21.3765038299641,-0.325181706377507,
3.62610702345576));
#61628=CARTESIAN_POINT('Ctrl Pts',(21.4003617479955,-0.106275286691508,
3.51601171139131));
#61629=CARTESIAN_POINT('Ctrl Pts',(21.424219666027,0.138618335471326,3.52426471946798));
#61630=CARTESIAN_POINT('Ctrl Pts',(21.4480775840584,0.349615998723735,3.64884796240357));
#61631=CARTESIAN_POINT('Ctrl Pts',(21.4719355020898,0.475123026939619,3.85929744372095));
#61632=CARTESIAN_POINT('Ctrl Pts',(21.4957934201212,0.484449532977353,4.10415253270923));
#61633=CARTESIAN_POINT('Ctrl Pts',(21.5196513381527,0.375314932061802,4.32353949039209));
#61634=CARTESIAN_POINT('Ctrl Pts',(21.543509256184,0.174405606883644,4.4638122296353));
#61635=CARTESIAN_POINT('Ctrl Pts',(21.5673671742155,-0.069150639890911,
4.49067024474121));
#61636=CARTESIAN_POINT('Ctrl Pts',(21.5912250922469,-0.29579767158652,4.39754601941878));
#61637=CARTESIAN_POINT('Ctrl Pts',(21.6150830102783,-0.450114115212426,
4.20721096341231));
#61638=CARTESIAN_POINT('Ctrl Pts',(21.6389409283097,-0.494365396806572,
3.96620718253823));
#61639=CARTESIAN_POINT('Ctrl Pts',(21.6627988463412,-0.417730872638478,
3.73346666603139));
#61640=CARTESIAN_POINT('Ctrl Pts',(21.6866567643726,-0.238949771349764,
3.56590080990214));
#61641=CARTESIAN_POINT('Ctrl Pts',(21.710514682404,-0.00173894210493873,
3.50448403037633));
#61642=CARTESIAN_POINT('Ctrl Pts',(21.7343726004354,0.235897105852373,3.56423440300754));
#61643=CARTESIAN_POINT('Ctrl Pts',(21.7582305184669,0.415849885720624,3.73054133411992));
#61644=CARTESIAN_POINT('Ctrl Pts',(21.7820884364982,0.49411604100673,3.96273824894669));
#61645=CARTESIAN_POINT('Ctrl Pts',(21.8059463545297,0.451557364815975,4.20404667689569));
#61646=CARTESIAN_POINT('Ctrl Pts',(21.8298042725611,0.29858061275206,4.39546013422383));
#61647=CARTESIAN_POINT('Ctrl Pts',(21.8536621905925,0.0725927676976751,
4.49017281661646));
#61648=CARTESIAN_POINT('Ctrl Pts',(21.8775201086239,-0.171145986446082,
4.46502489330693));
#61649=CARTESIAN_POINT('Ctrl Pts',(21.9013780266554,-0.373034884980705,
4.32616571656009));
#61650=CARTESIAN_POINT('Ctrl Pts',(21.9252359446868,-0.483706592871294,
4.10755013753858));
#61651=CARTESIAN_POINT('Ctrl Pts',(21.9490938627182,-0.476098862901817,
3.86263562028194));
#61652=CARTESIAN_POINT('Ctrl Pts',(21.9729517807496,-0.352071992280181,
3.65131043559696));
#61653=CARTESIAN_POINT('Ctrl Pts',(21.996809698781,-0.141953929297546,3.52524934752154));
#61654=CARTESIAN_POINT('Ctrl Pts',(22.0206676168125,0.102875736145779,3.51527772592526));
#61655=CARTESIAN_POINT('Ctrl Pts',(22.0445255348438,0.322549481822576,3.62383390390986));
#61656=CARTESIAN_POINT('Ctrl Pts',(22.0683834528753,0.46335109312246,3.82437293894729));
#61657=CARTESIAN_POINT('Ctrl Pts',(22.0922413709067,0.490850740723195,4.06785757439707));
#61658=CARTESIAN_POINT('Ctrl Pts',(22.1160992889381,0.398324011712033,4.29474918450382));
#61659=CARTESIAN_POINT('Ctrl Pts',(22.1399572069695,0.208396211707814,4.44956659019228));
#61660=CARTESIAN_POINT('Ctrl Pts',(22.163815125001,-0.0324901386554863,
4.49445271863166));
#61661=CARTESIAN_POINT('Ctrl Pts',(22.1876730430324,-0.265431765108271,
4.41843168874211));
#61662=CARTESIAN_POINT('Ctrl Pts',(22.2115309610638,-0.433468094767725,
4.24009271310828));
#61663=CARTESIAN_POINT('Ctrl Pts',(22.2353888790952,-0.495509667838209,
4.00304452911861));
#61664=CARTESIAN_POINT('Ctrl Pts',(22.2592467971266,-0.436385629680506,
3.76525187484075));
#61665=CARTESIAN_POINT('Ctrl Pts',(22.2831047151581,-0.270553418215538,
3.58486153155103));
#61666=CARTESIAN_POINT('Ctrl Pts',(22.3069626331895,-0.0385635261649252,
3.50598385198694));
#61667=CARTESIAN_POINT('Ctrl Pts',(22.3308205512209,0.202856198284482,3.54790657725669));
#61668=CARTESIAN_POINT('Ctrl Pts',(22.3546784692523,0.394672056935096,3.70037845932536));
#61669=CARTESIAN_POINT('Ctrl Pts',(22.3785363872837,0.489979846308564,3.9261159693126));
#61670=CARTESIAN_POINT('Ctrl Pts',(22.4023943053151,0.465474217808745,4.1699201379362));
#61671=CARTESIAN_POINT('Ctrl Pts',(22.4262522233466,0.327147461276091,4.37217420322137));
#61672=CARTESIAN_POINT('Ctrl Pts',(22.450110141378,0.108824243893236,4.4834215400391));
#61673=CARTESIAN_POINT('Ctrl Pts',(22.4739680594094,-0.136109474402841,
4.47645913832327));
#61674=CARTESIAN_POINT('Ctrl Pts',(22.4978259774408,-0.347760701725541,
4.3529895060813));
#61675=CARTESIAN_POINT('Ctrl Pts',(22.5216838954723,-0.474374996640319,
4.1432043106148));
#61676=CARTESIAN_POINT('Ctrl Pts',(22.5455418135036,-0.484991622785221,
3.89840178635216));
#61677=CARTESIAN_POINT('Ctrl Pts',(22.5693997315351,-0.377014700254462,
3.67844274379546));
#61678=CARTESIAN_POINT('Ctrl Pts',(22.5932576495665,-0.176847198578467,
3.53711330196678));
#61679=CARTESIAN_POINT('Ctrl Pts',(22.6171155675979,0.0665638539184235,
3.50897209184919));
#61680=CARTESIAN_POINT('Ctrl Pts',(22.6409734856293,0.293698998435555,3.60090091054846));
#61681=CARTESIAN_POINT('Ctrl Pts',(22.6648314036608,0.449015288492166,3.79041970485759));
#61682=CARTESIAN_POINT('Ctrl Pts',(22.6886893216922,0.494537845944295,4.03118776656693));
#61683=CARTESIAN_POINT('Ctrl Pts',(22.7125472397236,0.419127261608858,4.26432734830583));
#61684=CARTESIAN_POINT('Ctrl Pts',(22.736405157755,0.241238408088568,4.43283588997321));
#61685=CARTESIAN_POINT('Ctrl Pts',(22.7602630757865,0.00434171083240793,
4.49549632518638));
#61686=CARTESIAN_POINT('Ctrl Pts',(22.7841209938178,-0.233581370990537,
4.43700954435219));
#61687=CARTESIAN_POINT('Ctrl Pts',(22.8079789118493,-0.414457183229959,
4.27163232278894));
#61688=CARTESIAN_POINT('Ctrl Pts',(22.8238841905369,-0.46737397936094,4.11714349286348));
#61689=CARTESIAN_POINT('Ctrl Pts',(22.8318368298807,-0.473742730682552,
4.03823705100924));
#61690=CARTESIAN_POINT('Ctrl Pts',(4.,-0.219892372743211,3.64701365460636));
#61691=CARTESIAN_POINT('Ctrl Pts',(4.00795263934381,-0.161099076858729,
3.61038844940468));
#61692=CARTESIAN_POINT('Ctrl Pts',(4.02385791803142,-0.0249198690254346,
3.56711791692558));
#61693=CARTESIAN_POINT('Ctrl Pts',(4.04771583606284,0.185569069288609,3.60813812632505));
#61694=CARTESIAN_POINT('Ctrl Pts',(4.07157375409426,0.350624105231944,3.74494568050885));
#61695=CARTESIAN_POINT('Ctrl Pts',(4.09543167212568,0.429971014252744,3.94413788601839));
#61696=CARTESIAN_POINT('Ctrl Pts',(4.1192895901571,0.40416308778273,4.15698104289539));
#61697=CARTESIAN_POINT('Ctrl Pts',(4.14314750818851,0.279534313346206,4.3314427366163));
#61698=CARTESIAN_POINT('Ctrl Pts',(4.16700542621994,0.0865475313004802,
4.42485517705098));
#61699=CARTESIAN_POINT('Ctrl Pts',(4.19086334425134,-0.127600227202394,
4.41438026490915));
#61700=CARTESIAN_POINT('Ctrl Pts',(4.21472126228278,-0.310547447266788,
4.30257739619942));
#61701=CARTESIAN_POINT('Ctrl Pts',(4.23857918031418,-0.417556725585918,
4.11678647978038));
#61702=CARTESIAN_POINT('Ctrl Pts',(4.26243709834561,-0.422462345057068,
3.90243789311793));
#61703=CARTESIAN_POINT('Ctrl Pts',(4.28629501637703,-0.324064236326554,
3.71194600226016));
#61704=CARTESIAN_POINT('Ctrl Pts',(4.31015293440845,-0.146423688323203,
3.59189110566319));
#61705=CARTESIAN_POINT('Ctrl Pts',(4.33401085243986,0.0670214896752265,
3.5716299793216));
#61706=CARTESIAN_POINT('Ctrl Pts',(4.35786877047129,0.264078061498623,3.65611697628114));
#61707=CARTESIAN_POINT('Ctrl Pts',(4.38172668850271,0.396560367883193,3.82469274783887));
#61708=CARTESIAN_POINT('Ctrl Pts',(4.40558460653412,0.432072854850341,4.03613591352675));
#61709=CARTESIAN_POINT('Ctrl Pts',(4.42944252456555,0.361931763288092,4.23874286631049));
#61710=CARTESIAN_POINT('Ctrl Pts',(4.45330044259696,0.203288494707987,4.382970683851));
#61711=CARTESIAN_POINT('Ctrl Pts',(4.47715836062838,-0.00506434719902249,
4.43355173791626));
#61712=CARTESIAN_POINT('Ctrl Pts',(4.5010162786598,-0.212178818846594,4.37811758201071));
#61713=CARTESIAN_POINT('Ctrl Pts',(4.52487419669122,-0.367409789343613,
4.23022337776645));
#61714=CARTESIAN_POINT('Ctrl Pts',(4.54873211472264,-0.432799058467291,
4.02603328640456));
#61715=CARTESIAN_POINT('Ctrl Pts',(4.57259003275406,-0.392357168499796,
3.8154773474345));
#61716=CARTESIAN_POINT('Ctrl Pts',(4.59644795078547,-0.255973263285106,
3.65004222328625));
#61717=CARTESIAN_POINT('Ctrl Pts',(4.6203058688169,-0.0569969226013119,
3.57018130821703));
#61718=CARTESIAN_POINT('Ctrl Pts',(4.64416378684831,0.155916718210686,3.59542277130738));
#61719=CARTESIAN_POINT('Ctrl Pts',(4.66802170487973,0.330704474340828,3.71959438727947));
#61720=CARTESIAN_POINT('Ctrl Pts',(4.69187962291115,0.424625978282027,3.91233281365517));
#61721=CARTESIAN_POINT('Ctrl Pts',(4.71573754094257,0.41471486395576,4.1265082550995));
#61722=CARTESIAN_POINT('Ctrl Pts',(4.73959545897399,0.303394668785218,4.30974898215573));
#61723=CARTESIAN_POINT('Ctrl Pts',(4.76345337700541,0.117886212792376,4.41724764568232));
#61724=CARTESIAN_POINT('Ctrl Pts',(4.78731129503683,-0.0964486333844469,
4.42271789424177));
#61725=CARTESIAN_POINT('Ctrl Pts',(4.81116921306824,-0.287199161490599,
4.32482210305491));
#61726=CARTESIAN_POINT('Ctrl Pts',(4.83502713109967,-0.407721671464292,
4.14749845969467));
#61727=CARTESIAN_POINT('Ctrl Pts',(4.85888504913109,-0.42854512664958,3.93410742516172));
#61728=CARTESIAN_POINT('Ctrl Pts',(4.8827429671625,-0.344577625034195,3.73682892005441));
#61729=CARTESIAN_POINT('Ctrl Pts',(4.90660088519393,-0.176351507991885,
3.60390291263011));
#61730=CARTESIAN_POINT('Ctrl Pts',(4.93045880322534,0.0349973564730633,
3.56783343253575));
#61731=CARTESIAN_POINT('Ctrl Pts',(4.95431672125677,0.237788413971502,3.63744045016736));
#61732=CARTESIAN_POINT('Ctrl Pts',(4.97817463928818,0.382433727027559,3.79570315365689));
#61733=CARTESIAN_POINT('Ctrl Pts',(5.0020325573196,0.433563576539811,4.00392200101168));
#61734=CARTESIAN_POINT('Ctrl Pts',(5.02589047535102,0.378675321553375,4.21118181228595));
#61735=CARTESIAN_POINT('Ctrl Pts',(5.04974839338244,0.231190635538481,4.36680191797922));
#61736=CARTESIAN_POINT('Ctrl Pts',(5.07360631141386,0.0271735416279573,
4.43272896324296));
#61737=CARTESIAN_POINT('Ctrl Pts',(5.09746422944527,-0.183488223403015,
4.39284198969348));
#61738=CARTESIAN_POINT('Ctrl Pts',(5.1213221474767,-0.349282119693095,4.256894448863));
#61739=CARTESIAN_POINT('Ctrl Pts',(5.1451800655081,-0.4296670234643,4.05812921762123));
#61740=CARTESIAN_POINT('Ctrl Pts',(5.16903798353954,-0.404986636103755,
3.84514980926298));
#61741=CARTESIAN_POINT('Ctrl Pts',(5.19289590157095,-0.281275984601366,
3.67003549057442));
#61742=CARTESIAN_POINT('Ctrl Pts',(5.21675381960238,-0.0887856930599551,
3.5756064824932));
#61743=CARTESIAN_POINT('Ctrl Pts',(5.24061173763379,0.125415118908336,3.58495324968971));
#61744=CARTESIAN_POINT('Ctrl Pts',(5.26446965566521,0.308948518064291,3.69579025298356));
#61745=CARTESIAN_POINT('Ctrl Pts',(5.28832757369662,0.416935588964862,3.88101482593007));
#61746=CARTESIAN_POINT('Ctrl Pts',(5.31218549172805,0.422970551266107,4.09533451502773));
#61747=CARTESIAN_POINT('Ctrl Pts',(5.33604340975946,0.325577692296299,4.28634231834109));
#61748=CARTESIAN_POINT('Ctrl Pts',(5.35990132779089,0.148572219001774,4.40733162501188));
#61749=CARTESIAN_POINT('Ctrl Pts',(5.3837592458223,-0.0647632088646815,
4.42871725387658));
#61750=CARTESIAN_POINT('Ctrl Pts',(5.40761716385372,-0.26226226804932,4.34526983614494));
#61751=CARTESIAN_POINT('Ctrl Pts',(5.43147508188515,-0.395631058815178,
4.17739453851434));
#61752=CARTESIAN_POINT('Ctrl Pts',(5.45533299991656,-0.432257278927009,
3.96614144408682));
#61753=CARTESIAN_POINT('Ctrl Pts',(5.47919091794798,-0.363184819889405,
3.76316768886851));
#61754=CARTESIAN_POINT('Ctrl Pts',(5.5030488359794,-0.205303779432806,3.61810588490468));
#61755=CARTESIAN_POINT('Ctrl Pts',(5.52690675401082,0.00277962745745752,
3.56642759466814));
#61756=CARTESIAN_POINT('Ctrl Pts',(5.55076467204224,0.210183339719457,3.62076956781107));
#61757=CARTESIAN_POINT('Ctrl Pts',(5.57462259007365,0.36619150013966,3.76784371165257));
#61758=CARTESIAN_POINT('Ctrl Pts',(5.59848050810508,0.432655863921731,3.97168639180759));
#61759=CARTESIAN_POINT('Ctrl Pts',(5.62233842613649,0.393324083661671,4.18245252040861));
#61760=CARTESIAN_POINT('Ctrl Pts',(5.64619634416792,0.257813851021257,4.34860403787086));
#61761=CARTESIAN_POINT('Ctrl Pts',(5.67005426219933,0.0592611090830247,
4.42951237227525));
#61762=CARTESIAN_POINT('Ctrl Pts',(5.69391218023075,-0.153782588238227,
4.40539323200473));
#61763=CARTESIAN_POINT('Ctrl Pts',(5.71777009826218,-0.329222253834466,
4.28214440376531));
#61764=CARTESIAN_POINT('Ctrl Pts',(5.74162801629359,-0.424158110434281,
4.08990358344764));
#61765=CARTESIAN_POINT('Ctrl Pts',(5.76548593432501,-0.415375755386326,
3.8756788878607));
#61766=CARTESIAN_POINT('Ctrl Pts',(5.78934385235642,-0.305022713182347,
3.69185409099321));
#61767=CARTESIAN_POINT('Ctrl Pts',(5.81320177038785,-0.120083309624962,
3.58337936191985));
#61768=CARTESIAN_POINT('Ctrl Pts',(5.83705968841926,0.0942197354074567,
3.57677972866706));
#61769=CARTESIAN_POINT('Ctrl Pts',(5.86091760645069,0.285483486244351,3.673668977605));
#61770=CARTESIAN_POINT('Ctrl Pts',(5.8847755244821,0.406938752801468,3.85035505520226));
#61771=CARTESIAN_POINT('Ctrl Pts',(5.90863344251353,0.428886400972996,4.06363338935351));
#61772=CARTESIAN_POINT('Ctrl Pts',(5.93249136054494,0.345959657594393,4.261351642888));
#61773=CARTESIAN_POINT('Ctrl Pts',(5.95634927857636,0.178436323746589,4.39516226965834));
#61774=CARTESIAN_POINT('Ctrl Pts',(5.98020719660778,-0.0327194942966983,
4.4323450160316));
#61775=CARTESIAN_POINT('Ctrl Pts',(6.0040651146392,-0.23587461323539,4.36380751861078));
#61776=CARTESIAN_POINT('Ctrl Pts',(6.02792303267061,-0.381351759249696,
4.20630938167977));
#61777=CARTESIAN_POINT('Ctrl Pts',(6.05178095070204,-0.433578399193506,
3.9983625870902));
#61778=CARTESIAN_POINT('Ctrl Pts',(6.07563886873346,-0.379782579589031,
3.79081692866841));
#61779=CARTESIAN_POINT('Ctrl Pts',(6.09949678676487,-0.233120953551068,
3.63442082419035));
#61780=CARTESIAN_POINT('Ctrl Pts',(6.12335470479629,-0.0294522997972467,
3.5674214393556));
#61781=CARTESIAN_POINT('Ctrl Pts',(6.14721262282771,0.181413325723775,3.60619428643423));
#61782=CARTESIAN_POINT('Ctrl Pts',(6.17107054085913,0.347927737305898,3.74127281623538));
#61783=CARTESIAN_POINT('Ctrl Pts',(6.19492845889055,0.429346806292137,3.93959933010928));
#61784=CARTESIAN_POINT('Ctrl Pts',(6.21878637692197,0.405811992579865,4.15272917617017));
#61785=CARTESIAN_POINT('Ctrl Pts',(6.24264429495339,0.282982581651336,4.32844890303245));
#61786=CARTESIAN_POINT('Ctrl Pts',(6.26650221298481,0.0910742457207041,
4.42397415233781));
#61787=CARTESIAN_POINT('Ctrl Pts',(6.29036013101623,-0.123327005978964,
4.41559921078967));
#61788=CARTESIAN_POINT('Ctrl Pts',(6.31421804904765,-0.307151379675736,
4.3060270879454));
#61789=CARTESIAN_POINT('Ctrl Pts',(6.33807596707907,-0.416657206472865,
4.12081787696614));
#61790=CARTESIAN_POINT('Ctrl Pts',(6.36193388511048,-0.422829889105799,
3.9075587958503));
#61791=CARTESIAN_POINT('Ctrl Pts',(6.39374444248571,-0.296437506874183,
3.64987069373525));
#61792=CARTESIAN_POINT('Ctrl Pts',(6.43350763920474,0.0703302468340302,
3.51324810367198));
#61793=CARTESIAN_POINT('Ctrl Pts',(6.48122347526758,0.448014600657906,3.7964368525222));
#61794=CARTESIAN_POINT('Ctrl Pts',(6.52893931133042,0.413240052911115,4.26646358767058));
#61795=CARTESIAN_POINT('Ctrl Pts',(6.57665514739325,-0.000480251589724132,
4.49184654025612));
#61796=CARTESIAN_POINT('Ctrl Pts',(6.62437098345609,-0.41404349770976,4.26553045144514));
#61797=CARTESIAN_POINT('Ctrl Pts',(6.67208681951894,-0.447234019333667,
3.79538894860702));
#61798=CARTESIAN_POINT('Ctrl Pts',(6.71980265558177,-0.0698021891909718,
3.51313682319347));
#61799=CARTESIAN_POINT('Ctrl Pts',(6.76751849164461,0.371772181936036,3.67798293440124));
#61800=CARTESIAN_POINT('Ctrl Pts',(6.81523432770745,0.471920133146607,4.13853999974893));
#61801=CARTESIAN_POINT('Ctrl Pts',(6.86295016377028,0.138708377331583,4.4718748549198));
#61802=CARTESIAN_POINT('Ctrl Pts',(6.91066599983312,-0.32188767172048,4.37187913281409));
#61803=CARTESIAN_POINT('Ctrl Pts',(6.95838183589596,-0.486886005735063,
3.93038141845316));
#61804=CARTESIAN_POINT('Ctrl Pts',(7.0060976719588,-0.204771183672361,3.55281534000283));
#61805=CARTESIAN_POINT('Ctrl Pts',(7.05381350802163,0.265389096458903,3.58590591031157));
#61806=CARTESIAN_POINT('Ctrl Pts',(7.10152934408448,0.491837993618785,3.99926540470374));
#61807=CARTESIAN_POINT('Ctrl Pts',(7.14924518014731,0.266624753986561,4.41329951581085));
#61808=CARTESIAN_POINT('Ctrl Pts',(7.19696101621015,-0.203434237821079,
4.44779430805676));
#61809=CARTESIAN_POINT('Ctrl Pts',(7.24467685227299,-0.486676365692783,
4.07107270446015));
#61810=CARTESIAN_POINT('Ctrl Pts',(7.29239268833582,-0.322996137187983,
3.62908393881966));
#61811=CARTESIAN_POINT('Ctrl Pts',(7.34010852439867,0.137296434535941,3.52771310152703));
#61812=CARTESIAN_POINT('Ctrl Pts',(7.3878243604615,0.471507566988788,3.86005058906394));
#61813=CARTESIAN_POINT('Ctrl Pts',(7.43554019652434,0.372726051350611,4.32090577464778));
#61814=CARTESIAN_POINT('Ctrl Pts',(7.48325603258718,-0.0683355354161961,
4.48706824929225));
#61815=CARTESIAN_POINT('Ctrl Pts',(7.53097186865002,-0.44664354691983,4.20594845626764));
#61816=CARTESIAN_POINT('Ctrl Pts',(7.57868770471286,-0.414791917646955,
3.73570302684109));
#61817=CARTESIAN_POINT('Ctrl Pts',(7.62640354077569,-0.00203048755240202,
3.50816557464413));
#61818=CARTESIAN_POINT('Ctrl Pts',(7.67411937683853,0.412595570264971,3.73228724307244));
#61819=CARTESIAN_POINT('Ctrl Pts',(7.72183521290137,0.448328767436039,4.20225365549051));
#61820=CARTESIAN_POINT('Ctrl Pts',(7.7695510489642,0.0723547589785895,4.48648742399228));
#61821=CARTESIAN_POINT('Ctrl Pts',(7.81726688502705,-0.370063737934377,
4.32397230547438));
#61822=CARTESIAN_POINT('Ctrl Pts',(7.86498272108989,-0.472647010158531,
3.86394843388276));
#61823=CARTESIAN_POINT('Ctrl Pts',(7.91269855715272,-0.141191260335066,
3.52886280888004));
#61824=CARTESIAN_POINT('Ctrl Pts',(7.96041439321556,0.31992259635559,3.62642971585976));
#61825=CARTESIAN_POINT('Ctrl Pts',(8.0081302292784,0.48724661017382,4.0670519628834));
#61826=CARTESIAN_POINT('Ctrl Pts',(8.05584606534124,0.207124564615173,4.44609936066402));
#61827=CARTESIAN_POINT('Ctrl Pts',(8.10356190140407,-0.263203155649882,
4.41548685142597));
#61828=CARTESIAN_POINT('Ctrl Pts',(8.15127773746691,-0.491827368180951,
4.00332637343646));
#61829=CARTESIAN_POINT('Ctrl Pts',(8.19899357352975,-0.268798940774433,
3.58811123553743));
#61830=CARTESIAN_POINT('Ctrl Pts',(8.24670940959259,0.201071689948468,3.55113988776764));
#61831=CARTESIAN_POINT('Ctrl Pts',(8.29442524565542,0.486295093906121,3.92636368766143));
#61832=CARTESIAN_POINT('Ctrl Pts',(8.34214108171827,0.324946230517931,4.36920884621601));
#61833=CARTESIAN_POINT('Ctrl Pts',(8.3898569177811,-0.134805756295296,4.47300384028212));
#61834=CARTESIAN_POINT('Ctrl Pts',(8.43757275384394,-0.470763542849379,
4.14243212971755));
#61835=CARTESIAN_POINT('Ctrl Pts',(8.48528858990678,-0.37441192437669,3.68106280283335));
#61836=CARTESIAN_POINT('Ctrl Pts',(8.53300442596962,0.0657679253190804,
3.51257841158684));
#61837=CARTESIAN_POINT('Ctrl Pts',(8.58072026203246,0.445552077224736,3.79170076492532));
#61838=CARTESIAN_POINT('Ctrl Pts',(8.62843609809529,0.41617890091499,4.26210751092856));
#61839=CARTESIAN_POINT('Ctrl Pts',(8.67615193415813,0.0046222361594965,
4.49181689660367));
#61840=CARTESIAN_POINT('Ctrl Pts',(8.72386777022097,-0.411179099183508,
4.26988325855195));
#61841=CARTESIAN_POINT('Ctrl Pts',(8.7715836062838,-0.449388340942622,3.80011167148426));
#61842=CARTESIAN_POINT('Ctrl Pts',(8.81929944234665,-0.0749173544856965,
3.51390061216986));
#61843=CARTESIAN_POINT('Ctrl Pts',(8.86701527840948,0.368351391347115,3.67408210030036));
#61844=CARTESIAN_POINT('Ctrl Pts',(8.91473111447233,0.473357386691186,4.13355901061654));
#61845=CARTESIAN_POINT('Ctrl Pts',(8.96244695053515,0.14367201029714,4.47038662641401));
#61846=CARTESIAN_POINT('Ctrl Pts',(9.01016278659801,-0.317949583830803,
4.37525096534692));
#61847=CARTESIAN_POINT('Ctrl Pts',(9.05787862266083,-0.487593182843731,
3.93551656882348));
#61848=CARTESIAN_POINT('Ctrl Pts',(9.10559445872368,-0.209472459465777,
3.55499829935456));
#61849=CARTESIAN_POINT('Ctrl Pts',(9.15331029478651,0.261010046587687,3.58313193881964));
#61850=CARTESIAN_POINT('Ctrl Pts',(9.20102613084934,0.491803010703882,3.99408193320625));
#61851=CARTESIAN_POINT('Ctrl Pts',(9.2487419669122,0.270965702728691,4.41046657939073));
#61852=CARTESIAN_POINT('Ctrl Pts',(9.29645780297501,-0.198703579405513,
4.44991344988054));
#61853=CARTESIAN_POINT('Ctrl Pts',(9.34417363903789,-0.485900307124067,
4.07619787653679));
#61854=CARTESIAN_POINT('Ctrl Pts',(9.39188947510068,-0.326887306273347,
3.63250862071426));
#61855=CARTESIAN_POINT('Ctrl Pts',(9.43960531116356,0.13231133773591,3.52629235307153));
#61856=CARTESIAN_POINT('Ctrl Pts',(9.48732114722637,0.470006444430667,3.85508910653225));
#61857=CARTESIAN_POINT('Ctrl Pts',(9.53503698328922,0.376087401226012,4.31695976320512));
#61858=CARTESIAN_POINT('Ctrl Pts',(9.58275281935206,-0.0631984893729827,
4.48776139227388));
#61859=CARTESIAN_POINT('Ctrl Pts',(9.63046865541489,-0.444448234747017,
4.21064422964382));
#61860=CARTESIAN_POINT('Ctrl Pts',(9.67818449147773,-0.41755432743774,3.74008922975375));
#61861=CARTESIAN_POINT('Ctrl Pts',(9.72590032754057,-0.00721385634321597,
3.50821428942208));
#61862=CARTESIAN_POINT('Ctrl Pts',(9.77361616360341,0.40975121003073,3.72795373420991));
#61863=CARTESIAN_POINT('Ctrl Pts',(9.82133199966624,0.450435435400681,4.19751745084266));
#61864=CARTESIAN_POINT('Ctrl Pts',(9.86904783572909,0.077477869602138,4.48569785316993));
#61865=CARTESIAN_POINT('Ctrl Pts',(9.91676367179192,-0.366628816002305,
4.3278544435092));
#61866=CARTESIAN_POINT('Ctrl Pts',(9.96447950785476,-0.474054618562381,
3.8689372536849));
#61867=CARTESIAN_POINT('Ctrl Pts',(10.0121953439176,-0.146148770628728,
3.53037700046135));
#61868=CARTESIAN_POINT('Ctrl Pts',(10.0599111799804,0.315967742161179,3.62307877379278));
#61869=CARTESIAN_POINT('Ctrl Pts',(10.1076270160433,0.487926215535836,4.06191310882887));
#61870=CARTESIAN_POINT('Ctrl Pts',(10.1553428521061,0.211814537474087,4.44389168337175));
#61871=CARTESIAN_POINT('Ctrl Pts',(10.203058688169,-0.258809689535701,4.4182376949229));
#61872=CARTESIAN_POINT('Ctrl Pts',(10.2507745242318,-0.491764996345908,
4.00850959581219));
#61873=CARTESIAN_POINT('Ctrl Pts',(10.2984903602946,-0.273124940234581,
3.59096700393021));
#61874=CARTESIAN_POINT('Ctrl Pts',(10.3462061963575,0.196329951061554,3.54904570612073));
#61875=CARTESIAN_POINT('Ctrl Pts',(10.3939220324203,0.485492027373267,3.92124267520431));
#61876=CARTESIAN_POINT('Ctrl Pts',(10.4416378684831,0.328819304693055,4.36576370748498));
#61877=CARTESIAN_POINT('Ctrl Pts',(10.489353704546,-0.129813245022134,4.47439829918413));
#61878=CARTESIAN_POINT('Ctrl Pts',(10.5370695406088,-0.469236294399976,
4.14738563318641));
#61879=CARTESIAN_POINT('Ctrl Pts',(10.5847853766716,-0.377752434501872,
3.68502647241413));
#61880=CARTESIAN_POINT('Ctrl Pts',(10.6325012127345,0.0606272984676223,
3.51191234851464));
#61881=CARTESIAN_POINT('Ctrl Pts',(10.6802170487973,0.443332050383407,3.78701662516801));
#61882=CARTESIAN_POINT('Ctrl Pts',(10.7279328848602,0.418918158891686,4.25770681210006));
#61883=CARTESIAN_POINT('Ctrl Pts',(10.775648720923,0.00980527620531799,
4.49174086815163));
#61884=CARTESIAN_POINT('Ctrl Pts',(10.8233645569858,-0.408311942493964,
4.27420171857372));
#61885=CARTESIAN_POINT('Ctrl Pts',(10.8710803930487,-0.451470021714238,
3.80485891169382));
#61886=CARTESIAN_POINT('Ctrl Pts',(10.9187962291115,-0.080036233235122,
3.51471716883706));
#61887=CARTESIAN_POINT('Ctrl Pts',(10.9665120651743,0.364896059739551,3.6702181168734));
#61888=CARTESIAN_POINT('Ctrl Pts',(11.0142279012372,0.47473868640782,4.1285628425314));
#61889=CARTESIAN_POINT('Ctrl Pts',(11.0619437373,0.148621472554162,4.46884633169921));
#61890=CARTESIAN_POINT('Ctrl Pts',(11.1096595733629,-0.313977126381285,
4.37858102033954));
#61891=CARTESIAN_POINT('Ctrl Pts',(11.1573754094257,-0.488245699001722,
3.94065893278431));
#61892=CARTESIAN_POINT('Ctrl Pts',(11.2050912454886,-0.214150733603143,
3.55723066033293));
#61893=CARTESIAN_POINT('Ctrl Pts',(11.2528070815514,0.256602145595791,3.58040428537983));
#61894=CARTESIAN_POINT('Ctrl Pts',(11.3005229176142,0.491713326162588,3.98889911147238));
#61895=CARTESIAN_POINT('Ctrl Pts',(11.3482387536771,0.275276593332242,4.40758805430897));
#61896=CARTESIAN_POINT('Ctrl Pts',(11.3959545897399,-0.193950870829933,
4.45198261532529));
#61897=CARTESIAN_POINT('Ctrl Pts',(11.4436704258028,-0.485070265991237,
4.08131458604192));
#61898=CARTESIAN_POINT('Ctrl Pts',(11.4913862618656,-0.330742172127369,
3.63597412121053));
#61899=CARTESIAN_POINT('Ctrl Pts',(11.5391020979284,0.127311547523522,3.52492422212962));
#61900=CARTESIAN_POINT('Ctrl Pts',(11.5868179339912,0.468453114143607,3.85014371984754));
#61901=CARTESIAN_POINT('Ctrl Pts',(11.6345337700541,0.379406977967949,4.31297854546471));
#61902=CARTESIAN_POINT('Ctrl Pts',(11.6822496061169,-0.0580544240024287,
4.48840035698771));
#61903=CARTESIAN_POINT('Ctrl Pts',(11.7299654421798,-0.44220355512924,4.21531660568344));
#61904=CARTESIAN_POINT('Ctrl Pts',(11.7776812782426,-0.420270357404582,
3.74450430230823));
#61905=CARTESIAN_POINT('Ctrl Pts',(11.8253971143054,-0.0123964237846327,
3.50831762943));
#61906=CARTESIAN_POINT('Ctrl Pts',(11.8731129503683,0.406861336540243,3.72365044295193));
#61907=CARTESIAN_POINT('Ctrl Pts',(11.9208287864311,0.452492071153857,4.1927593068956));
#61908=CARTESIAN_POINT('Ctrl Pts',(11.968544622494,0.0825923743414284,4.48485433333386));
#61909=CARTESIAN_POINT('Ctrl Pts',(12.0162604585568,-0.363153170675764,
4.33170016502878));
#61910=CARTESIAN_POINT('Ctrl Pts',(12.0639762946196,-0.475409571231627,
3.87394063131468));
#61911=CARTESIAN_POINT('Ctrl Pts',(12.1116921306825,-0.151090047408964,
3.53194335553704));
#61912=CARTESIAN_POINT('Ctrl Pts',(12.1594079667453,0.311977791768556,3.61976969834691));
#61913=CARTESIAN_POINT('Ctrl Pts',(12.2071238028081,0.488551624369653,4.05676737776005));
#61914=CARTESIAN_POINT('Ctrl Pts',(12.254839638871,0.216480982979095,4.44163470069774));
#61915=CARTESIAN_POINT('Ctrl Pts',(12.3025554749338,-0.254387476069249,
4.42094208256136));
#61916=CARTESIAN_POINT('Ctrl Pts',(12.3502713109967,-0.49164800158875,4.0136918729824));
#61917=CARTESIAN_POINT('Ctrl Pts',(12.3979871470595,-0.277420602272412,
3.59386820576715));
#61918=CARTESIAN_POINT('Ctrl Pts',(12.4457029831224,0.191566404775332,3.54700161433684));
#61919=CARTESIAN_POINT('Ctrl Pts',(12.4934188191852,0.484635034689867,3.91613041073711));
#61920=CARTESIAN_POINT('Ctrl Pts',(12.541134655248,0.332655855180181,4.362277941457));
#61921=CARTESIAN_POINT('Ctrl Pts',(12.5888504913109,-0.124806314709729,
4.47574006417428));
#61922=CARTESIAN_POINT('Ctrl Pts',(12.6365663273737,-0.4676569254097,4.15232276575852));
#61923=CARTESIAN_POINT('Ctrl Pts',(12.6842821634365,-0.381050985679211,
3.68902512775968));
#61924=CARTESIAN_POINT('Ctrl Pts',(12.7319979994994,0.0554799374235607,
3.5113004999026));
#61925=CARTESIAN_POINT('Ctrl Pts',(12.7797138355622,0.441062780321708,3.78235614259331));
#61926=CARTESIAN_POINT('Ctrl Pts',(12.8274296716251,0.421610885427219,4.2532774884218));
#61927=CARTESIAN_POINT('Ctrl Pts',(12.8751455076879,0.0149872271275763,
4.49161021945745));
#61928=CARTESIAN_POINT('Ctrl Pts',(12.9228613437507,-0.405399432451448,
4.27848972156979));
#61929=CARTESIAN_POINT('Ctrl Pts',(12.9705771798136,-0.453501555338242,
3.80962782724943));
#61930=CARTESIAN_POINT('Ctrl Pts',(13.0182930158764,-0.0851462219395619,
3.51558762841831));
#61931=CARTESIAN_POINT('Ctrl Pts',(13.0660088519392,0.361400197209248,3.66639076405307));
#61932=CARTESIAN_POINT('Ctrl Pts',(13.1137246880021,0.476067254403989,4.1235523942958));
#61933=CARTESIAN_POINT('Ctrl Pts',(13.1614405240649,0.153554426643267,4.46725395975876));
#61934=CARTESIAN_POINT('Ctrl Pts',(13.2091563601278,-0.30996979384252,4.38186902434892));
#61935=CARTESIAN_POINT('Ctrl Pts',(13.2568721961906,-0.488843983144383,
3.94580788806928));
#61936=CARTESIAN_POINT('Ctrl Pts',(13.3045880322534,-0.218805220893238,
3.55951220202843));
#61937=CARTESIAN_POINT('Ctrl Pts',(13.3523038683163,0.252165742455243,3.57772323864086));
#61938=CARTESIAN_POINT('Ctrl Pts',(13.4000197043791,0.491569024438394,3.98371752277252));
#61939=CARTESIAN_POINT('Ctrl Pts',(13.447735540442,0.279556907518101,4.40466425628032));
#61940=CARTESIAN_POINT('Ctrl Pts',(13.4954513765048,-0.189176619112,4.45400157668594));
#61941=CARTESIAN_POINT('Ctrl Pts',(13.5431672125676,-0.484186345555107,
4.08642226350871));
#61942=CARTESIAN_POINT('Ctrl Pts',(13.5908830486304,-0.334560300710407,
3.63948005597396));
#61943=CARTESIAN_POINT('Ctrl Pts',(13.6385988846933,0.122297616148583,3.52360886035071));
#61944=CARTESIAN_POINT('Ctrl Pts',(13.6863147207561,0.466847750307624,3.8452149784873));
#61945=CARTESIAN_POINT('Ctrl Pts',(13.734030556819,0.3826844119832,4.30896256355269));
#61946=CARTESIAN_POINT('Ctrl Pts',(13.7817463928818,-0.0529039102219543,
4.48898507250754));
#61947=CARTESIAN_POINT('Ctrl Pts',(13.8294622289446,-0.439909757638992,
4.21996506537626));
#61948=CARTESIAN_POINT('Ctrl Pts',(13.8771780650075,-0.422939705734467,
3.74894775411238));
#61949=CARTESIAN_POINT('Ctrl Pts',(13.9248939010703,-0.0175776142901187,
3.50847558318244));
#61950=CARTESIAN_POINT('Ctrl Pts',(13.9726097371332,0.403926270823208,3.71937784729135));
#61951=CARTESIAN_POINT('Ctrl Pts',(14.020325573196,0.454498446235019,4.18797975215946));
#61952=CARTESIAN_POINT('Ctrl Pts',(14.0680414092588,0.0876977051117048,
4.48395695817926));
#61953=CARTESIAN_POINT('Ctrl Pts',(14.1157572453217,-0.359637188018331,
4.33550904286807));
#61954=CARTESIAN_POINT('Ctrl Pts',(14.1634730813845,-0.476711717661702,
3.87895801102093));
#61955=CARTESIAN_POINT('Ctrl Pts',(14.2111889174473,-0.156014541823709,
3.53356170012368));
#61956=CARTESIAN_POINT('Ctrl Pts',(14.2589047535102,0.307953188363286,3.61650285707861));
#61957=CARTESIAN_POINT('Ctrl Pts',(14.306620589573,0.4891227672074,4.05161534124029));
#61958=CARTESIAN_POINT('Ctrl Pts',(14.3543364256359,0.2211233828038,4.4393286633369));
#61959=CARTESIAN_POINT('Ctrl Pts',(14.4020522616987,-0.249937006449114,
4.42359971395084));
#61960=CARTESIAN_POINT('Ctrl Pts',(14.4497680977616,-0.491476396904638,
4.01887262932433));
#61961=CARTESIAN_POINT('Ctrl Pts',(14.4974839338244,-0.281685449746218,
3.59681451879656));
#61962=CARTESIAN_POINT('Ctrl Pts',(14.5451997698872,0.186781580201919,3.54500783946397));
#61963=CARTESIAN_POINT('Ctrl Pts',(14.59291560595,0.483724211046603,3.91102746210588));
#61964=CARTESIAN_POINT('Ctrl Pts',(14.6406314420129,0.33645545583349,4.35875193531444));
#61965=CARTESIAN_POINT('Ctrl Pts',(14.6883472780757,-0.119785521504147,
4.47702898621568));
#61966=CARTESIAN_POINT('Ctrl Pts',(14.7360631141386,-0.466025611307368,
4.15724297904063));
#61967=CARTESIAN_POINT('Ctrl Pts',(14.7837789502014,-0.38430721152129,3.69305832471834));
#61968=CARTESIAN_POINT('Ctrl Pts',(14.8314947862642,0.0503264139313189,
3.51074293371195));
#61969=CARTESIAN_POINT('Ctrl Pts',(14.8792106223271,0.438744519099385,3.77771983486548));
#61970=CARTESIAN_POINT('Ctrl Pts',(14.9269264583899,0.42425678142631,4.24882003188202));
#61971=CARTESIAN_POINT('Ctrl Pts',(14.9746422944528,0.0201675133397715,
4.49142496503298));
#61972=CARTESIAN_POINT('Ctrl Pts',(15.0223581305156,-0.402441892563756,
4.28274679124913));
#61973=CARTESIAN_POINT('Ctrl Pts',(15.0700739665785,-0.455482716161518,
3.8144178884426));
#61974=CARTESIAN_POINT('Ctrl Pts',(15.1177898026413,-0.0902467530057116,
3.51651189422706));
#61975=CARTESIAN_POINT('Ctrl Pts',(15.1655056387041,0.357864192060027,3.66260046696357));
#61976=CARTESIAN_POINT('Ctrl Pts',(15.2132214747669,0.47734294310866,4.11852822244656));
#61977=CARTESIAN_POINT('Ctrl Pts',(15.2609373108298,0.15847032463534,4.46560968746574));
#61978=CARTESIAN_POINT('Ctrl Pts',(15.3086531468926,-0.305928031329979,
4.38511461215921));
#61979=CARTESIAN_POINT('Ctrl Pts',(15.3563689829555,-0.489387968817152,
3.95096286275689));
#61980=CARTESIAN_POINT('Ctrl Pts',(15.4040848190183,-0.223435404337718,
3.56184267101825));
#61981=CARTESIAN_POINT('Ctrl Pts',(15.4518006550811,0.24770132994065,3.57508909640066));
#61982=CARTESIAN_POINT('Ctrl Pts',(15.499516491144,0.491370121559653,3.97853774265298));
#61983=CARTESIAN_POINT('Ctrl Pts',(15.5472323272068,0.283806169849271,4.40169551006635));
#61984=CARTESIAN_POINT('Ctrl Pts',(15.5949481632697,-0.184381354552937,
4.4559701097059));
#61985=CARTESIAN_POINT('Ctrl Pts',(15.6426639993325,-0.483248643997369,
4.09152034160055));
#61986=CARTESIAN_POINT('Ctrl Pts',(15.6903798353953,-0.338341267922855,
3.64302603558196));
#61987=CARTESIAN_POINT('Ctrl Pts',(15.7380956714582,0.117270100534806,3.52234641383892));
#61988=CARTESIAN_POINT('Ctrl Pts',(15.785811507521,0.465190531238913,3.84030342991275));
#61989=CARTESIAN_POINT('Ctrl Pts',(15.8335273435838,0.385919339229949,4.30491226354526));
#61990=CARTESIAN_POINT('Ctrl Pts',(15.8812431796467,-0.0477475201261761,
4.48951547388594));
#61991=CARTESIAN_POINT('Ctrl Pts',(15.9289590157095,-0.437567097060412,
4.22458909239344));
#61992=CARTESIAN_POINT('Ctrl Pts',(15.9766748517724,-0.425562075928853,
3.75341909160864));
#61993=CARTESIAN_POINT('Ctrl Pts',(16.0243906878352,-0.0227568523576073,
3.50868813313462));
#61994=CARTESIAN_POINT('Ctrl Pts',(16.072106523898,0.400946338892803,3.71513642180785));
#61995=CARTESIAN_POINT('Ctrl Pts',(16.1198223599609,0.456454337785543,4.1831793175245));
#61996=CARTESIAN_POINT('Ctrl Pts',(16.1675381960237,0.0927932948370443,
4.4830058273823));
#61997=CARTESIAN_POINT('Ctrl Pts',(16.2152540320865,-0.356081258568678,
4.33928065395499));
#61998=CARTESIAN_POINT('Ctrl Pts',(16.2629698681494,-0.477960913216358,
3.88398883549692));
#61999=CARTESIAN_POINT('Ctrl Pts',(16.3106857042122,-0.160921706883503,
3.53523185446324));
#62000=CARTESIAN_POINT('Ctrl Pts',(16.358401540275,0.303894378979202,3.6132786128531));
#62001=CARTESIAN_POINT('Ctrl Pts',(16.4061173763379,0.489639580609251,4.04645757153336));
#62002=CARTESIAN_POINT('Ctrl Pts',(16.4538332124007,0.225741221292456,4.43697382743292));
#62003=CARTESIAN_POINT('Ctrl Pts',(16.5015490484636,-0.245458775012363,
4.42621029389423));
#62004=CARTESIAN_POINT('Ctrl Pts',(16.5492648845264,-0.4912502013546,4.02405128938415));
#62005=CARTESIAN_POINT('Ctrl Pts',(16.5969807205893,-0.285919008936969,
3.59980561575594));
#62006=CARTESIAN_POINT('Ctrl Pts',(16.6446965566521,0.181976008816936,3.54306460296116));
#62007=CARTESIAN_POINT('Ctrl Pts',(16.6924123927149,0.482759657613431,3.90593439612197));
#62008=CARTESIAN_POINT('Ctrl Pts',(16.7401282287778,0.340217684611379,4.35518608070932));
#62009=CARTESIAN_POINT('Ctrl Pts',(16.7878440648406,-0.114751423091257,
4.47826492214097));
#62010=CARTESIAN_POINT('Ctrl Pts',(16.8355599009034,-0.464342533291602,
4.16214572651883));
#62011=CARTESIAN_POINT('Ctrl Pts',(16.8832757369663,-0.387520750342007,
3.69712561530174));
#62012=CARTESIAN_POINT('Ctrl Pts',(16.9309915730291,0.0451673004198413,
3.51023971187451));
#62013=CARTESIAN_POINT('Ctrl Pts',(16.978707409092,0.436377524217892,3.7731082169636));
#62014=CARTESIAN_POINT('Ctrl Pts',(17.0264232451548,0.426855552995382,4.24433493759383));
#62015=CARTESIAN_POINT('Ctrl Pts',(17.0741390812176,0.0253455594402812,
4.49118512545541));
#62016=CARTESIAN_POINT('Ctrl Pts',(17.1218549172805,-0.399439651340385,
4.28697245475663));
#62017=CARTESIAN_POINT('Ctrl Pts',(17.1695707533433,-0.457413284126125,
3.81922856321607));
#62018=CARTESIAN_POINT('Ctrl Pts',(17.2172865894061,-0.0953372598908034,
3.51748986360026));
#62019=CARTESIAN_POINT('Ctrl Pts',(17.265002425469,0.354288437054553,3.6588476466131));
#62020=CARTESIAN_POINT('Ctrl Pts',(17.3127182615318,0.478565610824392,4.11349088504481));
#62021=CARTESIAN_POINT('Ctrl Pts',(17.3604340975947,0.163368620495752,4.46391369745815));
#62022=CARTESIAN_POINT('Ctrl Pts',(17.4081499336575,-0.301852287783465,
4.38831742326589));
#62023=CARTESIAN_POINT('Ctrl Pts',(17.4558657697204,-0.489877595596684,
3.956123284257));
#62024=CARTESIAN_POINT('Ctrl Pts',(17.5035816057832,-0.228040769637767,
3.56422180844494));
#62025=CARTESIAN_POINT('Ctrl Pts',(17.551297441846,0.243209403937772,3.57250215124727));
#62026=CARTESIAN_POINT('Ctrl Pts',(17.5990132779089,0.491116639619549,3.97336034645914));
#62027=CARTESIAN_POINT('Ctrl Pts',(17.6467291139717,0.288023908337871,4.39868214542132));
#62028=CARTESIAN_POINT('Ctrl Pts',(17.6944449500345,-0.179565609787963,
4.45788799572981));
#62029=CARTESIAN_POINT('Ctrl Pts',(17.7421607860973,-0.48225726547346,4.09660825404716));
#62030=CARTESIAN_POINT('Ctrl Pts',(17.7898766221602,-0.342084653792828,
3.64661166616396));
#62031=CARTESIAN_POINT('Ctrl Pts',(17.837592458223,0.112229559114723,3.52113702282083));
#62032=CARTESIAN_POINT('Ctrl Pts',(17.8853082942859,0.463481641013499,3.83540961967535));
#62033=CARTESIAN_POINT('Ctrl Pts',(17.9330241303487,0.389111400387848,4.30082809533052));
#62034=CARTESIAN_POINT('Ctrl Pts',(17.9807399664116,-0.0425858264624495,
4.48999150220845));
#62035=CARTESIAN_POINT('Ctrl Pts',(18.0284558024744,-0.435175833605105,
4.22918817311999));
#62036=CARTESIAN_POINT('Ctrl Pts',(18.0761716385373,-0.428137176707308,
3.75791781814212));
#62037=CARTESIAN_POINT('Ctrl Pts',(18.1238874746,-0.0279335627019553,3.5089552556775));
#62038=CARTESIAN_POINT('Ctrl Pts',(18.1716033106629,0.397921871745719,3.71092663761881));
#62039=CARTESIAN_POINT('Ctrl Pts',(18.2193191467257,0.458359528554279,4.17835853620019));
#62040=CARTESIAN_POINT('Ctrl Pts',(18.2670349827886,0.097878577523561,4.48200104659009));
#62041=CARTESIAN_POINT('Ctrl Pts',(18.3147508188514,-0.352485777302551,
4.34301457935691));
#62042=CARTESIAN_POINT('Ctrl Pts',(18.3624666549143,-0.479157019140895,
3.88903254594255));
#62043=CARTESIAN_POINT('Ctrl Pts',(18.4101824909771,-0.165810997523729,
3.5369536330429));
#62044=CARTESIAN_POINT('Ctrl Pts',(18.4578983270399,0.299801814449608,3.61009732380414));
#62045=CARTESIAN_POINT('Ctrl Pts',(18.5056141631028,0.49010200717001,4.04129464153984));
#62046=CARTESIAN_POINT('Ctrl Pts',(18.5533299991656,0.230333985517487,4.43457045454981));
#62047=CARTESIAN_POINT('Ctrl Pts',(18.6010458352284,-0.24095327917969,4.42877353242069));
#62048=CARTESIAN_POINT('Ctrl Pts',(18.6487616712913,-0.49096944006335,4.0292272779409));
#62049=CARTESIAN_POINT('Ctrl Pts',(18.6964775073541,-0.290120809601049,
3.60284116440841));
#62050=CARTESIAN_POINT('Ctrl Pts',(18.744193343417,0.177150224400508,3.54117212067402));
#62051=CARTESIAN_POINT('Ctrl Pts',(18.7919091794797,0.481741481528227,3.90085177849878));
#62052=CARTESIAN_POINT('Ctrl Pts',(18.8396250155427,0.343942123623612,4.35158077372017));
#62053=CARTESIAN_POINT('Ctrl Pts',(18.8873408516054,-0.109704578635382,
4.47944773466767));
#62054=CARTESIAN_POINT('Ctrl Pts',(18.9350566876684,-0.462607878309702,
4.16703046362027));
#62055=CARTESIAN_POINT('Ctrl Pts',(18.9827725237311,-0.39069124519864,3.70122654773242));
#62056=CARTESIAN_POINT('Ctrl Pts',(19.030488359794,0.0400031699426168,3.50979089028978));
#62057=CARTESIAN_POINT('Ctrl Pts',(19.0782041958568,0.433962058584907,3.76852180111673));
#62058=CARTESIAN_POINT('Ctrl Pts',(19.1259200319197,0.429406911488226,4.23982270375453));
#62059=CARTESIAN_POINT('Ctrl Pts',(19.1736358679825,0.0305207902517796,
4.49089072733801));
#62060=CARTESIAN_POINT('Ctrl Pts',(19.2213517040454,-0.396393042209671,
4.29116624277653));
#62061=CARTESIAN_POINT('Ctrl Pts',(19.2690675401082,-0.459293044881286,
3.82405931712685));
#62062=CARTESIAN_POINT('Ctrl Pts',(19.316783376171,-0.100417177000157,3.51852142809106));
#62063=CARTESIAN_POINT('Ctrl Pts',(19.3644992122339,0.350673329058588,3.65513271950473));
#62064=CARTESIAN_POINT('Ctrl Pts',(19.4122150482967,0.479735122332443,4.10844094226069));
#62065=CARTESIAN_POINT('Ctrl Pts',(19.4599308843596,0.168248769032157,4.46216617689766));
#62066=CARTESIAN_POINT('Ctrl Pts',(19.5076467204224,-0.297743013815871,
4.39147710422109));
#62067=CARTESIAN_POINT('Ctrl Pts',(19.5553625564852,-0.490312813065352,
3.96128857502183));
#62068=CARTESIAN_POINT('Ctrl Pts',(19.603078392548,-0.232620797759261,3.56664935826393));
#62069=CARTESIAN_POINT('Ctrl Pts',(19.6507942286109,0.238690449241969,3.56996267500769));
#62070=CARTESIAN_POINT('Ctrl Pts',(19.6985100646737,0.490808633485035,3.96818593857384));
#62071=CARTESIAN_POINT('Ctrl Pts',(19.7462259007366,0.292209604061002,4.39562444172689));
#62072=CARTESIAN_POINT('Ctrl Pts',(19.7939417367994,-0.174729824492781,
4.45975512619968));
#62073=CARTESIAN_POINT('Ctrl Pts',(19.8416575728622,-0.481212499922896,
4.10168523844358));
#62074=CARTESIAN_POINT('Ctrl Pts',(19.8893734089251,-0.345789702982467,
3.65023692191923));
#62075=CARTESIAN_POINT('Ctrl Pts',(19.9370892449879,0.107175910646637,3.51998011832295));
#62076=CARTESIAN_POINT('Ctrl Pts',(19.9848050810508,0.461722480014006,3.83053541934297));
#62077=CARTESIAN_POINT('Ctrl Pts',(20.0325209171136,0.392257955100357,4.29670800504879));
#62078=CARTESIAN_POINT('Ctrl Pts',(20.0802367531764,-0.0374150865130887,
4.49041783929577));
#62079=CARTESIAN_POINT('Ctrl Pts',(20.1279525892393,-0.432744382500041,
4.23375285658289));
#62080=CARTESIAN_POINT('Ctrl Pts',(20.1756684253021,-0.430649333670284,
3.76246031529274));
#62081=CARTESIAN_POINT('Ctrl Pts',(20.223384261365,-0.033136228617316,3.50924504180455));
#62082=CARTESIAN_POINT('Ctrl Pts',(20.2711000974278,0.394908089060633,3.70680919012016));
#62083=CARTESIAN_POINT('Ctrl Pts',(20.3188159334906,0.460110046434968,4.17340395051402));
#62084=CARTESIAN_POINT('Ctrl Pts',(20.3665317695535,0.103149962306437,4.48116018402389));
#62085=CARTESIAN_POINT('Ctrl Pts',(20.4142476056163,-0.34923165553999,4.34628168153608));
#62086=CARTESIAN_POINT('Ctrl Pts',(20.4540108023354,-0.457800032585507,
3.97025345815189));
#62087=CARTESIAN_POINT('Ctrl Pts',(20.4858213597105,-0.325993724402262,
3.71529210935379));
#62088=CARTESIAN_POINT('Ctrl Pts',(20.509679277742,-0.15096738523986,3.59329490328468));
#62089=CARTESIAN_POINT('Ctrl Pts',(20.5335371957734,0.0630371972956549,
3.57102347342756));
#62090=CARTESIAN_POINT('Ctrl Pts',(20.5573951138048,0.260511246441404,3.65349437971329));
#62091=CARTESIAN_POINT('Ctrl Pts',(20.5812530318362,0.394877283734959,3.82077798440408));
#62092=CARTESIAN_POINT('Ctrl Pts',(20.6051109498677,0.432370081305563,4.03184236506754));
#62093=CARTESIAN_POINT('Ctrl Pts',(20.6289688678991,0.364303478986858,4.23514367899931));
#62094=CARTESIAN_POINT('Ctrl Pts',(20.6528267859305,0.207066376217976,4.38093363836299));
#62095=CARTESIAN_POINT('Ctrl Pts',(20.6766847039619,-0.000757290757721993,
4.43358147160167));
#62096=CARTESIAN_POINT('Ctrl Pts',(20.7005426219933,-0.208420567790133,
4.38020336888205));
#62097=CARTESIAN_POINT('Ctrl Pts',(20.7244005400248,-0.365106210756856,
4.23385701605743));
#62098=CARTESIAN_POINT('Ctrl Pts',(20.7482584580562,-0.432520392530856,
4.03032528343114));
#62099=CARTESIAN_POINT('Ctrl Pts',(20.7721163760876,-0.394167874571092,
3.81937870627435));
#62100=CARTESIAN_POINT('Ctrl Pts',(20.795974294119,-0.259432524437891,3.65259868360638));
#62101=CARTESIAN_POINT('Ctrl Pts',(20.8198322121504,-0.0612578225112809,
3.57076788979259));
#62102=CARTESIAN_POINT('Ctrl Pts',(20.8436901301819,0.151895538690754,3.5938959627232));
#62103=CARTESIAN_POINT('Ctrl Pts',(20.8675480482132,0.327906592802717,3.71632757520176));
#62104=CARTESIAN_POINT('Ctrl Pts',(20.8914059662447,0.423735399567132,3.90812480123879));
#62105=CARTESIAN_POINT('Ctrl Pts',(20.9152638842761,0.415949440063929,4.12238802732943));
#62106=CARTESIAN_POINT('Ctrl Pts',(20.9391218023075,0.30645246920106,4.30672404095661));
#62107=CARTESIAN_POINT('Ctrl Pts',(20.962979720339,0.122019544809087,4.41605767475162));
#62108=CARTESIAN_POINT('Ctrl Pts',(20.9868376383703,-0.0922504941031022,
4.42365387220386));
#62109=CARTESIAN_POINT('Ctrl Pts',(21.0106955564018,-0.28396276796243,4.32765515869354));
#62110=CARTESIAN_POINT('Ctrl Pts',(21.0345534744332,-0.40623841344949,4.15153583326342));
#62111=CARTESIAN_POINT('Ctrl Pts',(21.0584113924646,-0.429177699343215,
3.93836186909709));
#62112=CARTESIAN_POINT('Ctrl Pts',(21.082269310496,-0.347171348131155,3.74026010679315));
#62113=CARTESIAN_POINT('Ctrl Pts',(21.1061272285274,-0.180272145040548,
3.605671823621));
#62114=CARTESIAN_POINT('Ctrl Pts',(21.1299851465589,0.0307085077608185,
3.56750752082027));
#62115=CARTESIAN_POINT('Ctrl Pts',(21.1538430645903,0.234180094072738,3.63509941005724));
#62116=CARTESIAN_POINT('Ctrl Pts',(21.1777009826217,0.380388268371489,3.79191943321731));
#62117=CARTESIAN_POINT('Ctrl Pts',(21.2015589006531,0.433581149524578,3.99962082296209));
#62118=CARTESIAN_POINT('Ctrl Pts',(21.2254168186846,0.380751629084578,4.2074149318183));
#62119=CARTESIAN_POINT('Ctrl Pts',(21.2492747367159,0.234817963878357,4.36449043997717));
#62120=CARTESIAN_POINT('Ctrl Pts',(21.2731326547474,0.0314649101850846,
4.43243810704058));
#62121=CARTESIAN_POINT('Ctrl Pts',(21.2969905727788,-0.179582171132277,
4.39464287755545));
#62122=CARTESIAN_POINT('Ctrl Pts',(21.3208484908102,-0.346716519889314,
4.26034671465164));
#62123=CARTESIAN_POINT('Ctrl Pts',(21.3447064088417,-0.429069235164158,
4.0623886883135));
#62124=CARTESIAN_POINT('Ctrl Pts',(21.368564326873,-0.406502834830527,3.8491749282489));
#62125=CARTESIAN_POINT('Ctrl Pts',(21.3924222449045,-0.284535418465691,
3.67284200661995));
#62126=CARTESIAN_POINT('Ctrl Pts',(21.4162801629359,-0.0929913416969399,
3.5765081259772));
#62127=CARTESIAN_POINT('Ctrl Pts',(21.4401380809674,0.121291651150069,3.58372954422009));
#62128=CARTESIAN_POINT('Ctrl Pts',(21.4639959989987,0.305915531372611,3.69274042788069));
#62129=CARTESIAN_POINT('Ctrl Pts',(21.4878539170302,0.415734731202803,3.87688464650718));
#62130=CARTESIAN_POINT('Ctrl Pts',(21.5117118350615,0.423895464867194,4.09113392265755));
#62131=CARTESIAN_POINT('Ctrl Pts',(21.535569753093,0.328402210690932,4.28309847227994));
#62132=CARTESIAN_POINT('Ctrl Pts',(21.5594276711244,0.152605670504114,4.40583773398234));
#62133=CARTESIAN_POINT('Ctrl Pts',(21.5832855891559,-0.0605071130159612,
4.42933861492812));
#62134=CARTESIAN_POINT('Ctrl Pts',(21.6071435071872,-0.258824259222961,
4.34785450957493));
#62135=CARTESIAN_POINT('Ctrl Pts',(21.6310014252187,-0.39385182381868,4.18131050126406));
#62136=CARTESIAN_POINT('Ctrl Pts',(21.6548593432501,-0.432571889182456,
3.97043113659525));
#62137=CARTESIAN_POINT('Ctrl Pts',(21.6787172612815,-0.365516344619441,
3.76678216446856));
#62138=CARTESIAN_POINT('Ctrl Pts',(21.702575179313,-0.209082097331647,3.62016130585559));
#62139=CARTESIAN_POINT('Ctrl Pts',(21.7264330973443,-0.00152158196427748,
3.56642135455923));
#62140=CARTESIAN_POINT('Ctrl Pts',(21.7502910153758,0.206411001640417,3.61870319251831));
#62141=CARTESIAN_POINT('Ctrl Pts',(21.7741489334072,0.363870472821225,3.76422248622317));
#62142=CARTESIAN_POINT('Ctrl Pts',(21.7980068514386,0.432353701764573,3.96739580449697));
#62143=CARTESIAN_POINT('Ctrl Pts',(21.82186476947,0.395114673548107,4.17854173669174));
#62144=CARTESIAN_POINT('Ctrl Pts',(21.8457226875014,0.261259344941517,4.3460293508861));
#62145=CARTESIAN_POINT('Ctrl Pts',(21.8695806055329,0.0635189899350569,
4.42890336313855));
#62146=CARTESIAN_POINT('Ctrl Pts',(21.8934385235643,-0.14975348833307,4.40689882001058));
#62147=CARTESIAN_POINT('Ctrl Pts',(21.9172964415957,-0.326407159500644,
4.28539643168872));
#62148=CARTESIAN_POINT('Ctrl Pts',(21.9411543596271,-0.423245389017799,
4.09410684177624));
#62149=CARTESIAN_POINT('Ctrl Pts',(21.9650122776585,-0.416588591947193,
3.87980556563057));
#62150=CARTESIAN_POINT('Ctrl Pts',(21.98887019569,-0.30806453650007,3.69489510271888));
#62151=CARTESIAN_POINT('Ctrl Pts',(22.0127281137213,-0.12421031036921,3.58459109808296));
#62152=CARTESIAN_POINT('Ctrl Pts',(22.0365860317528,0.0900167200678817,
3.57586588547707));
#62153=CARTESIAN_POINT('Ctrl Pts',(22.0604439497842,0.282232210442068,3.67085301705332));
#62154=CARTESIAN_POINT('Ctrl Pts',(22.0843018678157,0.405434237512275,3.8463255517439));
#62155=CARTESIAN_POINT('Ctrl Pts',(22.108159785847,0.429496549703537,4.05937567504088));
#62156=CARTESIAN_POINT('Ctrl Pts',(22.1320177038785,0.348535256241736,4.25790682842971));
#62157=CARTESIAN_POINT('Ctrl Pts',(22.1558756219099,0.182347598717988,4.39337273702606));
#62158=CARTESIAN_POINT('Ctrl Pts',(22.1797335399413,-0.0284290137391457,
4.43264829616218));
#62159=CARTESIAN_POINT('Ctrl Pts',(22.2035914579727,-0.232253957950086,
4.36612956178204));
#62160=CARTESIAN_POINT('Ctrl Pts',(22.2274493760041,-0.379286482964224,
4.21008217638027));
#62161=CARTESIAN_POINT('Ctrl Pts',(22.2513072940356,-0.433573131350875,
4.00266397632408));
#62162=CARTESIAN_POINT('Ctrl Pts',(22.275165212067,-0.381839338801546,3.79459436150246));
#62163=CARTESIAN_POINT('Ctrl Pts',(22.2990231300984,-0.236735426869051,
3.63675202040985));
#62164=CARTESIAN_POINT('Ctrl Pts',(22.3228810481298,-0.0337432544318164,
3.56773370504276));
#62165=CARTESIAN_POINT('Ctrl Pts',(22.3467389661613,0.177500062688638,3.60441627341574));
#62166=CARTESIAN_POINT('Ctrl Pts',(22.3705968841926,0.345339779804043,3.73782983856348));
#62167=CARTESIAN_POINT('Ctrl Pts',(22.3944548022241,0.428734513273282,3.93535114928888));
#62168=CARTESIAN_POINT('Ctrl Pts',(22.4183127202555,0.407291980919218,4.1486808655136));
#62169=CARTESIAN_POINT('Ctrl Pts',(22.4421706382869,0.286255462618544,4.32565405918856));
#62170=CARTESIAN_POINT('Ctrl Pts',(22.4660285563183,0.0952216904214238,
4.42299596654013));
#62171=CARTESIAN_POINT('Ctrl Pts',(22.4898864743497,-0.119096386717928,
4.41690383452019));
#62172=CARTESIAN_POINT('Ctrl Pts',(22.5137443923812,-0.304292138366774,
4.30886736509782));
#62173=CARTESIAN_POINT('Ctrl Pts',(22.5376023104126,-0.415080201412036,
4.12530439950267));
#62174=CARTESIAN_POINT('Ctrl Pts',(22.561460228444,-0.424369795825249,3.91110111771763));
#62175=CARTESIAN_POINT('Ctrl Pts',(22.5853181464754,-0.329889515310188,
3.71863599132299));
#62176=CARTESIAN_POINT('Ctrl Pts',(22.6091760645068,-0.154742073939436,
3.59497211022641));
#62177=CARTESIAN_POINT('Ctrl Pts',(22.6330339825383,0.0582436639512456,
3.57034842802071));
#62178=CARTESIAN_POINT('Ctrl Pts',(22.6568919005697,0.256987911016647,3.65078654733876));
#62179=CARTESIAN_POINT('Ctrl Pts',(22.6807498186011,0.39289034562191,3.81661632308649));
#62180=CARTESIAN_POINT('Ctrl Pts',(22.7046077366325,0.432722782933869,4.02728943245291));
#62181=CARTESIAN_POINT('Ctrl Pts',(22.7284656546639,0.366738191089385,4.2312875884069));
#62182=CARTESIAN_POINT('Ctrl Pts',(22.7523235726953,0.211084664509997,4.37873330099785));
#62183=CARTESIAN_POINT('Ctrl Pts',(22.7761814907268,0.00379901600965994,
4.43356145647204));
#62184=CARTESIAN_POINT('Ctrl Pts',(22.8000394087582,-0.204384723485633,
4.3823852668741));
#62185=CARTESIAN_POINT('Ctrl Pts',(22.8238973267896,-0.36265185203719,4.2376794731));
#62186=CARTESIAN_POINT('Ctrl Pts',(22.8398026054772,-0.408954280604672,
4.10250106973657));
#62187=CARTESIAN_POINT('Ctrl Pts',(22.847755244821,-0.414526965927561,4.03345758723954));
#62188=CARTESIAN_POINT('',(22.8,-0.592174260192535,4.04779597854866));
#62189=CARTESIAN_POINT('Ctrl Pts',(22.8,-0.19576256658266,4.36695865185836));
#62190=CARTESIAN_POINT('Ctrl Pts',(22.8,-0.195886593570853,4.36694806728808));
#62191=CARTESIAN_POINT('Ctrl Pts',(22.8,-0.196010613870461,4.36693742279878));
#62192=CARTESIAN_POINT('Ctrl Pts',(22.8,-0.196134627427637,4.36692671841166));
#62193=CARTESIAN_POINT('Ctrl Pts',(22.8,-0.216622178843513,4.36515830948628));
#62194=CARTESIAN_POINT('Ctrl Pts',(22.8,-0.236921239981942,4.36175743074964));
#62195=CARTESIAN_POINT('Ctrl Pts',(22.8,-0.256857422940798,4.35688458679081));
#62196=CARTESIAN_POINT('Ctrl Pts',(22.8,-0.271809560159941,4.35322995382169));
#62197=CARTESIAN_POINT('Ctrl Pts',(22.8,-0.286558947067823,4.34874691155445));
#62198=CARTESIAN_POINT('Ctrl Pts',(22.8,-0.301048271828705,4.34349077646485));
#62199=CARTESIAN_POINT('Ctrl Pts',(22.8,-0.310003423377303,4.3402422133286));
#62200=CARTESIAN_POINT('Ctrl Pts',(22.8,-0.318859482942331,4.33669811041118));
#62201=CARTESIAN_POINT('Ctrl Pts',(22.8,-0.327604744452034,4.33286912874946));
#62202=CARTESIAN_POINT('Ctrl Pts',(22.8,-0.333457186121174,4.33030672489195));
#62203=CARTESIAN_POINT('Ctrl Pts',(22.8,-0.33926207870774,4.32761569029118));
#62204=CARTESIAN_POINT('Ctrl Pts',(22.8,-0.345009487597299,4.32480202294401));
#62205=CARTESIAN_POINT('Ctrl Pts',(22.8,-0.365309066997251,4.31486428146495));
#62206=CARTESIAN_POINT('Ctrl Pts',(22.8,-0.384828901796994,4.30343044333042));
#62207=CARTESIAN_POINT('Ctrl Pts',(22.8,-0.403416958856431,4.29067119823496));
#62208=CARTESIAN_POINT('Ctrl Pts',(22.8,-0.409874425773003,4.28623865303559));
#62209=CARTESIAN_POINT('Ctrl Pts',(22.8,-0.416219739836017,4.28164578247975));
#62210=CARTESIAN_POINT('Ctrl Pts',(22.8,-0.422447327171508,4.27689854297234));
#62211=CARTESIAN_POINT('Ctrl Pts',(22.8,-0.43500295340691,4.2673274905416));
#62212=CARTESIAN_POINT('Ctrl Pts',(22.8,-0.447079966647781,4.25712966465555));
#62213=CARTESIAN_POINT('Ctrl Pts',(22.8,-0.458660056443695,4.24636133358853));
#62214=CARTESIAN_POINT('Ctrl Pts',(22.8,-0.465333929961841,4.24015529539631));
#62215=CARTESIAN_POINT('Ctrl Pts',(22.8,-0.471842796551704,4.23375955955572));
#62216=CARTESIAN_POINT('Ctrl Pts',(22.8,-0.478183280583292,4.22718326898633));
#62217=CARTESIAN_POINT('Ctrl Pts',(22.8,-0.48330469601013,4.22187138494));
#62218=CARTESIAN_POINT('Ctrl Pts',(22.8,-0.488310096860405,4.21644792156372));
#62219=CARTESIAN_POINT('Ctrl Pts',(22.8,-0.49319389770791,4.21092357737429));
#62220=CARTESIAN_POINT('Ctrl Pts',(22.8,-0.509882204568999,4.19204648678071));
#62221=CARTESIAN_POINT('Ctrl Pts',(22.8,-0.525164669297395,4.17198027236651));
#62222=CARTESIAN_POINT('Ctrl Pts',(22.8,-0.538985569877159,4.15095378743758));
#62223=CARTESIAN_POINT('Ctrl Pts',(22.8,-0.553292287721507,4.12918820238033));
#62224=CARTESIAN_POINT('Ctrl Pts',(22.8,-0.566034197593199,4.10639346234103));
#62225=CARTESIAN_POINT('Ctrl Pts',(22.8,-0.577149101532509,4.08276767497818));
#62226=CARTESIAN_POINT('Ctrl Pts',(22.8,-0.582543745751794,4.07130084468266));
#62227=CARTESIAN_POINT('Ctrl Pts',(22.8,-0.587554988912119,4.05963744408228));
#62228=CARTESIAN_POINT('Ctrl Pts',(22.8,-0.592174260192535,4.04779597854866));
#62229=CARTESIAN_POINT('Ctrl Pts',(22.8,-0.592174260192532,4.04779597854869));
#62230=CARTESIAN_POINT('Ctrl Pts',(22.7920473606562,-0.584213376873468,
4.14642833911734));
#62231=CARTESIAN_POINT('Ctrl Pts',(22.7840947213124,-0.551140611244481,
4.24298318064208));
#62232=CARTESIAN_POINT('Ctrl Pts',(22.7761420819686,-0.496922031827459,
4.32571394759471));
#62233=CARTESIAN_POINT('Ctrl Pts',(22.7681894426248,-0.442703452410443,
4.40844471454734));
#62234=CARTESIAN_POINT('Ctrl Pts',(22.760236803281,-0.367339059205388,4.47735140692785));
#62235=CARTESIAN_POINT('Ctrl Pts',(22.7522841639372,-0.280089901523161,
4.52398941366922));
#62236=CARTESIAN_POINT('Ctrl Pts',(22.7444712463773,-0.194373644734646,
4.56980802634291));
#62237=CARTESIAN_POINT('Ctrl Pts',(22.7366583288174,-0.0971865673270821,
4.59413356703531));
#62238=CARTESIAN_POINT('Ctrl Pts',(22.7288454112575,-7.11440487624268E-7,
4.59414971000239));
#62239=CARTESIAN_POINT('Origin',(27.2,0.3,2.9));
#62240=CARTESIAN_POINT('',(29.2,0.3,3.04606079858305));
#62241=CARTESIAN_POINT('',(27.2,0.3,3.04606079858305));
#62242=CARTESIAN_POINT('',(23.3,0.3,3.04606079858305));
#62243=CARTESIAN_POINT('',(29.2,0.3,3.35));
#62244=CARTESIAN_POINT('',(29.2,0.3,2.9));
#62245=CARTESIAN_POINT('',(27.2,0.3,3.35));
#62246=CARTESIAN_POINT('',(27.2,0.3,3.35));
#62247=CARTESIAN_POINT('',(27.2,0.3,2.9));
#62248=CARTESIAN_POINT('Origin',(27.2,0.,3.125));
#62249=CARTESIAN_POINT('',(27.2,-0.3,3.04606079858305));
#62250=CARTESIAN_POINT('Origin',(27.2,0.,4.));
#62251=CARTESIAN_POINT('',(27.2,-0.3,3.35));
#62252=CARTESIAN_POINT('',(27.2,0.3,3.35));
#62253=CARTESIAN_POINT('',(27.2,-0.3,3.35));
#62254=CARTESIAN_POINT('Origin',(27.2,0.3,3.35));
#62255=CARTESIAN_POINT('',(29.2,-0.3,3.35));
#62256=CARTESIAN_POINT('',(29.2,0.3,3.35));
#62257=CARTESIAN_POINT('',(27.2,-0.3,3.35));
#62258=CARTESIAN_POINT('Origin',(27.2,-0.3,3.35));
#62259=CARTESIAN_POINT('',(29.2,-0.3,3.04606079858305));
#62260=CARTESIAN_POINT('',(23.3,-0.3,3.04606079858305));
#62261=CARTESIAN_POINT('',(29.2,-0.3,3.35));
#62262=CARTESIAN_POINT('Origin',(29.2,0.,3.125));
#62263=CARTESIAN_POINT('Origin',(29.2,0.,4.));
#62264=CARTESIAN_POINT('Origin',(23.3,0.,4.));
#62265=CARTESIAN_POINT('',(29.4,-1.22464679914735E-16,5.));
#62266=CARTESIAN_POINT('Origin',(29.4,0.,4.));
#62267=CARTESIAN_POINT('',(23.3,-1.22464679914735E-16,5.));
#62268=CARTESIAN_POINT('',(23.3,-1.22464679914735E-16,5.));
#62269=CARTESIAN_POINT('Origin',(23.3,0.,4.));
#62270=CARTESIAN_POINT('Origin',(29.4,0.,4.));
#62271=CARTESIAN_POINT('Origin',(22.8,0.,4.));
#62272=CARTESIAN_POINT('',(22.8,-1.65327317884893E-16,5.35));
#62273=CARTESIAN_POINT('Origin',(22.8,0.,4.));
#62274=CARTESIAN_POINT('Origin',(22.8,0.,4.));
#62275=CARTESIAN_POINT('Origin',(22.8,0.,4.));
#62276=CARTESIAN_POINT('',(23.3,-1.65327317884893E-16,5.35));
#62277=CARTESIAN_POINT('Origin',(23.3,0.,4.));
#62278=CARTESIAN_POINT('',(22.8,-1.65327317884893E-16,5.35));
#62279=CARTESIAN_POINT('Origin',(23.3,0.,4.));
#62280=CARTESIAN_POINT('Origin',(4.,0.,4.));
#62875=UNCERTAINTY_MEASURE_WITH_UNIT(LENGTH_MEASURE(0.001),#62985,
'DISTANCE_ACCURACY_VALUE',
'Maximum model space distance between geometric entities at asserted c
onnectivities');
#62885=UNCERTAINTY_MEASURE_WITH_UNIT(LENGTH_MEASURE(0.001),#62985,
'DISTANCE_ACCURACY_VALUE',
'Maximum model space distance between geometric entities at asserted c
onnectivities');
#62974=(
GEOMETRIC_REPRESENTATION_CONTEXT(3)
GLOBAL_UNCERTAINTY_ASSIGNED_CONTEXT((#62875))
GLOBAL_UNIT_ASSIGNED_CONTEXT((#62985,#62987,#62988))
REPRESENTATION_CONTEXT('','3D')
);
#62984=(
GEOMETRIC_REPRESENTATION_CONTEXT(3)
GLOBAL_UNCERTAINTY_ASSIGNED_CONTEXT((#62885))
GLOBAL_UNIT_ASSIGNED_CONTEXT((#62985,#62987,#62988))
REPRESENTATION_CONTEXT('','3D')
);
#62985=(
LENGTH_UNIT()
NAMED_UNIT(*)
SI_UNIT(.CENTI.,.METRE.)
);
#62987=(
NAMED_UNIT(*)
PLANE_ANGLE_UNIT()
SI_UNIT($,.RADIAN.)
);
#62988=(
NAMED_UNIT(*)
SI_UNIT($,.STERADIAN.)
SOLID_ANGLE_UNIT()
);
#63077=SHAPE_DEFINITION_REPRESENTATION(#63288,#63437);
#63288=PRODUCT_DEFINITION_SHAPE('',$,#63536);
#63437=SHAPE_REPRESENTATION('',(#26127),#62974);
#63447=PRODUCT_DEFINITION_CONTEXT('part definition',#63743,'design');
#63536=PRODUCT_DEFINITION('Y Stage - 01 Supported TR12x3 screw',
'Y Stage - 01 Supported TR12x3 screw',#63634,#63447);
#63634=PRODUCT_DEFINITION_FORMATION('',$,#63833);
#63743=APPLICATION_CONTEXT(
'Core Data for Automotive Mechanical Design Process');
#63744=PRODUCT_CONTEXT('part definition',#63743,'mechanical');
#63833=PRODUCT('Y Stage - 01 Supported TR12x3 screw',
'Y Stage - 01 Supported TR12x3 screw',
'Y Stage - 01 Supported TR12x3 screw',(#63744));
#63913=COLOUR_RGB('Black',0.12,0.14,0.17);
#63914=FILL_AREA_STYLE_COLOUR('',#63913);
#63915=FILL_AREA_STYLE('',(#63914));
#63916=SURFACE_STYLE_FILL_AREA(#63915);
#63917=SURFACE_SIDE_STYLE('',(#63916));
#63918=SURFACE_STYLE_USAGE(.BOTH.,#63917);
#63919=PRESENTATION_STYLE_ASSIGNMENT((#63918));
ENDSEC;
END-ISO-10303-21;
